ISO-10303-21;
HEADER;
/* Generated by software containing ST-Developer
 * from STEP Tools, Inc. (www.steptools.com) 
 */

FILE_DESCRIPTION(
/* description */ (''),
/* implementation_level */ '2;1');

FILE_NAME(
/* name */ '16_Tie_Bolt_M8x110_ISO_4017_Hex_Head.step',
/* time_stamp */ '2026-10-26T06:13:19-07:00',
/* author */ (''),
/* organization */ (''),
/* preprocessor_version */ 'ST-DEVELOPER v20.2',
/* originating_system */ 'Autodesk Translation Framework v15.15.0.0',
/* authorisation */ '');

FILE_SCHEMA (('AUTOMOTIVE_DESIGN { 1 0 10303 214 3 1 1 }','TECHNICAL_DATA_PACKAGING'));
ENDSEC;

DATA;
#10=MECHANICAL_DESIGN_GEOMETRIC_PRESENTATION_REPRESENTATION('',(#315),#56639);
#275=SHAPE_REPRESENTATION_RELATIONSHIP('SRR','None',#56763,#295);
#295=ADVANCED_BREP_SHAPE_REPRESENTATION('',(#335),#56637);
#315=STYLED_ITEM('',(#56922),#335);
#335=MANIFOLD_SOLID_BREP('Body1',#16967);
#359=B_SPLINE_SURFACE_WITH_KNOTS('',3,3,((#50971,#50972,#50973,#50974,#50975,
#50976,#50977,#50978,#50979,#50980,#50981,#50982,#50983,#50984,#50985,#50986,
#50987,#50988,#50989,#50990,#50991,#50992,#50993,#50994,#50995,#50996,#50997,
#50998,#50999,#51000,#51001,#51002,#51003,#51004,#51005,#51006,#51007,#51008,
#51009,#51010,#51011,#51012,#51013,#51014,#51015,#51016,#51017,#51018,#51019,
#51020,#51021,#51022,#51023,#51024,#51025,#51026,#51027,#51028,#51029,#51030,
#51031,#51032,#51033,#51034,#51035,#51036,#51037,#51038,#51039,#51040,#51041,
#51042,#51043,#51044,#51045,#51046,#51047,#51048,#51049,#51050,#51051,#51052,
#51053,#51054,#51055,#51056,#51057,#51058,#51059,#51060,#51061,#51062,#51063,
#51064,#51065,#51066,#51067,#51068,#51069,#51070,#51071,#51072,#51073,#51074,
#51075,#51076,#51077,#51078,#51079,#51080,#51081,#51082,#51083,#51084,#51085,
#51086,#51087,#51088,#51089,#51090,#51091,#51092,#51093,#51094,#51095,#51096,
#51097,#51098,#51099,#51100,#51101,#51102,#51103,#51104,#51105,#51106,#51107,
#51108,#51109,#51110,#51111,#51112,#51113,#51114,#51115,#51116,#51117,#51118,
#51119,#51120,#51121,#51122,#51123,#51124,#51125,#51126,#51127,#51128,#51129,
#51130,#51131,#51132,#51133,#51134,#51135,#51136,#51137,#51138,#51139,#51140,
#51141,#51142,#51143,#51144,#51145,#51146,#51147,#51148,#51149,#51150,#51151,
#51152,#51153,#51154,#51155,#51156,#51157,#51158,#51159,#51160,#51161,#51162,
#51163,#51164,#51165,#51166,#51167,#51168,#51169,#51170,#51171,#51172,#51173,
#51174,#51175,#51176,#51177,#51178,#51179,#51180,#51181,#51182,#51183,#51184,
#51185,#51186,#51187,#51188,#51189,#51190,#51191,#51192,#51193,#51194,#51195,
#51196,#51197,#51198,#51199,#51200,#51201,#51202,#51203,#51204,#51205,#51206,
#51207,#51208,#51209,#51210,#51211,#51212,#51213,#51214,#51215,#51216,#51217,
#51218,#51219,#51220,#51221,#51222,#51223,#51224,#51225,#51226,#51227,#51228,
#51229,#51230,#51231,#51232,#51233,#51234,#51235,#51236,#51237,#51238,#51239,
#51240,#51241,#51242,#51243,#51244,#51245,#51246,#51247,#51248,#51249,#51250,
#51251,#51252,#51253,#51254,#51255,#51256,#51257,#51258,#51259,#51260,#51261,
#51262,#51263,#51264,#51265,#51266,#51267,#51268,#51269,#51270,#51271,#51272,
#51273,#51274,#51275,#51276,#51277,#51278,#51279,#51280,#51281,#51282,#51283,
#51284,#51285,#51286,#51287,#51288,#51289,#51290,#51291,#51292,#51293,#51294,
#51295,#51296,#51297,#51298,#51299,#51300,#51301,#51302,#51303,#51304,#51305,
#51306,#51307,#51308,#51309,#51310,#51311,#51312,#51313,#51314,#51315,#51316,
#51317,#51318,#51319,#51320,#51321,#51322,#51323,#51324,#51325,#51326,#51327,
#51328,#51329,#51330,#51331,#51332,#51333,#51334,#51335,#51336,#51337,#51338,
#51339,#51340,#51341,#51342,#51343,#51344,#51345,#51346,#51347,#51348,#51349,
#51350,#51351,#51352,#51353,#51354,#51355,#51356,#51357,#51358,#51359,#51360,
#51361,#51362,#51363,#51364,#51365,#51366,#51367,#51368,#51369,#51370,#51371,
#51372,#51373,#51374,#51375,#51376,#51377,#51378,#51379,#51380,#51381,#51382,
#51383,#51384,#51385,#51386,#51387,#51388,#51389,#51390,#51391,#51392,#51393,
#51394,#51395,#51396,#51397,#51398,#51399,#51400,#51401,#51402,#51403,#51404,
#51405,#51406,#51407,#51408,#51409,#51410,#51411,#51412,#51413,#51414,#51415,
#51416,#51417,#51418,#51419,#51420,#51421,#51422,#51423,#51424,#51425,#51426,
#51427,#51428,#51429,#51430,#51431,#51432,#51433,#51434,#51435,#51436,#51437,
#51438,#51439,#51440,#51441,#51442,#51443,#51444,#51445,#51446,#51447,#51448,
#51449,#51450,#51451,#51452,#51453,#51454,#51455,#51456,#51457,#51458,#51459,
#51460,#51461,#51462,#51463,#51464,#51465,#51466,#51467,#51468,#51469,#51470,
#51471,#51472,#51473,#51474,#51475,#51476,#51477,#51478,#51479,#51480,#51481,
#51482,#51483,#51484,#51485,#51486,#51487,#51488,#51489,#51490,#51491,#51492,
#51493,#51494,#51495,#51496,#51497,#51498,#51499,#51500,#51501,#51502,#51503,
#51504,#51505,#51506,#51507,#51508,#51509,#51510,#51511,#51512,#51513,#51514,
#51515,#51516,#51517,#51518,#51519,#51520,#51521,#51522,#51523,#51524,#51525,
#51526),(#51527,#51528,#51529,#51530,#51531,#51532,#51533,#51534,#51535,
#51536,#51537,#51538,#51539,#51540,#51541,#51542,#51543,#51544,#51545,#51546,
#51547,#51548,#51549,#51550,#51551,#51552,#51553,#51554,#51555,#51556,#51557,
#51558,#51559,#51560,#51561,#51562,#51563,#51564,#51565,#51566,#51567,#51568,
#51569,#51570,#51571,#51572,#51573,#51574,#51575,#51576,#51577,#51578,#51579,
#51580,#51581,#51582,#51583,#51584,#51585,#51586,#51587,#51588,#51589,#51590,
#51591,#51592,#51593,#51594,#51595,#51596,#51597,#51598,#51599,#51600,#51601,
#51602,#51603,#51604,#51605,#51606,#51607,#51608,#51609,#51610,#51611,#51612,
#51613,#51614,#51615,#51616,#51617,#51618,#51619,#51620,#51621,#51622,#51623,
#51624,#51625,#51626,#51627,#51628,#51629,#51630,#51631,#51632,#51633,#51634,
#51635,#51636,#51637,#51638,#51639,#51640,#51641,#51642,#51643,#51644,#51645,
#51646,#51647,#51648,#51649,#51650,#51651,#51652,#51653,#51654,#51655,#51656,
#51657,#51658,#51659,#51660,#51661,#51662,#51663,#51664,#51665,#51666,#51667,
#51668,#51669,#51670,#51671,#51672,#51673,#51674,#51675,#51676,#51677,#51678,
#51679,#51680,#51681,#51682,#51683,#51684,#51685,#51686,#51687,#51688,#51689,
#51690,#51691,#51692,#51693,#51694,#51695,#51696,#51697,#51698,#51699,#51700,
#51701,#51702,#51703,#51704,#51705,#51706,#51707,#51708,#51709,#51710,#51711,
#51712,#51713,#51714,#51715,#51716,#51717,#51718,#51719,#51720,#51721,#51722,
#51723,#51724,#51725,#51726,#51727,#51728,#51729,#51730,#51731,#51732,#51733,
#51734,#51735,#51736,#51737,#51738,#51739,#51740,#51741,#51742,#51743,#51744,
#51745,#51746,#51747,#51748,#51749,#51750,#51751,#51752,#51753,#51754,#51755,
#51756,#51757,#51758,#51759,#51760,#51761,#51762,#51763,#51764,#51765,#51766,
#51767,#51768,#51769,#51770,#51771,#51772,#51773,#51774,#51775,#51776,#51777,
#51778,#51779,#51780,#51781,#51782,#51783,#51784,#51785,#51786,#51787,#51788,
#51789,#51790,#51791,#51792,#51793,#51794,#51795,#51796,#51797,#51798,#51799,
#51800,#51801,#51802,#51803,#51804,#51805,#51806,#51807,#51808,#51809,#51810,
#51811,#51812,#51813,#51814,#51815,#51816,#51817,#51818,#51819,#51820,#51821,
#51822,#51823,#51824,#51825,#51826,#51827,#51828,#51829,#51830,#51831,#51832,
#51833,#51834,#51835,#51836,#51837,#51838,#51839,#51840,#51841,#51842,#51843,
#51844,#51845,#51846,#51847,#51848,#51849,#51850,#51851,#51852,#51853,#51854,
#51855,#51856,#51857,#51858,#51859,#51860,#51861,#51862,#51863,#51864,#51865,
#51866,#51867,#51868,#51869,#51870,#51871,#51872,#51873,#51874,#51875,#51876,
#51877,#51878,#51879,#51880,#51881,#51882,#51883,#51884,#51885,#51886,#51887,
#51888,#51889,#51890,#51891,#51892,#51893,#51894,#51895,#51896,#51897,#51898,
#51899,#51900,#51901,#51902,#51903,#51904,#51905,#51906,#51907,#51908,#51909,
#51910,#51911,#51912,#51913,#51914,#51915,#51916,#51917,#51918,#51919,#51920,
#51921,#51922,#51923,#51924,#51925,#51926,#51927,#51928,#51929,#51930,#51931,
#51932,#51933,#51934,#51935,#51936,#51937,#51938,#51939,#51940,#51941,#51942,
#51943,#51944,#51945,#51946,#51947,#51948,#51949,#51950,#51951,#51952,#51953,
#51954,#51955,#51956,#51957,#51958,#51959,#51960,#51961,#51962,#51963,#51964,
#51965,#51966,#51967,#51968,#51969,#51970,#51971,#51972,#51973,#51974,#51975,
#51976,#51977,#51978,#51979,#51980,#51981,#51982,#51983,#51984,#51985,#51986,
#51987,#51988,#51989,#51990,#51991,#51992,#51993,#51994,#51995,#51996,#51997,
#51998,#51999,#52000,#52001,#52002,#52003,#52004,#52005,#52006,#52007,#52008,
#52009,#52010,#52011,#52012,#52013,#52014,#52015,#52016,#52017,#52018,#52019,
#52020,#52021,#52022,#52023,#52024,#52025,#52026,#52027,#52028,#52029,#52030,
#52031,#52032,#52033,#52034,#52035,#52036,#52037,#52038,#52039,#52040,#52041,
#52042,#52043,#52044,#52045,#52046,#52047,#52048,#52049,#52050,#52051,#52052,
#52053,#52054,#52055,#52056,#52057,#52058,#52059,#52060,#52061,#52062,#52063,
#52064,#52065,#52066,#52067,#52068,#52069,#52070,#52071,#52072,#52073,#52074,
#52075,#52076,#52077,#52078,#52079,#52080,#52081,#52082),(#52083,#52084,
#52085,#52086,#52087,#52088,#52089,#52090,#52091,#52092,#52093,#52094,#52095,
#52096,#52097,#52098,#52099,#52100,#52101,#52102,#52103,#52104,#52105,#52106,
#52107,#52108,#52109,#52110,#52111,#52112,#52113,#52114,#52115,#52116,#52117,
#52118,#52119,#52120,#52121,#52122,#52123,#52124,#52125,#52126,#52127,#52128,
#52129,#52130,#52131,#52132,#52133,#52134,#52135,#52136,#52137,#52138,#52139,
#52140,#52141,#52142,#52143,#52144,#52145,#52146,#52147,#52148,#52149,#52150,
#52151,#52152,#52153,#52154,#52155,#52156,#52157,#52158,#52159,#52160,#52161,
#52162,#52163,#52164,#52165,#52166,#52167,#52168,#52169,#52170,#52171,#52172,
#52173,#52174,#52175,#52176,#52177,#52178,#52179,#52180,#52181,#52182,#52183,
#52184,#52185,#52186,#52187,#52188,#52189,#52190,#52191,#52192,#52193,#52194,
#52195,#52196,#52197,#52198,#52199,#52200,#52201,#52202,#52203,#52204,#52205,
#52206,#52207,#52208,#52209,#52210,#52211,#52212,#52213,#52214,#52215,#52216,
#52217,#52218,#52219,#52220,#52221,#52222,#52223,#52224,#52225,#52226,#52227,
#52228,#52229,#52230,#52231,#52232,#52233,#52234,#52235,#52236,#52237,#52238,
#52239,#52240,#52241,#52242,#52243,#52244,#52245,#52246,#52247,#52248,#52249,
#52250,#52251,#52252,#52253,#52254,#52255,#52256,#52257,#52258,#52259,#52260,
#52261,#52262,#52263,#52264,#52265,#52266,#52267,#52268,#52269,#52270,#52271,
#52272,#52273,#52274,#52275,#52276,#52277,#52278,#52279,#52280,#52281,#52282,
#52283,#52284,#52285,#52286,#52287,#52288,#52289,#52290,#52291,#52292,#52293,
#52294,#52295,#52296,#52297,#52298,#52299,#52300,#52301,#52302,#52303,#52304,
#52305,#52306,#52307,#52308,#52309,#52310,#52311,#52312,#52313,#52314,#52315,
#52316,#52317,#52318,#52319,#52320,#52321,#52322,#52323,#52324,#52325,#52326,
#52327,#52328,#52329,#52330,#52331,#52332,#52333,#52334,#52335,#52336,#52337,
#52338,#52339,#52340,#52341,#52342,#52343,#52344,#52345,#52346,#52347,#52348,
#52349,#52350,#52351,#52352,#52353,#52354,#52355,#52356,#52357,#52358,#52359,
#52360,#52361,#52362,#52363,#52364,#52365,#52366,#52367,#52368,#52369,#52370,
#52371,#52372,#52373,#52374,#52375,#52376,#52377,#52378,#52379,#52380,#52381,
#52382,#52383,#52384,#52385,#52386,#52387,#52388,#52389,#52390,#52391,#52392,
#52393,#52394,#52395,#52396,#52397,#52398,#52399,#52400,#52401,#52402,#52403,
#52404,#52405,#52406,#52407,#52408,#52409,#52410,#52411,#52412,#52413,#52414,
#52415,#52416,#52417,#52418,#52419,#52420,#52421,#52422,#52423,#52424,#52425,
#52426,#52427,#52428,#52429,#52430,#52431,#52432,#52433,#52434,#52435,#52436,
#52437,#52438,#52439,#52440,#52441,#52442,#52443,#52444,#52445,#52446,#52447,
#52448,#52449,#52450,#52451,#52452,#52453,#52454,#52455,#52456,#52457,#52458,
#52459,#52460,#52461,#52462,#52463,#52464,#52465,#52466,#52467,#52468,#52469,
#52470,#52471,#52472,#52473,#52474,#52475,#52476,#52477,#52478,#52479,#52480,
#52481,#52482,#52483,#52484,#52485,#52486,#52487,#52488,#52489,#52490,#52491,
#52492,#52493,#52494,#52495,#52496,#52497,#52498,#52499,#52500,#52501,#52502,
#52503,#52504,#52505,#52506,#52507,#52508,#52509,#52510,#52511,#52512,#52513,
#52514,#52515,#52516,#52517,#52518,#52519,#52520,#52521,#52522,#52523,#52524,
#52525,#52526,#52527,#52528,#52529,#52530,#52531,#52532,#52533,#52534,#52535,
#52536,#52537,#52538,#52539,#52540,#52541,#52542,#52543,#52544,#52545,#52546,
#52547,#52548,#52549,#52550,#52551,#52552,#52553,#52554,#52555,#52556,#52557,
#52558,#52559,#52560,#52561,#52562,#52563,#52564,#52565,#52566,#52567,#52568,
#52569,#52570,#52571,#52572,#52573,#52574,#52575,#52576,#52577,#52578,#52579,
#52580,#52581,#52582,#52583,#52584,#52585,#52586,#52587,#52588,#52589,#52590,
#52591,#52592,#52593,#52594,#52595,#52596,#52597,#52598,#52599,#52600,#52601,
#52602,#52603,#52604,#52605,#52606,#52607,#52608,#52609,#52610,#52611,#52612,
#52613,#52614,#52615,#52616,#52617,#52618,#52619,#52620,#52621,#52622,#52623,
#52624,#52625,#52626,#52627,#52628,#52629,#52630,#52631,#52632,#52633,#52634,
#52635,#52636,#52637,#52638),(#52639,#52640,#52641,#52642,#52643,#52644,
#52645,#52646,#52647,#52648,#52649,#52650,#52651,#52652,#52653,#52654,#52655,
#52656,#52657,#52658,#52659,#52660,#52661,#52662,#52663,#52664,#52665,#52666,
#52667,#52668,#52669,#52670,#52671,#52672,#52673,#52674,#52675,#52676,#52677,
#52678,#52679,#52680,#52681,#52682,#52683,#52684,#52685,#52686,#52687,#52688,
#52689,#52690,#52691,#52692,#52693,#52694,#52695,#52696,#52697,#52698,#52699,
#52700,#52701,#52702,#52703,#52704,#52705,#52706,#52707,#52708,#52709,#52710,
#52711,#52712,#52713,#52714,#52715,#52716,#52717,#52718,#52719,#52720,#52721,
#52722,#52723,#52724,#52725,#52726,#52727,#52728,#52729,#52730,#52731,#52732,
#52733,#52734,#52735,#52736,#52737,#52738,#52739,#52740,#52741,#52742,#52743,
#52744,#52745,#52746,#52747,#52748,#52749,#52750,#52751,#52752,#52753,#52754,
#52755,#52756,#52757,#52758,#52759,#52760,#52761,#52762,#52763,#52764,#52765,
#52766,#52767,#52768,#52769,#52770,#52771,#52772,#52773,#52774,#52775,#52776,
#52777,#52778,#52779,#52780,#52781,#52782,#52783,#52784,#52785,#52786,#52787,
#52788,#52789,#52790,#52791,#52792,#52793,#52794,#52795,#52796,#52797,#52798,
#52799,#52800,#52801,#52802,#52803,#52804,#52805,#52806,#52807,#52808,#52809,
#52810,#52811,#52812,#52813,#52814,#52815,#52816,#52817,#52818,#52819,#52820,
#52821,#52822,#52823,#52824,#52825,#52826,#52827,#52828,#52829,#52830,#52831,
#52832,#52833,#52834,#52835,#52836,#52837,#52838,#52839,#52840,#52841,#52842,
#52843,#52844,#52845,#52846,#52847,#52848,#52849,#52850,#52851,#52852,#52853,
#52854,#52855,#52856,#52857,#52858,#52859,#52860,#52861,#52862,#52863,#52864,
#52865,#52866,#52867,#52868,#52869,#52870,#52871,#52872,#52873,#52874,#52875,
#52876,#52877,#52878,#52879,#52880,#52881,#52882,#52883,#52884,#52885,#52886,
#52887,#52888,#52889,#52890,#52891,#52892,#52893,#52894,#52895,#52896,#52897,
#52898,#52899,#52900,#52901,#52902,#52903,#52904,#52905,#52906,#52907,#52908,
#52909,#52910,#52911,#52912,#52913,#52914,#52915,#52916,#52917,#52918,#52919,
#52920,#52921,#52922,#52923,#52924,#52925,#52926,#52927,#52928,#52929,#52930,
#52931,#52932,#52933,#52934,#52935,#52936,#52937,#52938,#52939,#52940,#52941,
#52942,#52943,#52944,#52945,#52946,#52947,#52948,#52949,#52950,#52951,#52952,
#52953,#52954,#52955,#52956,#52957,#52958,#52959,#52960,#52961,#52962,#52963,
#52964,#52965,#52966,#52967,#52968,#52969,#52970,#52971,#52972,#52973,#52974,
#52975,#52976,#52977,#52978,#52979,#52980,#52981,#52982,#52983,#52984,#52985,
#52986,#52987,#52988,#52989,#52990,#52991,#52992,#52993,#52994,#52995,#52996,
#52997,#52998,#52999,#53000,#53001,#53002,#53003,#53004,#53005,#53006,#53007,
#53008,#53009,#53010,#53011,#53012,#53013,#53014,#53015,#53016,#53017,#53018,
#53019,#53020,#53021,#53022,#53023,#53024,#53025,#53026,#53027,#53028,#53029,
#53030,#53031,#53032,#53033,#53034,#53035,#53036,#53037,#53038,#53039,#53040,
#53041,#53042,#53043,#53044,#53045,#53046,#53047,#53048,#53049,#53050,#53051,
#53052,#53053,#53054,#53055,#53056,#53057,#53058,#53059,#53060,#53061,#53062,
#53063,#53064,#53065,#53066,#53067,#53068,#53069,#53070,#53071,#53072,#53073,
#53074,#53075,#53076,#53077,#53078,#53079,#53080,#53081,#53082,#53083,#53084,
#53085,#53086,#53087,#53088,#53089,#53090,#53091,#53092,#53093,#53094,#53095,
#53096,#53097,#53098,#53099,#53100,#53101,#53102,#53103,#53104,#53105,#53106,
#53107,#53108,#53109,#53110,#53111,#53112,#53113,#53114,#53115,#53116,#53117,
#53118,#53119,#53120,#53121,#53122,#53123,#53124,#53125,#53126,#53127,#53128,
#53129,#53130,#53131,#53132,#53133,#53134,#53135,#53136,#53137,#53138,#53139,
#53140,#53141,#53142,#53143,#53144,#53145,#53146,#53147,#53148,#53149,#53150,
#53151,#53152,#53153,#53154,#53155,#53156,#53157,#53158,#53159,#53160,#53161,
#53162,#53163,#53164,#53165,#53166,#53167,#53168,#53169,#53170,#53171,#53172,
#53173,#53174,#53175,#53176,#53177,#53178,#53179,#53180,#53181,#53182,#53183,
#53184,#53185,#53186,#53187,#53188,#53189,#53190,#53191,#53192,#53193,#53194)),
 .UNSPECIFIED.,.F.,.F.,.F.,(4,4),(4,1,1,1,1,1,1,1,1,1,1,1,1,1,1,1,1,1,1,
1,1,1,1,1,1,1,1,1,1,1,1,1,1,1,1,1,1,1,1,1,1,1,1,1,1,1,1,1,1,1,1,1,1,1,1,
1,1,1,1,1,1,1,1,1,1,1,1,1,1,1,1,1,1,1,1,1,1,1,1,1,1,1,1,1,1,1,1,1,1,1,1,
1,1,1,1,1,1,1,1,1,1,1,1,1,1,1,1,1,1,1,1,1,1,1,1,1,1,1,1,1,1,1,1,1,1,1,1,
1,1,1,1,1,1,1,1,1,1,1,1,1,1,1,1,1,1,1,1,1,1,1,1,1,1,1,1,1,1,1,1,1,1,1,1,
1,1,1,1,1,1,1,1,1,1,1,1,1,1,1,1,1,1,1,1,1,1,1,1,1,1,1,1,1,1,1,1,1,1,1,1,
1,1,1,1,1,1,1,1,1,1,1,1,1,1,1,1,1,1,1,1,1,1,1,1,1,1,1,1,1,1,1,1,1,1,1,1,
1,1,1,1,1,1,1,1,1,1,1,1,1,1,1,1,1,1,1,1,1,1,1,1,1,1,1,1,1,1,1,1,1,1,1,1,
1,1,1,1,1,1,1,1,1,1,1,1,1,1,1,1,1,1,1,1,1,1,1,1,1,1,1,1,1,1,1,1,1,1,1,1,
1,1,1,1,1,1,1,1,1,1,1,1,1,1,1,1,1,1,1,1,1,1,1,1,1,1,1,1,1,1,1,1,1,1,1,1,
1,1,1,1,1,1,1,1,1,1,1,1,1,1,1,1,1,1,1,1,1,1,1,1,1,1,1,1,1,1,1,1,1,1,1,1,
1,1,1,1,1,1,1,1,1,1,1,1,1,1,1,1,1,1,1,1,1,1,1,1,1,1,1,1,1,1,1,1,1,1,1,1,
1,1,1,1,1,1,1,1,1,1,1,1,1,1,1,1,1,1,1,1,1,1,1,1,1,1,1,1,1,1,1,1,1,1,1,1,
1,1,1,1,1,1,1,1,1,1,1,1,1,1,1,1,1,1,1,1,1,1,1,1,1,1,1,1,1,1,1,1,1,1,1,1,
1,1,1,1,1,1,1,1,1,1,1,1,1,1,1,1,1,1,1,1,1,1,1,1,1,1,1,1,1,1,1,1,1,1,1,1,
1,1,1,1,1,1,1,1,1,1,1,1,1,1,1,1,1,1,1,1,1,1,1,1,1,1,1,1,1,1,4),(0.,0.0820126057383858),
(8.31473274985908,9.31438015173777,10.3140275536165,11.3136749554951,12.3133223573738,
13.3129697592525,14.3126171611312,15.3122645630099,16.3119119648886,17.3115593667672,
18.3112067686459,19.3108541705246,20.3105015724033,21.310148974282,22.3097963761607,
23.3094437780394,24.309091179918,25.3087385817967,26.3083859836754,27.3080333855541,
28.3076807874328,29.3073281893115,30.3069755911901,31.3066229930688,32.3062703949475,
33.3059177968262,34.3055651987049,35.3052126005836,36.3048600024622,37.3045074043409,
38.3041548062196,39.3038022080983,40.303449609977,41.3030970118557,42.3027444137344,
43.302391815613,44.3020392174917,45.3016866193704,46.3013340212491,47.3009814231278,
48.3006288250065,49.3002762268852,50.2999236287638,51.2995710306425,52.2992184325212,
53.2988658343999,54.2985132362786,55.2981606381573,56.2978080400359,57.2974554419146,
58.2971028437933,59.296750245672,60.2963976475507,61.2960450494294,62.295692451308,
63.2953398531867,64.2949872550654,65.2946346569441,66.2942820588228,67.2939294607015,
68.2935768625802,69.2932242644588,70.2928716663375,71.2925190682162,72.2921664700949,
73.2918138719736,74.2914612738523,75.291108675731,76.2907560776096,77.2904034794883,
78.290050881367,79.2896982832457,80.2893456851244,81.2889930870031,82.2886404888818,
83.2882878907604,84.2879352926391,85.2875826945178,86.2872300963965,87.2868774982752,
88.2865249001539,89.2861723020325,90.2858197039112,91.2854671057899,92.2851145076686,
93.2847619095473,94.2844093114259,95.2840567133046,96.2837041151833,97.283351517062,
98.2829989189407,99.2826463208194,100.282293722698,101.281941124577,102.281588526455,
103.281235928334,104.280883330213,105.280530732091,106.28017813397,107.279825535849,
108.279472937728,109.279120339606,110.278767741485,111.278415143364,112.278062545242,
113.277709947121,114.277357349,115.277004750878,116.276652152757,117.276299554636,
118.275946956514,119.275594358393,120.275241760272,121.27488916215,122.274536564029,
123.274183965908,124.273831367786,125.273478769665,126.273126171544,127.272773573423,
128.272420975301,129.27206837718,130.271715779059,131.271363180937,132.271010582816,
133.270657984695,134.270305386573,135.269952788452,136.269600190331,137.269247592209,
138.268894994088,139.268542395967,140.268189797845,141.267837199724,142.267484601603,
143.267132003481,144.26677940536,145.266426807239,146.266074209118,147.265721610996,
148.265369012875,149.265016414754,150.264663816632,151.264311218511,152.26395862039,
153.263606022268,154.263253424147,155.262900826026,156.262548227904,157.262195629783,
158.261843031662,159.26149043354,160.261137835419,161.260785237298,162.260432639177,
163.260080041055,164.259727442934,165.259374844813,166.259022246691,167.25866964857,
168.258317050449,169.257964452327,170.257611854206,171.257259256085,172.256906657963,
173.256554059842,174.256201461721,175.255848863599,176.255496265478,177.255143667357,
178.254791069235,179.254438471114,180.254085872993,181.253733274872,182.25338067675,
183.253028078629,184.252675480508,185.252322882386,186.251970284265,187.251617686144,
188.251265088022,189.250912489901,190.25055989178,191.250207293658,192.249854695537,
193.249502097416,194.249149499294,195.248796901173,196.248444303052,197.24809170493,
198.247739106809,199.247386508688,200.247033910567,201.246681312445,202.246328714324,
203.245976116203,204.245623518081,205.24527091996,206.244918321839,207.244565723717,
208.244213125596,209.243860527475,210.243507929353,211.243155331232,212.242802733111,
213.242450134989,214.242097536868,215.241744938747,216.241392340625,217.241039742504,
218.240687144383,219.240334546262,220.23998194814,221.239629350019,222.239276751898,
223.238924153776,224.238571555655,225.238218957534,226.237866359412,227.237513761291,
228.23716116317,229.236808565048,230.236455966927,231.236103368806,232.235750770684,
233.235398172563,234.235045574442,235.23469297632,236.234340378199,237.233987780078,
238.233635181957,239.233282583835,240.232929985714,241.232577387593,242.232224789471,
243.23187219135,244.231519593229,245.231166995107,246.230814396986,247.230461798865,
248.230109200743,249.229756602622,250.229404004501,251.229051406379,252.228698808258,
253.228346210137,254.227993612015,255.227641013894,256.227288415773,257.226935817652,
258.22658321953,259.226230621409,260.225878023288,261.225525425166,262.225172827045,
263.224820228924,264.224467630802,265.224115032681,266.22376243456,267.223409836438,
268.223057238317,269.222704640196,270.222352042074,271.221999443953,272.221646845832,
273.221294247711,274.220941649589,275.220589051468,276.220236453347,277.219883855225,
278.219531257104,279.219178658983,280.218826060861,281.21847346274,282.218120864619,
283.217768266497,284.217415668376,285.217063070255,286.216710472133,287.216357874012,
288.216005275891,289.215652677769,290.215300079648,291.214947481527,292.214594883406,
293.214242285284,294.213889687163,295.213537089042,296.21318449092,297.212831892799,
298.212479294678,299.212126696556,300.211774098435,301.211421500314,302.211068902192,
303.210716304071,304.21036370595,305.210011107828,306.209658509707,307.209305911586,
308.208953313464,309.208600715343,310.208248117222,311.207895519101,312.207542920979,
313.207190322858,314.206837724737,315.206485126615,316.206132528494,317.205779930373,
318.205427332251,319.20507473413,320.204722136009,321.204369537887,322.204016939766,
323.203664341645,324.203311743523,325.202959145402,326.202606547281,327.20225394916,
328.201901351038,329.201548752917,330.201196154796,331.200843556674,332.200490958553,
333.200138360432,334.19978576231,335.199433164189,336.199080566068,337.198727967946,
338.198375369825,339.198022771704,340.197670173582,341.197317575461,342.19696497734,
343.196612379218,344.196259781097,345.195907182976,346.195554584855,347.195201986733,
348.194849388612,349.194496790491,350.194144192369,351.193791594248,352.193438996127,
353.193086398005,354.192733799884,355.192381201763,356.192028603641,357.19167600552,
358.191323407399,359.190970809277,360.190618211156,361.190265613035,362.189913014913,
363.189560416792,364.189207818671,365.188855220549,366.188502622428,367.188150024307,
368.187797426186,369.187444828064,370.187092229943,371.186739631822,372.1863870337,
373.186034435579,374.185681837458,375.185329239336,376.184976641215,377.184624043094,
378.184271444972,379.183918846851,380.18356624873,381.183213650608,382.182861052487,
383.182508454366,384.182155856244,385.181803258123,386.181450660002,387.181098061881,
388.180745463759,389.180392865638,390.180040267517,391.179687669395,392.179335071274,
393.178982473153,394.178629875031,395.17827727691,396.177924678789,397.177572080667,
398.177219482546,399.176866884425,400.176514286303,401.176161688182,402.175809090061,
403.17545649194,404.175103893818,405.174751295697,406.174398697576,407.174046099454,
408.173693501333,409.173340903212,410.17298830509,411.172635706969,412.172283108848,
413.171930510726,414.171577912605,415.171225314484,416.170872716362,417.170520118241,
418.17016752012,419.169814921998,420.169462323877,421.169109725756,422.168757127635,
423.168404529513,424.168051931392,425.167699333271,426.167346735149,427.166994137028,
428.166641538907,429.166288940785,430.165936342664,431.165583744543,432.165231146421,
433.1648785483,434.164525950179,435.164173352057,436.163820753936,437.163468155815,
438.163115557694,439.162762959572,440.162410361451,441.16205776333,442.161705165208,
443.161352567087,444.160999968966,445.160647370844,446.160294772723,447.159942174602,
448.15958957648,449.159236978359,450.158884380238,451.158531782116,452.158179183995,
453.157826585874,454.157473987752,455.157121389631,456.15676879151,457.156416193389,
458.156063595267,459.155710997146,460.155358399025,461.155005800903,462.154653202782,
463.154300604661,464.153948006539,465.153595408418,466.153242810297,467.152890212175,
468.152537614054,469.152185015933,470.151832417811,471.15147981969,472.151127221569,
473.150774623447,474.150422025326,475.150069427205,476.149716829084,477.149364230962,
478.149011632841,479.14865903472,480.148306436598,481.147953838477,482.147601240356,
483.147248642234,484.146896044113,485.146543445992,486.14619084787,487.145838249749,
488.145485651628,489.145133053506,490.144780455385,491.144427857264,492.144075259142,
493.143722661021,494.1433700629,495.143017464778,496.142664866657,497.142312268536,
498.141959670415,499.141607072293,500.141254474172,501.140901876051,502.140549277929,
503.140196679808,504.139844081687,505.139491483565,506.139138885444,507.138786287323,
508.138433689201,509.13808109108,510.137728492959,511.137375894837,512.137023296716,
513.136670698595,514.136318100474,515.135965502352,516.135612904231,517.13526030611,
518.134907707988,519.134555109867,520.134202511746,521.133849913624,522.133497315503,
523.133144717382,524.13279211926,525.132439521139,526.132086923018,527.131734324896,
528.131381726775,529.131029128654,530.130676530532,531.130323932411,532.12997133429,
533.129618736168,534.129266138047,535.128913539926,536.128560941805,537.128208343683,
538.127855745562,539.127503147441,540.127150549319,541.126797951198,542.126445353077,
543.126092754955,544.125740156834,545.125387558713,546.125034960591,547.12468236247,
548.124329764349,549.123977166228,550.123624568106,551.123271969985,552.122919371864,
553.122566773742,554.122214175621,555.1218615775,556.121508979378,557.121156381257,
558.120803783136,559.120451185014,560.120098586893,561.119745988772),
 .UNSPECIFIED.);
#360=B_SPLINE_SURFACE_WITH_KNOTS('',3,3,((#53525,#53526,#53527,#53528,#53529,
#53530,#53531,#53532,#53533,#53534,#53535,#53536,#53537,#53538,#53539,#53540,
#53541,#53542,#53543,#53544,#53545,#53546,#53547,#53548,#53549,#53550,#53551,
#53552,#53553,#53554,#53555,#53556,#53557,#53558,#53559,#53560,#53561,#53562,
#53563,#53564,#53565,#53566,#53567,#53568,#53569,#53570,#53571,#53572,#53573,
#53574,#53575,#53576,#53577,#53578,#53579,#53580,#53581,#53582,#53583,#53584,
#53585,#53586,#53587,#53588,#53589,#53590,#53591,#53592,#53593,#53594,#53595,
#53596,#53597,#53598,#53599,#53600,#53601,#53602,#53603,#53604,#53605,#53606,
#53607,#53608,#53609,#53610,#53611,#53612,#53613,#53614,#53615,#53616,#53617,
#53618,#53619,#53620,#53621,#53622,#53623,#53624,#53625,#53626,#53627,#53628,
#53629,#53630,#53631,#53632,#53633,#53634,#53635,#53636,#53637,#53638,#53639,
#53640,#53641,#53642,#53643,#53644,#53645,#53646,#53647,#53648,#53649,#53650,
#53651,#53652,#53653,#53654,#53655,#53656,#53657,#53658,#53659,#53660,#53661,
#53662,#53663,#53664,#53665,#53666,#53667,#53668,#53669,#53670,#53671,#53672,
#53673,#53674,#53675,#53676,#53677,#53678,#53679,#53680,#53681,#53682,#53683,
#53684,#53685,#53686,#53687,#53688,#53689,#53690,#53691,#53692,#53693,#53694,
#53695,#53696,#53697,#53698,#53699,#53700,#53701,#53702,#53703,#53704,#53705,
#53706,#53707,#53708,#53709,#53710,#53711,#53712,#53713,#53714,#53715,#53716,
#53717,#53718,#53719,#53720,#53721,#53722,#53723,#53724,#53725,#53726,#53727,
#53728,#53729,#53730,#53731,#53732,#53733,#53734,#53735,#53736,#53737,#53738,
#53739,#53740,#53741,#53742,#53743,#53744,#53745,#53746,#53747,#53748,#53749,
#53750,#53751,#53752,#53753,#53754,#53755,#53756,#53757,#53758,#53759,#53760,
#53761,#53762,#53763,#53764,#53765,#53766,#53767,#53768,#53769,#53770,#53771,
#53772,#53773,#53774,#53775,#53776,#53777,#53778,#53779,#53780,#53781,#53782,
#53783,#53784,#53785,#53786,#53787,#53788,#53789,#53790,#53791,#53792,#53793,
#53794,#53795,#53796,#53797,#53798,#53799,#53800,#53801,#53802,#53803,#53804,
#53805,#53806,#53807,#53808,#53809,#53810,#53811,#53812,#53813,#53814,#53815,
#53816,#53817,#53818,#53819,#53820,#53821,#53822,#53823,#53824,#53825,#53826,
#53827,#53828,#53829,#53830,#53831,#53832,#53833,#53834,#53835,#53836,#53837,
#53838,#53839,#53840,#53841,#53842,#53843,#53844,#53845,#53846,#53847,#53848,
#53849,#53850,#53851,#53852,#53853,#53854,#53855,#53856,#53857,#53858,#53859,
#53860,#53861,#53862,#53863,#53864,#53865,#53866,#53867,#53868,#53869,#53870,
#53871,#53872,#53873,#53874,#53875,#53876,#53877,#53878,#53879,#53880,#53881,
#53882,#53883,#53884,#53885,#53886,#53887,#53888,#53889,#53890,#53891,#53892,
#53893,#53894,#53895,#53896,#53897,#53898,#53899,#53900,#53901,#53902,#53903,
#53904,#53905,#53906,#53907,#53908,#53909,#53910,#53911,#53912,#53913,#53914,
#53915,#53916,#53917,#53918,#53919,#53920,#53921,#53922,#53923,#53924,#53925,
#53926,#53927,#53928,#53929,#53930,#53931,#53932,#53933,#53934,#53935,#53936,
#53937,#53938,#53939,#53940,#53941,#53942,#53943,#53944,#53945,#53946,#53947,
#53948,#53949,#53950,#53951,#53952,#53953,#53954,#53955,#53956,#53957,#53958,
#53959,#53960,#53961,#53962,#53963,#53964,#53965,#53966,#53967,#53968,#53969,
#53970,#53971,#53972,#53973,#53974,#53975,#53976,#53977,#53978,#53979,#53980,
#53981,#53982,#53983,#53984,#53985,#53986,#53987,#53988,#53989,#53990,#53991,
#53992,#53993,#53994,#53995,#53996,#53997,#53998,#53999,#54000,#54001,#54002,
#54003,#54004,#54005,#54006,#54007,#54008,#54009,#54010,#54011,#54012,#54013,
#54014,#54015,#54016,#54017,#54018,#54019,#54020,#54021,#54022,#54023,#54024,
#54025,#54026,#54027,#54028,#54029,#54030,#54031,#54032,#54033,#54034,#54035,
#54036,#54037,#54038,#54039,#54040,#54041,#54042,#54043,#54044,#54045,#54046,
#54047,#54048,#54049,#54050,#54051,#54052,#54053,#54054,#54055,#54056,#54057,
#54058,#54059,#54060,#54061,#54062,#54063,#54064,#54065,#54066,#54067,#54068,
#54069,#54070,#54071,#54072,#54073,#54074,#54075,#54076,#54077,#54078,#54079,
#54080),(#54081,#54082,#54083,#54084,#54085,#54086,#54087,#54088,#54089,
#54090,#54091,#54092,#54093,#54094,#54095,#54096,#54097,#54098,#54099,#54100,
#54101,#54102,#54103,#54104,#54105,#54106,#54107,#54108,#54109,#54110,#54111,
#54112,#54113,#54114,#54115,#54116,#54117,#54118,#54119,#54120,#54121,#54122,
#54123,#54124,#54125,#54126,#54127,#54128,#54129,#54130,#54131,#54132,#54133,
#54134,#54135,#54136,#54137,#54138,#54139,#54140,#54141,#54142,#54143,#54144,
#54145,#54146,#54147,#54148,#54149,#54150,#54151,#54152,#54153,#54154,#54155,
#54156,#54157,#54158,#54159,#54160,#54161,#54162,#54163,#54164,#54165,#54166,
#54167,#54168,#54169,#54170,#54171,#54172,#54173,#54174,#54175,#54176,#54177,
#54178,#54179,#54180,#54181,#54182,#54183,#54184,#54185,#54186,#54187,#54188,
#54189,#54190,#54191,#54192,#54193,#54194,#54195,#54196,#54197,#54198,#54199,
#54200,#54201,#54202,#54203,#54204,#54205,#54206,#54207,#54208,#54209,#54210,
#54211,#54212,#54213,#54214,#54215,#54216,#54217,#54218,#54219,#54220,#54221,
#54222,#54223,#54224,#54225,#54226,#54227,#54228,#54229,#54230,#54231,#54232,
#54233,#54234,#54235,#54236,#54237,#54238,#54239,#54240,#54241,#54242,#54243,
#54244,#54245,#54246,#54247,#54248,#54249,#54250,#54251,#54252,#54253,#54254,
#54255,#54256,#54257,#54258,#54259,#54260,#54261,#54262,#54263,#54264,#54265,
#54266,#54267,#54268,#54269,#54270,#54271,#54272,#54273,#54274,#54275,#54276,
#54277,#54278,#54279,#54280,#54281,#54282,#54283,#54284,#54285,#54286,#54287,
#54288,#54289,#54290,#54291,#54292,#54293,#54294,#54295,#54296,#54297,#54298,
#54299,#54300,#54301,#54302,#54303,#54304,#54305,#54306,#54307,#54308,#54309,
#54310,#54311,#54312,#54313,#54314,#54315,#54316,#54317,#54318,#54319,#54320,
#54321,#54322,#54323,#54324,#54325,#54326,#54327,#54328,#54329,#54330,#54331,
#54332,#54333,#54334,#54335,#54336,#54337,#54338,#54339,#54340,#54341,#54342,
#54343,#54344,#54345,#54346,#54347,#54348,#54349,#54350,#54351,#54352,#54353,
#54354,#54355,#54356,#54357,#54358,#54359,#54360,#54361,#54362,#54363,#54364,
#54365,#54366,#54367,#54368,#54369,#54370,#54371,#54372,#54373,#54374,#54375,
#54376,#54377,#54378,#54379,#54380,#54381,#54382,#54383,#54384,#54385,#54386,
#54387,#54388,#54389,#54390,#54391,#54392,#54393,#54394,#54395,#54396,#54397,
#54398,#54399,#54400,#54401,#54402,#54403,#54404,#54405,#54406,#54407,#54408,
#54409,#54410,#54411,#54412,#54413,#54414,#54415,#54416,#54417,#54418,#54419,
#54420,#54421,#54422,#54423,#54424,#54425,#54426,#54427,#54428,#54429,#54430,
#54431,#54432,#54433,#54434,#54435,#54436,#54437,#54438,#54439,#54440,#54441,
#54442,#54443,#54444,#54445,#54446,#54447,#54448,#54449,#54450,#54451,#54452,
#54453,#54454,#54455,#54456,#54457,#54458,#54459,#54460,#54461,#54462,#54463,
#54464,#54465,#54466,#54467,#54468,#54469,#54470,#54471,#54472,#54473,#54474,
#54475,#54476,#54477,#54478,#54479,#54480,#54481,#54482,#54483,#54484,#54485,
#54486,#54487,#54488,#54489,#54490,#54491,#54492,#54493,#54494,#54495,#54496,
#54497,#54498,#54499,#54500,#54501,#54502,#54503,#54504,#54505,#54506,#54507,
#54508,#54509,#54510,#54511,#54512,#54513,#54514,#54515,#54516,#54517,#54518,
#54519,#54520,#54521,#54522,#54523,#54524,#54525,#54526,#54527,#54528,#54529,
#54530,#54531,#54532,#54533,#54534,#54535,#54536,#54537,#54538,#54539,#54540,
#54541,#54542,#54543,#54544,#54545,#54546,#54547,#54548,#54549,#54550,#54551,
#54552,#54553,#54554,#54555,#54556,#54557,#54558,#54559,#54560,#54561,#54562,
#54563,#54564,#54565,#54566,#54567,#54568,#54569,#54570,#54571,#54572,#54573,
#54574,#54575,#54576,#54577,#54578,#54579,#54580,#54581,#54582,#54583,#54584,
#54585,#54586,#54587,#54588,#54589,#54590,#54591,#54592,#54593,#54594,#54595,
#54596,#54597,#54598,#54599,#54600,#54601,#54602,#54603,#54604,#54605,#54606,
#54607,#54608,#54609,#54610,#54611,#54612,#54613,#54614,#54615,#54616,#54617,
#54618,#54619,#54620,#54621,#54622,#54623,#54624,#54625,#54626,#54627,#54628,
#54629,#54630,#54631,#54632,#54633,#54634,#54635,#54636),(#54637,#54638,
#54639,#54640,#54641,#54642,#54643,#54644,#54645,#54646,#54647,#54648,#54649,
#54650,#54651,#54652,#54653,#54654,#54655,#54656,#54657,#54658,#54659,#54660,
#54661,#54662,#54663,#54664,#54665,#54666,#54667,#54668,#54669,#54670,#54671,
#54672,#54673,#54674,#54675,#54676,#54677,#54678,#54679,#54680,#54681,#54682,
#54683,#54684,#54685,#54686,#54687,#54688,#54689,#54690,#54691,#54692,#54693,
#54694,#54695,#54696,#54697,#54698,#54699,#54700,#54701,#54702,#54703,#54704,
#54705,#54706,#54707,#54708,#54709,#54710,#54711,#54712,#54713,#54714,#54715,
#54716,#54717,#54718,#54719,#54720,#54721,#54722,#54723,#54724,#54725,#54726,
#54727,#54728,#54729,#54730,#54731,#54732,#54733,#54734,#54735,#54736,#54737,
#54738,#54739,#54740,#54741,#54742,#54743,#54744,#54745,#54746,#54747,#54748,
#54749,#54750,#54751,#54752,#54753,#54754,#54755,#54756,#54757,#54758,#54759,
#54760,#54761,#54762,#54763,#54764,#54765,#54766,#54767,#54768,#54769,#54770,
#54771,#54772,#54773,#54774,#54775,#54776,#54777,#54778,#54779,#54780,#54781,
#54782,#54783,#54784,#54785,#54786,#54787,#54788,#54789,#54790,#54791,#54792,
#54793,#54794,#54795,#54796,#54797,#54798,#54799,#54800,#54801,#54802,#54803,
#54804,#54805,#54806,#54807,#54808,#54809,#54810,#54811,#54812,#54813,#54814,
#54815,#54816,#54817,#54818,#54819,#54820,#54821,#54822,#54823,#54824,#54825,
#54826,#54827,#54828,#54829,#54830,#54831,#54832,#54833,#54834,#54835,#54836,
#54837,#54838,#54839,#54840,#54841,#54842,#54843,#54844,#54845,#54846,#54847,
#54848,#54849,#54850,#54851,#54852,#54853,#54854,#54855,#54856,#54857,#54858,
#54859,#54860,#54861,#54862,#54863,#54864,#54865,#54866,#54867,#54868,#54869,
#54870,#54871,#54872,#54873,#54874,#54875,#54876,#54877,#54878,#54879,#54880,
#54881,#54882,#54883,#54884,#54885,#54886,#54887,#54888,#54889,#54890,#54891,
#54892,#54893,#54894,#54895,#54896,#54897,#54898,#54899,#54900,#54901,#54902,
#54903,#54904,#54905,#54906,#54907,#54908,#54909,#54910,#54911,#54912,#54913,
#54914,#54915,#54916,#54917,#54918,#54919,#54920,#54921,#54922,#54923,#54924,
#54925,#54926,#54927,#54928,#54929,#54930,#54931,#54932,#54933,#54934,#54935,
#54936,#54937,#54938,#54939,#54940,#54941,#54942,#54943,#54944,#54945,#54946,
#54947,#54948,#54949,#54950,#54951,#54952,#54953,#54954,#54955,#54956,#54957,
#54958,#54959,#54960,#54961,#54962,#54963,#54964,#54965,#54966,#54967,#54968,
#54969,#54970,#54971,#54972,#54973,#54974,#54975,#54976,#54977,#54978,#54979,
#54980,#54981,#54982,#54983,#54984,#54985,#54986,#54987,#54988,#54989,#54990,
#54991,#54992,#54993,#54994,#54995,#54996,#54997,#54998,#54999,#55000,#55001,
#55002,#55003,#55004,#55005,#55006,#55007,#55008,#55009,#55010,#55011,#55012,
#55013,#55014,#55015,#55016,#55017,#55018,#55019,#55020,#55021,#55022,#55023,
#55024,#55025,#55026,#55027,#55028,#55029,#55030,#55031,#55032,#55033,#55034,
#55035,#55036,#55037,#55038,#55039,#55040,#55041,#55042,#55043,#55044,#55045,
#55046,#55047,#55048,#55049,#55050,#55051,#55052,#55053,#55054,#55055,#55056,
#55057,#55058,#55059,#55060,#55061,#55062,#55063,#55064,#55065,#55066,#55067,
#55068,#55069,#55070,#55071,#55072,#55073,#55074,#55075,#55076,#55077,#55078,
#55079,#55080,#55081,#55082,#55083,#55084,#55085,#55086,#55087,#55088,#55089,
#55090,#55091,#55092,#55093,#55094,#55095,#55096,#55097,#55098,#55099,#55100,
#55101,#55102,#55103,#55104,#55105,#55106,#55107,#55108,#55109,#55110,#55111,
#55112,#55113,#55114,#55115,#55116,#55117,#55118,#55119,#55120,#55121,#55122,
#55123,#55124,#55125,#55126,#55127,#55128,#55129,#55130,#55131,#55132,#55133,
#55134,#55135,#55136,#55137,#55138,#55139,#55140,#55141,#55142,#55143,#55144,
#55145,#55146,#55147,#55148,#55149,#55150,#55151,#55152,#55153,#55154,#55155,
#55156,#55157,#55158,#55159,#55160,#55161,#55162,#55163,#55164,#55165,#55166,
#55167,#55168,#55169,#55170,#55171,#55172,#55173,#55174,#55175,#55176,#55177,
#55178,#55179,#55180,#55181,#55182,#55183,#55184,#55185,#55186,#55187,#55188,
#55189,#55190,#55191,#55192),(#55193,#55194,#55195,#55196,#55197,#55198,
#55199,#55200,#55201,#55202,#55203,#55204,#55205,#55206,#55207,#55208,#55209,
#55210,#55211,#55212,#55213,#55214,#55215,#55216,#55217,#55218,#55219,#55220,
#55221,#55222,#55223,#55224,#55225,#55226,#55227,#55228,#55229,#55230,#55231,
#55232,#55233,#55234,#55235,#55236,#55237,#55238,#55239,#55240,#55241,#55242,
#55243,#55244,#55245,#55246,#55247,#55248,#55249,#55250,#55251,#55252,#55253,
#55254,#55255,#55256,#55257,#55258,#55259,#55260,#55261,#55262,#55263,#55264,
#55265,#55266,#55267,#55268,#55269,#55270,#55271,#55272,#55273,#55274,#55275,
#55276,#55277,#55278,#55279,#55280,#55281,#55282,#55283,#55284,#55285,#55286,
#55287,#55288,#55289,#55290,#55291,#55292,#55293,#55294,#55295,#55296,#55297,
#55298,#55299,#55300,#55301,#55302,#55303,#55304,#55305,#55306,#55307,#55308,
#55309,#55310,#55311,#55312,#55313,#55314,#55315,#55316,#55317,#55318,#55319,
#55320,#55321,#55322,#55323,#55324,#55325,#55326,#55327,#55328,#55329,#55330,
#55331,#55332,#55333,#55334,#55335,#55336,#55337,#55338,#55339,#55340,#55341,
#55342,#55343,#55344,#55345,#55346,#55347,#55348,#55349,#55350,#55351,#55352,
#55353,#55354,#55355,#55356,#55357,#55358,#55359,#55360,#55361,#55362,#55363,
#55364,#55365,#55366,#55367,#55368,#55369,#55370,#55371,#55372,#55373,#55374,
#55375,#55376,#55377,#55378,#55379,#55380,#55381,#55382,#55383,#55384,#55385,
#55386,#55387,#55388,#55389,#55390,#55391,#55392,#55393,#55394,#55395,#55396,
#55397,#55398,#55399,#55400,#55401,#55402,#55403,#55404,#55405,#55406,#55407,
#55408,#55409,#55410,#55411,#55412,#55413,#55414,#55415,#55416,#55417,#55418,
#55419,#55420,#55421,#55422,#55423,#55424,#55425,#55426,#55427,#55428,#55429,
#55430,#55431,#55432,#55433,#55434,#55435,#55436,#55437,#55438,#55439,#55440,
#55441,#55442,#55443,#55444,#55445,#55446,#55447,#55448,#55449,#55450,#55451,
#55452,#55453,#55454,#55455,#55456,#55457,#55458,#55459,#55460,#55461,#55462,
#55463,#55464,#55465,#55466,#55467,#55468,#55469,#55470,#55471,#55472,#55473,
#55474,#55475,#55476,#55477,#55478,#55479,#55480,#55481,#55482,#55483,#55484,
#55485,#55486,#55487,#55488,#55489,#55490,#55491,#55492,#55493,#55494,#55495,
#55496,#55497,#55498,#55499,#55500,#55501,#55502,#55503,#55504,#55505,#55506,
#55507,#55508,#55509,#55510,#55511,#55512,#55513,#55514,#55515,#55516,#55517,
#55518,#55519,#55520,#55521,#55522,#55523,#55524,#55525,#55526,#55527,#55528,
#55529,#55530,#55531,#55532,#55533,#55534,#55535,#55536,#55537,#55538,#55539,
#55540,#55541,#55542,#55543,#55544,#55545,#55546,#55547,#55548,#55549,#55550,
#55551,#55552,#55553,#55554,#55555,#55556,#55557,#55558,#55559,#55560,#55561,
#55562,#55563,#55564,#55565,#55566,#55567,#55568,#55569,#55570,#55571,#55572,
#55573,#55574,#55575,#55576,#55577,#55578,#55579,#55580,#55581,#55582,#55583,
#55584,#55585,#55586,#55587,#55588,#55589,#55590,#55591,#55592,#55593,#55594,
#55595,#55596,#55597,#55598,#55599,#55600,#55601,#55602,#55603,#55604,#55605,
#55606,#55607,#55608,#55609,#55610,#55611,#55612,#55613,#55614,#55615,#55616,
#55617,#55618,#55619,#55620,#55621,#55622,#55623,#55624,#55625,#55626,#55627,
#55628,#55629,#55630,#55631,#55632,#55633,#55634,#55635,#55636,#55637,#55638,
#55639,#55640,#55641,#55642,#55643,#55644,#55645,#55646,#55647,#55648,#55649,
#55650,#55651,#55652,#55653,#55654,#55655,#55656,#55657,#55658,#55659,#55660,
#55661,#55662,#55663,#55664,#55665,#55666,#55667,#55668,#55669,#55670,#55671,
#55672,#55673,#55674,#55675,#55676,#55677,#55678,#55679,#55680,#55681,#55682,
#55683,#55684,#55685,#55686,#55687,#55688,#55689,#55690,#55691,#55692,#55693,
#55694,#55695,#55696,#55697,#55698,#55699,#55700,#55701,#55702,#55703,#55704,
#55705,#55706,#55707,#55708,#55709,#55710,#55711,#55712,#55713,#55714,#55715,
#55716,#55717,#55718,#55719,#55720,#55721,#55722,#55723,#55724,#55725,#55726,
#55727,#55728,#55729,#55730,#55731,#55732,#55733,#55734,#55735,#55736,#55737,
#55738,#55739,#55740,#55741,#55742,#55743,#55744,#55745,#55746,#55747,#55748)),
 .UNSPECIFIED.,.F.,.F.,.F.,(4,4),(4,1,1,1,1,1,1,1,1,1,1,1,1,1,1,1,1,1,1,
1,1,1,1,1,1,1,1,1,1,1,1,1,1,1,1,1,1,1,1,1,1,1,1,1,1,1,1,1,1,1,1,1,1,1,1,
1,1,1,1,1,1,1,1,1,1,1,1,1,1,1,1,1,1,1,1,1,1,1,1,1,1,1,1,1,1,1,1,1,1,1,1,
1,1,1,1,1,1,1,1,1,1,1,1,1,1,1,1,1,1,1,1,1,1,1,1,1,1,1,1,1,1,1,1,1,1,1,1,
1,1,1,1,1,1,1,1,1,1,1,1,1,1,1,1,1,1,1,1,1,1,1,1,1,1,1,1,1,1,1,1,1,1,1,1,
1,1,1,1,1,1,1,1,1,1,1,1,1,1,1,1,1,1,1,1,1,1,1,1,1,1,1,1,1,1,1,1,1,1,1,1,
1,1,1,1,1,1,1,1,1,1,1,1,1,1,1,1,1,1,1,1,1,1,1,1,1,1,1,1,1,1,1,1,1,1,1,1,
1,1,1,1,1,1,1,1,1,1,1,1,1,1,1,1,1,1,1,1,1,1,1,1,1,1,1,1,1,1,1,1,1,1,1,1,
1,1,1,1,1,1,1,1,1,1,1,1,1,1,1,1,1,1,1,1,1,1,1,1,1,1,1,1,1,1,1,1,1,1,1,1,
1,1,1,1,1,1,1,1,1,1,1,1,1,1,1,1,1,1,1,1,1,1,1,1,1,1,1,1,1,1,1,1,1,1,1,1,
1,1,1,1,1,1,1,1,1,1,1,1,1,1,1,1,1,1,1,1,1,1,1,1,1,1,1,1,1,1,1,1,1,1,1,1,
1,1,1,1,1,1,1,1,1,1,1,1,1,1,1,1,1,1,1,1,1,1,1,1,1,1,1,1,1,1,1,1,1,1,1,1,
1,1,1,1,1,1,1,1,1,1,1,1,1,1,1,1,1,1,1,1,1,1,1,1,1,1,1,1,1,1,1,1,1,1,1,1,
1,1,1,1,1,1,1,1,1,1,1,1,1,1,1,1,1,1,1,1,1,1,1,1,1,1,1,1,1,1,1,1,1,1,1,1,
1,1,1,1,1,1,1,1,1,1,1,1,1,1,1,1,1,1,1,1,1,1,1,1,1,1,1,1,1,1,1,1,1,1,1,1,
1,1,1,1,1,1,1,1,1,1,1,1,1,1,1,1,1,1,1,1,1,1,1,1,1,1,1,1,1,1,4),(0.,0.0820126057383858),
(11.6152142277561,12.6148616296348,13.6145090315135,14.6141564333922,15.6138038352709,
16.6134512371495,17.6130986390282,18.6127460409069,19.6123934427856,20.6120408446643,
21.611688246543,22.6113356484216,23.6109830503003,24.610630452179,25.6102778540577,
26.6099252559364,27.6095726578151,28.6092200596937,29.6088674615724,30.6085148634511,
31.6081622653298,32.6078096672085,33.6074570690872,34.6071044709659,35.6067518728445,
36.6063992747232,37.6060466766019,38.6056940784806,39.6053414803593,40.604988882238,
41.6046362841166,42.6042836859953,43.603931087874,44.6035784897527,45.6032258916314,
46.6028732935101,47.6025206953887,48.6021680972674,49.6018154991461,50.6014629010248,
51.6011103029035,52.6007577047822,53.6004051066608,54.6000525085395,55.5996999104182,
56.5993473122969,57.5989947141756,58.5986421160543,59.5982895179329,60.5979369198116,
61.5975843216903,62.597231723569,63.5968791254477,64.5965265273264,65.5961739292051,
66.5958213310837,67.5954687329624,68.5951161348411,69.5947635367198,70.5944109385985,
71.5940583404772,72.5937057423558,73.5933531442345,74.5930005461132,75.5926479479919,
76.5922953498706,77.5919427517493,78.5915901536279,79.5912375555066,80.5908849573853,
81.590532359264,82.5901797611427,83.5898271630214,84.5894745649001,85.5891219667787,
86.5887693686574,87.5884167705361,88.5880641724148,89.5877115742935,90.5873589761722,
91.5870063780508,92.5866537799295,93.5863011818082,94.5859485836869,95.5855959855656,
96.5852433874443,97.5848907893229,98.5845381912016,99.5841855930803,100.583832994959,
101.583480396838,102.583127798716,103.582775200595,104.582422602474,105.582070004352,
106.581717406231,107.58136480811,108.581012209988,109.580659611867,110.580307013746,
111.579954415625,112.579601817503,113.579249219382,114.578896621261,115.578544023139,
116.578191425018,117.577838826897,118.577486228775,119.577133630654,120.576781032533,
121.576428434411,122.57607583629,123.575723238169,124.575370640047,125.575018041926,
126.574665443805,127.574312845683,128.573960247562,129.573607649441,130.57325505132,
131.572902453198,132.572549855077,133.572197256956,134.571844658834,135.571492060713,
136.571139462592,137.57078686447,138.570434266349,139.570081668228,140.569729070106,
141.569376471985,142.569023873864,143.568671275742,144.568318677621,145.5679660795,
146.567613481378,147.567260883257,148.566908285136,149.566555687014,150.566203088893,
151.565850490772,152.565497892651,153.565145294529,154.564792696408,155.564440098287,
156.564087500165,157.563734902044,158.563382303923,159.563029705801,160.56267710768,
161.562324509559,162.561971911437,163.561619313316,164.561266715195,165.560914117073,
166.560561518952,167.560208920831,168.559856322709,169.559503724588,170.559151126467,
171.558798528346,172.558445930224,173.558093332103,174.557740733982,175.55738813586,
176.557035537739,177.556682939618,178.556330341496,179.555977743375,180.555625145254,
181.555272547132,182.554919949011,183.55456735089,184.554214752768,185.553862154647,
186.553509556526,187.553156958405,188.552804360283,189.552451762162,190.552099164041,
191.551746565919,192.551393967798,193.551041369677,194.550688771555,195.550336173434,
196.549983575313,197.549630977191,198.54927837907,199.548925780949,200.548573182827,
201.548220584706,202.547867986585,203.547515388463,204.547162790342,205.546810192221,
206.5464575941,207.546104995978,208.545752397857,209.545399799736,210.545047201614,
211.544694603493,212.544342005372,213.54398940725,214.543636809129,215.543284211008,
216.542931612886,217.542579014765,218.542226416644,219.541873818522,220.541521220401,
221.54116862228,222.540816024158,223.540463426037,224.540110827916,225.539758229795,
226.539405631673,227.539053033552,228.538700435431,229.538347837309,230.537995239188,
231.537642641067,232.537290042945,233.536937444824,234.536584846703,235.536232248581,
236.53587965046,237.535527052339,238.535174454217,239.534821856096,240.534469257975,
241.534116659853,242.533764061732,243.533411463611,244.533058865489,245.532706267368,
246.532353669247,247.532001071126,248.531648473004,249.531295874883,250.530943276762,
251.53059067864,252.530238080519,253.529885482398,254.529532884276,255.529180286155,
256.528827688034,257.528475089912,258.528122491791,259.52776989367,260.527417295548,
261.527064697427,262.526712099306,263.526359501184,264.526006903063,265.525654304942,
266.525301706821,267.524949108699,268.524596510578,269.524243912457,270.523891314335,
271.523538716214,272.523186118093,273.522833519971,274.52248092185,275.522128323729,
276.521775725607,277.521423127486,278.521070529365,279.520717931243,280.520365333122,
281.520012735001,282.519660136879,283.519307538758,284.518954940637,285.518602342516,
286.518249744394,287.517897146273,288.517544548152,289.51719195003,290.516839351909,
291.516486753788,292.516134155666,293.515781557545,294.515428959424,295.515076361302,
296.514723763181,297.51437116506,298.514018566938,299.513665968817,300.513313370696,
301.512960772574,302.512608174453,303.512255576332,304.511902978211,305.511550380089,
306.511197781968,307.510845183847,308.510492585725,309.510139987604,310.509787389483,
311.509434791361,312.50908219324,313.508729595119,314.508376996997,315.508024398876,
316.507671800755,317.507319202633,318.506966604512,319.506614006391,320.506261408269,
321.505908810148,322.505556212027,323.505203613906,324.504851015784,325.504498417663,
326.504145819542,327.50379322142,328.503440623299,329.503088025178,330.502735427056,
331.502382828935,332.502030230814,333.501677632692,334.501325034571,335.50097243645,
336.500619838328,337.500267240207,338.499914642086,339.499562043964,340.499209445843,
341.498856847722,342.498504249601,343.498151651479,344.497799053358,345.497446455237,
346.497093857115,347.496741258994,348.496388660873,349.496036062751,350.49568346463,
351.495330866509,352.494978268387,353.494625670266,354.494273072145,355.493920474023,
356.493567875902,357.493215277781,358.492862679659,359.492510081538,360.492157483417,
361.491804885295,362.491452287174,363.491099689053,364.490747090932,365.49039449281,
366.490041894689,367.489689296568,368.489336698446,369.488984100325,370.488631502204,
371.488278904082,372.487926305961,373.48757370784,374.487221109718,375.486868511597,
376.486515913476,377.486163315354,378.485810717233,379.485458119112,380.48510552099,
381.484752922869,382.484400324748,383.484047726626,384.483695128505,385.483342530384,
386.482989932263,387.482637334141,388.48228473602,389.481932137899,390.481579539777,
391.481226941656,392.480874343535,393.480521745413,394.480169147292,395.479816549171,
396.479463951049,397.479111352928,398.478758754807,399.478406156685,400.478053558564,
401.477700960443,402.477348362322,403.4769957642,404.476643166079,405.476290567958,
406.475937969836,407.475585371715,408.475232773594,409.474880175472,410.474527577351,
411.47417497923,412.473822381108,413.473469782987,414.473117184866,415.472764586744,
416.472411988623,417.472059390502,418.47170679238,419.471354194259,420.471001596138,
421.470648998017,422.470296399895,423.469943801774,424.469591203653,425.469238605531,
426.46888600741,427.468533409289,428.468180811167,429.467828213046,430.467475614925,
431.467123016803,432.466770418682,433.466417820561,434.466065222439,435.465712624318,
436.465360026197,437.465007428075,438.464654829954,439.464302231833,440.463949633712,
441.46359703559,442.463244437469,443.462891839348,444.462539241226,445.462186643105,
446.461834044984,447.461481446862,448.461128848741,449.46077625062,450.460423652498,
451.460071054377,452.459718456256,453.459365858134,454.459013260013,455.458660661892,
456.45830806377,457.457955465649,458.457602867528,459.457250269407,460.456897671285,
461.456545073164,462.456192475043,463.455839876921,464.4554872788,465.455134680679,
466.454782082557,467.454429484436,468.454076886315,469.453724288193,470.453371690072,
471.453019091951,472.452666493829,473.452313895708,474.451961297587,475.451608699465,
476.451256101344,477.450903503223,478.450550905102,479.45019830698,480.449845708859,
481.449493110738,482.449140512616,483.448787914495,484.448435316374,485.448082718252,
486.447730120131,487.44737752201,488.447024923888,489.446672325767,490.446319727646,
491.445967129524,492.445614531403,493.445261933282,494.44490933516,495.444556737039,
496.444204138918,497.443851540797,498.443498942675,499.443146344554,500.442793746433,
501.442441148311,502.44208855019,503.441735952069,504.441383353947,505.441030755826,
506.440678157705,507.440325559583,508.439972961462,509.439620363341,510.439267765219,
511.438915167098,512.438562568977,513.438209970855,514.437857372734,515.437504774613,
516.437152176492,517.43679957837,518.436446980249,519.436094382128,520.435741784006,
521.435389185885,522.435036587764,523.434683989642,524.434331391521,525.4339787934,
526.433626195278,527.433273597157,528.432920999036,529.432568400914,530.432215802793,
531.431863204672,532.431510606551,533.431158008429,534.430805410308,535.430452812187,
536.430100214065,537.429747615944,538.429395017823,539.429042419701,540.42868982158,
541.428337223459,542.427984625337,543.427632027216,544.427279429095,545.426926830973,
546.426574232852,547.426221634731,548.425869036609,549.425516438488,550.425163840367,
551.424811242245,552.424458644124,553.424106046003,554.423753447881,555.42340084976,
556.423048251639,557.422695653518,558.422343055396,559.421990457275,560.421637859154,
561.421285261032,562.420932662911,563.42058006479,564.420227466668),
 .UNSPECIFIED.);
#561=FACE_BOUND('',#3854,.T.);
#650=CONICAL_SURFACE('',#18672,7.25527674973257,1.046630884618);
#651=CONICAL_SURFACE('',#18685,3.75,0.785398163397442);
#1205=CIRCLE('',#18489,3.933);
#1206=CIRCLE('',#18578,3.22275);
#1207=CIRCLE('',#18580,3.22275);
#1208=CIRCLE('',#18668,3.933);
#1209=CIRCLE('',#18669,3.933);
#1210=CIRCLE('',#18670,3.22275);
#1211=CIRCLE('',#18673,6.17797863635533);
#1212=CIRCLE('',#18678,3.933);
#1213=CIRCLE('',#18684,3.5);
#1582=CYLINDRICAL_SURFACE('',#18488,3.933);
#1583=CYLINDRICAL_SURFACE('',#18490,3.933);
#1584=CYLINDRICAL_SURFACE('',#18491,3.933);
#1585=CYLINDRICAL_SURFACE('',#18492,3.933);
#1586=CYLINDRICAL_SURFACE('',#18493,3.933);
#1587=CYLINDRICAL_SURFACE('',#18494,3.933);
#1588=CYLINDRICAL_SURFACE('',#18495,3.933);
#1589=CYLINDRICAL_SURFACE('',#18496,3.933);
#1590=CYLINDRICAL_SURFACE('',#18497,3.933);
#1591=CYLINDRICAL_SURFACE('',#18498,3.933);
#1592=CYLINDRICAL_SURFACE('',#18499,3.933);
#1593=CYLINDRICAL_SURFACE('',#18500,3.933);
#1594=CYLINDRICAL_SURFACE('',#18501,3.933);
#1595=CYLINDRICAL_SURFACE('',#18502,3.933);
#1596=CYLINDRICAL_SURFACE('',#18503,3.933);
#1597=CYLINDRICAL_SURFACE('',#18504,3.933);
#1598=CYLINDRICAL_SURFACE('',#18505,3.933);
#1599=CYLINDRICAL_SURFACE('',#18506,3.933);
#1600=CYLINDRICAL_SURFACE('',#18507,3.933);
#1601=CYLINDRICAL_SURFACE('',#18508,3.933);
#1602=CYLINDRICAL_SURFACE('',#18509,3.933);
#1603=CYLINDRICAL_SURFACE('',#18510,3.933);
#1604=CYLINDRICAL_SURFACE('',#18511,3.933);
#1605=CYLINDRICAL_SURFACE('',#18512,3.933);
#1606=CYLINDRICAL_SURFACE('',#18513,3.933);
#1607=CYLINDRICAL_SURFACE('',#18514,3.933);
#1608=CYLINDRICAL_SURFACE('',#18515,3.933);
#1609=CYLINDRICAL_SURFACE('',#18516,3.933);
#1610=CYLINDRICAL_SURFACE('',#18517,3.933);
#1611=CYLINDRICAL_SURFACE('',#18518,3.933);
#1612=CYLINDRICAL_SURFACE('',#18519,3.933);
#1613=CYLINDRICAL_SURFACE('',#18520,3.933);
#1614=CYLINDRICAL_SURFACE('',#18521,3.933);
#1615=CYLINDRICAL_SURFACE('',#18522,3.933);
#1616=CYLINDRICAL_SURFACE('',#18523,3.933);
#1617=CYLINDRICAL_SURFACE('',#18524,3.933);
#1618=CYLINDRICAL_SURFACE('',#18525,3.933);
#1619=CYLINDRICAL_SURFACE('',#18526,3.933);
#1620=CYLINDRICAL_SURFACE('',#18527,3.933);
#1621=CYLINDRICAL_SURFACE('',#18528,3.933);
#1622=CYLINDRICAL_SURFACE('',#18529,3.933);
#1623=CYLINDRICAL_SURFACE('',#18530,3.933);
#1624=CYLINDRICAL_SURFACE('',#18531,3.933);
#1625=CYLINDRICAL_SURFACE('',#18532,3.933);
#1626=CYLINDRICAL_SURFACE('',#18533,3.933);
#1627=CYLINDRICAL_SURFACE('',#18534,3.933);
#1628=CYLINDRICAL_SURFACE('',#18535,3.933);
#1629=CYLINDRICAL_SURFACE('',#18536,3.933);
#1630=CYLINDRICAL_SURFACE('',#18537,3.933);
#1631=CYLINDRICAL_SURFACE('',#18538,3.933);
#1632=CYLINDRICAL_SURFACE('',#18539,3.933);
#1633=CYLINDRICAL_SURFACE('',#18540,3.933);
#1634=CYLINDRICAL_SURFACE('',#18541,3.933);
#1635=CYLINDRICAL_SURFACE('',#18542,3.933);
#1636=CYLINDRICAL_SURFACE('',#18543,3.933);
#1637=CYLINDRICAL_SURFACE('',#18544,3.933);
#1638=CYLINDRICAL_SURFACE('',#18545,3.933);
#1639=CYLINDRICAL_SURFACE('',#18546,3.933);
#1640=CYLINDRICAL_SURFACE('',#18547,3.933);
#1641=CYLINDRICAL_SURFACE('',#18548,3.933);
#1642=CYLINDRICAL_SURFACE('',#18549,3.933);
#1643=CYLINDRICAL_SURFACE('',#18550,3.933);
#1644=CYLINDRICAL_SURFACE('',#18551,3.933);
#1645=CYLINDRICAL_SURFACE('',#18552,3.933);
#1646=CYLINDRICAL_SURFACE('',#18553,3.933);
#1647=CYLINDRICAL_SURFACE('',#18554,3.933);
#1648=CYLINDRICAL_SURFACE('',#18555,3.933);
#1649=CYLINDRICAL_SURFACE('',#18556,3.933);
#1650=CYLINDRICAL_SURFACE('',#18557,3.933);
#1651=CYLINDRICAL_SURFACE('',#18558,3.933);
#1652=CYLINDRICAL_SURFACE('',#18559,3.933);
#1653=CYLINDRICAL_SURFACE('',#18560,3.933);
#1654=CYLINDRICAL_SURFACE('',#18561,3.933);
#1655=CYLINDRICAL_SURFACE('',#18562,3.933);
#1656=CYLINDRICAL_SURFACE('',#18563,3.933);
#1657=CYLINDRICAL_SURFACE('',#18564,3.933);
#1658=CYLINDRICAL_SURFACE('',#18565,3.933);
#1659=CYLINDRICAL_SURFACE('',#18566,3.933);
#1660=CYLINDRICAL_SURFACE('',#18567,3.933);
#1661=CYLINDRICAL_SURFACE('',#18568,3.933);
#1662=CYLINDRICAL_SURFACE('',#18569,3.933);
#1663=CYLINDRICAL_SURFACE('',#18570,3.933);
#1664=CYLINDRICAL_SURFACE('',#18571,3.933);
#1665=CYLINDRICAL_SURFACE('',#18572,3.933);
#1666=CYLINDRICAL_SURFACE('',#18573,3.933);
#1667=CYLINDRICAL_SURFACE('',#18574,3.933);
#1668=CYLINDRICAL_SURFACE('',#18575,3.933);
#1669=CYLINDRICAL_SURFACE('',#18576,3.933);
#1670=CYLINDRICAL_SURFACE('',#18577,3.22275);
#1671=CYLINDRICAL_SURFACE('',#18579,3.22275);
#1672=CYLINDRICAL_SURFACE('',#18581,3.22275);
#1673=CYLINDRICAL_SURFACE('',#18582,3.22275);
#1674=CYLINDRICAL_SURFACE('',#18583,3.22275);
#1675=CYLINDRICAL_SURFACE('',#18584,3.22275);
#1676=CYLINDRICAL_SURFACE('',#18585,3.22275);
#1677=CYLINDRICAL_SURFACE('',#18586,3.22275);
#1678=CYLINDRICAL_SURFACE('',#18587,3.22275);
#1679=CYLINDRICAL_SURFACE('',#18588,3.22275);
#1680=CYLINDRICAL_SURFACE('',#18589,3.22275);
#1681=CYLINDRICAL_SURFACE('',#18590,3.22275);
#1682=CYLINDRICAL_SURFACE('',#18591,3.22275);
#1683=CYLINDRICAL_SURFACE('',#18592,3.22275);
#1684=CYLINDRICAL_SURFACE('',#18593,3.22275);
#1685=CYLINDRICAL_SURFACE('',#18594,3.22275);
#1686=CYLINDRICAL_SURFACE('',#18595,3.22275);
#1687=CYLINDRICAL_SURFACE('',#18596,3.22275);
#1688=CYLINDRICAL_SURFACE('',#18597,3.22275);
#1689=CYLINDRICAL_SURFACE('',#18598,3.22275);
#1690=CYLINDRICAL_SURFACE('',#18599,3.22275);
#1691=CYLINDRICAL_SURFACE('',#18600,3.22275);
#1692=CYLINDRICAL_SURFACE('',#18601,3.22275);
#1693=CYLINDRICAL_SURFACE('',#18602,3.22275);
#1694=CYLINDRICAL_SURFACE('',#18603,3.22275);
#1695=CYLINDRICAL_SURFACE('',#18604,3.22275);
#1696=CYLINDRICAL_SURFACE('',#18605,3.22275);
#1697=CYLINDRICAL_SURFACE('',#18606,3.22275);
#1698=CYLINDRICAL_SURFACE('',#18607,3.22275);
#1699=CYLINDRICAL_SURFACE('',#18608,3.22275);
#1700=CYLINDRICAL_SURFACE('',#18609,3.22275);
#1701=CYLINDRICAL_SURFACE('',#18610,3.22275);
#1702=CYLINDRICAL_SURFACE('',#18611,3.22275);
#1703=CYLINDRICAL_SURFACE('',#18612,3.22275);
#1704=CYLINDRICAL_SURFACE('',#18613,3.22275);
#1705=CYLINDRICAL_SURFACE('',#18614,3.22275);
#1706=CYLINDRICAL_SURFACE('',#18615,3.22275);
#1707=CYLINDRICAL_SURFACE('',#18616,3.22275);
#1708=CYLINDRICAL_SURFACE('',#18617,3.22275);
#1709=CYLINDRICAL_SURFACE('',#18618,3.22275);
#1710=CYLINDRICAL_SURFACE('',#18619,3.22275);
#1711=CYLINDRICAL_SURFACE('',#18620,3.22275);
#1712=CYLINDRICAL_SURFACE('',#18621,3.22275);
#1713=CYLINDRICAL_SURFACE('',#18622,3.22275);
#1714=CYLINDRICAL_SURFACE('',#18623,3.22275);
#1715=CYLINDRICAL_SURFACE('',#18624,3.22275);
#1716=CYLINDRICAL_SURFACE('',#18625,3.22275);
#1717=CYLINDRICAL_SURFACE('',#18626,3.22275);
#1718=CYLINDRICAL_SURFACE('',#18627,3.22275);
#1719=CYLINDRICAL_SURFACE('',#18628,3.22275);
#1720=CYLINDRICAL_SURFACE('',#18629,3.22275);
#1721=CYLINDRICAL_SURFACE('',#18630,3.22275);
#1722=CYLINDRICAL_SURFACE('',#18631,3.22275);
#1723=CYLINDRICAL_SURFACE('',#18632,3.22275);
#1724=CYLINDRICAL_SURFACE('',#18633,3.22275);
#1725=CYLINDRICAL_SURFACE('',#18634,3.22275);
#1726=CYLINDRICAL_SURFACE('',#18635,3.22275);
#1727=CYLINDRICAL_SURFACE('',#18636,3.22275);
#1728=CYLINDRICAL_SURFACE('',#18637,3.22275);
#1729=CYLINDRICAL_SURFACE('',#18638,3.22275);
#1730=CYLINDRICAL_SURFACE('',#18639,3.22275);
#1731=CYLINDRICAL_SURFACE('',#18640,3.22275);
#1732=CYLINDRICAL_SURFACE('',#18641,3.22275);
#1733=CYLINDRICAL_SURFACE('',#18642,3.22275);
#1734=CYLINDRICAL_SURFACE('',#18643,3.22275);
#1735=CYLINDRICAL_SURFACE('',#18644,3.22275);
#1736=CYLINDRICAL_SURFACE('',#18645,3.22275);
#1737=CYLINDRICAL_SURFACE('',#18646,3.22275);
#1738=CYLINDRICAL_SURFACE('',#18647,3.22275);
#1739=CYLINDRICAL_SURFACE('',#18648,3.22275);
#1740=CYLINDRICAL_SURFACE('',#18649,3.22275);
#1741=CYLINDRICAL_SURFACE('',#18650,3.22275);
#1742=CYLINDRICAL_SURFACE('',#18651,3.22275);
#1743=CYLINDRICAL_SURFACE('',#18652,3.22275);
#1744=CYLINDRICAL_SURFACE('',#18653,3.22275);
#1745=CYLINDRICAL_SURFACE('',#18654,3.22275);
#1746=CYLINDRICAL_SURFACE('',#18655,3.22275);
#1747=CYLINDRICAL_SURFACE('',#18656,3.22275);
#1748=CYLINDRICAL_SURFACE('',#18657,3.22275);
#1749=CYLINDRICAL_SURFACE('',#18658,3.22275);
#1750=CYLINDRICAL_SURFACE('',#18659,3.22275);
#1751=CYLINDRICAL_SURFACE('',#18660,3.22275);
#1752=CYLINDRICAL_SURFACE('',#18661,3.22275);
#1753=CYLINDRICAL_SURFACE('',#18662,3.22275);
#1754=CYLINDRICAL_SURFACE('',#18663,3.22275);
#1755=CYLINDRICAL_SURFACE('',#18664,3.22275);
#1756=CYLINDRICAL_SURFACE('',#18665,3.22275);
#1757=CYLINDRICAL_SURFACE('',#18666,3.22275);
#1758=CYLINDRICAL_SURFACE('',#18671,3.22275);
#1759=CYLINDRICAL_SURFACE('',#18686,3.933);
#1785=(
BOUNDED_CURVE()
B_SPLINE_CURVE(2,(#55860,#55861,#55862),.UNSPECIFIED.,.F.,.F.)
B_SPLINE_CURVE_WITH_KNOTS((3,3),(0.149747849205877,0.971656649213287),
 .UNSPECIFIED.)
CURVE()
GEOMETRIC_REPRESENTATION_ITEM()
RATIONAL_B_SPLINE_CURVE((1.07140024848293,1.23714644374248,1.07140024848293))
REPRESENTATION_ITEM('')
);
#1786=(
BOUNDED_CURVE()
B_SPLINE_CURVE(2,(#55864,#55865,#55866),.UNSPECIFIED.,.F.,.F.)
B_SPLINE_CURVE_WITH_KNOTS((3,3),(0.149747849205876,0.971656649213287),
 .UNSPECIFIED.)
CURVE()
GEOMETRIC_REPRESENTATION_ITEM()
RATIONAL_B_SPLINE_CURVE((1.07140024848293,1.23714644374248,1.07140024848293))
REPRESENTATION_ITEM('')
);
#1787=(
BOUNDED_CURVE()
B_SPLINE_CURVE(2,(#55868,#55869,#55870),.UNSPECIFIED.,.F.,.F.)
B_SPLINE_CURVE_WITH_KNOTS((3,3),(0.149747849205877,0.971656649213287),
 .UNSPECIFIED.)
CURVE()
GEOMETRIC_REPRESENTATION_ITEM()
RATIONAL_B_SPLINE_CURVE((1.07140024848293,1.23714644374248,1.07140024848293))
REPRESENTATION_ITEM('')
);
#1788=(
BOUNDED_CURVE()
B_SPLINE_CURVE(2,(#55872,#55873,#55874),.UNSPECIFIED.,.F.,.F.)
B_SPLINE_CURVE_WITH_KNOTS((3,3),(0.149747849205876,0.971656649213287),
 .UNSPECIFIED.)
CURVE()
GEOMETRIC_REPRESENTATION_ITEM()
RATIONAL_B_SPLINE_CURVE((1.07140024848293,1.23714644374248,1.07140024848293))
REPRESENTATION_ITEM('')
);
#1789=(
BOUNDED_CURVE()
B_SPLINE_CURVE(2,(#55876,#55877,#55878),.UNSPECIFIED.,.F.,.F.)
B_SPLINE_CURVE_WITH_KNOTS((3,3),(0.560702249209475,0.971656649213286),
 .UNSPECIFIED.)
CURVE()
GEOMETRIC_REPRESENTATION_ITEM()
RATIONAL_B_SPLINE_CURVE((1.1542733461127,1.15427334611272,1.07140024848293))
REPRESENTATION_ITEM('')
);
#1790=(
BOUNDED_CURVE()
B_SPLINE_CURVE(2,(#55883,#55884,#55885),.UNSPECIFIED.,.F.,.F.)
B_SPLINE_CURVE_WITH_KNOTS((3,3),(0.149747849205877,0.560702249209475),
 .UNSPECIFIED.)
CURVE()
GEOMETRIC_REPRESENTATION_ITEM()
RATIONAL_B_SPLINE_CURVE((1.07140024848293,1.15427334611268,1.1542733461127))
REPRESENTATION_ITEM('')
);
#1791=(
BOUNDED_CURVE()
B_SPLINE_CURVE(2,(#55886,#55887,#55888),.UNSPECIFIED.,.F.,.F.)
B_SPLINE_CURVE_WITH_KNOTS((3,3),(0.149747849205877,0.971656649213287),
 .UNSPECIFIED.)
CURVE()
GEOMETRIC_REPRESENTATION_ITEM()
RATIONAL_B_SPLINE_CURVE((1.07140024848293,1.23714644374248,1.07140024848293))
REPRESENTATION_ITEM('')
);
#2549=FACE_OUTER_BOUND('',#3669,.T.);
#2550=FACE_OUTER_BOUND('',#3670,.T.);
#2551=FACE_OUTER_BOUND('',#3671,.T.);
#2552=FACE_OUTER_BOUND('',#3672,.T.);
#2553=FACE_OUTER_BOUND('',#3673,.T.);
#2554=FACE_OUTER_BOUND('',#3674,.T.);
#2555=FACE_OUTER_BOUND('',#3675,.T.);
#2556=FACE_OUTER_BOUND('',#3676,.T.);
#2557=FACE_OUTER_BOUND('',#3677,.T.);
#2558=FACE_OUTER_BOUND('',#3678,.T.);
#2559=FACE_OUTER_BOUND('',#3679,.T.);
#2560=FACE_OUTER_BOUND('',#3680,.T.);
#2561=FACE_OUTER_BOUND('',#3681,.T.);
#2562=FACE_OUTER_BOUND('',#3682,.T.);
#2563=FACE_OUTER_BOUND('',#3683,.T.);
#2564=FACE_OUTER_BOUND('',#3684,.T.);
#2565=FACE_OUTER_BOUND('',#3685,.T.);
#2566=FACE_OUTER_BOUND('',#3686,.T.);
#2567=FACE_OUTER_BOUND('',#3687,.T.);
#2568=FACE_OUTER_BOUND('',#3688,.T.);
#2569=FACE_OUTER_BOUND('',#3689,.T.);
#2570=FACE_OUTER_BOUND('',#3690,.T.);
#2571=FACE_OUTER_BOUND('',#3691,.T.);
#2572=FACE_OUTER_BOUND('',#3692,.T.);
#2573=FACE_OUTER_BOUND('',#3693,.T.);
#2574=FACE_OUTER_BOUND('',#3694,.T.);
#2575=FACE_OUTER_BOUND('',#3695,.T.);
#2576=FACE_OUTER_BOUND('',#3696,.T.);
#2577=FACE_OUTER_BOUND('',#3697,.T.);
#2578=FACE_OUTER_BOUND('',#3698,.T.);
#2579=FACE_OUTER_BOUND('',#3699,.T.);
#2580=FACE_OUTER_BOUND('',#3700,.T.);
#2581=FACE_OUTER_BOUND('',#3701,.T.);
#2582=FACE_OUTER_BOUND('',#3702,.T.);
#2583=FACE_OUTER_BOUND('',#3703,.T.);
#2584=FACE_OUTER_BOUND('',#3704,.T.);
#2585=FACE_OUTER_BOUND('',#3705,.T.);
#2586=FACE_OUTER_BOUND('',#3706,.T.);
#2587=FACE_OUTER_BOUND('',#3707,.T.);
#2588=FACE_OUTER_BOUND('',#3708,.T.);
#2589=FACE_OUTER_BOUND('',#3709,.T.);
#2590=FACE_OUTER_BOUND('',#3710,.T.);
#2591=FACE_OUTER_BOUND('',#3711,.T.);
#2592=FACE_OUTER_BOUND('',#3712,.T.);
#2593=FACE_OUTER_BOUND('',#3713,.T.);
#2594=FACE_OUTER_BOUND('',#3714,.T.);
#2595=FACE_OUTER_BOUND('',#3715,.T.);
#2596=FACE_OUTER_BOUND('',#3716,.T.);
#2597=FACE_OUTER_BOUND('',#3717,.T.);
#2598=FACE_OUTER_BOUND('',#3718,.T.);
#2599=FACE_OUTER_BOUND('',#3719,.T.);
#2600=FACE_OUTER_BOUND('',#3720,.T.);
#2601=FACE_OUTER_BOUND('',#3721,.T.);
#2602=FACE_OUTER_BOUND('',#3722,.T.);
#2603=FACE_OUTER_BOUND('',#3723,.T.);
#2604=FACE_OUTER_BOUND('',#3724,.T.);
#2605=FACE_OUTER_BOUND('',#3725,.T.);
#2606=FACE_OUTER_BOUND('',#3726,.T.);
#2607=FACE_OUTER_BOUND('',#3727,.T.);
#2608=FACE_OUTER_BOUND('',#3728,.T.);
#2609=FACE_OUTER_BOUND('',#3729,.T.);
#2610=FACE_OUTER_BOUND('',#3730,.T.);
#2611=FACE_OUTER_BOUND('',#3731,.T.);
#2612=FACE_OUTER_BOUND('',#3732,.T.);
#2613=FACE_OUTER_BOUND('',#3733,.T.);
#2614=FACE_OUTER_BOUND('',#3734,.T.);
#2615=FACE_OUTER_BOUND('',#3735,.T.);
#2616=FACE_OUTER_BOUND('',#3736,.T.);
#2617=FACE_OUTER_BOUND('',#3737,.T.);
#2618=FACE_OUTER_BOUND('',#3738,.T.);
#2619=FACE_OUTER_BOUND('',#3739,.T.);
#2620=FACE_OUTER_BOUND('',#3740,.T.);
#2621=FACE_OUTER_BOUND('',#3741,.T.);
#2622=FACE_OUTER_BOUND('',#3742,.T.);
#2623=FACE_OUTER_BOUND('',#3743,.T.);
#2624=FACE_OUTER_BOUND('',#3744,.T.);
#2625=FACE_OUTER_BOUND('',#3745,.T.);
#2626=FACE_OUTER_BOUND('',#3746,.T.);
#2627=FACE_OUTER_BOUND('',#3747,.T.);
#2628=FACE_OUTER_BOUND('',#3748,.T.);
#2629=FACE_OUTER_BOUND('',#3749,.T.);
#2630=FACE_OUTER_BOUND('',#3750,.T.);
#2631=FACE_OUTER_BOUND('',#3751,.T.);
#2632=FACE_OUTER_BOUND('',#3752,.T.);
#2633=FACE_OUTER_BOUND('',#3753,.T.);
#2634=FACE_OUTER_BOUND('',#3754,.T.);
#2635=FACE_OUTER_BOUND('',#3755,.T.);
#2636=FACE_OUTER_BOUND('',#3756,.T.);
#2637=FACE_OUTER_BOUND('',#3757,.T.);
#2638=FACE_OUTER_BOUND('',#3758,.T.);
#2639=FACE_OUTER_BOUND('',#3759,.T.);
#2640=FACE_OUTER_BOUND('',#3760,.T.);
#2641=FACE_OUTER_BOUND('',#3761,.T.);
#2642=FACE_OUTER_BOUND('',#3762,.T.);
#2643=FACE_OUTER_BOUND('',#3763,.T.);
#2644=FACE_OUTER_BOUND('',#3764,.T.);
#2645=FACE_OUTER_BOUND('',#3765,.T.);
#2646=FACE_OUTER_BOUND('',#3766,.T.);
#2647=FACE_OUTER_BOUND('',#3767,.T.);
#2648=FACE_OUTER_BOUND('',#3768,.T.);
#2649=FACE_OUTER_BOUND('',#3769,.T.);
#2650=FACE_OUTER_BOUND('',#3770,.T.);
#2651=FACE_OUTER_BOUND('',#3771,.T.);
#2652=FACE_OUTER_BOUND('',#3772,.T.);
#2653=FACE_OUTER_BOUND('',#3773,.T.);
#2654=FACE_OUTER_BOUND('',#3774,.T.);
#2655=FACE_OUTER_BOUND('',#3775,.T.);
#2656=FACE_OUTER_BOUND('',#3776,.T.);
#2657=FACE_OUTER_BOUND('',#3777,.T.);
#2658=FACE_OUTER_BOUND('',#3778,.T.);
#2659=FACE_OUTER_BOUND('',#3779,.T.);
#2660=FACE_OUTER_BOUND('',#3780,.T.);
#2661=FACE_OUTER_BOUND('',#3781,.T.);
#2662=FACE_OUTER_BOUND('',#3782,.T.);
#2663=FACE_OUTER_BOUND('',#3783,.T.);
#2664=FACE_OUTER_BOUND('',#3784,.T.);
#2665=FACE_OUTER_BOUND('',#3785,.T.);
#2666=FACE_OUTER_BOUND('',#3786,.T.);
#2667=FACE_OUTER_BOUND('',#3787,.T.);
#2668=FACE_OUTER_BOUND('',#3788,.T.);
#2669=FACE_OUTER_BOUND('',#3789,.T.);
#2670=FACE_OUTER_BOUND('',#3790,.T.);
#2671=FACE_OUTER_BOUND('',#3791,.T.);
#2672=FACE_OUTER_BOUND('',#3792,.T.);
#2673=FACE_OUTER_BOUND('',#3793,.T.);
#2674=FACE_OUTER_BOUND('',#3794,.T.);
#2675=FACE_OUTER_BOUND('',#3795,.T.);
#2676=FACE_OUTER_BOUND('',#3796,.T.);
#2677=FACE_OUTER_BOUND('',#3797,.T.);
#2678=FACE_OUTER_BOUND('',#3798,.T.);
#2679=FACE_OUTER_BOUND('',#3799,.T.);
#2680=FACE_OUTER_BOUND('',#3800,.T.);
#2681=FACE_OUTER_BOUND('',#3801,.T.);
#2682=FACE_OUTER_BOUND('',#3802,.T.);
#2683=FACE_OUTER_BOUND('',#3803,.T.);
#2684=FACE_OUTER_BOUND('',#3804,.T.);
#2685=FACE_OUTER_BOUND('',#3805,.T.);
#2686=FACE_OUTER_BOUND('',#3806,.T.);
#2687=FACE_OUTER_BOUND('',#3807,.T.);
#2688=FACE_OUTER_BOUND('',#3808,.T.);
#2689=FACE_OUTER_BOUND('',#3809,.T.);
#2690=FACE_OUTER_BOUND('',#3810,.T.);
#2691=FACE_OUTER_BOUND('',#3811,.T.);
#2692=FACE_OUTER_BOUND('',#3812,.T.);
#2693=FACE_OUTER_BOUND('',#3813,.T.);
#2694=FACE_OUTER_BOUND('',#3814,.T.);
#2695=FACE_OUTER_BOUND('',#3815,.T.);
#2696=FACE_OUTER_BOUND('',#3816,.T.);
#2697=FACE_OUTER_BOUND('',#3817,.T.);
#2698=FACE_OUTER_BOUND('',#3818,.T.);
#2699=FACE_OUTER_BOUND('',#3819,.T.);
#2700=FACE_OUTER_BOUND('',#3820,.T.);
#2701=FACE_OUTER_BOUND('',#3821,.T.);
#2702=FACE_OUTER_BOUND('',#3822,.T.);
#2703=FACE_OUTER_BOUND('',#3823,.T.);
#2704=FACE_OUTER_BOUND('',#3824,.T.);
#2705=FACE_OUTER_BOUND('',#3825,.T.);
#2706=FACE_OUTER_BOUND('',#3826,.T.);
#2707=FACE_OUTER_BOUND('',#3827,.T.);
#2708=FACE_OUTER_BOUND('',#3828,.T.);
#2709=FACE_OUTER_BOUND('',#3829,.T.);
#2710=FACE_OUTER_BOUND('',#3830,.T.);
#2711=FACE_OUTER_BOUND('',#3831,.T.);
#2712=FACE_OUTER_BOUND('',#3832,.T.);
#2713=FACE_OUTER_BOUND('',#3833,.T.);
#2714=FACE_OUTER_BOUND('',#3834,.T.);
#2715=FACE_OUTER_BOUND('',#3835,.T.);
#2716=FACE_OUTER_BOUND('',#3836,.T.);
#2717=FACE_OUTER_BOUND('',#3837,.T.);
#2718=FACE_OUTER_BOUND('',#3838,.T.);
#2719=FACE_OUTER_BOUND('',#3839,.T.);
#2720=FACE_OUTER_BOUND('',#3840,.T.);
#2721=FACE_OUTER_BOUND('',#3841,.T.);
#2722=FACE_OUTER_BOUND('',#3842,.T.);
#2723=FACE_OUTER_BOUND('',#3843,.T.);
#2724=FACE_OUTER_BOUND('',#3844,.T.);
#2725=FACE_OUTER_BOUND('',#3845,.T.);
#2726=FACE_OUTER_BOUND('',#3846,.T.);
#2727=FACE_OUTER_BOUND('',#3847,.T.);
#2728=FACE_OUTER_BOUND('',#3848,.T.);
#2729=FACE_OUTER_BOUND('',#3849,.T.);
#2730=FACE_OUTER_BOUND('',#3850,.T.);
#2731=FACE_OUTER_BOUND('',#3851,.T.);
#2732=FACE_OUTER_BOUND('',#3852,.T.);
#2733=FACE_OUTER_BOUND('',#3853,.T.);
#2734=FACE_OUTER_BOUND('',#3855,.T.);
#2735=FACE_OUTER_BOUND('',#3856,.T.);
#2736=FACE_OUTER_BOUND('',#3857,.T.);
#2737=FACE_OUTER_BOUND('',#3858,.T.);
#2738=FACE_OUTER_BOUND('',#3859,.T.);
#2739=FACE_OUTER_BOUND('',#3860,.T.);
#2740=FACE_OUTER_BOUND('',#3861,.T.);
#3669=EDGE_LOOP('',(#14414,#14415,#14416,#14417));
#3670=EDGE_LOOP('',(#14418,#14419,#14420,#14421));
#3671=EDGE_LOOP('',(#14422,#14423,#14424,#14425));
#3672=EDGE_LOOP('',(#14426,#14427,#14428,#14429));
#3673=EDGE_LOOP('',(#14430,#14431,#14432,#14433));
#3674=EDGE_LOOP('',(#14434,#14435,#14436,#14437));
#3675=EDGE_LOOP('',(#14438,#14439,#14440,#14441));
#3676=EDGE_LOOP('',(#14442,#14443,#14444,#14445));
#3677=EDGE_LOOP('',(#14446,#14447,#14448,#14449));
#3678=EDGE_LOOP('',(#14450,#14451,#14452,#14453));
#3679=EDGE_LOOP('',(#14454,#14455,#14456,#14457));
#3680=EDGE_LOOP('',(#14458,#14459,#14460,#14461));
#3681=EDGE_LOOP('',(#14462,#14463,#14464,#14465));
#3682=EDGE_LOOP('',(#14466,#14467,#14468,#14469));
#3683=EDGE_LOOP('',(#14470,#14471,#14472,#14473));
#3684=EDGE_LOOP('',(#14474,#14475,#14476,#14477));
#3685=EDGE_LOOP('',(#14478,#14479,#14480,#14481));
#3686=EDGE_LOOP('',(#14482,#14483,#14484,#14485));
#3687=EDGE_LOOP('',(#14486,#14487,#14488,#14489));
#3688=EDGE_LOOP('',(#14490,#14491,#14492,#14493));
#3689=EDGE_LOOP('',(#14494,#14495,#14496,#14497));
#3690=EDGE_LOOP('',(#14498,#14499,#14500,#14501));
#3691=EDGE_LOOP('',(#14502,#14503,#14504,#14505));
#3692=EDGE_LOOP('',(#14506,#14507,#14508,#14509));
#3693=EDGE_LOOP('',(#14510,#14511,#14512,#14513));
#3694=EDGE_LOOP('',(#14514,#14515,#14516,#14517));
#3695=EDGE_LOOP('',(#14518,#14519,#14520,#14521));
#3696=EDGE_LOOP('',(#14522,#14523,#14524,#14525));
#3697=EDGE_LOOP('',(#14526,#14527,#14528,#14529));
#3698=EDGE_LOOP('',(#14530,#14531,#14532,#14533));
#3699=EDGE_LOOP('',(#14534,#14535,#14536,#14537));
#3700=EDGE_LOOP('',(#14538,#14539,#14540,#14541));
#3701=EDGE_LOOP('',(#14542,#14543,#14544,#14545));
#3702=EDGE_LOOP('',(#14546,#14547,#14548,#14549));
#3703=EDGE_LOOP('',(#14550,#14551,#14552,#14553));
#3704=EDGE_LOOP('',(#14554,#14555,#14556,#14557));
#3705=EDGE_LOOP('',(#14558,#14559,#14560,#14561));
#3706=EDGE_LOOP('',(#14562,#14563,#14564,#14565));
#3707=EDGE_LOOP('',(#14566,#14567,#14568,#14569));
#3708=EDGE_LOOP('',(#14570,#14571,#14572,#14573));
#3709=EDGE_LOOP('',(#14574,#14575,#14576,#14577));
#3710=EDGE_LOOP('',(#14578,#14579,#14580,#14581));
#3711=EDGE_LOOP('',(#14582,#14583,#14584,#14585));
#3712=EDGE_LOOP('',(#14586,#14587,#14588,#14589));
#3713=EDGE_LOOP('',(#14590,#14591,#14592,#14593));
#3714=EDGE_LOOP('',(#14594,#14595,#14596,#14597));
#3715=EDGE_LOOP('',(#14598,#14599,#14600,#14601));
#3716=EDGE_LOOP('',(#14602,#14603,#14604,#14605));
#3717=EDGE_LOOP('',(#14606,#14607,#14608,#14609));
#3718=EDGE_LOOP('',(#14610,#14611,#14612,#14613));
#3719=EDGE_LOOP('',(#14614,#14615,#14616,#14617));
#3720=EDGE_LOOP('',(#14618,#14619,#14620,#14621));
#3721=EDGE_LOOP('',(#14622,#14623,#14624,#14625));
#3722=EDGE_LOOP('',(#14626,#14627,#14628,#14629));
#3723=EDGE_LOOP('',(#14630,#14631,#14632,#14633));
#3724=EDGE_LOOP('',(#14634,#14635,#14636,#14637));
#3725=EDGE_LOOP('',(#14638,#14639,#14640,#14641));
#3726=EDGE_LOOP('',(#14642,#14643,#14644,#14645));
#3727=EDGE_LOOP('',(#14646,#14647,#14648,#14649));
#3728=EDGE_LOOP('',(#14650,#14651,#14652,#14653));
#3729=EDGE_LOOP('',(#14654,#14655,#14656,#14657));
#3730=EDGE_LOOP('',(#14658,#14659,#14660,#14661));
#3731=EDGE_LOOP('',(#14662,#14663,#14664,#14665));
#3732=EDGE_LOOP('',(#14666,#14667,#14668,#14669));
#3733=EDGE_LOOP('',(#14670,#14671,#14672,#14673));
#3734=EDGE_LOOP('',(#14674,#14675,#14676,#14677));
#3735=EDGE_LOOP('',(#14678,#14679,#14680,#14681));
#3736=EDGE_LOOP('',(#14682,#14683,#14684,#14685));
#3737=EDGE_LOOP('',(#14686,#14687,#14688,#14689));
#3738=EDGE_LOOP('',(#14690,#14691,#14692,#14693));
#3739=EDGE_LOOP('',(#14694,#14695,#14696,#14697));
#3740=EDGE_LOOP('',(#14698,#14699,#14700,#14701));
#3741=EDGE_LOOP('',(#14702,#14703,#14704,#14705));
#3742=EDGE_LOOP('',(#14706,#14707,#14708,#14709));
#3743=EDGE_LOOP('',(#14710,#14711,#14712,#14713));
#3744=EDGE_LOOP('',(#14714,#14715,#14716,#14717));
#3745=EDGE_LOOP('',(#14718,#14719,#14720,#14721));
#3746=EDGE_LOOP('',(#14722,#14723,#14724,#14725));
#3747=EDGE_LOOP('',(#14726,#14727,#14728,#14729));
#3748=EDGE_LOOP('',(#14730,#14731,#14732,#14733));
#3749=EDGE_LOOP('',(#14734,#14735,#14736,#14737));
#3750=EDGE_LOOP('',(#14738,#14739,#14740,#14741));
#3751=EDGE_LOOP('',(#14742,#14743,#14744,#14745));
#3752=EDGE_LOOP('',(#14746,#14747,#14748,#14749));
#3753=EDGE_LOOP('',(#14750,#14751,#14752,#14753));
#3754=EDGE_LOOP('',(#14754,#14755,#14756,#14757));
#3755=EDGE_LOOP('',(#14758,#14759,#14760,#14761));
#3756=EDGE_LOOP('',(#14762,#14763,#14764,#14765));
#3757=EDGE_LOOP('',(#14766,#14767,#14768));
#3758=EDGE_LOOP('',(#14769,#14770,#14771,#14772,#14773));
#3759=EDGE_LOOP('',(#14774,#14775,#14776,#14777));
#3760=EDGE_LOOP('',(#14778,#14779,#14780,#14781));
#3761=EDGE_LOOP('',(#14782,#14783,#14784,#14785));
#3762=EDGE_LOOP('',(#14786,#14787,#14788,#14789));
#3763=EDGE_LOOP('',(#14790,#14791,#14792,#14793));
#3764=EDGE_LOOP('',(#14794,#14795,#14796,#14797));
#3765=EDGE_LOOP('',(#14798,#14799,#14800,#14801));
#3766=EDGE_LOOP('',(#14802,#14803,#14804,#14805));
#3767=EDGE_LOOP('',(#14806,#14807,#14808,#14809));
#3768=EDGE_LOOP('',(#14810,#14811,#14812,#14813));
#3769=EDGE_LOOP('',(#14814,#14815,#14816,#14817));
#3770=EDGE_LOOP('',(#14818,#14819,#14820,#14821));
#3771=EDGE_LOOP('',(#14822,#14823,#14824,#14825));
#3772=EDGE_LOOP('',(#14826,#14827,#14828,#14829));
#3773=EDGE_LOOP('',(#14830,#14831,#14832,#14833));
#3774=EDGE_LOOP('',(#14834,#14835,#14836,#14837));
#3775=EDGE_LOOP('',(#14838,#14839,#14840,#14841));
#3776=EDGE_LOOP('',(#14842,#14843,#14844,#14845));
#3777=EDGE_LOOP('',(#14846,#14847,#14848,#14849));
#3778=EDGE_LOOP('',(#14850,#14851,#14852,#14853));
#3779=EDGE_LOOP('',(#14854,#14855,#14856,#14857));
#3780=EDGE_LOOP('',(#14858,#14859,#14860,#14861));
#3781=EDGE_LOOP('',(#14862,#14863,#14864,#14865));
#3782=EDGE_LOOP('',(#14866,#14867,#14868,#14869));
#3783=EDGE_LOOP('',(#14870,#14871,#14872,#14873));
#3784=EDGE_LOOP('',(#14874,#14875,#14876,#14877));
#3785=EDGE_LOOP('',(#14878,#14879,#14880,#14881));
#3786=EDGE_LOOP('',(#14882,#14883,#14884,#14885));
#3787=EDGE_LOOP('',(#14886,#14887,#14888,#14889));
#3788=EDGE_LOOP('',(#14890,#14891,#14892,#14893));
#3789=EDGE_LOOP('',(#14894,#14895,#14896,#14897));
#3790=EDGE_LOOP('',(#14898,#14899,#14900,#14901));
#3791=EDGE_LOOP('',(#14902,#14903,#14904,#14905));
#3792=EDGE_LOOP('',(#14906,#14907,#14908,#14909));
#3793=EDGE_LOOP('',(#14910,#14911,#14912,#14913));
#3794=EDGE_LOOP('',(#14914,#14915,#14916,#14917));
#3795=EDGE_LOOP('',(#14918,#14919,#14920,#14921));
#3796=EDGE_LOOP('',(#14922,#14923,#14924,#14925));
#3797=EDGE_LOOP('',(#14926,#14927,#14928,#14929));
#3798=EDGE_LOOP('',(#14930,#14931,#14932,#14933));
#3799=EDGE_LOOP('',(#14934,#14935,#14936,#14937));
#3800=EDGE_LOOP('',(#14938,#14939,#14940,#14941));
#3801=EDGE_LOOP('',(#14942,#14943,#14944,#14945));
#3802=EDGE_LOOP('',(#14946,#14947,#14948,#14949));
#3803=EDGE_LOOP('',(#14950,#14951,#14952,#14953));
#3804=EDGE_LOOP('',(#14954,#14955,#14956,#14957));
#3805=EDGE_LOOP('',(#14958,#14959,#14960,#14961));
#3806=EDGE_LOOP('',(#14962,#14963,#14964,#14965));
#3807=EDGE_LOOP('',(#14966,#14967,#14968,#14969));
#3808=EDGE_LOOP('',(#14970,#14971,#14972,#14973));
#3809=EDGE_LOOP('',(#14974,#14975,#14976,#14977));
#3810=EDGE_LOOP('',(#14978,#14979,#14980,#14981));
#3811=EDGE_LOOP('',(#14982,#14983,#14984,#14985));
#3812=EDGE_LOOP('',(#14986,#14987,#14988,#14989));
#3813=EDGE_LOOP('',(#14990,#14991,#14992,#14993));
#3814=EDGE_LOOP('',(#14994,#14995,#14996,#14997));
#3815=EDGE_LOOP('',(#14998,#14999,#15000,#15001));
#3816=EDGE_LOOP('',(#15002,#15003,#15004,#15005));
#3817=EDGE_LOOP('',(#15006,#15007,#15008,#15009));
#3818=EDGE_LOOP('',(#15010,#15011,#15012,#15013));
#3819=EDGE_LOOP('',(#15014,#15015,#15016,#15017));
#3820=EDGE_LOOP('',(#15018,#15019,#15020,#15021));
#3821=EDGE_LOOP('',(#15022,#15023,#15024,#15025));
#3822=EDGE_LOOP('',(#15026,#15027,#15028,#15029));
#3823=EDGE_LOOP('',(#15030,#15031,#15032,#15033));
#3824=EDGE_LOOP('',(#15034,#15035,#15036,#15037));
#3825=EDGE_LOOP('',(#15038,#15039,#15040,#15041));
#3826=EDGE_LOOP('',(#15042,#15043,#15044,#15045));
#3827=EDGE_LOOP('',(#15046,#15047,#15048,#15049));
#3828=EDGE_LOOP('',(#15050,#15051,#15052,#15053));
#3829=EDGE_LOOP('',(#15054,#15055,#15056,#15057));
#3830=EDGE_LOOP('',(#15058,#15059,#15060,#15061));
#3831=EDGE_LOOP('',(#15062,#15063,#15064,#15065));
#3832=EDGE_LOOP('',(#15066,#15067,#15068,#15069));
#3833=EDGE_LOOP('',(#15070,#15071,#15072,#15073));
#3834=EDGE_LOOP('',(#15074,#15075,#15076,#15077));
#3835=EDGE_LOOP('',(#15078,#15079,#15080,#15081));
#3836=EDGE_LOOP('',(#15082,#15083,#15084,#15085));
#3837=EDGE_LOOP('',(#15086,#15087,#15088,#15089));
#3838=EDGE_LOOP('',(#15090,#15091,#15092,#15093));
#3839=EDGE_LOOP('',(#15094,#15095,#15096,#15097));
#3840=EDGE_LOOP('',(#15098,#15099,#15100,#15101));
#3841=EDGE_LOOP('',(#15102,#15103,#15104,#15105));
#3842=EDGE_LOOP('',(#15106,#15107,#15108,#15109));
#3843=EDGE_LOOP('',(#15110,#15111,#15112,#15113));
#3844=EDGE_LOOP('',(#15114,#15115,#15116,#15117));
#3845=EDGE_LOOP('',(#15118,#15119,#15120,#15121,#15122,#15123,#15124,#15125,
#15126,#15127,#15128,#15129,#15130,#15131,#15132,#15133,#15134,#15135,#15136,
#15137,#15138,#15139,#15140,#15141,#15142,#15143,#15144,#15145,#15146,#15147,
#15148,#15149,#15150,#15151,#15152,#15153,#15154,#15155,#15156,#15157,#15158,
#15159,#15160,#15161,#15162,#15163,#15164,#15165,#15166,#15167,#15168,#15169,
#15170,#15171,#15172,#15173,#15174,#15175,#15176,#15177,#15178,#15179,#15180,
#15181,#15182,#15183,#15184,#15185,#15186,#15187,#15188,#15189,#15190,#15191,
#15192,#15193,#15194,#15195,#15196,#15197,#15198,#15199,#15200,#15201,#15202,
#15203,#15204,#15205,#15206,#15207,#15208,#15209,#15210,#15211,#15212,#15213,
#15214,#15215,#15216,#15217,#15218,#15219,#15220,#15221,#15222,#15223,#15224,
#15225,#15226,#15227,#15228,#15229,#15230,#15231,#15232,#15233,#15234,#15235,
#15236,#15237,#15238,#15239,#15240,#15241,#15242,#15243,#15244,#15245,#15246,
#15247,#15248,#15249,#15250,#15251,#15252,#15253,#15254,#15255,#15256,#15257,
#15258,#15259,#15260,#15261,#15262,#15263,#15264,#15265,#15266,#15267,#15268,
#15269,#15270,#15271,#15272,#15273,#15274,#15275,#15276,#15277,#15278,#15279,
#15280,#15281,#15282,#15283,#15284,#15285,#15286,#15287,#15288,#15289,#15290,
#15291,#15292,#15293,#15294,#15295,#15296));
#3846=EDGE_LOOP('',(#15297,#15298,#15299,#15300,#15301));
#3847=EDGE_LOOP('',(#15302,#15303,#15304,#15305));
#3848=EDGE_LOOP('',(#15306,#15307,#15308,#15309,#15310,#15311,#15312,#15313,
#15314,#15315,#15316,#15317,#15318,#15319,#15320,#15321,#15322,#15323,#15324,
#15325,#15326,#15327,#15328,#15329,#15330,#15331,#15332,#15333,#15334,#15335,
#15336,#15337,#15338,#15339,#15340,#15341,#15342,#15343,#15344,#15345,#15346,
#15347,#15348,#15349,#15350,#15351,#15352,#15353,#15354,#15355,#15356,#15357,
#15358,#15359,#15360,#15361,#15362,#15363,#15364,#15365,#15366,#15367,#15368,
#15369,#15370,#15371,#15372,#15373,#15374,#15375,#15376,#15377,#15378,#15379,
#15380,#15381,#15382,#15383,#15384,#15385,#15386,#15387,#15388,#15389,#15390,
#15391,#15392,#15393,#15394,#15395,#15396,#15397,#15398,#15399,#15400,#15401,
#15402,#15403,#15404,#15405,#15406,#15407,#15408,#15409,#15410,#15411,#15412,
#15413,#15414,#15415,#15416,#15417,#15418,#15419,#15420,#15421,#15422,#15423,
#15424,#15425,#15426,#15427,#15428,#15429,#15430,#15431,#15432,#15433,#15434,
#15435,#15436,#15437,#15438,#15439,#15440,#15441,#15442,#15443,#15444,#15445,
#15446,#15447,#15448,#15449,#15450,#15451,#15452,#15453,#15454,#15455,#15456,
#15457,#15458,#15459,#15460,#15461,#15462,#15463,#15464,#15465,#15466,#15467,
#15468,#15469,#15470,#15471,#15472,#15473,#15474,#15475,#15476,#15477,#15478,
#15479,#15480,#15481,#15482,#15483,#15484,#15485));
#3849=EDGE_LOOP('',(#15486,#15487,#15488,#15489,#15490,#15491,#15492,#15493,
#15494,#15495));
#3850=EDGE_LOOP('',(#15496,#15497,#15498,#15499));
#3851=EDGE_LOOP('',(#15500,#15501,#15502,#15503));
#3852=EDGE_LOOP('',(#15504,#15505,#15506,#15507));
#3853=EDGE_LOOP('',(#15508,#15509,#15510,#15511,#15512,#15513));
#3854=EDGE_LOOP('',(#15514,#15515,#15516,#15517,#15518));
#3855=EDGE_LOOP('',(#15519,#15520,#15521,#15522));
#3856=EDGE_LOOP('',(#15523,#15524,#15525,#15526));
#3857=EDGE_LOOP('',(#15527,#15528,#15529,#15530,#15531));
#3858=EDGE_LOOP('',(#15532));
#3859=EDGE_LOOP('',(#15533));
#3860=EDGE_LOOP('',(#15534,#15535,#15536,#15537,#15538,#15539));
#3861=EDGE_LOOP('',(#15540,#15541,#15542,#15543));
#4642=LINE('',#44373,#5596);
#4643=LINE('',#44397,#5597);
#4644=LINE('',#44445,#5598);
#4645=LINE('',#44493,#5599);
#4646=LINE('',#44541,#5600);
#4647=LINE('',#44595,#5601);
#4648=LINE('',#44643,#5602);
#4649=LINE('',#44691,#5603);
#4650=LINE('',#44745,#5604);
#4651=LINE('',#44793,#5605);
#4652=LINE('',#44841,#5606);
#4653=LINE('',#44889,#5607);
#4654=LINE('',#44943,#5608);
#4655=LINE('',#44991,#5609);
#4656=LINE('',#45039,#5610);
#4657=LINE('',#45093,#5611);
#4658=LINE('',#45141,#5612);
#4659=LINE('',#45189,#5613);
#4660=LINE('',#45237,#5614);
#4661=LINE('',#45291,#5615);
#4662=LINE('',#45339,#5616);
#4663=LINE('',#45387,#5617);
#4664=LINE('',#45441,#5618);
#4665=LINE('',#45489,#5619);
#4666=LINE('',#45537,#5620);
#4667=LINE('',#45585,#5621);
#4668=LINE('',#45639,#5622);
#4669=LINE('',#45687,#5623);
#4670=LINE('',#45735,#5624);
#4671=LINE('',#45789,#5625);
#4672=LINE('',#45837,#5626);
#4673=LINE('',#45885,#5627);
#4674=LINE('',#45933,#5628);
#4675=LINE('',#45987,#5629);
#4676=LINE('',#46035,#5630);
#4677=LINE('',#46083,#5631);
#4678=LINE('',#46137,#5632);
#4679=LINE('',#46185,#5633);
#4680=LINE('',#46233,#5634);
#4681=LINE('',#46281,#5635);
#4682=LINE('',#46335,#5636);
#4683=LINE('',#46383,#5637);
#4684=LINE('',#46431,#5638);
#4685=LINE('',#46485,#5639);
#4686=LINE('',#46533,#5640);
#4687=LINE('',#46581,#5641);
#4688=LINE('',#46629,#5642);
#4689=LINE('',#46683,#5643);
#4690=LINE('',#46731,#5644);
#4691=LINE('',#46779,#5645);
#4692=LINE('',#46833,#5646);
#4693=LINE('',#46881,#5647);
#4694=LINE('',#46929,#5648);
#4695=LINE('',#46977,#5649);
#4696=LINE('',#47031,#5650);
#4697=LINE('',#47079,#5651);
#4698=LINE('',#47127,#5652);
#4699=LINE('',#47181,#5653);
#4700=LINE('',#47229,#5654);
#4701=LINE('',#47277,#5655);
#4702=LINE('',#47325,#5656);
#4703=LINE('',#47379,#5657);
#4704=LINE('',#47427,#5658);
#4705=LINE('',#47475,#5659);
#4706=LINE('',#47529,#5660);
#4707=LINE('',#47577,#5661);
#4708=LINE('',#47625,#5662);
#4709=LINE('',#47673,#5663);
#4710=LINE('',#47727,#5664);
#4711=LINE('',#47775,#5665);
#4712=LINE('',#47823,#5666);
#4713=LINE('',#47877,#5667);
#4714=LINE('',#47925,#5668);
#4715=LINE('',#47973,#5669);
#4716=LINE('',#48021,#5670);
#4717=LINE('',#48075,#5671);
#4718=LINE('',#48123,#5672);
#4719=LINE('',#48171,#5673);
#4720=LINE('',#48225,#5674);
#4721=LINE('',#48273,#5675);
#4722=LINE('',#48321,#5676);
#4723=LINE('',#48369,#5677);
#4724=LINE('',#48423,#5678);
#4725=LINE('',#48471,#5679);
#4726=LINE('',#48519,#5680);
#4727=LINE('',#48573,#5681);
#4728=LINE('',#48621,#5682);
#4729=LINE('',#48669,#5683);
#4730=LINE('',#48717,#5684);
#4731=LINE('',#48727,#5685);
#4732=LINE('',#48764,#5686);
#4733=LINE('',#48812,#5687);
#4734=LINE('',#48860,#5688);
#4735=LINE('',#48885,#5689);
#4736=LINE('',#48910,#5690);
#4737=LINE('',#48934,#5691);
#4738=LINE('',#48959,#5692);
#4739=LINE('',#48998,#5693);
#4740=LINE('',#49034,#5694);
#4741=LINE('',#49058,#5695);
#4742=LINE('',#49083,#5696);
#4743=LINE('',#49108,#5697);
#4744=LINE('',#49132,#5698);
#4745=LINE('',#49157,#5699);
#4746=LINE('',#49182,#5700);
#4747=LINE('',#49218,#5701);
#4748=LINE('',#49254,#5702);
#4749=LINE('',#49279,#5703);
#4750=LINE('',#49304,#5704);
#4751=LINE('',#49328,#5705);
#4752=LINE('',#49353,#5706);
#4753=LINE('',#49378,#5707);
#4754=LINE('',#49402,#5708);
#4755=LINE('',#49426,#5709);
#4756=LINE('',#49451,#5710);
#4757=LINE('',#49476,#5711);
#4758=LINE('',#49500,#5712);
#4759=LINE('',#49525,#5713);
#4760=LINE('',#49550,#5714);
#4761=LINE('',#49574,#5715);
#4762=LINE('',#49598,#5716);
#4763=LINE('',#49623,#5717);
#4764=LINE('',#49648,#5718);
#4765=LINE('',#49672,#5719);
#4766=LINE('',#49697,#5720);
#4767=LINE('',#49722,#5721);
#4768=LINE('',#49746,#5722);
#4769=LINE('',#49770,#5723);
#4770=LINE('',#49795,#5724);
#4771=LINE('',#49820,#5725);
#4772=LINE('',#49844,#5726);
#4773=LINE('',#49869,#5727);
#4774=LINE('',#49894,#5728);
#4775=LINE('',#49918,#5729);
#4776=LINE('',#49942,#5730);
#4777=LINE('',#49967,#5731);
#4778=LINE('',#49992,#5732);
#4779=LINE('',#50016,#5733);
#4780=LINE('',#50041,#5734);
#4781=LINE('',#50066,#5735);
#4782=LINE('',#50090,#5736);
#4783=LINE('',#50114,#5737);
#4784=LINE('',#50139,#5738);
#4785=LINE('',#50164,#5739);
#4786=LINE('',#50188,#5740);
#4787=LINE('',#50213,#5741);
#4788=LINE('',#50238,#5742);
#4789=LINE('',#50262,#5743);
#4790=LINE('',#50286,#5744);
#4791=LINE('',#50311,#5745);
#4792=LINE('',#50336,#5746);
#4793=LINE('',#50360,#5747);
#4794=LINE('',#50385,#5748);
#4795=LINE('',#50410,#5749);
#4796=LINE('',#50434,#5750);
#4797=LINE('',#50458,#5751);
#4798=LINE('',#50483,#5752);
#4799=LINE('',#50508,#5753);
#4800=LINE('',#50532,#5754);
#4801=LINE('',#50557,#5755);
#4802=LINE('',#50582,#5756);
#4803=LINE('',#50606,#5757);
#4804=LINE('',#50630,#5758);
#4805=LINE('',#50655,#5759);
#4806=LINE('',#50680,#5760);
#4807=LINE('',#50704,#5761);
#4808=LINE('',#50729,#5762);
#4809=LINE('',#50754,#5763);
#4810=LINE('',#50778,#5764);
#4811=LINE('',#50802,#5765);
#4812=LINE('',#50827,#5766);
#4813=LINE('',#50852,#5767);
#4814=LINE('',#50876,#5768);
#4815=LINE('',#50901,#5769);
#4816=LINE('',#50926,#5770);
#4817=LINE('',#50950,#5771);
#4818=LINE('',#55880,#5772);
#4819=LINE('',#55891,#5773);
#4820=LINE('',#55893,#5774);
#4821=LINE('',#55894,#5775);
#4822=LINE('',#55897,#5776);
#4823=LINE('',#55898,#5777);
#4824=LINE('',#55901,#5778);
#4825=LINE('',#55902,#5779);
#4826=LINE('',#55905,#5780);
#4827=LINE('',#55907,#5781);
#4828=LINE('',#55908,#5782);
#4829=LINE('',#55911,#5783);
#4830=LINE('',#55913,#5784);
#4831=LINE('',#55920,#5785);
#5596=VECTOR('',#22128,4.);
#5597=VECTOR('',#22133,4.);
#5598=VECTOR('',#22136,4.);
#5599=VECTOR('',#22139,4.);
#5600=VECTOR('',#22142,4.);
#5601=VECTOR('',#22145,4.);
#5602=VECTOR('',#22148,4.);
#5603=VECTOR('',#22151,4.);
#5604=VECTOR('',#22154,4.);
#5605=VECTOR('',#22157,4.);
#5606=VECTOR('',#22160,4.);
#5607=VECTOR('',#22163,4.);
#5608=VECTOR('',#22166,4.);
#5609=VECTOR('',#22169,4.);
#5610=VECTOR('',#22172,4.);
#5611=VECTOR('',#22175,4.);
#5612=VECTOR('',#22178,4.);
#5613=VECTOR('',#22181,4.);
#5614=VECTOR('',#22184,4.);
#5615=VECTOR('',#22187,4.);
#5616=VECTOR('',#22190,4.);
#5617=VECTOR('',#22193,4.);
#5618=VECTOR('',#22196,4.);
#5619=VECTOR('',#22199,4.);
#5620=VECTOR('',#22202,4.);
#5621=VECTOR('',#22205,4.);
#5622=VECTOR('',#22208,4.);
#5623=VECTOR('',#22211,4.);
#5624=VECTOR('',#22214,4.);
#5625=VECTOR('',#22217,4.);
#5626=VECTOR('',#22220,4.);
#5627=VECTOR('',#22223,4.);
#5628=VECTOR('',#22226,4.);
#5629=VECTOR('',#22229,4.);
#5630=VECTOR('',#22232,4.);
#5631=VECTOR('',#22235,4.);
#5632=VECTOR('',#22238,4.);
#5633=VECTOR('',#22241,4.);
#5634=VECTOR('',#22244,4.);
#5635=VECTOR('',#22247,4.);
#5636=VECTOR('',#22250,4.);
#5637=VECTOR('',#22253,4.);
#5638=VECTOR('',#22256,4.);
#5639=VECTOR('',#22259,4.);
#5640=VECTOR('',#22262,4.);
#5641=VECTOR('',#22265,4.);
#5642=VECTOR('',#22268,4.);
#5643=VECTOR('',#22271,4.);
#5644=VECTOR('',#22274,4.);
#5645=VECTOR('',#22277,4.);
#5646=VECTOR('',#22280,4.);
#5647=VECTOR('',#22283,4.);
#5648=VECTOR('',#22286,4.);
#5649=VECTOR('',#22289,4.);
#5650=VECTOR('',#22292,4.);
#5651=VECTOR('',#22295,4.);
#5652=VECTOR('',#22298,4.);
#5653=VECTOR('',#22301,4.);
#5654=VECTOR('',#22304,4.);
#5655=VECTOR('',#22307,4.);
#5656=VECTOR('',#22310,4.);
#5657=VECTOR('',#22313,4.);
#5658=VECTOR('',#22316,4.);
#5659=VECTOR('',#22319,4.);
#5660=VECTOR('',#22322,4.);
#5661=VECTOR('',#22325,4.);
#5662=VECTOR('',#22328,4.);
#5663=VECTOR('',#22331,4.);
#5664=VECTOR('',#22334,4.);
#5665=VECTOR('',#22337,4.);
#5666=VECTOR('',#22340,4.);
#5667=VECTOR('',#22343,4.);
#5668=VECTOR('',#22346,4.);
#5669=VECTOR('',#22349,4.);
#5670=VECTOR('',#22352,4.);
#5671=VECTOR('',#22355,4.);
#5672=VECTOR('',#22358,4.);
#5673=VECTOR('',#22361,4.);
#5674=VECTOR('',#22364,4.);
#5675=VECTOR('',#22367,4.);
#5676=VECTOR('',#22370,4.);
#5677=VECTOR('',#22373,4.);
#5678=VECTOR('',#22376,4.);
#5679=VECTOR('',#22379,4.);
#5680=VECTOR('',#22382,4.);
#5681=VECTOR('',#22385,4.);
#5682=VECTOR('',#22388,4.);
#5683=VECTOR('',#22391,4.);
#5684=VECTOR('',#22394,3.22275);
#5685=VECTOR('',#22399,3.22275);
#5686=VECTOR('',#22404,3.22275);
#5687=VECTOR('',#22407,3.22275);
#5688=VECTOR('',#22410,3.22275);
#5689=VECTOR('',#22413,3.22275);
#5690=VECTOR('',#22416,3.22275);
#5691=VECTOR('',#22419,3.22275);
#5692=VECTOR('',#22422,3.22275);
#5693=VECTOR('',#22425,3.22275);
#5694=VECTOR('',#22428,3.22275);
#5695=VECTOR('',#22431,3.22275);
#5696=VECTOR('',#22434,3.22275);
#5697=VECTOR('',#22437,3.22275);
#5698=VECTOR('',#22440,3.22275);
#5699=VECTOR('',#22443,3.22275);
#5700=VECTOR('',#22446,3.22275);
#5701=VECTOR('',#22449,3.22275);
#5702=VECTOR('',#22452,3.22275);
#5703=VECTOR('',#22455,3.22275);
#5704=VECTOR('',#22458,3.22275);
#5705=VECTOR('',#22461,3.22275);
#5706=VECTOR('',#22464,3.22275);
#5707=VECTOR('',#22467,3.22275);
#5708=VECTOR('',#22470,3.22275);
#5709=VECTOR('',#22473,3.22275);
#5710=VECTOR('',#22476,3.22275);
#5711=VECTOR('',#22479,3.22275);
#5712=VECTOR('',#22482,3.22275);
#5713=VECTOR('',#22485,3.22275);
#5714=VECTOR('',#22488,3.22275);
#5715=VECTOR('',#22491,3.22275);
#5716=VECTOR('',#22494,3.22275);
#5717=VECTOR('',#22497,3.22275);
#5718=VECTOR('',#22500,3.22275);
#5719=VECTOR('',#22503,3.22275);
#5720=VECTOR('',#22506,3.22275);
#5721=VECTOR('',#22509,3.22275);
#5722=VECTOR('',#22512,3.22275);
#5723=VECTOR('',#22515,3.22275);
#5724=VECTOR('',#22518,3.22275);
#5725=VECTOR('',#22521,3.22275);
#5726=VECTOR('',#22524,3.22275);
#5727=VECTOR('',#22527,3.22275);
#5728=VECTOR('',#22530,3.22275);
#5729=VECTOR('',#22533,3.22275);
#5730=VECTOR('',#22536,3.22275);
#5731=VECTOR('',#22539,3.22275);
#5732=VECTOR('',#22542,3.22275);
#5733=VECTOR('',#22545,3.22275);
#5734=VECTOR('',#22548,3.22275);
#5735=VECTOR('',#22551,3.22275);
#5736=VECTOR('',#22554,3.22275);
#5737=VECTOR('',#22557,3.22275);
#5738=VECTOR('',#22560,3.22275);
#5739=VECTOR('',#22563,3.22275);
#5740=VECTOR('',#22566,3.22275);
#5741=VECTOR('',#22569,3.22275);
#5742=VECTOR('',#22572,3.22275);
#5743=VECTOR('',#22575,3.22275);
#5744=VECTOR('',#22578,3.22275);
#5745=VECTOR('',#22581,3.22275);
#5746=VECTOR('',#22584,3.22275);
#5747=VECTOR('',#22587,3.22275);
#5748=VECTOR('',#22590,3.22275);
#5749=VECTOR('',#22593,3.22275);
#5750=VECTOR('',#22596,3.22275);
#5751=VECTOR('',#22599,3.22275);
#5752=VECTOR('',#22602,3.22275);
#5753=VECTOR('',#22605,3.22275);
#5754=VECTOR('',#22608,3.22275);
#5755=VECTOR('',#22611,3.22275);
#5756=VECTOR('',#22614,3.22275);
#5757=VECTOR('',#22617,3.22275);
#5758=VECTOR('',#22620,3.22275);
#5759=VECTOR('',#22623,3.22275);
#5760=VECTOR('',#22626,3.22275);
#5761=VECTOR('',#22629,3.22275);
#5762=VECTOR('',#22632,3.22275);
#5763=VECTOR('',#22635,3.22275);
#5764=VECTOR('',#22638,3.22275);
#5765=VECTOR('',#22641,3.22275);
#5766=VECTOR('',#22644,3.22275);
#5767=VECTOR('',#22647,3.22275);
#5768=VECTOR('',#22650,3.22275);
#5769=VECTOR('',#22653,3.22275);
#5770=VECTOR('',#22656,3.22275);
#5771=VECTOR('',#22659,3.22275);
#5772=VECTOR('',#22672,7.25527674973257);
#5773=VECTOR('',#22677,10.);
#5774=VECTOR('',#22678,10.);
#5775=VECTOR('',#22679,10.);
#5776=VECTOR('',#22682,10.);
#5777=VECTOR('',#22683,10.);
#5778=VECTOR('',#22686,10.);
#5779=VECTOR('',#22687,10.);
#5780=VECTOR('',#22690,10.);
#5781=VECTOR('',#22691,10.);
#5782=VECTOR('',#22692,10.);
#5783=VECTOR('',#22697,10.);
#5784=VECTOR('',#22700,10.);
#5785=VECTOR('',#22711,3.75);
#6313=B_SPLINE_CURVE_WITH_KNOTS('',3,(#44375,#44376,#44377,#44378,#44379,
#44380,#44381,#44382,#44383,#44384),.UNSPECIFIED.,.F.,.F.,(4,3,3,4),(-4.09274904019427,
-3.99858960751474,-2.99894220563605,-2.06120159751581),.UNSPECIFIED.);
#6314=B_SPLINE_CURVE_WITH_KNOTS('',3,(#44387,#44388,#44389,#44390,#44391,
#44392,#44393),.UNSPECIFIED.,.F.,.F.,(4,3,4),(0.,0.999647401878707,1.1100452109132),
 .UNSPECIFIED.);
#6315=B_SPLINE_CURVE_WITH_KNOTS('',3,(#44398,#44399,#44400,#44401,#44402,
#44403,#44404,#44405,#44406,#44407,#44408,#44409,#44410,#44411,#44412,#44413,
#44414,#44415,#44416,#44417,#44418,#44419),.UNSPECIFIED.,.F.,.F.,(4,3,3,
3,3,3,3,4),(-10.3759343473739,-9.99647401878684,-8.99682661690816,-7.99717921502947,
-6.99753181315079,-5.9978844112721,-4.99823700939342,-4.09274904019427),
 .UNSPECIFIED.);
#6316=B_SPLINE_CURVE_WITH_KNOTS('',3,(#44420,#44421,#44422,#44423,#44424,
#44425,#44426,#44427,#44428,#44429,#44430,#44431,#44432,#44433,#44434,#44435,
#44436,#44437,#44438,#44439,#44440,#44441),.UNSPECIFIED.,.F.,.F.,(4,3,3,
3,3,3,3,4),(1.1100452109132,1.9992948037574,2.99894220563608,3.99858960751477,
4.99823700939346,5.99788441127215,6.99753181315084,7.39323051809279),
 .UNSPECIFIED.);
#6317=B_SPLINE_CURVE_WITH_KNOTS('',3,(#44446,#44447,#44448,#44449,#44450,
#44451,#44452,#44453,#44454,#44455,#44456,#44457,#44458,#44459,#44460,#44461,
#44462,#44463,#44464,#44465,#44466,#44467),.UNSPECIFIED.,.F.,.F.,(4,3,3,
3,3,3,3,4),(-16.6591196545534,-15.9943584300589,-14.9947110281803,-13.9950636263016,
-12.9954162244229,-11.9957688225442,-10.9961214206655,-10.3759343473739),
 .UNSPECIFIED.);
#6318=B_SPLINE_CURVE_WITH_KNOTS('',3,(#44468,#44469,#44470,#44471,#44472,
#44473,#44474,#44475,#44476,#44477,#44478,#44479,#44480,#44481,#44482,#44483,
#44484,#44485,#44486,#44487,#44488,#44489),.UNSPECIFIED.,.F.,.F.,(4,3,3,
3,3,3,3,4),(7.39323051809279,7.99717921502952,8.99682661690821,9.99647401878689,
10.9961214206656,11.9957688225443,12.9954162244229,13.6764158252724),
 .UNSPECIFIED.);
#6319=B_SPLINE_CURVE_WITH_KNOTS('',3,(#44494,#44495,#44496,#44497,#44498,
#44499,#44500,#44501,#44502,#44503,#44504,#44505,#44506,#44507,#44508,#44509,
#44510,#44511,#44512,#44513,#44514,#44515),.UNSPECIFIED.,.F.,.F.,(4,3,3,
3,3,3,3,4),(-22.942304961733,-21.992242841331,-20.9925954394524,-19.9929480375737,
-18.993300635695,-17.9936532338163,-16.9940058319376,-16.6591196545534),
 .UNSPECIFIED.);
#6320=B_SPLINE_CURVE_WITH_KNOTS('',3,(#44516,#44517,#44518,#44519,#44520,
#44521,#44522,#44523,#44524,#44525,#44526,#44527,#44528,#44529,#44530,#44531,
#44532,#44533,#44534,#44535,#44536,#44537),.UNSPECIFIED.,.F.,.F.,(4,3,3,
3,3,3,3,4),(13.6764158252724,13.9950636263016,14.9947110281803,15.9943584300589,
16.9940058319376,17.9936532338163,18.9933006356949,19.959601132452),
 .UNSPECIFIED.);
#6321=B_SPLINE_CURVE_WITH_KNOTS('',3,(#44542,#44543,#44544,#44545,#44546,
#44547,#44548,#44549,#44550,#44551,#44552,#44553,#44554,#44555,#44556,#44557,
#44558,#44559,#44560,#44561,#44562,#44563,#44564,#44565,#44566),
 .UNSPECIFIED.,.F.,.F.,(4,3,3,3,3,3,3,3,4),(-29.2254902689126,-28.9897746544818,
-27.9901272526032,-26.9904798507245,-25.9908324488458,-24.9911850469671,
-23.9915376450884,-22.9918902432097,-22.942304961733),.UNSPECIFIED.);
#6322=B_SPLINE_CURVE_WITH_KNOTS('',3,(#44567,#44568,#44569,#44570,#44571,
#44572,#44573,#44574,#44575,#44576,#44577,#44578,#44579,#44580,#44581,#44582,
#44583,#44584,#44585,#44586,#44587,#44588,#44589,#44590,#44591),
 .UNSPECIFIED.,.F.,.F.,(4,3,3,3,3,3,3,3,4),(19.959601132452,19.9929480375736,
20.9925954394523,21.992242841331,22.9918902432097,23.9915376450884,24.9911850469671,
25.9908324488458,26.2427864396316),.UNSPECIFIED.);
#6323=B_SPLINE_CURVE_WITH_KNOTS('',3,(#44596,#44597,#44598,#44599,#44600,
#44601,#44602,#44603,#44604,#44605,#44606,#44607,#44608,#44609,#44610,#44611,
#44612,#44613,#44614,#44615,#44616,#44617),.UNSPECIFIED.,.F.,.F.,(4,3,3,
3,3,3,3,4),(-35.5086755760922,-34.9876590657539,-33.9880116638753,-32.9883642619966,
-31.9887168601179,-30.9890694582392,-29.9894220563605,-29.2254902689126),
 .UNSPECIFIED.);
#6324=B_SPLINE_CURVE_WITH_KNOTS('',3,(#44618,#44619,#44620,#44621,#44622,
#44623,#44624,#44625,#44626,#44627,#44628,#44629,#44630,#44631,#44632,#44633,
#44634,#44635,#44636,#44637,#44638,#44639),.UNSPECIFIED.,.F.,.F.,(4,3,3,
3,3,3,3,4),(26.2427864396316,26.9904798507245,27.9901272526032,28.9897746544819,
29.9894220563605,30.9890694582392,31.9887168601179,32.5259717468111),
 .UNSPECIFIED.);
#6325=B_SPLINE_CURVE_WITH_KNOTS('',3,(#44644,#44645,#44646,#44647,#44648,
#44649,#44650,#44651,#44652,#44653,#44654,#44655,#44656,#44657,#44658,#44659,
#44660,#44661,#44662,#44663,#44664,#44665),.UNSPECIFIED.,.F.,.F.,(4,3,3,
3,3,3,3,4),(-41.7918608832718,-40.985543477026,-39.9858960751474,-38.9862486732687,
-37.98660127139,-36.9869538695113,-35.9873064676326,-35.5086755760922),
 .UNSPECIFIED.);
#6326=B_SPLINE_CURVE_WITH_KNOTS('',3,(#44666,#44667,#44668,#44669,#44670,
#44671,#44672,#44673,#44674,#44675,#44676,#44677,#44678,#44679,#44680,#44681,
#44682,#44683,#44684,#44685,#44686,#44687),.UNSPECIFIED.,.F.,.F.,(4,3,3,
3,3,3,3,4),(32.5259717468111,32.9883642619966,33.9880116638753,34.987659065754,
35.9873064676326,36.9869538695113,37.98660127139,38.8091570539907),
 .UNSPECIFIED.);
#6327=B_SPLINE_CURVE_WITH_KNOTS('',3,(#44692,#44693,#44694,#44695,#44696,
#44697,#44698,#44699,#44700,#44701,#44702,#44703,#44704,#44705,#44706,#44707,
#44708,#44709,#44710,#44711,#44712,#44713,#44714,#44715,#44716),
 .UNSPECIFIED.,.F.,.F.,(4,3,3,3,3,3,3,3,4),(-48.0750461904514,-47.9830752901768,
-46.9834278882981,-45.9837804864195,-44.9841330845408,-43.9844856826621,
-42.9848382807834,-41.9851908789047,-41.7918608832718),.UNSPECIFIED.);
#6328=B_SPLINE_CURVE_WITH_KNOTS('',3,(#44717,#44718,#44719,#44720,#44721,
#44722,#44723,#44724,#44725,#44726,#44727,#44728,#44729,#44730,#44731,#44732,
#44733,#44734,#44735,#44736,#44737,#44738,#44739,#44740,#44741),
 .UNSPECIFIED.,.F.,.F.,(4,3,3,3,3,3,3,3,4),(38.8091570539907,38.9862486732687,
39.9858960751474,40.9855434770261,41.9851908789047,42.9848382807834,43.9844856826621,
44.9841330845408,45.0923423611703),.UNSPECIFIED.);
#6329=B_SPLINE_CURVE_WITH_KNOTS('',3,(#44746,#44747,#44748,#44749,#44750,
#44751,#44752,#44753,#44754,#44755,#44756,#44757,#44758,#44759,#44760,#44761,
#44762,#44763,#44764,#44765,#44766,#44767),.UNSPECIFIED.,.F.,.F.,(4,3,3,
3,3,3,3,4),(-54.358231497631,-53.9809597014489,-52.9813122995703,-51.9816648976916,
-50.9820174958129,-49.9823700939342,-48.9827226920555,-48.0750461904514),
 .UNSPECIFIED.);
#6330=B_SPLINE_CURVE_WITH_KNOTS('',3,(#44768,#44769,#44770,#44771,#44772,
#44773,#44774,#44775,#44776,#44777,#44778,#44779,#44780,#44781,#44782,#44783,
#44784,#44785,#44786,#44787,#44788,#44789),.UNSPECIFIED.,.F.,.F.,(4,3,3,
3,3,3,3,4),(45.0923423611703,45.9837804864195,46.9834278882981,47.9830752901768,
48.9827226920555,49.9823700939342,50.9820174958129,51.3755276683499),
 .UNSPECIFIED.);
#6331=B_SPLINE_CURVE_WITH_KNOTS('',3,(#44794,#44795,#44796,#44797,#44798,
#44799,#44800,#44801,#44802,#44803,#44804,#44805,#44806,#44807,#44808,#44809,
#44810,#44811,#44812,#44813,#44814,#44815),.UNSPECIFIED.,.F.,.F.,(4,3,3,
3,3,3,3,4),(-60.6414168048105,-59.978844112721,-58.9791967108424,-57.9795493089637,
-56.979901907085,-55.9802545052063,-54.9806071033276,-54.358231497631),
 .UNSPECIFIED.);
#6332=B_SPLINE_CURVE_WITH_KNOTS('',3,(#44816,#44817,#44818,#44819,#44820,
#44821,#44822,#44823,#44824,#44825,#44826,#44827,#44828,#44829,#44830,#44831,
#44832,#44833,#44834,#44835,#44836,#44837),.UNSPECIFIED.,.F.,.F.,(4,3,3,
3,3,3,3,4),(51.3755276683499,51.9816648976916,52.9813122995703,53.980959701449,
54.9806071033277,55.9802545052063,56.979901907085,57.6587129755296),
 .UNSPECIFIED.);
#6333=B_SPLINE_CURVE_WITH_KNOTS('',3,(#44842,#44843,#44844,#44845,#44846,
#44847,#44848,#44849,#44850,#44851,#44852,#44853,#44854,#44855,#44856,#44857,
#44858,#44859,#44860,#44861,#44862,#44863),.UNSPECIFIED.,.F.,.F.,(4,3,3,
3,3,3,3,4),(-66.9246021119901,-65.9767285239931,-64.9770811221145,-63.9774337202358,
-62.9777863183571,-61.9781389164784,-60.9784915145997,-60.6414168048105),
 .UNSPECIFIED.);
#6334=B_SPLINE_CURVE_WITH_KNOTS('',3,(#44864,#44865,#44866,#44867,#44868,
#44869,#44870,#44871,#44872,#44873,#44874,#44875,#44876,#44877,#44878,#44879,
#44880,#44881,#44882,#44883,#44884,#44885),.UNSPECIFIED.,.F.,.F.,(4,3,3,
3,3,3,3,4),(57.6587129755296,57.9795493089637,58.9791967108424,59.9788441127211,
60.9784915145998,61.9781389164785,62.9777863183572,63.9418982827091),
 .UNSPECIFIED.);
#6335=B_SPLINE_CURVE_WITH_KNOTS('',3,(#44890,#44891,#44892,#44893,#44894,
#44895,#44896,#44897,#44898,#44899,#44900,#44901,#44902,#44903,#44904,#44905,
#44906,#44907,#44908,#44909,#44910,#44911,#44912,#44913,#44914),
 .UNSPECIFIED.,.F.,.F.,(4,3,3,3,3,3,3,3,4),(-73.2077874191697,-72.9742603371439,
-71.9746129352653,-70.9749655333866,-69.9753181315079,-68.9756707296292,
-67.9760233277505,-66.9763759258718,-66.9246021119901),.UNSPECIFIED.);
#6336=B_SPLINE_CURVE_WITH_KNOTS('',3,(#44915,#44916,#44917,#44918,#44919,
#44920,#44921,#44922,#44923,#44924,#44925,#44926,#44927,#44928,#44929,#44930,
#44931,#44932,#44933,#44934,#44935,#44936,#44937,#44938,#44939),
 .UNSPECIFIED.,.F.,.F.,(4,3,3,3,3,3,3,3,4),(63.9418982827091,63.9774337202358,
64.9770811221145,65.9767285239932,66.9763759258719,67.9760233277506,68.9756707296293,
69.9753181315079,70.2250835898887),.UNSPECIFIED.);
#6337=B_SPLINE_CURVE_WITH_KNOTS('',3,(#44944,#44945,#44946,#44947,#44948,
#44949,#44950,#44951,#44952,#44953,#44954,#44955,#44956,#44957,#44958,#44959,
#44960,#44961,#44962,#44963,#44964,#44965),.UNSPECIFIED.,.F.,.F.,(4,3,3,
3,3,3,3,4),(-79.4909727263493,-78.972144748416,-77.9724973465374,-76.9728499446587,
-75.97320254278,-74.9735551409013,-73.9739077390226,-73.2077874191697),
 .UNSPECIFIED.);
#6338=B_SPLINE_CURVE_WITH_KNOTS('',3,(#44966,#44967,#44968,#44969,#44970,
#44971,#44972,#44973,#44974,#44975,#44976,#44977,#44978,#44979,#44980,#44981,
#44982,#44983,#44984,#44985,#44986,#44987),.UNSPECIFIED.,.F.,.F.,(4,3,3,
3,3,3,3,4),(70.2250835898887,70.9749655333866,71.9746129352653,72.974260337144,
73.9739077390227,74.9735551409013,75.97320254278,76.5082688970683),
 .UNSPECIFIED.);
#6339=B_SPLINE_CURVE_WITH_KNOTS('',3,(#44992,#44993,#44994,#44995,#44996,
#44997,#44998,#44999,#45000,#45001,#45002,#45003,#45004,#45005,#45006,#45007,
#45008,#45009,#45010,#45011,#45012,#45013),.UNSPECIFIED.,.F.,.F.,(4,3,3,
3,3,3,3,4),(-85.7741580335289,-84.9700291596882,-83.9703817578095,-82.9707343559308,
-81.9710869540521,-80.9714395521734,-79.9717921502947,-79.4909727263493),
 .UNSPECIFIED.);
#6340=B_SPLINE_CURVE_WITH_KNOTS('',3,(#45014,#45015,#45016,#45017,#45018,
#45019,#45020,#45021,#45022,#45023,#45024,#45025,#45026,#45027,#45028,#45029,
#45030,#45031,#45032,#45033,#45034,#45035),.UNSPECIFIED.,.F.,.F.,(4,3,3,
3,3,3,3,4),(76.5082688970683,76.9728499446587,77.9724973465374,78.9721447484161,
79.9717921502948,80.9714395521735,81.9710869540522,82.7914542042479),
 .UNSPECIFIED.);
#6341=B_SPLINE_CURVE_WITH_KNOTS('',3,(#45040,#45041,#45042,#45043,#45044,
#45045,#45046,#45047,#45048,#45049,#45050,#45051,#45052,#45053,#45054,#45055,
#45056,#45057,#45058,#45059,#45060,#45061,#45062,#45063,#45064),
 .UNSPECIFIED.,.F.,.F.,(4,3,3,3,3,3,3,3,4),(-92.0573433407085,-91.9675609728389,
-90.9679135709602,-89.9682661690816,-88.9686187672029,-87.9689713653242,
-86.9693239634455,-85.9696765615668,-85.7741580335289),.UNSPECIFIED.);
#6342=B_SPLINE_CURVE_WITH_KNOTS('',3,(#45065,#45066,#45067,#45068,#45069,
#45070,#45071,#45072,#45073,#45074,#45075,#45076,#45077,#45078,#45079,#45080,
#45081,#45082,#45083,#45084,#45085,#45086,#45087,#45088,#45089),
 .UNSPECIFIED.,.F.,.F.,(4,3,3,3,3,3,3,3,4),(82.7914542042479,82.9707343559309,
83.9703817578095,84.9700291596882,85.9696765615669,86.9693239634455,87.9689713653242,
88.9686187672029,89.0746395114275),.UNSPECIFIED.);
#6343=B_SPLINE_CURVE_WITH_KNOTS('',3,(#45094,#45095,#45096,#45097,#45098,
#45099,#45100,#45101,#45102,#45103,#45104,#45105,#45106,#45107,#45108,#45109,
#45110,#45111,#45112,#45113,#45114,#45115),.UNSPECIFIED.,.F.,.F.,(4,3,3,
3,3,3,3,4),(-98.3405286478881,-97.965445384111,-96.9657979822324,-95.9661505803537,
-94.966503178475,-93.9668557765963,-92.9672083747176,-92.0573433407085),
 .UNSPECIFIED.);
#6344=B_SPLINE_CURVE_WITH_KNOTS('',3,(#45116,#45117,#45118,#45119,#45120,
#45121,#45122,#45123,#45124,#45125,#45126,#45127,#45128,#45129,#45130,#45131,
#45132,#45133,#45134,#45135,#45136,#45137),.UNSPECIFIED.,.F.,.F.,(4,3,3,
3,3,3,3,4),(89.0746395114275,89.9682661690816,90.9679135709603,91.967560972839,
92.9672083747177,93.9668557765964,94.9665031784751,95.3578248186071),
 .UNSPECIFIED.);
#6345=B_SPLINE_CURVE_WITH_KNOTS('',3,(#45142,#45143,#45144,#45145,#45146,
#45147,#45148,#45149,#45150,#45151,#45152,#45153,#45154,#45155,#45156,#45157,
#45158,#45159,#45160,#45161,#45162,#45163),.UNSPECIFIED.,.F.,.F.,(4,3,3,
3,3,3,3,4),(-104.623713955068,-103.963329795383,-102.963682393504,-101.964034991626,
-100.964387589747,-99.9647401878684,-98.9650927859897,-98.3405286478881),
 .UNSPECIFIED.);
#6346=B_SPLINE_CURVE_WITH_KNOTS('',3,(#45164,#45165,#45166,#45167,#45168,
#45169,#45170,#45171,#45172,#45173,#45174,#45175,#45176,#45177,#45178,#45179,
#45180,#45181,#45182,#45183,#45184,#45185),.UNSPECIFIED.,.F.,.F.,(4,3,3,
3,3,3,3,4),(95.3578248186071,95.9661505803537,96.9657979822324,97.9654453841111,
98.9650927859898,99.9647401878685,100.964387589747,101.641010125787),
 .UNSPECIFIED.);
#6347=B_SPLINE_CURVE_WITH_KNOTS('',3,(#45190,#45191,#45192,#45193,#45194,
#45195,#45196,#45197,#45198,#45199,#45200,#45201,#45202,#45203,#45204,#45205,
#45206,#45207,#45208,#45209,#45210,#45211),.UNSPECIFIED.,.F.,.F.,(4,3,3,
3,3,3,3,4),(-110.906899262247,-109.961214206655,-108.961566804777,-107.961919402898,
-106.962272001019,-105.962624599141,-104.962977197262,-104.623713955068),
 .UNSPECIFIED.);
#6348=B_SPLINE_CURVE_WITH_KNOTS('',3,(#45212,#45213,#45214,#45215,#45216,
#45217,#45218,#45219,#45220,#45221,#45222,#45223,#45224,#45225,#45226,#45227,
#45228,#45229,#45230,#45231,#45232,#45233),.UNSPECIFIED.,.F.,.F.,(4,3,3,
3,3,3,3,4),(101.641010125787,101.964034991626,102.963682393505,103.963329795383,
104.962977197262,105.962624599141,106.962272001019,107.924195432966),
 .UNSPECIFIED.);
#6349=B_SPLINE_CURVE_WITH_KNOTS('',3,(#45238,#45239,#45240,#45241,#45242,
#45243,#45244,#45245,#45246,#45247,#45248,#45249,#45250,#45251,#45252,#45253,
#45254,#45255,#45256,#45257,#45258,#45259,#45260,#45261,#45262),
 .UNSPECIFIED.,.F.,.F.,(4,3,3,3,3,3,3,3,4),(-117.190084569427,-116.958746019806,
-115.959098617927,-114.959451216049,-113.95980381417,-112.960156412291,
-111.960509010413,-110.960861608534,-110.906899262247),.UNSPECIFIED.);
#6350=B_SPLINE_CURVE_WITH_KNOTS('',3,(#45263,#45264,#45265,#45266,#45267,
#45268,#45269,#45270,#45271,#45272,#45273,#45274,#45275,#45276,#45277,#45278,
#45279,#45280,#45281,#45282,#45283,#45284,#45285,#45286,#45287),
 .UNSPECIFIED.,.F.,.F.,(4,3,3,3,3,3,3,3,4),(107.924195432966,107.961919402898,
108.961566804777,109.961214206655,110.960861608534,111.960509010413,112.960156412291,
113.95980381417,114.207380740146),.UNSPECIFIED.);
#6351=B_SPLINE_CURVE_WITH_KNOTS('',3,(#45292,#45293,#45294,#45295,#45296,
#45297,#45298,#45299,#45300,#45301,#45302,#45303,#45304,#45305,#45306,#45307,
#45308,#45309,#45310,#45311,#45312,#45313),.UNSPECIFIED.,.F.,.F.,(4,3,3,
3,3,3,3,4),(-123.473269876606,-122.956630431078,-121.956983029199,-120.957335627321,
-119.957688225442,-118.958040823563,-117.958393421685,-117.190084569427),
 .UNSPECIFIED.);
#6352=B_SPLINE_CURVE_WITH_KNOTS('',3,(#45314,#45315,#45316,#45317,#45318,
#45319,#45320,#45321,#45322,#45323,#45324,#45325,#45326,#45327,#45328,#45329,
#45330,#45331,#45332,#45333,#45334,#45335),.UNSPECIFIED.,.F.,.F.,(4,3,3,
3,3,3,3,4),(114.207380740146,114.959451216049,115.959098617927,116.958746019806,
117.958393421685,118.958040823563,119.957688225442,120.490566047325),
 .UNSPECIFIED.);
#6353=B_SPLINE_CURVE_WITH_KNOTS('',3,(#45340,#45341,#45342,#45343,#45344,
#45345,#45346,#45347,#45348,#45349,#45350,#45351,#45352,#45353,#45354,#45355,
#45356,#45357,#45358,#45359,#45360,#45361),.UNSPECIFIED.,.F.,.F.,(4,3,3,
3,3,3,3,4),(-129.756455183786,-128.95451484235,-127.954867440472,-126.955220038593,
-125.955572636714,-124.955925234836,-123.956277832957,-123.473269876606),
 .UNSPECIFIED.);
#6354=B_SPLINE_CURVE_WITH_KNOTS('',3,(#45362,#45363,#45364,#45365,#45366,
#45367,#45368,#45369,#45370,#45371,#45372,#45373,#45374,#45375,#45376,#45377,
#45378,#45379,#45380,#45381,#45382,#45383),.UNSPECIFIED.,.F.,.F.,(4,3,3,
3,3,3,3,4),(120.490566047325,120.957335627321,121.9569830292,122.956630431078,
123.956277832957,124.955925234836,125.955572636714,126.773751354505),
 .UNSPECIFIED.);
#6355=B_SPLINE_CURVE_WITH_KNOTS('',3,(#45388,#45389,#45390,#45391,#45392,
#45393,#45394,#45395,#45396,#45397,#45398,#45399,#45400,#45401,#45402,#45403,
#45404,#45405,#45406,#45407,#45408,#45409,#45410,#45411,#45412),
 .UNSPECIFIED.,.F.,.F.,(4,3,3,3,3,3,3,3,4),(-136.039640490966,-135.952046655501,
-134.952399253622,-133.952751851744,-132.953104449865,-131.953457047986,
-130.953809646108,-129.954162244229,-129.756455183786),.UNSPECIFIED.);
#6356=B_SPLINE_CURVE_WITH_KNOTS('',3,(#45413,#45414,#45415,#45416,#45417,
#45418,#45419,#45420,#45421,#45422,#45423,#45424,#45425,#45426,#45427,#45428,
#45429,#45430,#45431,#45432,#45433,#45434,#45435,#45436,#45437),
 .UNSPECIFIED.,.F.,.F.,(4,3,3,3,3,3,3,3,4),(126.773751354505,126.955220038593,
127.954867440472,128.95451484235,129.954162244229,130.953809646108,131.953457047986,
132.953104449865,133.056936661685),.UNSPECIFIED.);
#6357=B_SPLINE_CURVE_WITH_KNOTS('',3,(#45442,#45443,#45444,#45445,#45446,
#45447,#45448,#45449,#45450,#45451,#45452,#45453,#45454,#45455,#45456,#45457,
#45458,#45459,#45460,#45461,#45462,#45463),.UNSPECIFIED.,.F.,.F.,(4,3,3,
3,3,3,3,4),(-142.322825798145,-141.949931066773,-140.950283664894,-139.950636263016,
-138.950988861137,-137.951341459258,-136.95169405738,-136.039640490966),
 .UNSPECIFIED.);
#6358=B_SPLINE_CURVE_WITH_KNOTS('',3,(#45464,#45465,#45466,#45467,#45468,
#45469,#45470,#45471,#45472,#45473,#45474,#45475,#45476,#45477,#45478,#45479,
#45480,#45481,#45482,#45483,#45484,#45485),.UNSPECIFIED.,.F.,.F.,(4,3,3,
3,3,3,3,4),(133.056936661685,133.952751851744,134.952399253622,135.952046655501,
136.95169405738,137.951341459259,138.950988861137,139.340121968864),
 .UNSPECIFIED.);
#6359=B_SPLINE_CURVE_WITH_KNOTS('',3,(#45490,#45491,#45492,#45493,#45494,
#45495,#45496,#45497,#45498,#45499,#45500,#45501,#45502,#45503,#45504,#45505,
#45506,#45507,#45508,#45509,#45510,#45511),.UNSPECIFIED.,.F.,.F.,(4,3,3,
3,3,3,3,4),(-148.606011105325,-147.947815478045,-146.948168076167,-145.948520674288,
-144.948873272409,-143.94922587053,-142.949578468652,-142.322825798145),
 .UNSPECIFIED.);
#6360=B_SPLINE_CURVE_WITH_KNOTS('',3,(#45512,#45513,#45514,#45515,#45516,
#45517,#45518,#45519,#45520,#45521,#45522,#45523,#45524,#45525,#45526,#45527,
#45528,#45529,#45530,#45531,#45532,#45533),.UNSPECIFIED.,.F.,.F.,(4,3,3,
3,3,3,3,4),(139.340121968864,139.950636263016,140.950283664895,141.949931066773,
142.949578468652,143.949225870531,144.948873272409,145.623307276044),
 .UNSPECIFIED.);
#6361=B_SPLINE_CURVE_WITH_KNOTS('',3,(#45538,#45539,#45540,#45541,#45542,
#45543,#45544,#45545,#45546,#45547,#45548,#45549,#45550,#45551,#45552,#45553,
#45554,#45555,#45556,#45557,#45558,#45559),.UNSPECIFIED.,.F.,.F.,(4,3,3,
3,3,3,3,4),(-154.889196412504,-153.945699889317,-152.946052487439,-151.94640508556,
-150.946757683681,-149.947110281803,-148.947462879924,-148.606011105325),
 .UNSPECIFIED.);
#6362=B_SPLINE_CURVE_WITH_KNOTS('',3,(#45560,#45561,#45562,#45563,#45564,
#45565,#45566,#45567,#45568,#45569,#45570,#45571,#45572,#45573,#45574,#45575,
#45576,#45577,#45578,#45579,#45580,#45581),.UNSPECIFIED.,.F.,.F.,(4,3,3,
3,3,3,3,4),(145.623307276044,145.948520674288,146.948168076167,147.947815478045,
148.947462879924,149.947110281803,150.946757683681,151.906492583223),
 .UNSPECIFIED.);
#6363=B_SPLINE_CURVE_WITH_KNOTS('',3,(#45586,#45587,#45588,#45589,#45590,
#45591,#45592,#45593,#45594,#45595,#45596,#45597,#45598,#45599,#45600,#45601,
#45602,#45603,#45604,#45605,#45606,#45607,#45608,#45609,#45610),
 .UNSPECIFIED.,.F.,.F.,(4,3,3,3,3,3,3,3,4),(-161.172381719684,-160.943231702468,
-159.943584300589,-158.943936898711,-157.944289496832,-156.944642094953,
-155.944994693075,-154.945347291196,-154.889196412504),.UNSPECIFIED.);
#6364=B_SPLINE_CURVE_WITH_KNOTS('',3,(#45611,#45612,#45613,#45614,#45615,
#45616,#45617,#45618,#45619,#45620,#45621,#45622,#45623,#45624,#45625,#45626,
#45627,#45628,#45629,#45630,#45631,#45632,#45633,#45634,#45635),
 .UNSPECIFIED.,.F.,.F.,(4,3,3,3,3,3,3,3,4),(151.906492583223,151.94640508556,
152.946052487439,153.945699889317,154.945347291196,155.944994693075,156.944642094953,
157.944289496832,158.189677890403),.UNSPECIFIED.);
#6365=B_SPLINE_CURVE_WITH_KNOTS('',3,(#45640,#45641,#45642,#45643,#45644,
#45645,#45646,#45647,#45648,#45649,#45650,#45651,#45652,#45653,#45654,#45655,
#45656,#45657,#45658,#45659,#45660,#45661),.UNSPECIFIED.,.F.,.F.,(4,3,3,
3,3,3,3,4),(-167.455567026863,-166.94111611374,-165.941468711862,-164.941821309983,
-163.942173908104,-162.942526506225,-161.942879104347,-161.172381719684),
 .UNSPECIFIED.);
#6366=B_SPLINE_CURVE_WITH_KNOTS('',3,(#45662,#45663,#45664,#45665,#45666,
#45667,#45668,#45669,#45670,#45671,#45672,#45673,#45674,#45675,#45676,#45677,
#45678,#45679,#45680,#45681,#45682,#45683),.UNSPECIFIED.,.F.,.F.,(4,3,3,
3,3,3,3,4),(158.189677890403,158.943936898711,159.94358430059,160.943231702468,
161.942879104347,162.942526506226,163.942173908104,164.472863197582),
 .UNSPECIFIED.);
#6367=B_SPLINE_CURVE_WITH_KNOTS('',3,(#45688,#45689,#45690,#45691,#45692,
#45693,#45694,#45695,#45696,#45697,#45698,#45699,#45700,#45701,#45702,#45703,
#45704,#45705,#45706,#45707,#45708,#45709),.UNSPECIFIED.,.F.,.F.,(4,3,3,
3,3,3,3,4),(-173.738752334043,-172.939000525012,-171.939353123134,-170.939705721255,
-169.940058319376,-168.940410917498,-167.940763515619,-167.455567026863),
 .UNSPECIFIED.);
#6368=B_SPLINE_CURVE_WITH_KNOTS('',3,(#45710,#45711,#45712,#45713,#45714,
#45715,#45716,#45717,#45718,#45719,#45720,#45721,#45722,#45723,#45724,#45725,
#45726,#45727,#45728,#45729,#45730,#45731),.UNSPECIFIED.,.F.,.F.,(4,3,3,
3,3,3,3,4),(164.472863197582,164.941821309983,165.941468711862,166.94111611374,
167.940763515619,168.940410917498,169.940058319376,170.756048504762),
 .UNSPECIFIED.);
#6369=B_SPLINE_CURVE_WITH_KNOTS('',3,(#45736,#45737,#45738,#45739,#45740,
#45741,#45742,#45743,#45744,#45745,#45746,#45747,#45748,#45749,#45750,#45751,
#45752,#45753,#45754,#45755,#45756,#45757,#45758,#45759,#45760),
 .UNSPECIFIED.,.F.,.F.,(4,3,3,3,3,3,3,3,4),(-180.021937641223,-179.936532338163,
-178.936884936284,-177.937237534406,-176.937590132527,-175.937942730648,
-174.93829532877,-173.938647926891,-173.738752334043),.UNSPECIFIED.);
#6370=B_SPLINE_CURVE_WITH_KNOTS('',3,(#45761,#45762,#45763,#45764,#45765,
#45766,#45767,#45768,#45769,#45770,#45771,#45772,#45773,#45774,#45775,#45776,
#45777,#45778,#45779,#45780,#45781,#45782,#45783,#45784,#45785),
 .UNSPECIFIED.,.F.,.F.,(4,3,3,3,3,3,3,3,4),(170.756048504762,170.939705721255,
171.939353123134,172.939000525012,173.938647926891,174.93829532877,175.937942730649,
176.937590132527,177.039233811942),.UNSPECIFIED.);
#6371=B_SPLINE_CURVE_WITH_KNOTS('',3,(#45790,#45791,#45792,#45793,#45794,
#45795,#45796,#45797,#45798,#45799,#45800,#45801,#45802,#45803,#45804,#45805,
#45806,#45807,#45808,#45809,#45810,#45811),.UNSPECIFIED.,.F.,.F.,(4,3,3,
3,3,3,3,4),(-186.305122948402,-185.934416749435,-184.934769347557,-183.935121945678,
-182.935474543799,-181.93582714192,-180.936179740042,-180.021937641223),
 .UNSPECIFIED.);
#6372=B_SPLINE_CURVE_WITH_KNOTS('',3,(#45812,#45813,#45814,#45815,#45816,
#45817,#45818,#45819,#45820,#45821,#45822,#45823,#45824,#45825,#45826,#45827,
#45828,#45829,#45830,#45831,#45832,#45833),.UNSPECIFIED.,.F.,.F.,(4,3,3,
3,3,3,3,4),(177.039233811942,177.937237534406,178.936884936285,179.936532338163,
180.936179740042,181.935827141921,182.935474543799,183.322419119121),
 .UNSPECIFIED.);
#6373=B_SPLINE_CURVE_WITH_KNOTS('',3,(#45838,#45839,#45840,#45841,#45842,
#45843,#45844,#45845,#45846,#45847,#45848,#45849,#45850,#45851,#45852,#45853,
#45854,#45855,#45856,#45857,#45858,#45859),.UNSPECIFIED.,.F.,.F.,(4,3,3,
3,3,3,3,4),(-192.588308255582,-191.932301160707,-190.932653758829,-189.93300635695,
-188.933358955071,-187.933711553193,-186.934064151314,-186.305122948402),
 .UNSPECIFIED.);
#6374=B_SPLINE_CURVE_WITH_KNOTS('',3,(#45860,#45861,#45862,#45863,#45864,
#45865,#45866,#45867,#45868,#45869,#45870,#45871,#45872,#45873,#45874,#45875,
#45876,#45877,#45878,#45879,#45880,#45881),.UNSPECIFIED.,.F.,.F.,(4,3,3,
3,3,3,3,4),(183.322419119121,183.935121945678,184.934769347557,185.934416749435,
186.934064151314,187.933711553193,188.933358955071,189.605604426301),
 .UNSPECIFIED.);
#6375=B_SPLINE_CURVE_WITH_KNOTS('',3,(#45886,#45887,#45888,#45889,#45890,
#45891,#45892,#45893,#45894,#45895,#45896,#45897,#45898,#45899,#45900,#45901,
#45902,#45903,#45904,#45905,#45906,#45907),.UNSPECIFIED.,.F.,.F.,(4,3,3,
3,3,3,3,4),(-198.871493562761,-197.930185571979,-196.930538170101,-195.930890768222,
-194.931243366343,-193.931595964465,-192.931948562586,-192.588308255582),
 .UNSPECIFIED.);
#6376=B_SPLINE_CURVE_WITH_KNOTS('',3,(#45908,#45909,#45910,#45911,#45912,
#45913,#45914,#45915,#45916,#45917,#45918,#45919,#45920,#45921,#45922,#45923,
#45924,#45925,#45926,#45927,#45928,#45929),.UNSPECIFIED.,.F.,.F.,(4,3,3,
3,3,3,3,4),(189.605604426301,189.93300635695,190.932653758829,191.932301160707,
192.931948562586,193.931595964465,194.931243366344,195.88878973348),
 .UNSPECIFIED.);
#6377=B_SPLINE_CURVE_WITH_KNOTS('',3,(#45934,#45935,#45936,#45937,#45938,
#45939,#45940,#45941,#45942,#45943,#45944,#45945,#45946,#45947,#45948,#45949,
#45950,#45951,#45952,#45953,#45954,#45955,#45956,#45957,#45958),
 .UNSPECIFIED.,.F.,.F.,(4,3,3,3,3,3,3,3,4),(-205.154678869941,-204.92771738513,
-203.928069983252,-202.928422581373,-201.928775179494,-200.929127777615,
-199.929480375737,-198.929832973858,-198.871493562761),.UNSPECIFIED.);
#6378=B_SPLINE_CURVE_WITH_KNOTS('',3,(#45959,#45960,#45961,#45962,#45963,
#45964,#45965,#45966,#45967,#45968,#45969,#45970,#45971,#45972,#45973,#45974,
#45975,#45976,#45977,#45978,#45979,#45980,#45981,#45982,#45983),
 .UNSPECIFIED.,.F.,.F.,(4,3,3,3,3,3,3,3,4),(195.88878973348,195.930890768222,
196.930538170101,197.93018557198,198.929832973858,199.929480375737,200.929127777616,
201.928775179494,202.17197504066),.UNSPECIFIED.);
#6379=B_SPLINE_CURVE_WITH_KNOTS('',3,(#45988,#45989,#45990,#45991,#45992,
#45993,#45994,#45995,#45996,#45997,#45998,#45999,#46000,#46001,#46002,#46003,
#46004,#46005,#46006,#46007,#46008,#46009),.UNSPECIFIED.,.F.,.F.,(4,3,3,
3,3,3,3,4),(-211.43786417712,-210.925601796402,-209.925954394524,-208.926306992645,
-207.926659590766,-206.927012188888,-205.927364787009,-205.154678869941),
 .UNSPECIFIED.);
#6380=B_SPLINE_CURVE_WITH_KNOTS('',3,(#46010,#46011,#46012,#46013,#46014,
#46015,#46016,#46017,#46018,#46019,#46020,#46021,#46022,#46023,#46024,#46025,
#46026,#46027,#46028,#46029,#46030,#46031),.UNSPECIFIED.,.F.,.F.,(4,3,3,
3,3,3,3,4),(202.17197504066,202.928422581373,203.928069983252,204.92771738513,
205.927364787009,206.927012188888,207.926659590766,208.455160347839),
 .UNSPECIFIED.);
#6381=B_SPLINE_CURVE_WITH_KNOTS('',3,(#46036,#46037,#46038,#46039,#46040,
#46041,#46042,#46043,#46044,#46045,#46046,#46047,#46048,#46049,#46050,#46051,
#46052,#46053,#46054,#46055,#46056,#46057),.UNSPECIFIED.,.F.,.F.,(4,3,3,
3,3,3,3,4),(-217.7210494843,-216.923486207674,-215.923838805796,-214.924191403917,
-213.924544002038,-212.92489660016,-211.925249198281,-211.43786417712),
 .UNSPECIFIED.);
#6382=B_SPLINE_CURVE_WITH_KNOTS('',3,(#46058,#46059,#46060,#46061,#46062,
#46063,#46064,#46065,#46066,#46067,#46068,#46069,#46070,#46071,#46072,#46073,
#46074,#46075,#46076,#46077,#46078,#46079),.UNSPECIFIED.,.F.,.F.,(4,3,3,
3,3,3,3,4),(208.455160347839,208.926306992645,209.925954394524,210.925601796402,
211.925249198281,212.92489660016,213.924544002039,214.738345655019),
 .UNSPECIFIED.);
#6383=B_SPLINE_CURVE_WITH_KNOTS('',3,(#46084,#46085,#46086,#46087,#46088,
#46089,#46090,#46091,#46092,#46093,#46094,#46095,#46096,#46097,#46098,#46099,
#46100,#46101,#46102,#46103,#46104,#46105,#46106,#46107,#46108),
 .UNSPECIFIED.,.F.,.F.,(4,3,3,3,3,3,3,3,4),(-224.00423479148,-223.921018020825,
-222.921370618947,-221.921723217068,-220.922075815189,-219.92242841331,
-218.922781011432,-217.923133609553,-217.7210494843),.UNSPECIFIED.);
#6384=B_SPLINE_CURVE_WITH_KNOTS('',3,(#46109,#46110,#46111,#46112,#46113,
#46114,#46115,#46116,#46117,#46118,#46119,#46120,#46121,#46122,#46123,#46124,
#46125,#46126,#46127,#46128,#46129,#46130,#46131,#46132,#46133),
 .UNSPECIFIED.,.F.,.F.,(4,3,3,3,3,3,3,3,4),(214.738345655019,214.924191403917,
215.923838805796,216.923486207675,217.923133609553,218.922781011432,219.922428413311,
220.922075815189,221.021530962199),.UNSPECIFIED.);
#6385=B_SPLINE_CURVE_WITH_KNOTS('',3,(#46138,#46139,#46140,#46141,#46142,
#46143,#46144,#46145,#46146,#46147,#46148,#46149,#46150,#46151,#46152,#46153,
#46154,#46155,#46156,#46157,#46158,#46159),.UNSPECIFIED.,.F.,.F.,(4,3,3,
3,3,3,3,4),(-230.287420098659,-229.918902432097,-228.919255030219,-227.91960762834,
-226.919960226461,-225.920312824583,-224.920665422704,-224.00423479148),
 .UNSPECIFIED.);
#6386=B_SPLINE_CURVE_WITH_KNOTS('',3,(#46160,#46161,#46162,#46163,#46164,
#46165,#46166,#46167,#46168,#46169,#46170,#46171,#46172,#46173,#46174,#46175,
#46176,#46177,#46178,#46179,#46180,#46181),.UNSPECIFIED.,.F.,.F.,(4,3,3,
3,3,3,3,4),(221.021530962199,221.921723217068,222.921370618947,223.921018020825,
224.920665422704,225.920312824583,226.919960226461,227.304716269378),
 .UNSPECIFIED.);
#6387=B_SPLINE_CURVE_WITH_KNOTS('',3,(#46186,#46187,#46188,#46189,#46190,
#46191,#46192,#46193,#46194,#46195,#46196,#46197,#46198,#46199,#46200,#46201,
#46202,#46203,#46204,#46205,#46206,#46207),.UNSPECIFIED.,.F.,.F.,(4,3,3,
3,3,3,3,4),(-236.570605405839,-235.916786843369,-234.917139441491,-233.917492039612,
-232.917844637733,-231.918197235855,-230.918549833976,-230.287420098659),
 .UNSPECIFIED.);
#6388=B_SPLINE_CURVE_WITH_KNOTS('',3,(#46208,#46209,#46210,#46211,#46212,
#46213,#46214,#46215,#46216,#46217,#46218,#46219,#46220,#46221,#46222,#46223,
#46224,#46225,#46226,#46227,#46228,#46229),.UNSPECIFIED.,.F.,.F.,(4,3,3,
3,3,3,3,4),(227.304716269378,227.91960762834,228.919255030219,229.918902432097,
230.918549833976,231.918197235855,232.917844637733,233.587901576558),
 .UNSPECIFIED.);
#6389=B_SPLINE_CURVE_WITH_KNOTS('',3,(#46234,#46235,#46236,#46237,#46238,
#46239,#46240,#46241,#46242,#46243,#46244,#46245,#46246,#46247,#46248,#46249,
#46250,#46251,#46252,#46253,#46254,#46255),.UNSPECIFIED.,.F.,.F.,(4,3,3,
3,3,3,3,4),(-242.853790713018,-241.914671254642,-240.915023852763,-239.915376450884,
-238.915729049006,-237.916081647127,-236.916434245248,-236.570605405839),
 .UNSPECIFIED.);
#6390=B_SPLINE_CURVE_WITH_KNOTS('',3,(#46256,#46257,#46258,#46259,#46260,
#46261,#46262,#46263,#46264,#46265,#46266,#46267,#46268,#46269,#46270,#46271,
#46272,#46273,#46274,#46275,#46276,#46277),.UNSPECIFIED.,.F.,.F.,(4,3,3,
3,3,3,3,4),(233.587901576558,233.917492039612,234.917139441491,235.91678684337,
236.916434245248,237.916081647127,238.915729049006,239.871086883737),
 .UNSPECIFIED.);
#6391=B_SPLINE_CURVE_WITH_KNOTS('',3,(#46282,#46283,#46284,#46285,#46286,
#46287,#46288,#46289,#46290,#46291,#46292,#46293,#46294,#46295,#46296,#46297,
#46298,#46299,#46300,#46301,#46302,#46303,#46304,#46305,#46306),
 .UNSPECIFIED.,.F.,.F.,(4,3,3,3,3,3,3,3,4),(-249.136976020198,-248.912203067792,
-247.912555665914,-246.912908264035,-245.913260862156,-244.913613460278,
-243.913966058399,-242.91431865652,-242.853790713018),.UNSPECIFIED.);
#6392=B_SPLINE_CURVE_WITH_KNOTS('',3,(#46307,#46308,#46309,#46310,#46311,
#46312,#46313,#46314,#46315,#46316,#46317,#46318,#46319,#46320,#46321,#46322,
#46323,#46324,#46325,#46326,#46327,#46328,#46329,#46330,#46331),
 .UNSPECIFIED.,.F.,.F.,(4,3,3,3,3,3,3,3,4),(239.871086883737,239.915376450884,
240.915023852763,241.914671254642,242.91431865652,243.913966058399,244.913613460278,
245.913260862156,246.154272190917),.UNSPECIFIED.);
#6393=B_SPLINE_CURVE_WITH_KNOTS('',3,(#46336,#46337,#46338,#46339,#46340,
#46341,#46342,#46343,#46344,#46345,#46346,#46347,#46348,#46349,#46350,#46351,
#46352,#46353,#46354,#46355,#46356,#46357),.UNSPECIFIED.,.F.,.F.,(4,3,3,
3,3,3,3,4),(-255.420161327377,-254.910087479064,-253.910440077186,-252.910792675307,
-251.911145273428,-250.91149787155,-249.911850469671,-249.136976020198),
 .UNSPECIFIED.);
#6394=B_SPLINE_CURVE_WITH_KNOTS('',3,(#46358,#46359,#46360,#46361,#46362,
#46363,#46364,#46365,#46366,#46367,#46368,#46369,#46370,#46371,#46372,#46373,
#46374,#46375,#46376,#46377,#46378,#46379),.UNSPECIFIED.,.F.,.F.,(4,3,3,
3,3,3,3,4),(246.154272190917,246.912908264035,247.912555665914,248.912203067792,
249.911850469671,250.91149787155,251.911145273429,252.437457498096),
 .UNSPECIFIED.);
#6395=B_SPLINE_CURVE_WITH_KNOTS('',3,(#46384,#46385,#46386,#46387,#46388,
#46389,#46390,#46391,#46392,#46393,#46394,#46395,#46396,#46397,#46398,#46399,
#46400,#46401,#46402,#46403,#46404,#46405),.UNSPECIFIED.,.F.,.F.,(4,3,3,
3,3,3,3,4),(-261.703346634557,-260.907971890337,-259.908324488458,-258.908677086579,
-257.9090296847,-256.909382282822,-255.909734880943,-255.420161327377),
 .UNSPECIFIED.);
#6396=B_SPLINE_CURVE_WITH_KNOTS('',3,(#46406,#46407,#46408,#46409,#46410,
#46411,#46412,#46413,#46414,#46415,#46416,#46417,#46418,#46419,#46420,#46421,
#46422,#46423,#46424,#46425,#46426,#46427),.UNSPECIFIED.,.F.,.F.,(4,3,3,
3,3,3,3,4),(252.437457498096,252.910792675307,253.910440077186,254.910087479065,
255.909734880943,256.909382282822,257.909029684701,258.720642805276),
 .UNSPECIFIED.);
#6397=B_SPLINE_CURVE_WITH_KNOTS('',3,(#46432,#46433,#46434,#46435,#46436,
#46437,#46438,#46439,#46440,#46441,#46442,#46443,#46444,#46445,#46446,#46447,
#46448,#46449,#46450,#46451,#46452,#46453,#46454,#46455,#46456),
 .UNSPECIFIED.,.F.,.F.,(4,3,3,3,3,3,3,3,4),(-267.986531941737,-267.905503703487,
-266.905856301609,-265.90620889973,-264.906561497851,-263.906914095973,
-262.907266694094,-261.907619292215,-261.703346634557),.UNSPECIFIED.);
#6398=B_SPLINE_CURVE_WITH_KNOTS('',3,(#46457,#46458,#46459,#46460,#46461,
#46462,#46463,#46464,#46465,#46466,#46467,#46468,#46469,#46470,#46471,#46472,
#46473,#46474,#46475,#46476,#46477,#46478,#46479,#46480,#46481),
 .UNSPECIFIED.,.F.,.F.,(4,3,3,3,3,3,3,3,4),(258.720642805276,258.908677086579,
259.908324488458,260.907971890337,261.907619292215,262.907266694094,263.906914095973,
264.906561497851,265.003828112455),.UNSPECIFIED.);
#6399=B_SPLINE_CURVE_WITH_KNOTS('',3,(#46486,#46487,#46488,#46489,#46490,
#46491,#46492,#46493,#46494,#46495,#46496,#46497,#46498,#46499,#46500,#46501,
#46502,#46503,#46504,#46505,#46506,#46507),.UNSPECIFIED.,.F.,.F.,(4,3,3,
3,3,3,3,4),(-274.269717248916,-273.903388114759,-272.903740712881,-271.904093311002,
-270.904445909123,-269.904798507245,-268.905151105366,-267.986531941737),
 .UNSPECIFIED.);
#6400=B_SPLINE_CURVE_WITH_KNOTS('',3,(#46508,#46509,#46510,#46511,#46512,
#46513,#46514,#46515,#46516,#46517,#46518,#46519,#46520,#46521,#46522,#46523,
#46524,#46525,#46526,#46527,#46528,#46529),.UNSPECIFIED.,.F.,.F.,(4,3,3,
3,3,3,3,4),(265.003828112455,265.90620889973,266.905856301609,267.905503703488,
268.905151105366,269.904798507245,270.904445909124,271.287013419635),
 .UNSPECIFIED.);
#6401=B_SPLINE_CURVE_WITH_KNOTS('',3,(#46534,#46535,#46536,#46537,#46538,
#46539,#46540,#46541,#46542,#46543,#46544,#46545,#46546,#46547,#46548,#46549,
#46550,#46551,#46552,#46553,#46554,#46555),.UNSPECIFIED.,.F.,.F.,(4,3,3,
3,3,3,3,4),(-280.552902556096,-279.901272526031,-278.901625124153,-277.901977722274,
-276.902330320395,-275.902682918517,-274.903035516638,-274.269717248916),
 .UNSPECIFIED.);
#6402=B_SPLINE_CURVE_WITH_KNOTS('',3,(#46556,#46557,#46558,#46559,#46560,
#46561,#46562,#46563,#46564,#46565,#46566,#46567,#46568,#46569,#46570,#46571,
#46572,#46573,#46574,#46575,#46576,#46577),.UNSPECIFIED.,.F.,.F.,(4,3,3,
3,3,3,3,4),(271.287013419635,271.904093311002,272.903740712881,273.90338811476,
274.903035516638,275.902682918517,276.902330320396,277.570198726815),
 .UNSPECIFIED.);
#6403=B_SPLINE_CURVE_WITH_KNOTS('',3,(#46582,#46583,#46584,#46585,#46586,
#46587,#46588,#46589,#46590,#46591,#46592,#46593,#46594,#46595,#46596,#46597,
#46598,#46599,#46600,#46601,#46602,#46603),.UNSPECIFIED.,.F.,.F.,(4,3,3,
3,3,3,3,4),(-286.836087863275,-285.899156937304,-284.899509535425,-283.899862133546,
-282.900214731668,-281.900567329789,-280.90091992791,-280.552902556096),
 .UNSPECIFIED.);
#6404=B_SPLINE_CURVE_WITH_KNOTS('',3,(#46604,#46605,#46606,#46607,#46608,
#46609,#46610,#46611,#46612,#46613,#46614,#46615,#46616,#46617,#46618,#46619,
#46620,#46621,#46622,#46623,#46624,#46625),.UNSPECIFIED.,.F.,.F.,(4,3,3,
3,3,3,3,4),(277.570198726815,277.901977722274,278.901625124153,279.901272526032,
280.90091992791,281.900567329789,282.900214731668,283.853384033994),
 .UNSPECIFIED.);
#6405=B_SPLINE_CURVE_WITH_KNOTS('',3,(#46630,#46631,#46632,#46633,#46634,
#46635,#46636,#46637,#46638,#46639,#46640,#46641,#46642,#46643,#46644,#46645,
#46646,#46647,#46648,#46649,#46650,#46651,#46652,#46653,#46654),
 .UNSPECIFIED.,.F.,.F.,(4,3,3,3,3,3,3,3,4),(-293.119273170455,-292.896688750454,
-291.897041348576,-290.897393946697,-289.897746544818,-288.89809914294,
-287.898451741061,-286.898804339182,-286.836087863275),.UNSPECIFIED.);
#6406=B_SPLINE_CURVE_WITH_KNOTS('',3,(#46655,#46656,#46657,#46658,#46659,
#46660,#46661,#46662,#46663,#46664,#46665,#46666,#46667,#46668,#46669,#46670,
#46671,#46672,#46673,#46674,#46675,#46676,#46677,#46678,#46679),
 .UNSPECIFIED.,.F.,.F.,(4,3,3,3,3,3,3,3,4),(283.853384033994,283.899862133546,
284.899509535425,285.899156937304,286.898804339183,287.898451741061,288.89809914294,
289.897746544819,290.136569341174),.UNSPECIFIED.);
#6407=B_SPLINE_CURVE_WITH_KNOTS('',3,(#46684,#46685,#46686,#46687,#46688,
#46689,#46690,#46691,#46692,#46693,#46694,#46695,#46696,#46697,#46698,#46699,
#46700,#46701,#46702,#46703,#46704,#46705),.UNSPECIFIED.,.F.,.F.,(4,3,3,
3,3,3,3,4),(-299.402458477634,-298.894573161726,-297.894925759848,-296.895278357969,
-295.89563095609,-294.895983554212,-293.896336152333,-293.119273170455),
 .UNSPECIFIED.);
#6408=B_SPLINE_CURVE_WITH_KNOTS('',3,(#46706,#46707,#46708,#46709,#46710,
#46711,#46712,#46713,#46714,#46715,#46716,#46717,#46718,#46719,#46720,#46721,
#46722,#46723,#46724,#46725,#46726,#46727),.UNSPECIFIED.,.F.,.F.,(4,3,3,
3,3,3,3,4),(290.136569341174,290.897393946697,291.897041348576,292.896688750455,
293.896336152333,294.895983554212,295.895630956091,296.419754648353),
 .UNSPECIFIED.);
#6409=B_SPLINE_CURVE_WITH_KNOTS('',3,(#46732,#46733,#46734,#46735,#46736,
#46737,#46738,#46739,#46740,#46741,#46742,#46743,#46744,#46745,#46746,#46747,
#46748,#46749,#46750,#46751,#46752,#46753),.UNSPECIFIED.,.F.,.F.,(4,3,3,
3,3,3,3,4),(-305.685643784814,-304.892457572999,-303.89281017112,-302.893162769241,
-301.893515367363,-300.893867965484,-299.894220563605,-299.402458477634),
 .UNSPECIFIED.);
#6410=B_SPLINE_CURVE_WITH_KNOTS('',3,(#46754,#46755,#46756,#46757,#46758,
#46759,#46760,#46761,#46762,#46763,#46764,#46765,#46766,#46767,#46768,#46769,
#46770,#46771,#46772,#46773,#46774,#46775),.UNSPECIFIED.,.F.,.F.,(4,3,3,
3,3,3,3,4),(296.419754648353,296.895278357969,297.894925759848,298.894573161727,
299.894220563605,300.893867965484,301.893515367363,302.702939955533),
 .UNSPECIFIED.);
#6411=B_SPLINE_CURVE_WITH_KNOTS('',3,(#46780,#46781,#46782,#46783,#46784,
#46785,#46786,#46787,#46788,#46789,#46790,#46791,#46792,#46793,#46794,#46795,
#46796,#46797,#46798,#46799,#46800,#46801,#46802,#46803,#46804),
 .UNSPECIFIED.,.F.,.F.,(4,3,3,3,3,3,3,3,4),(-311.968829091993,-311.889989386149,
-310.890341984271,-309.890694582392,-308.891047180513,-307.891399778635,
-306.891752376756,-305.892104974877,-305.685643784814),.UNSPECIFIED.);
#6412=B_SPLINE_CURVE_WITH_KNOTS('',3,(#46805,#46806,#46807,#46808,#46809,
#46810,#46811,#46812,#46813,#46814,#46815,#46816,#46817,#46818,#46819,#46820,
#46821,#46822,#46823,#46824,#46825,#46826,#46827,#46828,#46829),
 .UNSPECIFIED.,.F.,.F.,(4,3,3,3,3,3,3,3,4),(302.702939955533,302.893162769242,
303.89281017112,304.892457572999,305.892104974878,306.891752376756,307.891399778635,
308.891047180514,308.986125262712),.UNSPECIFIED.);
#6413=B_SPLINE_CURVE_WITH_KNOTS('',3,(#46834,#46835,#46836,#46837,#46838,
#46839,#46840,#46841,#46842,#46843,#46844,#46845,#46846,#46847,#46848,#46849,
#46850,#46851,#46852,#46853,#46854,#46855),.UNSPECIFIED.,.F.,.F.,(4,3,3,
3,3,3,3,4),(-318.252014399173,-317.887873797421,-316.888226395543,-315.888578993664,
-314.888931591785,-313.889284189907,-312.889636788028,-311.968829091993),
 .UNSPECIFIED.);
#6414=B_SPLINE_CURVE_WITH_KNOTS('',3,(#46856,#46857,#46858,#46859,#46860,
#46861,#46862,#46863,#46864,#46865,#46866,#46867,#46868,#46869,#46870,#46871,
#46872,#46873,#46874,#46875,#46876,#46877),.UNSPECIFIED.,.F.,.F.,(4,3,3,
3,3,3,3,4),(308.986125262712,309.890694582392,310.890341984271,311.88998938615,
312.889636788028,313.889284189907,314.888931591786,315.269310569892),
 .UNSPECIFIED.);
#6415=B_SPLINE_CURVE_WITH_KNOTS('',3,(#46882,#46883,#46884,#46885,#46886,
#46887,#46888,#46889,#46890,#46891,#46892,#46893,#46894,#46895,#46896,#46897,
#46898,#46899,#46900,#46901,#46902,#46903),.UNSPECIFIED.,.F.,.F.,(4,3,3,
3,3,3,3,4),(-324.535199706353,-323.885758208694,-322.886110806815,-321.886463404936,
-320.886816003058,-319.887168601179,-318.8875211993,-318.252014399173),
 .UNSPECIFIED.);
#6416=B_SPLINE_CURVE_WITH_KNOTS('',3,(#46904,#46905,#46906,#46907,#46908,
#46909,#46910,#46911,#46912,#46913,#46914,#46915,#46916,#46917,#46918,#46919,
#46920,#46921,#46922,#46923,#46924,#46925),.UNSPECIFIED.,.F.,.F.,(4,3,3,
3,3,3,3,4),(315.269310569892,315.888578993664,316.888226395543,317.887873797422,
318.8875211993,319.887168601179,320.886816003058,321.552495877072),
 .UNSPECIFIED.);
#6417=B_SPLINE_CURVE_WITH_KNOTS('',3,(#46930,#46931,#46932,#46933,#46934,
#46935,#46936,#46937,#46938,#46939,#46940,#46941,#46942,#46943,#46944,#46945,
#46946,#46947,#46948,#46949,#46950,#46951),.UNSPECIFIED.,.F.,.F.,(4,3,3,
3,3,3,3,4),(-330.818385013532,-329.883642619966,-328.883995218087,-327.884347816208,
-326.88470041433,-325.885053012451,-324.885405610572,-324.535199706353),
 .UNSPECIFIED.);
#6418=B_SPLINE_CURVE_WITH_KNOTS('',3,(#46952,#46953,#46954,#46955,#46956,
#46957,#46958,#46959,#46960,#46961,#46962,#46963,#46964,#46965,#46966,#46967,
#46968,#46969,#46970,#46971,#46972,#46973),.UNSPECIFIED.,.F.,.F.,(4,3,3,
3,3,3,3,4),(321.552495877072,321.886463404936,322.886110806815,323.885758208694,
324.885405610572,325.885053012451,326.88470041433,327.835681184251),
 .UNSPECIFIED.);
#6419=B_SPLINE_CURVE_WITH_KNOTS('',3,(#46978,#46979,#46980,#46981,#46982,
#46983,#46984,#46985,#46986,#46987,#46988,#46989,#46990,#46991,#46992,#46993,
#46994,#46995,#46996,#46997,#46998,#46999,#47000,#47001,#47002),
 .UNSPECIFIED.,.F.,.F.,(4,3,3,3,3,3,3,3,4),(-337.101570320712,-336.881174433116,
-335.881527031238,-334.881879629359,-333.88223222748,-332.882584825602,
-331.882937423723,-330.883290021844,-330.818385013532),.UNSPECIFIED.);
#6420=B_SPLINE_CURVE_WITH_KNOTS('',3,(#47003,#47004,#47005,#47006,#47007,
#47008,#47009,#47010,#47011,#47012,#47013,#47014,#47015,#47016,#47017,#47018,
#47019,#47020,#47021,#47022,#47023,#47024,#47025,#47026,#47027),
 .UNSPECIFIED.,.F.,.F.,(4,3,3,3,3,3,3,3,4),(327.835681184251,327.884347816209,
328.883995218087,329.883642619966,330.883290021845,331.882937423723,332.882584825602,
333.882232227481,334.118866491431),.UNSPECIFIED.);
#6421=B_SPLINE_CURVE_WITH_KNOTS('',3,(#47032,#47033,#47034,#47035,#47036,
#47037,#47038,#47039,#47040,#47041,#47042,#47043,#47044,#47045,#47046,#47047,
#47048,#47049,#47050,#47051,#47052,#47053),.UNSPECIFIED.,.F.,.F.,(4,3,3,
3,3,3,3,4),(-343.384755627891,-342.879058844389,-341.87941144251,-340.879764040631,
-339.880116638753,-338.880469236874,-337.880821834995,-337.101570320712),
 .UNSPECIFIED.);
#6422=B_SPLINE_CURVE_WITH_KNOTS('',3,(#47054,#47055,#47056,#47057,#47058,
#47059,#47060,#47061,#47062,#47063,#47064,#47065,#47066,#47067,#47068,#47069,
#47070,#47071,#47072,#47073,#47074,#47075),.UNSPECIFIED.,.F.,.F.,(4,3,3,
3,3,3,3,4),(334.118866491431,334.881879629359,335.881527031238,336.881174433117,
337.880821834995,338.880469236874,339.880116638753,340.40205179861),
 .UNSPECIFIED.);
#6423=B_SPLINE_CURVE_WITH_KNOTS('',3,(#47080,#47081,#47082,#47083,#47084,
#47085,#47086,#47087,#47088,#47089,#47090,#47091,#47092,#47093,#47094,#47095,
#47096,#47097,#47098,#47099,#47100,#47101),.UNSPECIFIED.,.F.,.F.,(4,3,3,
3,3,3,3,4),(-349.667940935071,-348.876943255661,-347.877295853782,-346.877648451903,
-345.878001050025,-344.878353648146,-343.878706246267,-343.384755627891),
 .UNSPECIFIED.);
#6424=B_SPLINE_CURVE_WITH_KNOTS('',3,(#47102,#47103,#47104,#47105,#47106,
#47107,#47108,#47109,#47110,#47111,#47112,#47113,#47114,#47115,#47116,#47117,
#47118,#47119,#47120,#47121,#47122,#47123),.UNSPECIFIED.,.F.,.F.,(4,3,3,
3,3,3,3,4),(340.40205179861,340.879764040631,341.87941144251,342.879058844389,
343.878706246268,344.878353648146,345.878001050025,346.68523710579),
 .UNSPECIFIED.);
#6425=B_SPLINE_CURVE_WITH_KNOTS('',3,(#47128,#47129,#47130,#47131,#47132,
#47133,#47134,#47135,#47136,#47137,#47138,#47139,#47140,#47141,#47142,#47143,
#47144,#47145,#47146,#47147,#47148,#47149,#47150,#47151,#47152),
 .UNSPECIFIED.,.F.,.F.,(4,3,3,3,3,3,3,3,4),(-355.95112624225,-355.874475068811,
-354.874827666933,-353.875180265054,-352.875532863175,-351.875885461297,
-350.876238059418,-349.876590657539,-349.667940935071),.UNSPECIFIED.);
#6426=B_SPLINE_CURVE_WITH_KNOTS('',3,(#47153,#47154,#47155,#47156,#47157,
#47158,#47159,#47160,#47161,#47162,#47163,#47164,#47165,#47166,#47167,#47168,
#47169,#47170,#47171,#47172,#47173,#47174,#47175,#47176,#47177),
 .UNSPECIFIED.,.F.,.F.,(4,3,3,3,3,3,3,3,4),(346.68523710579,346.877648451904,
347.877295853782,348.876943255661,349.87659065754,350.876238059418,351.875885461297,
352.875532863176,352.968422412969),.UNSPECIFIED.);
#6427=B_SPLINE_CURVE_WITH_KNOTS('',3,(#47182,#47183,#47184,#47185,#47186,
#47187,#47188,#47189,#47190,#47191,#47192,#47193,#47194,#47195,#47196,#47197,
#47198,#47199,#47200,#47201,#47202,#47203),.UNSPECIFIED.,.F.,.F.,(4,3,3,
3,3,3,3,4),(-362.23431154943,-361.872359480084,-360.872712078205,-359.873064676326,
-358.873417274448,-357.873769872569,-356.87412247069,-355.95112624225),
 .UNSPECIFIED.);
#6428=B_SPLINE_CURVE_WITH_KNOTS('',3,(#47204,#47205,#47206,#47207,#47208,
#47209,#47210,#47211,#47212,#47213,#47214,#47215,#47216,#47217,#47218,#47219,
#47220,#47221,#47222,#47223,#47224,#47225),.UNSPECIFIED.,.F.,.F.,(4,3,3,
3,3,3,3,4),(352.968422412969,353.875180265054,354.874827666933,355.874475068812,
356.87412247069,357.873769872569,358.873417274448,359.251607720149),
 .UNSPECIFIED.);
#6429=B_SPLINE_CURVE_WITH_KNOTS('',3,(#47230,#47231,#47232,#47233,#47234,
#47235,#47236,#47237,#47238,#47239,#47240,#47241,#47242,#47243,#47244,#47245,
#47246,#47247,#47248,#47249,#47250,#47251),.UNSPECIFIED.,.F.,.F.,(4,3,3,
3,3,3,3,4),(-368.51749685661,-367.870243891356,-366.870596489477,-365.870949087598,
-364.87130168572,-363.871654283841,-362.872006881962,-362.23431154943),
 .UNSPECIFIED.);
#6430=B_SPLINE_CURVE_WITH_KNOTS('',3,(#47252,#47253,#47254,#47255,#47256,
#47257,#47258,#47259,#47260,#47261,#47262,#47263,#47264,#47265,#47266,#47267,
#47268,#47269,#47270,#47271,#47272,#47273),.UNSPECIFIED.,.F.,.F.,(4,3,3,
3,3,3,3,4),(359.251607720149,359.873064676327,360.872712078205,361.872359480084,
362.872006881963,363.871654283841,364.87130168572,365.534793027328),
 .UNSPECIFIED.);
#6431=B_SPLINE_CURVE_WITH_KNOTS('',3,(#47278,#47279,#47280,#47281,#47282,
#47283,#47284,#47285,#47286,#47287,#47288,#47289,#47290,#47291,#47292,#47293,
#47294,#47295,#47296,#47297,#47298,#47299),.UNSPECIFIED.,.F.,.F.,(4,3,3,
3,3,3,3,4),(-374.800682163789,-373.868128302628,-372.868480900749,-371.86883349887,
-370.869186096992,-369.869538695113,-368.869891293234,-368.51749685661),
 .UNSPECIFIED.);
#6432=B_SPLINE_CURVE_WITH_KNOTS('',3,(#47300,#47301,#47302,#47303,#47304,
#47305,#47306,#47307,#47308,#47309,#47310,#47311,#47312,#47313,#47314,#47315,
#47316,#47317,#47318,#47319,#47320,#47321),.UNSPECIFIED.,.F.,.F.,(4,3,3,
3,3,3,3,4),(365.534793027328,365.870949087599,366.870596489477,367.870243891356,
368.869891293235,369.869538695113,370.869186096992,371.817978334508),
 .UNSPECIFIED.);
#6433=B_SPLINE_CURVE_WITH_KNOTS('',3,(#47326,#47327,#47328,#47329,#47330,
#47331,#47332,#47333,#47334,#47335,#47336,#47337,#47338,#47339,#47340,#47341,
#47342,#47343,#47344,#47345,#47346,#47347,#47348,#47349,#47350),
 .UNSPECIFIED.,.F.,.F.,(4,3,3,3,3,3,3,3,4),(-381.083867470969,-380.865660115779,
-379.8660127139,-378.866365312021,-377.866717910143,-376.867070508264,-375.867423106385,
-374.867775704506,-374.800682163789),.UNSPECIFIED.);
#6434=B_SPLINE_CURVE_WITH_KNOTS('',3,(#47351,#47352,#47353,#47354,#47355,
#47356,#47357,#47358,#47359,#47360,#47361,#47362,#47363,#47364,#47365,#47366,
#47367,#47368,#47369,#47370,#47371,#47372,#47373,#47374,#47375),
 .UNSPECIFIED.,.F.,.F.,(4,3,3,3,3,3,3,3,4),(371.817978334508,371.868833498871,
372.868480900749,373.868128302628,374.867775704507,375.867423106385,376.867070508264,
377.866717910143,378.101163641688),.UNSPECIFIED.);
#6435=B_SPLINE_CURVE_WITH_KNOTS('',3,(#47380,#47381,#47382,#47383,#47384,
#47385,#47386,#47387,#47388,#47389,#47390,#47391,#47392,#47393,#47394,#47395,
#47396,#47397,#47398,#47399,#47400,#47401),.UNSPECIFIED.,.F.,.F.,(4,3,3,
3,3,3,3,4),(-387.367052778148,-386.863544527051,-385.863897125172,-384.864249723293,
-383.864602321415,-382.864954919536,-381.865307517657,-381.083867470969),
 .UNSPECIFIED.);
#6436=B_SPLINE_CURVE_WITH_KNOTS('',3,(#47402,#47403,#47404,#47405,#47406,
#47407,#47408,#47409,#47410,#47411,#47412,#47413,#47414,#47415,#47416,#47417,
#47418,#47419,#47420,#47421,#47422,#47423),.UNSPECIFIED.,.F.,.F.,(4,3,3,
3,3,3,3,4),(378.101163641688,378.866365312022,379.8660127139,380.865660115779,
381.865307517658,382.864954919536,383.864602321415,384.384348948867),
 .UNSPECIFIED.);
#6437=B_SPLINE_CURVE_WITH_KNOTS('',3,(#47428,#47429,#47430,#47431,#47432,
#47433,#47434,#47435,#47436,#47437,#47438,#47439,#47440,#47441,#47442,#47443,
#47444,#47445,#47446,#47447,#47448,#47449),.UNSPECIFIED.,.F.,.F.,(4,3,3,
3,3,3,3,4),(-393.650238085328,-392.861428938323,-391.861781536444,-390.862134134565,
-389.862486732687,-388.862839330808,-387.863191928929,-387.367052778148),
 .UNSPECIFIED.);
#6438=B_SPLINE_CURVE_WITH_KNOTS('',3,(#47450,#47451,#47452,#47453,#47454,
#47455,#47456,#47457,#47458,#47459,#47460,#47461,#47462,#47463,#47464,#47465,
#47466,#47467,#47468,#47469,#47470,#47471),.UNSPECIFIED.,.F.,.F.,(4,3,3,
3,3,3,3,4),(384.384348948867,384.864249723294,385.863897125172,386.863544527051,
387.86319192893,388.862839330808,389.862486732687,390.667534256047),
 .UNSPECIFIED.);
#6439=B_SPLINE_CURVE_WITH_KNOTS('',3,(#47476,#47477,#47478,#47479,#47480,
#47481,#47482,#47483,#47484,#47485,#47486,#47487,#47488,#47489,#47490,#47491,
#47492,#47493,#47494,#47495,#47496,#47497,#47498,#47499,#47500),
 .UNSPECIFIED.,.F.,.F.,(4,3,3,3,3,3,3,3,4),(-399.933423392507,-399.858960751474,
-398.859313349595,-397.859665947716,-396.860018545838,-395.860371143959,
-394.86072374208,-393.861076340201,-393.650238085328),.UNSPECIFIED.);
#6440=B_SPLINE_CURVE_WITH_KNOTS('',3,(#47501,#47502,#47503,#47504,#47505,
#47506,#47507,#47508,#47509,#47510,#47511,#47512,#47513,#47514,#47515,#47516,
#47517,#47518,#47519,#47520,#47521,#47522,#47523,#47524,#47525),
 .UNSPECIFIED.,.F.,.F.,(4,3,3,3,3,3,3,3,4),(390.667534256047,390.862134134566,
391.861781536444,392.861428938323,393.861076340202,394.86072374208,395.860371143959,
396.860018545838,396.950719563226),.UNSPECIFIED.);
#6441=B_SPLINE_CURVE_WITH_KNOTS('',3,(#47530,#47531,#47532,#47533,#47534,
#47535,#47536,#47537,#47538,#47539,#47540,#47541,#47542,#47543,#47544,#47545,
#47546,#47547,#47548,#47549,#47550,#47551),.UNSPECIFIED.,.F.,.F.,(4,3,3,
3,3,3,3,4),(-406.216608699687,-405.856845162746,-404.857197760867,-403.857550358988,
-402.85790295711,-401.858255555231,-400.858608153352,-399.933423392507),
 .UNSPECIFIED.);
#6442=B_SPLINE_CURVE_WITH_KNOTS('',3,(#47552,#47553,#47554,#47555,#47556,
#47557,#47558,#47559,#47560,#47561,#47562,#47563,#47564,#47565,#47566,#47567,
#47568,#47569,#47570,#47571,#47572,#47573),.UNSPECIFIED.,.F.,.F.,(4,3,3,
3,3,3,3,4),(396.950719563226,397.859665947717,398.859313349595,399.858960751474,
400.858608153353,401.858255555231,402.85790295711,403.233904870406),
 .UNSPECIFIED.);
#6443=B_SPLINE_CURVE_WITH_KNOTS('',3,(#47578,#47579,#47580,#47581,#47582,
#47583,#47584,#47585,#47586,#47587,#47588,#47589,#47590,#47591,#47592,#47593,
#47594,#47595,#47596,#47597,#47598,#47599),.UNSPECIFIED.,.F.,.F.,(4,3,3,
3,3,3,3,4),(-412.499794006867,-411.854729574018,-410.855082172139,-409.85543477026,
-408.855787368382,-407.856139966503,-406.856492564624,-406.216608699687),
 .UNSPECIFIED.);
#6444=B_SPLINE_CURVE_WITH_KNOTS('',3,(#47600,#47601,#47602,#47603,#47604,
#47605,#47606,#47607,#47608,#47609,#47610,#47611,#47612,#47613,#47614,#47615,
#47616,#47617,#47618,#47619,#47620,#47621),.UNSPECIFIED.,.F.,.F.,(4,3,3,
3,3,3,3,4),(403.233904870406,403.857550358989,404.857197760867,405.856845162746,
406.856492564625,407.856139966503,408.855787368382,409.517090177585),
 .UNSPECIFIED.);
#6445=B_SPLINE_CURVE_WITH_KNOTS('',3,(#47626,#47627,#47628,#47629,#47630,
#47631,#47632,#47633,#47634,#47635,#47636,#47637,#47638,#47639,#47640,#47641,
#47642,#47643,#47644,#47645,#47646,#47647),.UNSPECIFIED.,.F.,.F.,(4,3,3,
3,3,3,3,4),(-418.782979314046,-417.85261398529,-416.852966583411,-415.853319181532,
-414.853671779654,-413.854024377775,-412.854376975896,-412.499794006867),
 .UNSPECIFIED.);
#6446=B_SPLINE_CURVE_WITH_KNOTS('',3,(#47648,#47649,#47650,#47651,#47652,
#47653,#47654,#47655,#47656,#47657,#47658,#47659,#47660,#47661,#47662,#47663,
#47664,#47665,#47666,#47667,#47668,#47669),.UNSPECIFIED.,.F.,.F.,(4,3,3,
3,3,3,3,4),(409.517090177585,409.855434770261,410.855082172139,411.854729574018,
412.854376975897,413.854024377775,414.853671779654,415.800275484765),
 .UNSPECIFIED.);
#6447=B_SPLINE_CURVE_WITH_KNOTS('',3,(#47674,#47675,#47676,#47677,#47678,
#47679,#47680,#47681,#47682,#47683,#47684,#47685,#47686,#47687,#47688,#47689,
#47690,#47691,#47692,#47693,#47694,#47695,#47696,#47697,#47698),
 .UNSPECIFIED.,.F.,.F.,(4,3,3,3,3,3,3,3,4),(-425.066164621226,-424.850145798441,
-423.850498396562,-422.850850994683,-421.851203592805,-420.851556190926,
-419.851908789047,-418.852261387169,-418.782979314046),.UNSPECIFIED.);
#6448=B_SPLINE_CURVE_WITH_KNOTS('',3,(#47699,#47700,#47701,#47702,#47703,
#47704,#47705,#47706,#47707,#47708,#47709,#47710,#47711,#47712,#47713,#47714,
#47715,#47716,#47717,#47718,#47719,#47720,#47721,#47722,#47723),
 .UNSPECIFIED.,.F.,.F.,(4,3,3,3,3,3,3,3,4),(415.800275484765,415.853319181533,
416.852966583412,417.85261398529,418.852261387169,419.851908789048,420.851556190926,
421.851203592805,422.083460791945),.UNSPECIFIED.);
#6449=B_SPLINE_CURVE_WITH_KNOTS('',3,(#47728,#47729,#47730,#47731,#47732,
#47733,#47734,#47735,#47736,#47737,#47738,#47739,#47740,#47741,#47742,#47743,
#47744,#47745,#47746,#47747,#47748,#47749),.UNSPECIFIED.,.F.,.F.,(4,3,3,
3,3,3,3,4),(-431.349349928405,-430.848030209713,-429.848382807834,-428.848735405955,
-427.849088004077,-426.849440602198,-425.849793200319,-425.066164621226),
 .UNSPECIFIED.);
#6450=B_SPLINE_CURVE_WITH_KNOTS('',3,(#47750,#47751,#47752,#47753,#47754,
#47755,#47756,#47757,#47758,#47759,#47760,#47761,#47762,#47763,#47764,#47765,
#47766,#47767,#47768,#47769,#47770,#47771),.UNSPECIFIED.,.F.,.F.,(4,3,3,
3,3,3,3,4),(422.083460791945,422.850850994684,423.850498396562,424.850145798441,
425.84979320032,426.849440602198,427.849088004077,428.366646099124),
 .UNSPECIFIED.);
#6451=B_SPLINE_CURVE_WITH_KNOTS('',3,(#47776,#47777,#47778,#47779,#47780,
#47781,#47782,#47783,#47784,#47785,#47786,#47787,#47788,#47789,#47790,#47791,
#47792,#47793,#47794,#47795,#47796,#47797),.UNSPECIFIED.,.F.,.F.,(4,3,3,
3,3,3,3,4),(-437.632535235585,-436.845914620985,-435.846267219106,-434.846619817227,
-433.846972415349,-432.84732501347,-431.847677611592,-431.349349928405),
 .UNSPECIFIED.);
#6452=B_SPLINE_CURVE_WITH_KNOTS('',3,(#47798,#47799,#47800,#47801,#47802,
#47803,#47804,#47805,#47806,#47807,#47808,#47809,#47810,#47811,#47812,#47813,
#47814,#47815,#47816,#47817,#47818,#47819),.UNSPECIFIED.,.F.,.F.,(4,3,3,
3,3,3,3,4),(428.366646099124,428.848735405956,429.848382807834,430.848030209713,
431.847677611592,432.84732501347,433.846972415349,434.649831406304),
 .UNSPECIFIED.);
#6453=B_SPLINE_CURVE_WITH_KNOTS('',3,(#47824,#47825,#47826,#47827,#47828,
#47829,#47830,#47831,#47832,#47833,#47834,#47835,#47836,#47837,#47838,#47839,
#47840,#47841,#47842,#47843,#47844,#47845,#47846,#47847,#47848),
 .UNSPECIFIED.,.F.,.F.,(4,3,3,3,3,3,3,3,4),(-443.915720542764,-443.843446434136,
-442.843799032257,-441.844151630378,-440.8445042285,-439.844856826621,-438.845209424742,
-437.845562022864,-437.632535235585),.UNSPECIFIED.);
#6454=B_SPLINE_CURVE_WITH_KNOTS('',3,(#47849,#47850,#47851,#47852,#47853,
#47854,#47855,#47856,#47857,#47858,#47859,#47860,#47861,#47862,#47863,#47864,
#47865,#47866,#47867,#47868,#47869,#47870,#47871,#47872,#47873),
 .UNSPECIFIED.,.F.,.F.,(4,3,3,3,3,3,3,3,4),(434.649831406304,434.846619817228,
435.846267219106,436.845914620985,437.845562022864,438.845209424743,439.844856826621,
440.8445042285,440.933016713483),.UNSPECIFIED.);
#6455=B_SPLINE_CURVE_WITH_KNOTS('',3,(#47878,#47879,#47880,#47881,#47882,
#47883,#47884,#47885,#47886,#47887,#47888,#47889,#47890,#47891,#47892,#47893,
#47894,#47895,#47896,#47897,#47898,#47899),.UNSPECIFIED.,.F.,.F.,(4,3,3,
3,3,3,3,4),(-450.198905849944,-449.841330845408,-448.841683443529,-447.84203604165,
-446.842388639772,-445.842741237893,-444.843093836014,-443.915720542764),
 .UNSPECIFIED.);
#6456=B_SPLINE_CURVE_WITH_KNOTS('',3,(#47900,#47901,#47902,#47903,#47904,
#47905,#47906,#47907,#47908,#47909,#47910,#47911,#47912,#47913,#47914,#47915,
#47916,#47917,#47918,#47919,#47920,#47921),.UNSPECIFIED.,.F.,.F.,(4,3,3,
3,3,3,3,4),(440.933016713483,441.844151630379,442.843799032257,443.843446434136,
444.843093836015,445.842741237893,446.842388639772,447.216202020663),
 .UNSPECIFIED.);
#6457=B_SPLINE_CURVE_WITH_KNOTS('',3,(#47926,#47927,#47928,#47929,#47930,
#47931,#47932,#47933,#47934,#47935,#47936,#47937,#47938,#47939,#47940,#47941,
#47942,#47943,#47944,#47945,#47946,#47947),.UNSPECIFIED.,.F.,.F.,(4,3,3,
3,3,3,3,4),(-456.482091157123,-455.83921525668,-454.839567854801,-453.839920452923,
-452.840273051044,-451.840625649165,-450.840978247287,-450.198905849944),
 .UNSPECIFIED.);
#6458=B_SPLINE_CURVE_WITH_KNOTS('',3,(#47948,#47949,#47950,#47951,#47952,
#47953,#47954,#47955,#47956,#47957,#47958,#47959,#47960,#47961,#47962,#47963,
#47964,#47965,#47966,#47967,#47968,#47969),.UNSPECIFIED.,.F.,.F.,(4,3,3,
3,3,3,3,4),(447.216202020663,447.842036041651,448.841683443529,449.841330845408,
450.840978247287,451.840625649165,452.840273051044,453.499387327842),
 .UNSPECIFIED.);
#6459=B_SPLINE_CURVE_WITH_KNOTS('',3,(#47974,#47975,#47976,#47977,#47978,
#47979,#47980,#47981,#47982,#47983,#47984,#47985,#47986,#47987,#47988,#47989,
#47990,#47991,#47992,#47993,#47994,#47995),.UNSPECIFIED.,.F.,.F.,(4,3,3,
3,3,3,3,4),(-462.765276464303,-461.837099667952,-460.837452266073,-459.837804864195,
-458.838157462316,-457.838510060437,-456.838862658559,-456.482091157123),
 .UNSPECIFIED.);
#6460=B_SPLINE_CURVE_WITH_KNOTS('',3,(#47996,#47997,#47998,#47999,#48000,
#48001,#48002,#48003,#48004,#48005,#48006,#48007,#48008,#48009,#48010,#48011,
#48012,#48013,#48014,#48015,#48016,#48017),.UNSPECIFIED.,.F.,.F.,(4,3,3,
3,3,3,3,4),(453.499387327842,453.839920452923,454.839567854801,455.83921525668,
456.838862658559,457.838510060438,458.838157462316,459.782572635022),
 .UNSPECIFIED.);
#6461=B_SPLINE_CURVE_WITH_KNOTS('',3,(#48022,#48023,#48024,#48025,#48026,
#48027,#48028,#48029,#48030,#48031,#48032,#48033,#48034,#48035,#48036,#48037,
#48038,#48039,#48040,#48041,#48042,#48043,#48044,#48045,#48046),
 .UNSPECIFIED.,.F.,.F.,(4,3,3,3,3,3,3,3,4),(-469.048461771483,-468.834631481103,
-467.834984079224,-466.835336677345,-465.835689275467,-464.836041873588,
-463.836394471709,-462.836747069831,-462.765276464303),.UNSPECIFIED.);
#6462=B_SPLINE_CURVE_WITH_KNOTS('',3,(#48047,#48048,#48049,#48050,#48051,
#48052,#48053,#48054,#48055,#48056,#48057,#48058,#48059,#48060,#48061,#48062,
#48063,#48064,#48065,#48066,#48067,#48068,#48069,#48070,#48071),
 .UNSPECIFIED.,.F.,.F.,(4,3,3,3,3,3,3,3,4),(459.782572635022,459.837804864195,
460.837452266074,461.837099667952,462.836747069831,463.83639447171,464.836041873588,
465.835689275467,466.065757942202),.UNSPECIFIED.);
#6463=B_SPLINE_CURVE_WITH_KNOTS('',3,(#48076,#48077,#48078,#48079,#48080,
#48081,#48082,#48083,#48084,#48085,#48086,#48087,#48088,#48089,#48090,#48091,
#48092,#48093,#48094,#48095,#48096,#48097),.UNSPECIFIED.,.F.,.F.,(4,3,3,
3,3,3,3,4),(-475.331647078662,-474.832515892375,-473.832868490496,-472.833221088618,
-471.833573686739,-470.83392628486,-469.834278882981,-469.048461771483),
 .UNSPECIFIED.);
#6464=B_SPLINE_CURVE_WITH_KNOTS('',3,(#48098,#48099,#48100,#48101,#48102,
#48103,#48104,#48105,#48106,#48107,#48108,#48109,#48110,#48111,#48112,#48113,
#48114,#48115,#48116,#48117,#48118,#48119),.UNSPECIFIED.,.F.,.F.,(4,3,3,
3,3,3,3,4),(466.065757942202,466.835336677346,467.834984079224,468.834631481103,
469.834278882982,470.833926284861,471.833573686739,472.348943249381),
 .UNSPECIFIED.);
#6465=B_SPLINE_CURVE_WITH_KNOTS('',3,(#48124,#48125,#48126,#48127,#48128,
#48129,#48130,#48131,#48132,#48133,#48134,#48135,#48136,#48137,#48138,#48139,
#48140,#48141,#48142,#48143,#48144,#48145),.UNSPECIFIED.,.F.,.F.,(4,3,3,
3,3,3,3,4),(-481.614832385842,-480.830400303647,-479.830752901768,-478.83110549989,
-477.831458098011,-476.831810696132,-475.832163294254,-475.331647078662),
 .UNSPECIFIED.);
#6466=B_SPLINE_CURVE_WITH_KNOTS('',3,(#48146,#48147,#48148,#48149,#48150,
#48151,#48152,#48153,#48154,#48155,#48156,#48157,#48158,#48159,#48160,#48161,
#48162,#48163,#48164,#48165,#48166,#48167),.UNSPECIFIED.,.F.,.F.,(4,3,3,
3,3,3,3,4),(472.348943249381,472.833221088618,473.832868490496,474.832515892375,
475.832163294254,476.831810696133,477.831458098011,478.632128556561),
 .UNSPECIFIED.);
#6467=B_SPLINE_CURVE_WITH_KNOTS('',3,(#48172,#48173,#48174,#48175,#48176,
#48177,#48178,#48179,#48180,#48181,#48182,#48183,#48184,#48185,#48186,#48187,
#48188,#48189,#48190,#48191,#48192,#48193,#48194,#48195,#48196),
 .UNSPECIFIED.,.F.,.F.,(4,3,3,3,3,3,3,3,4),(-487.898017693021,-487.827932116798,
-486.828284714919,-485.82863731304,-484.828989911162,-483.829342509283,
-482.829695107404,-481.830047705526,-481.614832385842),.UNSPECIFIED.);
#6468=B_SPLINE_CURVE_WITH_KNOTS('',3,(#48197,#48198,#48199,#48200,#48201,
#48202,#48203,#48204,#48205,#48206,#48207,#48208,#48209,#48210,#48211,#48212,
#48213,#48214,#48215,#48216,#48217,#48218,#48219,#48220,#48221),
 .UNSPECIFIED.,.F.,.F.,(4,3,3,3,3,3,3,3,4),(478.632128556561,478.83110549989,
479.830752901769,480.830400303647,481.830047705526,482.829695107405,483.829342509283,
484.828989911162,484.91531386374),.UNSPECIFIED.);
#6469=B_SPLINE_CURVE_WITH_KNOTS('',3,(#48226,#48227,#48228,#48229,#48230,
#48231,#48232,#48233,#48234,#48235,#48236,#48237,#48238,#48239,#48240,#48241,
#48242,#48243,#48244,#48245,#48246,#48247),.UNSPECIFIED.,.F.,.F.,(4,3,3,
3,3,3,3,4),(-494.181203000201,-493.82581652807,-492.826169126191,-491.826521724312,
-490.826874322434,-489.827226920555,-488.827579518676,-487.898017693021),
 .UNSPECIFIED.);
#6470=B_SPLINE_CURVE_WITH_KNOTS('',3,(#48248,#48249,#48250,#48251,#48252,
#48253,#48254,#48255,#48256,#48257,#48258,#48259,#48260,#48261,#48262,#48263,
#48264,#48265,#48266,#48267,#48268,#48269),.UNSPECIFIED.,.F.,.F.,(4,3,3,
3,3,3,3,4),(484.91531386374,485.828637313041,486.828284714919,487.827932116798,
488.827579518677,489.827226920556,490.826874322434,491.19849917092),
 .UNSPECIFIED.);
#6471=B_SPLINE_CURVE_WITH_KNOTS('',3,(#48274,#48275,#48276,#48277,#48278,
#48279,#48280,#48281,#48282,#48283,#48284,#48285,#48286,#48287,#48288,#48289,
#48290,#48291,#48292,#48293,#48294,#48295),.UNSPECIFIED.,.F.,.F.,(4,3,3,
3,3,3,3,4),(-500.46438830738,-499.823700939342,-498.824053537463,-497.824406135585,
-496.824758733706,-495.825111331827,-494.825463929949,-494.181203000201),
 .UNSPECIFIED.);
#6472=B_SPLINE_CURVE_WITH_KNOTS('',3,(#48296,#48297,#48298,#48299,#48300,
#48301,#48302,#48303,#48304,#48305,#48306,#48307,#48308,#48309,#48310,#48311,
#48312,#48313,#48314,#48315,#48316,#48317),.UNSPECIFIED.,.F.,.F.,(4,3,3,
3,3,3,3,4),(491.19849917092,491.826521724313,492.826169126192,493.82581652807,
494.825463929949,495.825111331828,496.824758733706,497.481684478099),
 .UNSPECIFIED.);
#6473=B_SPLINE_CURVE_WITH_KNOTS('',3,(#48322,#48323,#48324,#48325,#48326,
#48327,#48328,#48329,#48330,#48331,#48332,#48333,#48334,#48335,#48336,#48337,
#48338,#48339,#48340,#48341,#48342,#48343),.UNSPECIFIED.,.F.,.F.,(4,3,3,
3,3,3,3,4),(-506.74757361456,-505.821585350614,-504.821937948735,-503.822290546857,
-502.822643144978,-501.822995743099,-500.823348341221,-500.46438830738),
 .UNSPECIFIED.);
#6474=B_SPLINE_CURVE_WITH_KNOTS('',3,(#48344,#48345,#48346,#48347,#48348,
#48349,#48350,#48351,#48352,#48353,#48354,#48355,#48356,#48357,#48358,#48359,
#48360,#48361,#48362,#48363,#48364,#48365),.UNSPECIFIED.,.F.,.F.,(4,3,3,
3,3,3,3,4),(497.481684478099,497.824406135585,498.824053537464,499.823700939342,
500.823348341221,501.8229957431,502.822643144978,503.764869785279),
 .UNSPECIFIED.);
#6475=B_SPLINE_CURVE_WITH_KNOTS('',3,(#48370,#48371,#48372,#48373,#48374,
#48375,#48376,#48377,#48378,#48379,#48380,#48381,#48382,#48383,#48384,#48385,
#48386,#48387,#48388,#48389,#48390,#48391,#48392,#48393,#48394),
 .UNSPECIFIED.,.F.,.F.,(4,3,3,3,3,3,3,3,4),(-513.03075892174,-512.819117163765,
-511.819469761886,-510.819822360007,-509.820174958129,-508.82052755625,
-507.820880154371,-506.821232752493,-506.74757361456),.UNSPECIFIED.);
#6476=B_SPLINE_CURVE_WITH_KNOTS('',3,(#48395,#48396,#48397,#48398,#48399,
#48400,#48401,#48402,#48403,#48404,#48405,#48406,#48407,#48408,#48409,#48410,
#48411,#48412,#48413,#48414,#48415,#48416,#48417,#48418,#48419),
 .UNSPECIFIED.,.F.,.F.,(4,3,3,3,3,3,3,3,4),(503.764869785279,503.822290546857,
504.821937948736,505.821585350615,506.821232752493,507.820880154372,508.820527556251,
509.820174958129,510.048055092458),.UNSPECIFIED.);
#6477=B_SPLINE_CURVE_WITH_KNOTS('',3,(#48424,#48425,#48426,#48427,#48428,
#48429,#48430,#48431,#48432,#48433,#48434,#48435,#48436,#48437,#48438,#48439,
#48440,#48441,#48442,#48443,#48444,#48445),.UNSPECIFIED.,.F.,.F.,(4,3,3,
3,3,3,3,4),(-519.313944228919,-518.817001575037,-517.817354173158,-516.81770677128,
-515.818059369401,-514.818411967522,-513.818764565644,-513.03075892174),
 .UNSPECIFIED.);
#6478=B_SPLINE_CURVE_WITH_KNOTS('',3,(#48446,#48447,#48448,#48449,#48450,
#48451,#48452,#48453,#48454,#48455,#48456,#48457,#48458,#48459,#48460,#48461,
#48462,#48463,#48464,#48465,#48466,#48467),.UNSPECIFIED.,.F.,.F.,(4,3,3,
3,3,3,3,4),(510.048055092458,510.819822360008,511.819469761886,512.819117163765,
513.818764565644,514.818411967523,515.818059369401,516.331240399638),
 .UNSPECIFIED.);
#6479=B_SPLINE_CURVE_WITH_KNOTS('',3,(#48472,#48473,#48474,#48475,#48476,
#48477,#48478,#48479,#48480,#48481,#48482,#48483,#48484,#48485,#48486,#48487,
#48488,#48489,#48490,#48491,#48492,#48493),.UNSPECIFIED.,.F.,.F.,(4,3,3,
3,3,3,3,4),(-525.597129536099,-524.814885986309,-523.815238584431,-522.815591182552,
-521.815943780673,-520.816296378794,-519.816648976916,-519.313944228919),
 .UNSPECIFIED.);
#6480=B_SPLINE_CURVE_WITH_KNOTS('',3,(#48494,#48495,#48496,#48497,#48498,
#48499,#48500,#48501,#48502,#48503,#48504,#48505,#48506,#48507,#48508,#48509,
#48510,#48511,#48512,#48513,#48514,#48515),.UNSPECIFIED.,.F.,.F.,(4,3,3,
3,3,3,3,4),(516.331240399638,516.81770677128,517.817354173159,518.817001575037,
519.816648976916,520.816296378795,521.815943780673,522.614425706818),
 .UNSPECIFIED.);
#6481=B_SPLINE_CURVE_WITH_KNOTS('',3,(#48520,#48521,#48522,#48523,#48524,
#48525,#48526,#48527,#48528,#48529,#48530,#48531,#48532,#48533,#48534,#48535,
#48536,#48537,#48538,#48539,#48540,#48541,#48542,#48543,#48544),
 .UNSPECIFIED.,.F.,.F.,(4,3,3,3,3,3,3,3,4),(-531.880314843278,-531.81241779946,
-530.812770397581,-529.813122995703,-528.813475593824,-527.813828191945,
-526.814180790067,-525.814533388188,-525.597129536099),.UNSPECIFIED.);
#6482=B_SPLINE_CURVE_WITH_KNOTS('',3,(#48545,#48546,#48547,#48548,#48549,
#48550,#48551,#48552,#48553,#48554,#48555,#48556,#48557,#48558,#48559,#48560,
#48561,#48562,#48563,#48564,#48565,#48566,#48567,#48568,#48569),
 .UNSPECIFIED.,.F.,.F.,(4,3,3,3,3,3,3,3,4),(522.614425706818,522.815591182552,
523.815238584431,524.814885986309,525.814533388188,526.814180790067,527.813828191946,
528.813475593824,528.897611013997),.UNSPECIFIED.);
#6483=B_SPLINE_CURVE_WITH_KNOTS('',3,(#48574,#48575,#48576,#48577,#48578,
#48579,#48580,#48581,#48582,#48583,#48584,#48585,#48586,#48587,#48588,#48589,
#48590,#48591,#48592,#48593,#48594,#48595),.UNSPECIFIED.,.F.,.F.,(4,3,3,
3,3,3,3,4),(-538.163500150458,-537.810302210732,-536.810654808853,-535.811007406975,
-534.811360005096,-533.811712603217,-532.812065201339,-531.880314843278),
 .UNSPECIFIED.);
#6484=B_SPLINE_CURVE_WITH_KNOTS('',3,(#48596,#48597,#48598,#48599,#48600,
#48601,#48602,#48603,#48604,#48605,#48606,#48607,#48608,#48609,#48610,#48611,
#48612,#48613,#48614,#48615,#48616,#48617),.UNSPECIFIED.,.F.,.F.,(4,3,3,
3,3,3,3,4),(528.897611013997,529.813122995703,530.812770397582,531.81241779946,
532.812065201339,533.811712603218,534.811360005096,535.180796321177),
 .UNSPECIFIED.);
#6485=B_SPLINE_CURVE_WITH_KNOTS('',3,(#48622,#48623,#48624,#48625,#48626,
#48627,#48628,#48629,#48630,#48631,#48632,#48633,#48634,#48635,#48636,#48637,
#48638,#48639,#48640,#48641,#48642,#48643),.UNSPECIFIED.,.F.,.F.,(4,3,3,
3,3,3,3,4),(-544.446685457637,-543.808186622004,-542.808539220125,-541.808891818247,
-540.809244416368,-539.809597014489,-538.809949612611,-538.163500150458),
 .UNSPECIFIED.);
#6486=B_SPLINE_CURVE_WITH_KNOTS('',3,(#48644,#48645,#48646,#48647,#48648,
#48649,#48650,#48651,#48652,#48653,#48654,#48655,#48656,#48657,#48658,#48659,
#48660,#48661,#48662,#48663,#48664,#48665),.UNSPECIFIED.,.F.,.F.,(4,3,3,
3,3,3,3,4),(535.180796321177,535.811007406975,536.810654808854,537.810302210732,
538.809949612611,539.80959701449,540.809244416369,541.463981628356),
 .UNSPECIFIED.);
#6487=B_SPLINE_CURVE_WITH_KNOTS('',3,(#48670,#48671,#48672,#48673,#48674,
#48675,#48676,#48677,#48678,#48679,#48680,#48681,#48682,#48683,#48684,#48685,
#48686,#48687,#48688,#48689,#48690,#48691),.UNSPECIFIED.,.F.,.F.,(4,3,3,
3,3,3,3,4),(-550.729870764817,-549.806071033276,-548.806423631398,-547.806776229519,
-546.80712882764,-545.807481425761,-544.807834023883,-544.446685457637),
 .UNSPECIFIED.);
#6488=B_SPLINE_CURVE_WITH_KNOTS('',3,(#48692,#48693,#48694,#48695,#48696,
#48697,#48698,#48699,#48700,#48701,#48702,#48703,#48704,#48705,#48706,#48707,
#48708,#48709,#48710,#48711,#48712,#48713),.UNSPECIFIED.,.F.,.F.,(4,3,3,
3,3,3,3,4),(541.463981628356,541.808891818247,542.808539220126,543.808186622004,
544.807834023883,545.807481425762,546.80712882764,547.747166935536),
 .UNSPECIFIED.);
#6489=B_SPLINE_CURVE_WITH_KNOTS('',3,(#48719,#48720,#48721,#48722),
 .UNSPECIFIED.,.F.,.F.,(4,4),(562.345084992573,562.359025869153),
 .UNSPECIFIED.);
#6490=B_SPLINE_CURVE_WITH_KNOTS('',3,(#48728,#48729,#48730,#48731,#48732,
#48733,#48734,#48735,#48736,#48737,#48738,#48739,#48740,#48741,#48742,#48743,
#48744,#48745,#48746,#48747,#48748,#48749),.UNSPECIFIED.,.F.,.F.,(4,3,3,
3,3,3,3,4),(556.061899685393,556.423048251639,557.422695653518,558.422343055396,
559.421990457275,560.421637859154,561.421285261032,562.345084992573),
 .UNSPECIFIED.);
#6491=B_SPLINE_CURVE_WITH_KNOTS('',3,(#48752,#48753,#48754,#48755,#48756,
#48757,#48758,#48759,#48760),.UNSPECIFIED.,.F.,.F.,(4,1,1,1,1,1,4),(556.061899685393,
556.121508979378,557.121156381257,558.120803783136,559.120451185014,560.120098586893,
561.119745988772),.UNSPECIFIED.);
#6492=B_SPLINE_CURVE_WITH_KNOTS('',3,(#48765,#48766,#48767,#48768,#48769,
#48770,#48771,#48772,#48773,#48774,#48775,#48776,#48777,#48778,#48779,#48780,
#48781,#48782,#48783,#48784,#48785,#48786),.UNSPECIFIED.,.F.,.F.,(4,3,3,
3,3,3,3,4),(549.778714378214,550.425163840367,551.424811242246,552.424458644124,
553.424106046003,554.423753447882,555.42340084976,556.061899685393),
 .UNSPECIFIED.);
#6493=B_SPLINE_CURVE_WITH_KNOTS('',3,(#48787,#48788,#48789,#48790,#48791,
#48792,#48793,#48794,#48795,#48796,#48797,#48798,#48799,#48800,#48801,#48802,
#48803,#48804,#48805,#48806,#48807,#48808),.UNSPECIFIED.,.F.,.F.,(4,3,3,
3,3,3,3,4),(549.778714378214,550.123624568106,551.123271969985,552.122919371864,
553.122566773742,554.122214175621,555.1218615775,556.061899685393),
 .UNSPECIFIED.);
#6494=B_SPLINE_CURVE_WITH_KNOTS('',3,(#48813,#48814,#48815,#48816,#48817,
#48818,#48819,#48820,#48821,#48822,#48823,#48824,#48825,#48826,#48827,#48828,
#48829,#48830,#48831,#48832,#48833,#48834),.UNSPECIFIED.,.F.,.F.,(4,3,3,
3,3,3,3,4),(543.495529071034,544.427279429095,545.426926830973,546.426574232852,
547.426221634731,548.42586903661,549.425516438488,549.778714378214),
 .UNSPECIFIED.);
#6495=B_SPLINE_CURVE_WITH_KNOTS('',3,(#48835,#48836,#48837,#48838,#48839,
#48840,#48841,#48842,#48843,#48844,#48845,#48846,#48847,#48848,#48849,#48850,
#48851,#48852,#48853,#48854,#48855,#48856),.UNSPECIFIED.,.F.,.F.,(4,3,3,
3,3,3,3,4),(543.495529071034,544.125740156834,545.125387558713,546.125034960591,
547.12468236247,548.124329764349,549.123977166228,549.778714378214),
 .UNSPECIFIED.);
#6496=B_SPLINE_CURVE_WITH_KNOTS('',3,(#48861,#48862,#48863,#48864,#48865,
#48866,#48867,#48868,#48869,#48870,#48871),.UNSPECIFIED.,.F.,.F.,(4,1,1,
1,1,1,1,1,4),(537.212343763854,537.429747615944,538.429395017823,539.429042419701,
540.42868982158,541.428337223459,542.427984625337,543.427632027216,543.495529071034),
 .UNSPECIFIED.);
#6497=B_SPLINE_CURVE_WITH_KNOTS('',3,(#48872,#48873,#48874,#48875,#48876,
#48877,#48878,#48879,#48880,#48881),.UNSPECIFIED.,.F.,.F.,(4,1,1,1,1,1,
1,4),(537.212343763855,538.127855745562,539.127503147441,540.127150549319,
541.126797951198,542.126445353077,543.126092754955,543.495529071034),
 .UNSPECIFIED.);
#6498=B_SPLINE_CURVE_WITH_KNOTS('',3,(#48886,#48887,#48888,#48889,#48890,
#48891,#48892,#48893,#48894,#48895),.UNSPECIFIED.,.F.,.F.,(4,1,1,1,1,1,
1,4),(530.929158456675,531.431863204672,532.431510606551,533.431158008429,
534.430805410308,535.430452812187,536.430100214065,537.212343763854),
 .UNSPECIFIED.);
#6499=B_SPLINE_CURVE_WITH_KNOTS('',3,(#48896,#48897,#48898,#48899,#48900,
#48901,#48902,#48903,#48904,#48905,#48906),.UNSPECIFIED.,.F.,.F.,(4,1,1,
1,1,1,1,1,4),(530.929158456675,531.130323932411,532.12997133429,533.129618736168,
534.129266138047,535.128913539926,536.128560941805,537.128208343683,537.212343763855),
 .UNSPECIFIED.);
#6500=B_SPLINE_CURVE_WITH_KNOTS('',3,(#48911,#48912,#48913,#48914,#48915,
#48916,#48917,#48918,#48919,#48920),.UNSPECIFIED.,.F.,.F.,(4,1,1,1,1,1,
1,4),(524.645973149495,525.4339787934,526.433626195278,527.433273597157,
528.432920999036,529.432568400914,530.432215802793,530.929158456675),
 .UNSPECIFIED.);
#6501=B_SPLINE_CURVE_WITH_KNOTS('',3,(#48921,#48922,#48923,#48924,#48925,
#48926,#48927,#48928,#48929,#48930),.UNSPECIFIED.,.F.,.F.,(4,1,1,1,1,1,
1,4),(524.645973149496,525.132439521139,526.132086923018,527.131734324896,
528.131381726775,529.131029128654,530.130676530532,530.929158456675),
 .UNSPECIFIED.);
#6502=B_SPLINE_CURVE_WITH_KNOTS('',3,(#48935,#48936,#48937,#48938,#48939,
#48940,#48941,#48942,#48943,#48944,#48945),.UNSPECIFIED.,.F.,.F.,(4,1,1,
1,1,1,1,1,4),(518.362787842316,518.436446980249,519.436094382128,520.435741784006,
521.435389185885,522.435036587764,523.434683989642,524.434331391521,524.645973149495),
 .UNSPECIFIED.);
#6503=B_SPLINE_CURVE_WITH_KNOTS('',3,(#48946,#48947,#48948,#48949,#48950,
#48951,#48952,#48953,#48954,#48955),.UNSPECIFIED.,.F.,.F.,(4,1,1,1,1,1,
1,4),(518.362787842316,519.134555109867,520.134202511746,521.133849913624,
522.133497315503,523.133144717382,524.13279211926,524.645973149496),
 .UNSPECIFIED.);
#6504=B_SPLINE_CURVE_WITH_KNOTS('',3,(#48960,#48961,#48962,#48963,#48964,
#48965,#48966,#48967,#48968,#48969),.UNSPECIFIED.,.F.,.F.,(4,1,1,1,1,1,
1,4),(512.079602535136,512.438562568977,513.438209970855,514.437857372734,
515.437504774613,516.437152176492,517.43679957837,518.362787842316),
 .UNSPECIFIED.);
#6505=B_SPLINE_CURVE_WITH_KNOTS('',3,(#48970,#48971,#48972,#48973,#48974,
#48975,#48976,#48977,#48978,#48979,#48980,#48981,#48982,#48983,#48984,#48985,
#48986,#48987,#48988,#48989,#48990,#48991,#48992,#48993,#48994),
 .UNSPECIFIED.,.F.,.F.,(4,3,3,3,3,3,3,3,4),(512.079602535136,512.137023296716,
513.136670698595,514.136318100474,515.135965502352,516.135612904231,517.13526030611,
518.134907707988,518.362787842316),.UNSPECIFIED.);
#6506=B_SPLINE_CURVE_WITH_KNOTS('',3,(#48999,#49000,#49001,#49002,#49003,
#49004,#49005,#49006,#49007,#49008),.UNSPECIFIED.,.F.,.F.,(4,1,1,1,1,1,
1,4),(505.796417227957,506.440678157705,507.440325559583,508.439972961462,
509.439620363341,510.439267765219,511.438915167098,512.079602535136),
 .UNSPECIFIED.);
#6507=B_SPLINE_CURVE_WITH_KNOTS('',3,(#49009,#49010,#49011,#49012,#49013,
#49014,#49015,#49016,#49017,#49018,#49019,#49020,#49021,#49022,#49023,#49024,
#49025,#49026,#49027,#49028,#49029,#49030),.UNSPECIFIED.,.F.,.F.,(4,3,3,
3,3,3,3,4),(505.796417227957,506.139138885444,507.138786287323,508.138433689201,
509.13808109108,510.137728492959,511.137375894838,512.079602535136),
 .UNSPECIFIED.);
#6508=B_SPLINE_CURVE_WITH_KNOTS('',3,(#49035,#49036,#49037,#49038,#49039,
#49040,#49041,#49042,#49043,#49044),.UNSPECIFIED.,.F.,.F.,(4,1,1,1,1,1,
1,4),(499.513231920777,500.442793746433,501.442441148311,502.44208855019,
503.441735952069,504.441383353947,505.441030755826,505.796417227957),
 .UNSPECIFIED.);
#6509=B_SPLINE_CURVE_WITH_KNOTS('',3,(#49045,#49046,#49047,#49048,#49049,
#49050,#49051,#49052,#49053,#49054),.UNSPECIFIED.,.F.,.F.,(4,1,1,1,1,1,
1,4),(499.513231920777,500.141254474172,501.140901876051,502.140549277929,
503.140196679808,504.139844081687,505.139491483565,505.796417227957),
 .UNSPECIFIED.);
#6510=B_SPLINE_CURVE_WITH_KNOTS('',3,(#49059,#49060,#49061,#49062,#49063,
#49064,#49065,#49066,#49067,#49068,#49069),.UNSPECIFIED.,.F.,.F.,(4,1,1,
1,1,1,1,1,4),(493.230046613597,493.445261933282,494.44490933516,495.444556737039,
496.444204138918,497.443851540797,498.443498942675,499.443146344554,499.513231920777),
 .UNSPECIFIED.);
#6511=B_SPLINE_CURVE_WITH_KNOTS('',3,(#49070,#49071,#49072,#49073,#49074,
#49075,#49076,#49077,#49078,#49079),.UNSPECIFIED.,.F.,.F.,(4,1,1,1,1,1,
1,4),(493.230046613598,494.1433700629,495.143017464778,496.142664866657,
497.142312268536,498.141959670415,499.141607072293,499.513231920777),
 .UNSPECIFIED.);
#6512=B_SPLINE_CURVE_WITH_KNOTS('',3,(#49084,#49085,#49086,#49087,#49088,
#49089,#49090,#49091,#49092,#49093),.UNSPECIFIED.,.F.,.F.,(4,1,1,1,1,1,
1,4),(486.946861306418,487.44737752201,488.447024923888,489.446672325767,
490.446319727646,491.445967129524,492.445614531403,493.230046613597),
 .UNSPECIFIED.);
#6513=B_SPLINE_CURVE_WITH_KNOTS('',3,(#49094,#49095,#49096,#49097,#49098,
#49099,#49100,#49101,#49102,#49103,#49104),.UNSPECIFIED.,.F.,.F.,(4,1,1,
1,1,1,1,1,4),(486.946861306418,487.145838249749,488.145485651628,489.145133053506,
490.144780455385,491.144427857264,492.144075259142,493.143722661021,493.230046613598),
 .UNSPECIFIED.);
#6514=B_SPLINE_CURVE_WITH_KNOTS('',3,(#49109,#49110,#49111,#49112,#49113,
#49114,#49115,#49116,#49117,#49118),.UNSPECIFIED.,.F.,.F.,(4,1,1,1,1,1,
1,4),(480.663675999238,481.449493110738,482.449140512616,483.448787914495,
484.448435316374,485.448082718252,486.447730120131,486.946861306418),
 .UNSPECIFIED.);
#6515=B_SPLINE_CURVE_WITH_KNOTS('',3,(#49119,#49120,#49121,#49122,#49123,
#49124,#49125,#49126,#49127,#49128),.UNSPECIFIED.,.F.,.F.,(4,1,1,1,1,1,
1,4),(480.663675999239,481.147953838477,482.147601240356,483.147248642234,
484.146896044113,485.146543445992,486.14619084787,486.946861306418),
 .UNSPECIFIED.);
#6516=B_SPLINE_CURVE_WITH_KNOTS('',3,(#49133,#49134,#49135,#49136,#49137,
#49138,#49139,#49140,#49141,#49142,#49143),.UNSPECIFIED.,.F.,.F.,(4,1,1,
1,1,1,1,1,4),(474.380490692059,474.451961297587,475.451608699465,476.451256101344,
477.450903503223,478.450550905102,479.45019830698,480.449845708859,480.663675999238),
 .UNSPECIFIED.);
#6517=B_SPLINE_CURVE_WITH_KNOTS('',3,(#49144,#49145,#49146,#49147,#49148,
#49149,#49150,#49151,#49152,#49153),.UNSPECIFIED.,.F.,.F.,(4,1,1,1,1,1,
1,4),(474.380490692059,475.150069427205,476.149716829084,477.149364230962,
478.149011632841,479.14865903472,480.148306436598,480.663675999239),
 .UNSPECIFIED.);
#6518=B_SPLINE_CURVE_WITH_KNOTS('',3,(#49158,#49159,#49160,#49161,#49162,
#49163,#49164,#49165,#49166,#49167),.UNSPECIFIED.,.F.,.F.,(4,1,1,1,1,1,
1,4),(468.097305384879,468.454076886315,469.453724288193,470.453371690072,
471.453019091951,472.452666493829,473.452313895708,474.380490692059),
 .UNSPECIFIED.);
#6519=B_SPLINE_CURVE_WITH_KNOTS('',3,(#49168,#49169,#49170,#49171,#49172,
#49173,#49174,#49175,#49176,#49177,#49178),.UNSPECIFIED.,.F.,.F.,(4,1,1,
1,1,1,1,1,4),(468.09730538488,468.152537614054,469.152185015933,470.151832417811,
471.15147981969,472.151127221569,473.150774623447,474.150422025326,474.380490692059),
 .UNSPECIFIED.);
#6520=B_SPLINE_CURVE_WITH_KNOTS('',3,(#49183,#49184,#49185,#49186,#49187,
#49188,#49189,#49190,#49191,#49192,#49193,#49194,#49195,#49196,#49197,#49198,
#49199,#49200,#49201,#49202,#49203,#49204),.UNSPECIFIED.,.F.,.F.,(4,3,3,
3,3,3,3,4),(461.814120077699,462.456192475043,463.455839876921,464.4554872788,
465.455134680679,466.454782082557,467.454429484436,468.097305384879),
 .UNSPECIFIED.);
#6521=B_SPLINE_CURVE_WITH_KNOTS('',3,(#49205,#49206,#49207,#49208,#49209,
#49210,#49211,#49212,#49213,#49214),.UNSPECIFIED.,.F.,.F.,(4,1,1,1,1,1,
1,4),(461.8141200777,462.154653202782,463.154300604661,464.153948006539,
465.153595408418,466.153242810297,467.152890212175,468.09730538488),
 .UNSPECIFIED.);
#6522=B_SPLINE_CURVE_WITH_KNOTS('',3,(#49219,#49220,#49221,#49222,#49223,
#49224,#49225,#49226,#49227,#49228,#49229,#49230,#49231,#49232,#49233,#49234,
#49235,#49236,#49237,#49238,#49239,#49240),.UNSPECIFIED.,.F.,.F.,(4,3,3,
3,3,3,3,4),(455.53093477052,456.458308063771,457.457955465649,458.457602867528,
459.457250269407,460.456897671285,461.456545073164,461.814120077699),
 .UNSPECIFIED.);
#6523=B_SPLINE_CURVE_WITH_KNOTS('',3,(#49241,#49242,#49243,#49244,#49245,
#49246,#49247,#49248,#49249,#49250),.UNSPECIFIED.,.F.,.F.,(4,1,1,1,1,1,
1,4),(455.53093477052,456.15676879151,457.156416193389,458.156063595267,
459.155710997146,460.155358399025,461.155005800903,461.8141200777),
 .UNSPECIFIED.);
#6524=B_SPLINE_CURVE_WITH_KNOTS('',3,(#49255,#49256,#49257,#49258,#49259,
#49260,#49261,#49262,#49263,#49264,#49265),.UNSPECIFIED.,.F.,.F.,(4,1,1,
1,1,1,1,1,4),(449.24774946334,449.46077625062,450.460423652498,451.460071054377,
452.459718456256,453.459365858134,454.459013260013,455.458660661892,455.53093477052),
 .UNSPECIFIED.);
#6525=B_SPLINE_CURVE_WITH_KNOTS('',3,(#49266,#49267,#49268,#49269,#49270,
#49271,#49272,#49273,#49274,#49275),.UNSPECIFIED.,.F.,.F.,(4,1,1,1,1,1,
1,4),(449.247749463341,450.158884380238,451.158531782116,452.158179183995,
453.157826585874,454.157473987752,455.157121389631,455.53093477052),
 .UNSPECIFIED.);
#6526=B_SPLINE_CURVE_WITH_KNOTS('',3,(#49280,#49281,#49282,#49283,#49284,
#49285,#49286,#49287,#49288,#49289),.UNSPECIFIED.,.F.,.F.,(4,1,1,1,1,1,
1,4),(442.964564156161,443.462891839348,444.462539241226,445.462186643105,
446.461834044984,447.461481446862,448.461128848741,449.24774946334),
 .UNSPECIFIED.);
#6527=B_SPLINE_CURVE_WITH_KNOTS('',3,(#49290,#49291,#49292,#49293,#49294,
#49295,#49296,#49297,#49298,#49299,#49300),.UNSPECIFIED.,.F.,.F.,(4,1,1,
1,1,1,1,1,4),(442.964564156161,443.161352567087,444.160999968966,445.160647370844,
446.160294772723,447.159942174602,448.15958957648,449.159236978359,449.247749463341),
 .UNSPECIFIED.);
#6528=B_SPLINE_CURVE_WITH_KNOTS('',3,(#49305,#49306,#49307,#49308,#49309,
#49310,#49311,#49312,#49313,#49314),.UNSPECIFIED.,.F.,.F.,(4,1,1,1,1,1,
1,4),(436.681378848981,437.465007428075,438.464654829954,439.464302231833,
440.463949633712,441.46359703559,442.463244437469,442.964564156161),
 .UNSPECIFIED.);
#6529=B_SPLINE_CURVE_WITH_KNOTS('',3,(#49315,#49316,#49317,#49318,#49319,
#49320,#49321,#49322,#49323,#49324),.UNSPECIFIED.,.F.,.F.,(4,1,1,1,1,1,
1,4),(436.681378848982,437.163468155815,438.163115557694,439.162762959572,
440.162410361451,441.16205776333,442.161705165208,442.964564156161),
 .UNSPECIFIED.);
#6530=B_SPLINE_CURVE_WITH_KNOTS('',3,(#49329,#49330,#49331,#49332,#49333,
#49334,#49335,#49336,#49337,#49338,#49339),.UNSPECIFIED.,.F.,.F.,(4,1,1,
1,1,1,1,1,4),(430.398193541802,430.467475614925,431.467123016803,432.466770418682,
433.466417820561,434.466065222439,435.465712624318,436.465360026197,436.681378848981),
 .UNSPECIFIED.);
#6531=B_SPLINE_CURVE_WITH_KNOTS('',3,(#49340,#49341,#49342,#49343,#49344,
#49345,#49346,#49347,#49348,#49349),.UNSPECIFIED.,.F.,.F.,(4,1,1,1,1,1,
1,4),(430.398193541802,431.165583744543,432.165231146421,433.1648785483,
434.164525950179,435.164173352057,436.163820753936,436.681378848982),
 .UNSPECIFIED.);
#6532=B_SPLINE_CURVE_WITH_KNOTS('',3,(#49354,#49355,#49356,#49357,#49358,
#49359,#49360,#49361,#49362,#49363),.UNSPECIFIED.,.F.,.F.,(4,1,1,1,1,1,
1,4),(424.115008234622,424.469591203653,425.469238605531,426.46888600741,
427.468533409289,428.468180811167,429.467828213046,430.398193541802),
 .UNSPECIFIED.);
#6533=B_SPLINE_CURVE_WITH_KNOTS('',3,(#49364,#49365,#49366,#49367,#49368,
#49369,#49370,#49371,#49372,#49373,#49374),.UNSPECIFIED.,.F.,.F.,(4,1,1,
1,1,1,1,1,4),(424.115008234623,424.168051931392,425.167699333271,426.167346735149,
427.166994137028,428.166641538907,429.166288940785,430.165936342664,430.398193541802),
 .UNSPECIFIED.);
#6534=B_SPLINE_CURVE_WITH_KNOTS('',3,(#49379,#49380,#49381,#49382,#49383,
#49384,#49385,#49386,#49387,#49388),.UNSPECIFIED.,.F.,.F.,(4,1,1,1,1,1,
1,4),(417.831822927443,418.47170679238,419.471354194259,420.471001596138,
421.470648998017,422.470296399895,423.469943801774,424.115008234622),
 .UNSPECIFIED.);
#6535=B_SPLINE_CURVE_WITH_KNOTS('',3,(#49389,#49390,#49391,#49392,#49393,
#49394,#49395,#49396,#49397,#49398),.UNSPECIFIED.,.F.,.F.,(4,1,1,1,1,1,
1,4),(417.831822927443,418.17016752012,419.169814921998,420.169462323877,
421.169109725756,422.168757127635,423.168404529513,424.115008234623),
 .UNSPECIFIED.);
#6536=B_SPLINE_CURVE_WITH_KNOTS('',3,(#49403,#49404,#49405,#49406,#49407,
#49408,#49409,#49410,#49411,#49412),.UNSPECIFIED.,.F.,.F.,(4,1,1,1,1,1,
1,4),(411.548637620263,412.473822381108,413.473469782987,414.473117184866,
415.472764586744,416.472411988623,417.472059390502,417.831822927443),
 .UNSPECIFIED.);
#6537=B_SPLINE_CURVE_WITH_KNOTS('',3,(#49413,#49414,#49415,#49416,#49417,
#49418,#49419,#49420,#49421,#49422),.UNSPECIFIED.,.F.,.F.,(4,1,1,1,1,1,
1,4),(411.548637620263,412.172283108848,413.171930510726,414.171577912605,
415.171225314484,416.170872716362,417.170520118241,417.831822927443),
 .UNSPECIFIED.);
#6538=B_SPLINE_CURVE_WITH_KNOTS('',3,(#49427,#49428,#49429,#49430,#49431,
#49432,#49433,#49434,#49435,#49436,#49437),.UNSPECIFIED.,.F.,.F.,(4,1,1,
1,1,1,1,1,4),(405.265452313084,405.476290567958,406.475937969836,407.475585371715,
408.475232773594,409.474880175472,410.474527577351,411.47417497923,411.548637620263),
 .UNSPECIFIED.);
#6539=B_SPLINE_CURVE_WITH_KNOTS('',3,(#49438,#49439,#49440,#49441,#49442,
#49443,#49444,#49445,#49446,#49447),.UNSPECIFIED.,.F.,.F.,(4,1,1,1,1,1,
1,4),(405.265452313084,406.174398697576,407.174046099454,408.173693501333,
409.173340903212,410.17298830509,411.172635706969,411.548637620263),
 .UNSPECIFIED.);
#6540=B_SPLINE_CURVE_WITH_KNOTS('',3,(#49452,#49453,#49454,#49455,#49456,
#49457,#49458,#49459,#49460,#49461),.UNSPECIFIED.,.F.,.F.,(4,1,1,1,1,1,
1,4),(398.982267005904,399.478406156685,400.478053558564,401.477700960443,
402.477348362322,403.4769957642,404.476643166079,405.265452313084),
 .UNSPECIFIED.);
#6541=B_SPLINE_CURVE_WITH_KNOTS('',3,(#49462,#49463,#49464,#49465,#49466,
#49467,#49468,#49469,#49470,#49471,#49472),.UNSPECIFIED.,.F.,.F.,(4,1,1,
1,1,1,1,1,4),(398.982267005904,399.176866884425,400.176514286303,401.176161688182,
402.175809090061,403.17545649194,404.175103893818,405.174751295697,405.265452313084),
 .UNSPECIFIED.);
#6542=B_SPLINE_CURVE_WITH_KNOTS('',3,(#49477,#49478,#49479,#49480,#49481,
#49482,#49483,#49484,#49485,#49486),.UNSPECIFIED.,.F.,.F.,(4,1,1,1,1,1,
1,4),(392.699081698724,393.480521745413,394.480169147292,395.479816549171,
396.479463951049,397.479111352928,398.478758754807,398.982267005904),
 .UNSPECIFIED.);
#6543=B_SPLINE_CURVE_WITH_KNOTS('',3,(#49487,#49488,#49489,#49490,#49491,
#49492,#49493,#49494,#49495,#49496),.UNSPECIFIED.,.F.,.F.,(4,1,1,1,1,1,
1,4),(392.699081698725,393.178982473153,394.178629875031,395.17827727691,
396.177924678789,397.177572080667,398.177219482546,398.982267005904),
 .UNSPECIFIED.);
#6544=B_SPLINE_CURVE_WITH_KNOTS('',3,(#49501,#49502,#49503,#49504,#49505,
#49506,#49507,#49508,#49509,#49510,#49511),.UNSPECIFIED.,.F.,.F.,(4,1,1,
1,1,1,1,1,4),(386.415896391545,386.482989932263,387.482637334141,388.48228473602,
389.481932137899,390.481579539777,391.481226941656,392.480874343535,392.699081698724),
 .UNSPECIFIED.);
#6545=B_SPLINE_CURVE_WITH_KNOTS('',3,(#49512,#49513,#49514,#49515,#49516,
#49517,#49518,#49519,#49520,#49521),.UNSPECIFIED.,.F.,.F.,(4,1,1,1,1,1,
1,4),(386.415896391545,387.181098061881,388.180745463759,389.180392865638,
390.180040267517,391.179687669395,392.179335071274,392.699081698725),
 .UNSPECIFIED.);
#6546=B_SPLINE_CURVE_WITH_KNOTS('',3,(#49526,#49527,#49528,#49529,#49530,
#49531,#49532,#49533,#49534,#49535),.UNSPECIFIED.,.F.,.F.,(4,1,1,1,1,1,
1,4),(380.132711084365,380.48510552099,381.484752922869,382.484400324748,
383.484047726626,384.483695128505,385.483342530384,386.415896391545),
 .UNSPECIFIED.);
#6547=B_SPLINE_CURVE_WITH_KNOTS('',3,(#49536,#49537,#49538,#49539,#49540,
#49541,#49542,#49543,#49544,#49545,#49546),.UNSPECIFIED.,.F.,.F.,(4,1,1,
1,1,1,1,1,4),(380.132711084366,380.18356624873,381.183213650608,382.182861052487,
383.182508454366,384.182155856244,385.181803258123,386.181450660002,386.415896391545),
 .UNSPECIFIED.);
#6548=B_SPLINE_CURVE_WITH_KNOTS('',3,(#49551,#49552,#49553,#49554,#49555,
#49556,#49557,#49558,#49559,#49560),.UNSPECIFIED.,.F.,.F.,(4,1,1,1,1,1,
1,4),(373.849525777186,374.487221109718,375.486868511597,376.486515913476,
377.486163315354,378.485810717233,379.485458119112,380.132711084365),
 .UNSPECIFIED.);
#6549=B_SPLINE_CURVE_WITH_KNOTS('',3,(#49561,#49562,#49563,#49564,#49565,
#49566,#49567,#49568,#49569,#49570),.UNSPECIFIED.,.F.,.F.,(4,1,1,1,1,1,
1,4),(373.849525777186,374.185681837458,375.185329239336,376.184976641215,
377.184624043094,378.184271444972,379.183918846851,380.132711084366),
 .UNSPECIFIED.);
#6550=B_SPLINE_CURVE_WITH_KNOTS('',3,(#49575,#49576,#49577,#49578,#49579,
#49580,#49581,#49582,#49583,#49584),.UNSPECIFIED.,.F.,.F.,(4,1,1,1,1,1,
1,4),(367.566340470006,368.489336698446,369.488984100325,370.488631502204,
371.488278904082,372.487926305961,373.48757370784,373.849525777186),
 .UNSPECIFIED.);
#6551=B_SPLINE_CURVE_WITH_KNOTS('',3,(#49585,#49586,#49587,#49588,#49589,
#49590,#49591,#49592,#49593,#49594),.UNSPECIFIED.,.F.,.F.,(4,1,1,1,1,1,
1,4),(367.566340470006,368.187797426186,369.187444828064,370.187092229943,
371.186739631822,372.1863870337,373.186034435579,373.849525777186),
 .UNSPECIFIED.);
#6552=B_SPLINE_CURVE_WITH_KNOTS('',3,(#49599,#49600,#49601,#49602,#49603,
#49604,#49605,#49606,#49607,#49608,#49609),.UNSPECIFIED.,.F.,.F.,(4,1,1,
1,1,1,1,1,4),(361.283155162827,361.491804885295,362.491452287174,363.491099689053,
364.490747090932,365.49039449281,366.490041894689,367.489689296568,367.566340470006),
 .UNSPECIFIED.);
#6553=B_SPLINE_CURVE_WITH_KNOTS('',3,(#49610,#49611,#49612,#49613,#49614,
#49615,#49616,#49617,#49618,#49619),.UNSPECIFIED.,.F.,.F.,(4,1,1,1,1,1,
1,4),(361.283155162827,362.189913014913,363.189560416792,364.189207818671,
365.188855220549,366.188502622428,367.188150024307,367.566340470006),
 .UNSPECIFIED.);
#6554=B_SPLINE_CURVE_WITH_KNOTS('',3,(#49624,#49625,#49626,#49627,#49628,
#49629,#49630,#49631,#49632,#49633),.UNSPECIFIED.,.F.,.F.,(4,1,1,1,1,1,
1,4),(354.999969855647,355.493920474023,356.493567875902,357.493215277781,
358.492862679659,359.492510081538,360.492157483417,361.283155162827),
 .UNSPECIFIED.);
#6555=B_SPLINE_CURVE_WITH_KNOTS('',3,(#49634,#49635,#49636,#49637,#49638,
#49639,#49640,#49641,#49642,#49643,#49644),.UNSPECIFIED.,.F.,.F.,(4,1,1,
1,1,1,1,1,4),(354.999969855647,355.192381201763,356.192028603641,357.19167600552,
358.191323407399,359.190970809277,360.190618211156,361.190265613035,361.283155162827),
 .UNSPECIFIED.);
#6556=B_SPLINE_CURVE_WITH_KNOTS('',3,(#49649,#49650,#49651,#49652,#49653,
#49654,#49655,#49656,#49657,#49658),.UNSPECIFIED.,.F.,.F.,(4,1,1,1,1,1,
1,4),(348.716784548467,349.496036062751,350.49568346463,351.495330866509,
352.494978268387,353.494625670266,354.494273072145,354.999969855647),
 .UNSPECIFIED.);
#6557=B_SPLINE_CURVE_WITH_KNOTS('',3,(#49659,#49660,#49661,#49662,#49663,
#49664,#49665,#49666,#49667,#49668),.UNSPECIFIED.,.F.,.F.,(4,1,1,1,1,1,
1,4),(348.716784548468,349.194496790491,350.194144192369,351.193791594248,
352.193438996127,353.193086398005,354.192733799884,354.999969855647),
 .UNSPECIFIED.);
#6558=B_SPLINE_CURVE_WITH_KNOTS('',3,(#49673,#49674,#49675,#49676,#49677,
#49678,#49679,#49680,#49681,#49682,#49683),.UNSPECIFIED.,.F.,.F.,(4,1,1,
1,1,1,1,1,4),(342.433599241288,342.498504249601,343.498151651479,344.497799053358,
345.497446455237,346.497093857115,347.496741258994,348.496388660873,348.716784548467),
 .UNSPECIFIED.);
#6559=B_SPLINE_CURVE_WITH_KNOTS('',3,(#49684,#49685,#49686,#49687,#49688,
#49689,#49690,#49691,#49692,#49693),.UNSPECIFIED.,.F.,.F.,(4,1,1,1,1,1,
1,4),(342.433599241288,343.196612379218,344.196259781097,345.195907182976,
346.195554584855,347.195201986733,348.194849388612,348.716784548468),
 .UNSPECIFIED.);
#6560=B_SPLINE_CURVE_WITH_KNOTS('',3,(#49698,#49699,#49700,#49701,#49702,
#49703,#49704,#49705,#49706,#49707),.UNSPECIFIED.,.F.,.F.,(4,1,1,1,1,1,
1,4),(336.150413934108,336.500619838328,337.500267240207,338.499914642086,
339.499562043964,340.499209445843,341.498856847722,342.433599241288),
 .UNSPECIFIED.);
#6561=B_SPLINE_CURVE_WITH_KNOTS('',3,(#49708,#49709,#49710,#49711,#49712,
#49713,#49714,#49715,#49716,#49717,#49718),.UNSPECIFIED.,.F.,.F.,(4,1,1,
1,1,1,1,1,4),(336.150413934109,336.199080566068,337.198727967946,338.198375369825,
339.198022771704,340.197670173582,341.197317575461,342.19696497734,342.433599241288),
 .UNSPECIFIED.);
#6562=B_SPLINE_CURVE_WITH_KNOTS('',3,(#49723,#49724,#49725,#49726,#49727,
#49728,#49729,#49730,#49731,#49732),.UNSPECIFIED.,.F.,.F.,(4,1,1,1,1,1,
1,4),(329.867228626929,330.502735427056,331.502382828935,332.502030230814,
333.501677632692,334.501325034571,335.50097243645,336.150413934108),
 .UNSPECIFIED.);
#6563=B_SPLINE_CURVE_WITH_KNOTS('',3,(#49733,#49734,#49735,#49736,#49737,
#49738,#49739,#49740,#49741,#49742),.UNSPECIFIED.,.F.,.F.,(4,1,1,1,1,1,
1,4),(329.867228626929,330.201196154796,331.200843556674,332.200490958553,
333.200138360432,334.19978576231,335.199433164189,336.150413934109),
 .UNSPECIFIED.);
#6564=B_SPLINE_CURVE_WITH_KNOTS('',3,(#49747,#49748,#49749,#49750,#49751,
#49752,#49753,#49754,#49755,#49756),.UNSPECIFIED.,.F.,.F.,(4,1,1,1,1,1,
1,4),(323.584043319749,324.504851015784,325.504498417663,326.504145819542,
327.50379322142,328.503440623299,329.503088025178,329.867228626929),
 .UNSPECIFIED.);
#6565=B_SPLINE_CURVE_WITH_KNOTS('',3,(#49757,#49758,#49759,#49760,#49761,
#49762,#49763,#49764,#49765,#49766),.UNSPECIFIED.,.F.,.F.,(4,1,1,1,1,1,
1,4),(323.58404331975,324.203311743523,325.202959145402,326.202606547281,
327.20225394916,328.201901351038,329.201548752917,329.867228626929),
 .UNSPECIFIED.);
#6566=B_SPLINE_CURVE_WITH_KNOTS('',3,(#49771,#49772,#49773,#49774,#49775,
#49776,#49777,#49778,#49779,#49780,#49781),.UNSPECIFIED.,.F.,.F.,(4,1,1,
1,1,1,1,1,4),(317.30085801257,317.507319202633,318.506966604512,319.506614006391,
320.506261408269,321.505908810148,322.505556212027,323.505203613906,323.584043319749),
 .UNSPECIFIED.);
#6567=B_SPLINE_CURVE_WITH_KNOTS('',3,(#49782,#49783,#49784,#49785,#49786,
#49787,#49788,#49789,#49790,#49791),.UNSPECIFIED.,.F.,.F.,(4,1,1,1,1,1,
1,4),(317.30085801257,318.205427332251,319.20507473413,320.204722136009,
321.204369537887,322.204016939766,323.203664341645,323.58404331975),
 .UNSPECIFIED.);
#6568=B_SPLINE_CURVE_WITH_KNOTS('',3,(#49796,#49797,#49798,#49799,#49800,
#49801,#49802,#49803,#49804,#49805),.UNSPECIFIED.,.F.,.F.,(4,1,1,1,1,1,
1,4),(311.01767270539,311.509434791361,312.50908219324,313.508729595119,
314.508376996997,315.508024398876,316.507671800755,317.30085801257),
 .UNSPECIFIED.);
#6569=B_SPLINE_CURVE_WITH_KNOTS('',3,(#49806,#49807,#49808,#49809,#49810,
#49811,#49812,#49813,#49814,#49815,#49816),.UNSPECIFIED.,.F.,.F.,(4,1,1,
1,1,1,1,1,4),(311.01767270539,311.207895519101,312.207542920979,313.207190322858,
314.206837724737,315.206485126615,316.206132528494,317.205779930373,317.30085801257),
 .UNSPECIFIED.);
#6570=B_SPLINE_CURVE_WITH_KNOTS('',3,(#49821,#49822,#49823,#49824,#49825,
#49826,#49827,#49828,#49829,#49830),.UNSPECIFIED.,.F.,.F.,(4,1,1,1,1,1,
1,4),(304.73448739821,305.511550380089,306.511197781968,307.510845183847,
308.510492585725,309.510139987604,310.509787389483,311.01767270539),
 .UNSPECIFIED.);
#6571=B_SPLINE_CURVE_WITH_KNOTS('',3,(#49831,#49832,#49833,#49834,#49835,
#49836,#49837,#49838,#49839,#49840),.UNSPECIFIED.,.F.,.F.,(4,1,1,1,1,1,
1,4),(304.734487398211,305.210011107828,306.209658509707,307.209305911586,
308.208953313464,309.208600715343,310.208248117222,311.01767270539),
 .UNSPECIFIED.);
#6572=B_SPLINE_CURVE_WITH_KNOTS('',3,(#49845,#49846,#49847,#49848,#49849,
#49850,#49851,#49852,#49853,#49854,#49855),.UNSPECIFIED.,.F.,.F.,(4,1,1,
1,1,1,1,1,4),(298.451302091031,298.514018566938,299.513665968817,300.513313370696,
301.512960772574,302.512608174453,303.512255576332,304.511902978211,304.73448739821),
 .UNSPECIFIED.);
#6573=B_SPLINE_CURVE_WITH_KNOTS('',3,(#49856,#49857,#49858,#49859,#49860,
#49861,#49862,#49863,#49864,#49865),.UNSPECIFIED.,.F.,.F.,(4,1,1,1,1,1,
1,4),(298.451302091031,299.212126696556,300.211774098435,301.211421500314,
302.211068902192,303.210716304071,304.21036370595,304.734487398211),
 .UNSPECIFIED.);
#6574=B_SPLINE_CURVE_WITH_KNOTS('',3,(#49870,#49871,#49872,#49873,#49874,
#49875,#49876,#49877,#49878,#49879),.UNSPECIFIED.,.F.,.F.,(4,1,1,1,1,1,
1,4),(292.168116783851,292.516134155666,293.515781557545,294.515428959424,
295.515076361302,296.514723763181,297.51437116506,298.451302091031),
 .UNSPECIFIED.);
#6575=B_SPLINE_CURVE_WITH_KNOTS('',3,(#49880,#49881,#49882,#49883,#49884,
#49885,#49886,#49887,#49888,#49889,#49890),.UNSPECIFIED.,.F.,.F.,(4,1,1,
1,1,1,1,1,4),(292.168116783852,292.214594883406,293.214242285284,294.213889687163,
295.213537089042,296.21318449092,297.212831892799,298.212479294678,298.451302091031),
 .UNSPECIFIED.);
#6576=B_SPLINE_CURVE_WITH_KNOTS('',3,(#49895,#49896,#49897,#49898,#49899,
#49900,#49901,#49902,#49903,#49904),.UNSPECIFIED.,.F.,.F.,(4,1,1,1,1,1,
1,4),(285.884931476672,286.518249744394,287.517897146273,288.517544548152,
289.51719195003,290.516839351909,291.516486753788,292.168116783851),
 .UNSPECIFIED.);
#6577=B_SPLINE_CURVE_WITH_KNOTS('',3,(#49905,#49906,#49907,#49908,#49909,
#49910,#49911,#49912,#49913,#49914),.UNSPECIFIED.,.F.,.F.,(4,1,1,1,1,1,
1,4),(285.884931476672,286.216710472133,287.216357874012,288.216005275891,
289.215652677769,290.215300079648,291.214947481527,292.168116783852),
 .UNSPECIFIED.);
#6578=B_SPLINE_CURVE_WITH_KNOTS('',3,(#49919,#49920,#49921,#49922,#49923,
#49924,#49925,#49926,#49927,#49928),.UNSPECIFIED.,.F.,.F.,(4,1,1,1,1,1,
1,4),(279.601746169492,280.520365333122,281.520012735001,282.519660136879,
283.519307538758,284.518954940637,285.518602342516,285.884931476672),
 .UNSPECIFIED.);
#6579=B_SPLINE_CURVE_WITH_KNOTS('',3,(#49929,#49930,#49931,#49932,#49933,
#49934,#49935,#49936,#49937,#49938),.UNSPECIFIED.,.F.,.F.,(4,1,1,1,1,1,
1,4),(279.601746169493,280.218826060861,281.21847346274,282.218120864619,
283.217768266497,284.217415668376,285.217063070255,285.884931476672),
 .UNSPECIFIED.);
#6580=B_SPLINE_CURVE_WITH_KNOTS('',3,(#49943,#49944,#49945,#49946,#49947,
#49948,#49949,#49950,#49951,#49952,#49953),.UNSPECIFIED.,.F.,.F.,(4,1,1,
1,1,1,1,1,4),(273.318560862313,273.522833519971,274.52248092185,275.522128323729,
276.521775725607,277.521423127486,278.521070529365,279.520717931243,279.601746169492),
 .UNSPECIFIED.);
#6581=B_SPLINE_CURVE_WITH_KNOTS('',3,(#49954,#49955,#49956,#49957,#49958,
#49959,#49960,#49961,#49962,#49963),.UNSPECIFIED.,.F.,.F.,(4,1,1,1,1,1,
1,4),(273.318560862313,274.220941649589,275.220589051468,276.220236453347,
277.219883855225,278.219531257104,279.219178658983,279.601746169493),
 .UNSPECIFIED.);
#6582=B_SPLINE_CURVE_WITH_KNOTS('',3,(#49968,#49969,#49970,#49971,#49972,
#49973,#49974,#49975,#49976,#49977),.UNSPECIFIED.,.F.,.F.,(4,1,1,1,1,1,
1,4),(267.035375555133,267.524949108699,268.524596510578,269.524243912457,
270.523891314335,271.523538716214,272.523186118093,273.318560862313),
 .UNSPECIFIED.);
#6583=B_SPLINE_CURVE_WITH_KNOTS('',3,(#49978,#49979,#49980,#49981,#49982,
#49983,#49984,#49985,#49986,#49987,#49988),.UNSPECIFIED.,.F.,.F.,(4,1,1,
1,1,1,1,1,4),(267.035375555133,267.223409836438,268.223057238317,269.222704640196,
270.222352042074,271.221999443953,272.221646845832,273.221294247711,273.318560862313),
 .UNSPECIFIED.);
#6584=B_SPLINE_CURVE_WITH_KNOTS('',3,(#49993,#49994,#49995,#49996,#49997,
#49998,#49999,#50000,#50001,#50002),.UNSPECIFIED.,.F.,.F.,(4,1,1,1,1,1,
1,4),(260.752190247954,261.527064697427,262.526712099306,263.526359501184,
264.526006903063,265.525654304942,266.525301706821,267.035375555133),
 .UNSPECIFIED.);
#6585=B_SPLINE_CURVE_WITH_KNOTS('',3,(#50003,#50004,#50005,#50006,#50007,
#50008,#50009,#50010,#50011,#50012),.UNSPECIFIED.,.F.,.F.,(4,1,1,1,1,1,
1,4),(260.752190247954,261.225525425166,262.225172827045,263.224820228924,
264.224467630802,265.224115032681,266.22376243456,267.035375555133),
 .UNSPECIFIED.);
#6586=B_SPLINE_CURVE_WITH_KNOTS('',3,(#50017,#50018,#50019,#50020,#50021,
#50022,#50023,#50024,#50025,#50026,#50027),.UNSPECIFIED.,.F.,.F.,(4,1,1,
1,1,1,1,1,4),(254.469004940774,254.529532884276,255.529180286155,256.528827688034,
257.528475089912,258.528122491791,259.52776989367,260.527417295548,260.752190247954),
 .UNSPECIFIED.);
#6587=B_SPLINE_CURVE_WITH_KNOTS('',3,(#50028,#50029,#50030,#50031,#50032,
#50033,#50034,#50035,#50036,#50037),.UNSPECIFIED.,.F.,.F.,(4,1,1,1,1,1,
1,4),(254.469004940774,255.227641013894,256.227288415773,257.226935817652,
258.22658321953,259.226230621409,260.225878023288,260.752190247954),
 .UNSPECIFIED.);
#6588=B_SPLINE_CURVE_WITH_KNOTS('',3,(#50042,#50043,#50044,#50045,#50046,
#50047,#50048,#50049,#50050,#50051),.UNSPECIFIED.,.F.,.F.,(4,1,1,1,1,1,
1,4),(248.185819633594,248.531648473004,249.531295874883,250.530943276762,
251.53059067864,252.530238080519,253.529885482398,254.469004940774),
 .UNSPECIFIED.);
#6589=B_SPLINE_CURVE_WITH_KNOTS('',3,(#50052,#50053,#50054,#50055,#50056,
#50057,#50058,#50059,#50060,#50061,#50062),.UNSPECIFIED.,.F.,.F.,(4,1,1,
1,1,1,1,1,4),(248.185819633595,248.230109200743,249.229756602622,250.229404004501,
251.229051406379,252.228698808258,253.228346210137,254.227993612015,254.469004940774),
 .UNSPECIFIED.);
#6590=B_SPLINE_CURVE_WITH_KNOTS('',3,(#50067,#50068,#50069,#50070,#50071,
#50072,#50073,#50074,#50075,#50076),.UNSPECIFIED.,.F.,.F.,(4,1,1,1,1,1,
1,4),(241.902634326415,242.533764061732,243.533411463611,244.533058865489,
245.532706267368,246.532353669247,247.532001071126,248.185819633594),
 .UNSPECIFIED.);
#6591=B_SPLINE_CURVE_WITH_KNOTS('',3,(#50077,#50078,#50079,#50080,#50081,
#50082,#50083,#50084,#50085,#50086),.UNSPECIFIED.,.F.,.F.,(4,1,1,1,1,1,
1,4),(241.902634326415,242.232224789471,243.23187219135,244.231519593229,
245.231166995107,246.230814396986,247.230461798865,248.185819633595),
 .UNSPECIFIED.);
#6592=B_SPLINE_CURVE_WITH_KNOTS('',3,(#50091,#50092,#50093,#50094,#50095,
#50096,#50097,#50098,#50099,#50100),.UNSPECIFIED.,.F.,.F.,(4,1,1,1,1,1,
1,4),(235.619449019235,236.53587965046,237.535527052339,238.535174454217,
239.534821856096,240.534469257975,241.534116659853,241.902634326415),
 .UNSPECIFIED.);
#6593=B_SPLINE_CURVE_WITH_KNOTS('',3,(#50101,#50102,#50103,#50104,#50105,
#50106,#50107,#50108,#50109,#50110),.UNSPECIFIED.,.F.,.F.,(4,1,1,1,1,1,
1,4),(235.619449019236,236.234340378199,237.233987780078,238.233635181957,
239.233282583835,240.232929985714,241.232577387593,241.902634326415),
 .UNSPECIFIED.);
#6594=B_SPLINE_CURVE_WITH_KNOTS('',3,(#50115,#50116,#50117,#50118,#50119,
#50120,#50121,#50122,#50123,#50124,#50125),.UNSPECIFIED.,.F.,.F.,(4,1,1,
1,1,1,1,1,4),(229.336263712056,229.538347837309,230.537995239188,231.537642641067,
232.537290042945,233.536937444824,234.536584846703,235.536232248581,235.619449019235),
 .UNSPECIFIED.);
#6595=B_SPLINE_CURVE_WITH_KNOTS('',3,(#50126,#50127,#50128,#50129,#50130,
#50131,#50132,#50133,#50134,#50135),.UNSPECIFIED.,.F.,.F.,(4,1,1,1,1,1,
1,4),(229.336263712056,230.236455966927,231.236103368806,232.235750770684,
233.235398172563,234.235045574442,235.23469297632,235.619449019236),
 .UNSPECIFIED.);
#6596=B_SPLINE_CURVE_WITH_KNOTS('',3,(#50140,#50141,#50142,#50143,#50144,
#50145,#50146,#50147,#50148,#50149),.UNSPECIFIED.,.F.,.F.,(4,1,1,1,1,1,
1,4),(223.053078404876,223.540463426037,224.540110827916,225.539758229795,
226.539405631673,227.539053033552,228.538700435431,229.336263712056),
 .UNSPECIFIED.);
#6597=B_SPLINE_CURVE_WITH_KNOTS('',3,(#50150,#50151,#50152,#50153,#50154,
#50155,#50156,#50157,#50158,#50159,#50160),.UNSPECIFIED.,.F.,.F.,(4,1,1,
1,1,1,1,1,4),(223.053078404876,223.238924153776,224.238571555655,225.238218957534,
226.237866359412,227.237513761291,228.23716116317,229.236808565048,229.336263712056),
 .UNSPECIFIED.);
#6598=B_SPLINE_CURVE_WITH_KNOTS('',3,(#50165,#50166,#50167,#50168,#50169,
#50170,#50171,#50172,#50173,#50174),.UNSPECIFIED.,.F.,.F.,(4,1,1,1,1,1,
1,4),(216.769893097697,217.542579014765,218.542226416644,219.541873818522,
220.541521220401,221.54116862228,222.540816024158,223.053078404876),
 .UNSPECIFIED.);
#6599=B_SPLINE_CURVE_WITH_KNOTS('',3,(#50175,#50176,#50177,#50178,#50179,
#50180,#50181,#50182,#50183,#50184),.UNSPECIFIED.,.F.,.F.,(4,1,1,1,1,1,
1,4),(216.769893097697,217.241039742504,218.240687144383,219.240334546262,
220.23998194814,221.239629350019,222.239276751898,223.053078404876),
 .UNSPECIFIED.);
#6600=B_SPLINE_CURVE_WITH_KNOTS('',3,(#50189,#50190,#50191,#50192,#50193,
#50194,#50195,#50196,#50197,#50198,#50199),.UNSPECIFIED.,.F.,.F.,(4,1,1,
1,1,1,1,1,4),(210.486707790517,210.545047201614,211.544694603493,212.544342005372,
213.54398940725,214.543636809129,215.543284211008,216.542931612886,216.769893097697),
 .UNSPECIFIED.);
#6601=B_SPLINE_CURVE_WITH_KNOTS('',3,(#50200,#50201,#50202,#50203,#50204,
#50205,#50206,#50207,#50208,#50209),.UNSPECIFIED.,.F.,.F.,(4,1,1,1,1,1,
1,4),(210.486707790517,211.243155331232,212.242802733111,213.242450134989,
214.242097536868,215.241744938747,216.241392340625,216.769893097697),
 .UNSPECIFIED.);
#6602=B_SPLINE_CURVE_WITH_KNOTS('',3,(#50214,#50215,#50216,#50217,#50218,
#50219,#50220,#50221,#50222,#50223),.UNSPECIFIED.,.F.,.F.,(4,1,1,1,1,1,
1,4),(204.203522483337,204.547162790342,205.546810192221,206.5464575941,
207.546104995978,208.545752397857,209.545399799736,210.486707790517),
 .UNSPECIFIED.);
#6603=B_SPLINE_CURVE_WITH_KNOTS('',3,(#50224,#50225,#50226,#50227,#50228,
#50229,#50230,#50231,#50232,#50233,#50234),.UNSPECIFIED.,.F.,.F.,(4,1,1,
1,1,1,1,1,4),(204.203522483338,204.245623518081,205.24527091996,206.244918321839,
207.244565723717,208.244213125596,209.243860527475,210.243507929353,210.486707790517),
 .UNSPECIFIED.);
#6604=B_SPLINE_CURVE_WITH_KNOTS('',3,(#50239,#50240,#50241,#50242,#50243,
#50244,#50245,#50246,#50247,#50248),.UNSPECIFIED.,.F.,.F.,(4,1,1,1,1,1,
1,4),(197.920337176158,198.54927837907,199.548925780949,200.548573182827,
201.548220584706,202.547867986585,203.547515388463,204.203522483337),
 .UNSPECIFIED.);
#6605=B_SPLINE_CURVE_WITH_KNOTS('',3,(#50249,#50250,#50251,#50252,#50253,
#50254,#50255,#50256,#50257,#50258),.UNSPECIFIED.,.F.,.F.,(4,1,1,1,1,1,
1,4),(197.920337176158,198.247739106809,199.247386508688,200.247033910567,
201.246681312445,202.246328714324,203.245976116203,204.203522483338),
 .UNSPECIFIED.);
#6606=B_SPLINE_CURVE_WITH_KNOTS('',3,(#50263,#50264,#50265,#50266,#50267,
#50268,#50269,#50270,#50271,#50272),.UNSPECIFIED.,.F.,.F.,(4,1,1,1,1,1,
1,4),(191.637151868978,192.551393967798,193.551041369677,194.550688771555,
195.550336173434,196.549983575313,197.549630977191,197.920337176158),
 .UNSPECIFIED.);
#6607=B_SPLINE_CURVE_WITH_KNOTS('',3,(#50273,#50274,#50275,#50276,#50277,
#50278,#50279,#50280,#50281,#50282),.UNSPECIFIED.,.F.,.F.,(4,1,1,1,1,1,
1,4),(191.637151868979,192.249854695537,193.249502097416,194.249149499294,
195.248796901173,196.248444303052,197.24809170493,197.920337176158),
 .UNSPECIFIED.);
#6608=B_SPLINE_CURVE_WITH_KNOTS('',3,(#50287,#50288,#50289,#50290,#50291,
#50292,#50293,#50294,#50295,#50296,#50297),.UNSPECIFIED.,.F.,.F.,(4,1,1,
1,1,1,1,1,4),(185.353966561799,185.553862154647,186.553509556526,187.553156958405,
188.552804360283,189.552451762162,190.552099164041,191.551746565919,191.637151868978),
 .UNSPECIFIED.);
#6609=B_SPLINE_CURVE_WITH_KNOTS('',3,(#50298,#50299,#50300,#50301,#50302,
#50303,#50304,#50305,#50306,#50307),.UNSPECIFIED.,.F.,.F.,(4,1,1,1,1,1,
1,4),(185.353966561799,186.251970284265,187.251617686144,188.251265088022,
189.250912489901,190.25055989178,191.250207293658,191.637151868979),
 .UNSPECIFIED.);
#6610=B_SPLINE_CURVE_WITH_KNOTS('',3,(#50312,#50313,#50314,#50315,#50316,
#50317,#50318,#50319,#50320,#50321),.UNSPECIFIED.,.F.,.F.,(4,1,1,1,1,1,
1,4),(179.070781254619,179.555977743375,180.555625145254,181.555272547132,
182.554919949011,183.55456735089,184.554214752768,185.353966561799),
 .UNSPECIFIED.);
#6611=B_SPLINE_CURVE_WITH_KNOTS('',3,(#50322,#50323,#50324,#50325,#50326,
#50327,#50328,#50329,#50330,#50331,#50332),.UNSPECIFIED.,.F.,.F.,(4,1,1,
1,1,1,1,1,4),(179.07078125462,179.254438471114,180.254085872993,181.253733274872,
182.25338067675,183.253028078629,184.252675480508,185.252322882386,185.353966561799),
 .UNSPECIFIED.);
#6612=B_SPLINE_CURVE_WITH_KNOTS('',3,(#50337,#50338,#50339,#50340,#50341,
#50342,#50343,#50344,#50345,#50346),.UNSPECIFIED.,.F.,.F.,(4,1,1,1,1,1,
1,4),(172.78759594744,173.558093332103,174.557740733982,175.55738813586,
176.557035537739,177.556682939618,178.556330341496,179.070781254619),
 .UNSPECIFIED.);
#6613=B_SPLINE_CURVE_WITH_KNOTS('',3,(#50347,#50348,#50349,#50350,#50351,
#50352,#50353,#50354,#50355,#50356),.UNSPECIFIED.,.F.,.F.,(4,1,1,1,1,1,
1,4),(172.78759594744,173.256554059842,174.256201461721,175.255848863599,
176.255496265478,177.255143667357,178.254791069235,179.07078125462),
 .UNSPECIFIED.);
#6614=B_SPLINE_CURVE_WITH_KNOTS('',3,(#50361,#50362,#50363,#50364,#50365,
#50366,#50367,#50368,#50369,#50370,#50371),.UNSPECIFIED.,.F.,.F.,(4,1,1,
1,1,1,1,1,4),(166.50441064026,166.560561518952,167.560208920831,168.559856322709,
169.559503724588,170.559151126467,171.558798528346,172.558445930224,172.78759594744),
 .UNSPECIFIED.);
#6615=B_SPLINE_CURVE_WITH_KNOTS('',3,(#50372,#50373,#50374,#50375,#50376,
#50377,#50378,#50379,#50380,#50381),.UNSPECIFIED.,.F.,.F.,(4,1,1,1,1,1,
1,4),(166.50441064026,167.25866964857,168.258317050449,169.257964452327,
170.257611854206,171.257259256085,172.256906657963,172.78759594744),
 .UNSPECIFIED.);
#6616=B_SPLINE_CURVE_WITH_KNOTS('',3,(#50386,#50387,#50388,#50389,#50390,
#50391,#50392,#50393,#50394,#50395),.UNSPECIFIED.,.F.,.F.,(4,1,1,1,1,1,
1,4),(160.22122533308,160.56267710768,161.562324509559,162.561971911437,
163.561619313316,164.561266715195,165.560914117073,166.50441064026),
 .UNSPECIFIED.);
#6617=B_SPLINE_CURVE_WITH_KNOTS('',3,(#50396,#50397,#50398,#50399,#50400,
#50401,#50402,#50403,#50404,#50405,#50406),.UNSPECIFIED.,.F.,.F.,(4,1,1,
1,1,1,1,1,4),(160.221225333081,160.261137835419,161.260785237298,162.260432639177,
163.260080041055,164.259727442934,165.259374844813,166.259022246691,166.50441064026),
 .UNSPECIFIED.);
#6618=B_SPLINE_CURVE_WITH_KNOTS('',3,(#50411,#50412,#50413,#50414,#50415,
#50416,#50417,#50418,#50419,#50420),.UNSPECIFIED.,.F.,.F.,(4,1,1,1,1,1,
1,4),(153.938040025901,154.564792696408,155.564440098287,156.564087500165,
157.563734902044,158.563382303923,159.563029705801,160.22122533308),
 .UNSPECIFIED.);
#6619=B_SPLINE_CURVE_WITH_KNOTS('',3,(#50421,#50422,#50423,#50424,#50425,
#50426,#50427,#50428,#50429,#50430),.UNSPECIFIED.,.F.,.F.,(4,1,1,1,1,1,
1,4),(153.938040025901,154.263253424147,155.262900826026,156.262548227904,
157.262195629783,158.261843031662,159.26149043354,160.221225333081),
 .UNSPECIFIED.);
#6620=B_SPLINE_CURVE_WITH_KNOTS('',3,(#50435,#50436,#50437,#50438,#50439,
#50440,#50441,#50442,#50443,#50444),.UNSPECIFIED.,.F.,.F.,(4,1,1,1,1,1,
1,4),(147.654854718721,148.566908285136,149.566555687014,150.566203088893,
151.565850490772,152.565497892651,153.565145294529,153.938040025901),
 .UNSPECIFIED.);
#6621=B_SPLINE_CURVE_WITH_KNOTS('',3,(#50445,#50446,#50447,#50448,#50449,
#50450,#50451,#50452,#50453,#50454),.UNSPECIFIED.,.F.,.F.,(4,1,1,1,1,1,
1,4),(147.654854718722,148.265369012875,149.265016414754,150.264663816632,
151.264311218511,152.26395862039,153.263606022268,153.938040025901),
 .UNSPECIFIED.);
#6622=B_SPLINE_CURVE_WITH_KNOTS('',3,(#50459,#50460,#50461,#50462,#50463,
#50464,#50465,#50466,#50467,#50468,#50469),.UNSPECIFIED.,.F.,.F.,(4,1,1,
1,1,1,1,1,4),(141.371669411542,141.569376471985,142.569023873864,143.568671275742,
144.568318677621,145.5679660795,146.567613481378,147.567260883257,147.654854718721),
 .UNSPECIFIED.);
#6623=B_SPLINE_CURVE_WITH_KNOTS('',3,(#50470,#50471,#50472,#50473,#50474,
#50475,#50476,#50477,#50478,#50479),.UNSPECIFIED.,.F.,.F.,(4,1,1,1,1,1,
1,4),(141.371669411542,142.267484601603,143.267132003481,144.26677940536,
145.266426807239,146.266074209118,147.265721610996,147.654854718722),
 .UNSPECIFIED.);
#6624=B_SPLINE_CURVE_WITH_KNOTS('',3,(#50484,#50485,#50486,#50487,#50488,
#50489,#50490,#50491,#50492,#50493),.UNSPECIFIED.,.F.,.F.,(4,1,1,1,1,1,
1,4),(135.088484104362,135.571492060713,136.571139462592,137.57078686447,
138.570434266349,139.570081668228,140.569729070106,141.371669411542),
 .UNSPECIFIED.);
#6625=B_SPLINE_CURVE_WITH_KNOTS('',3,(#50494,#50495,#50496,#50497,#50498,
#50499,#50500,#50501,#50502,#50503,#50504),.UNSPECIFIED.,.F.,.F.,(4,1,1,
1,1,1,1,1,4),(135.088484104362,135.269952788452,136.269600190331,137.269247592209,
138.268894994088,139.268542395967,140.268189797845,141.267837199724,141.371669411542),
 .UNSPECIFIED.);
#6626=B_SPLINE_CURVE_WITH_KNOTS('',3,(#50509,#50510,#50511,#50512,#50513,
#50514,#50515,#50516,#50517,#50518),.UNSPECIFIED.,.F.,.F.,(4,1,1,1,1,1,
1,4),(128.805298797183,129.573607649441,130.57325505132,131.572902453198,
132.572549855077,133.572197256956,134.571844658834,135.088484104362),
 .UNSPECIFIED.);
#6627=B_SPLINE_CURVE_WITH_KNOTS('',3,(#50519,#50520,#50521,#50522,#50523,
#50524,#50525,#50526,#50527,#50528),.UNSPECIFIED.,.F.,.F.,(4,1,1,1,1,1,
1,4),(128.805298797183,129.27206837718,130.271715779059,131.271363180937,
132.271010582816,133.270657984695,134.270305386573,135.088484104362),
 .UNSPECIFIED.);
#6628=B_SPLINE_CURVE_WITH_KNOTS('',3,(#50533,#50534,#50535,#50536,#50537,
#50538,#50539,#50540,#50541,#50542,#50543),.UNSPECIFIED.,.F.,.F.,(4,1,1,
1,1,1,1,1,4),(122.522113490003,122.57607583629,123.575723238169,124.575370640047,
125.575018041926,126.574665443805,127.574312845683,128.573960247562,128.805298797183),
 .UNSPECIFIED.);
#6629=B_SPLINE_CURVE_WITH_KNOTS('',3,(#50544,#50545,#50546,#50547,#50548,
#50549,#50550,#50551,#50552,#50553),.UNSPECIFIED.,.F.,.F.,(4,1,1,1,1,1,
1,4),(122.522113490003,123.274183965908,124.273831367786,125.273478769665,
126.273126171544,127.272773573423,128.272420975301,128.805298797183),
 .UNSPECIFIED.);
#6630=B_SPLINE_CURVE_WITH_KNOTS('',3,(#50558,#50559,#50560,#50561,#50562,
#50563,#50564,#50565,#50566,#50567),.UNSPECIFIED.,.F.,.F.,(4,1,1,1,1,1,
1,4),(116.238928182823,116.578191425018,117.577838826897,118.577486228775,
119.577133630654,120.576781032533,121.576428434411,122.522113490003),
 .UNSPECIFIED.);
#6631=B_SPLINE_CURVE_WITH_KNOTS('',3,(#50568,#50569,#50570,#50571,#50572,
#50573,#50574,#50575,#50576,#50577,#50578),.UNSPECIFIED.,.F.,.F.,(4,1,1,
1,1,1,1,1,4),(116.238928182824,116.276652152757,117.276299554636,118.275946956514,
119.275594358393,120.275241760272,121.27488916215,122.274536564029,122.522113490003),
 .UNSPECIFIED.);
#6632=B_SPLINE_CURVE_WITH_KNOTS('',3,(#50583,#50584,#50585,#50586,#50587,
#50588,#50589,#50590,#50591,#50592),.UNSPECIFIED.,.F.,.F.,(4,1,1,1,1,1,
1,4),(109.955742875644,110.580307013746,111.579954415625,112.579601817503,
113.579249219382,114.578896621261,115.578544023139,116.238928182823),
 .UNSPECIFIED.);
#6633=B_SPLINE_CURVE_WITH_KNOTS('',3,(#50593,#50594,#50595,#50596,#50597,
#50598,#50599,#50600,#50601,#50602),.UNSPECIFIED.,.F.,.F.,(4,1,1,1,1,1,
1,4),(109.955742875644,110.278767741485,111.278415143364,112.278062545242,
113.277709947121,114.277357349,115.277004750878,116.238928182824),
 .UNSPECIFIED.);
#6634=B_SPLINE_CURVE_WITH_KNOTS('',3,(#50607,#50608,#50609,#50610,#50611,
#50612,#50613,#50614,#50615,#50616),.UNSPECIFIED.,.F.,.F.,(4,1,1,1,1,1,
1,4),(103.672557568464,104.582422602474,105.582070004352,106.581717406231,
107.58136480811,108.581012209988,109.580659611867,109.955742875644),
 .UNSPECIFIED.);
#6635=B_SPLINE_CURVE_WITH_KNOTS('',3,(#50617,#50618,#50619,#50620,#50621,
#50622,#50623,#50624,#50625,#50626),.UNSPECIFIED.,.F.,.F.,(4,1,1,1,1,1,
1,4),(103.672557568465,104.280883330213,105.280530732091,106.28017813397,
107.279825535849,108.279472937728,109.279120339606,109.955742875644),
 .UNSPECIFIED.);
#6636=B_SPLINE_CURVE_WITH_KNOTS('',3,(#50631,#50632,#50633,#50634,#50635,
#50636,#50637,#50638,#50639,#50640,#50641),.UNSPECIFIED.,.F.,.F.,(4,1,1,
1,1,1,1,1,4),(97.3893722612846,97.5848907893229,98.5845381912016,99.5841855930803,
100.583832994959,101.583480396838,102.583127798716,103.582775200595,103.672557568464),
 .UNSPECIFIED.);
#6637=B_SPLINE_CURVE_WITH_KNOTS('',3,(#50642,#50643,#50644,#50645,#50646,
#50647,#50648,#50649,#50650,#50651),.UNSPECIFIED.,.F.,.F.,(4,1,1,1,1,1,
1,4),(97.389372261285,98.2829989189407,99.2826463208194,100.282293722698,
101.281941124577,102.281588526455,103.281235928334,103.672557568465),
 .UNSPECIFIED.);
#6638=B_SPLINE_CURVE_WITH_KNOTS('',3,(#50656,#50657,#50658,#50659,#50660,
#50661,#50662,#50663,#50664,#50665),.UNSPECIFIED.,.F.,.F.,(4,1,1,1,1,1,
1,4),(91.1061869541051,91.5870063780508,92.5866537799295,93.5863011818082,
94.5859485836869,95.5855959855656,96.5852433874443,97.3893722612846),
 .UNSPECIFIED.);
#6639=B_SPLINE_CURVE_WITH_KNOTS('',3,(#50666,#50667,#50668,#50669,#50670,
#50671,#50672,#50673,#50674,#50675,#50676),.UNSPECIFIED.,.F.,.F.,(4,1,1,
1,1,1,1,1,4),(91.1061869541054,91.2854671057899,92.2851145076686,93.2847619095473,
94.2844093114259,95.2840567133046,96.2837041151833,97.283351517062,97.389372261285),
 .UNSPECIFIED.);
#6640=B_SPLINE_CURVE_WITH_KNOTS('',3,(#50681,#50682,#50683,#50684,#50685,
#50686,#50687,#50688,#50689,#50690),.UNSPECIFIED.,.F.,.F.,(4,1,1,1,1,1,
1,4),(84.8230016469255,85.5891219667787,86.5887693686574,87.5884167705361,
88.5880641724148,89.5877115742935,90.5873589761722,91.1061869541051),
 .UNSPECIFIED.);
#6641=B_SPLINE_CURVE_WITH_KNOTS('',3,(#50691,#50692,#50693,#50694,#50695,
#50696,#50697,#50698,#50699,#50700),.UNSPECIFIED.,.F.,.F.,(4,1,1,1,1,1,
1,4),(84.8230016469258,85.2875826945178,86.2872300963965,87.2868774982752,
88.2865249001539,89.2861723020325,90.2858197039112,91.1061869541054),
 .UNSPECIFIED.);
#6642=B_SPLINE_CURVE_WITH_KNOTS('',3,(#50705,#50706,#50707,#50708,#50709,
#50710,#50711,#50712,#50713,#50714,#50715),.UNSPECIFIED.,.F.,.F.,(4,1,1,
1,1,1,1,1,4),(78.5398163397459,78.5915901536279,79.5912375555066,80.5908849573853,
81.590532359264,82.5901797611427,83.5898271630214,84.5894745649001,84.8230016469255),
 .UNSPECIFIED.);
#6643=B_SPLINE_CURVE_WITH_KNOTS('',3,(#50716,#50717,#50718,#50719,#50720,
#50721,#50722,#50723,#50724,#50725),.UNSPECIFIED.,.F.,.F.,(4,1,1,1,1,1,
1,4),(78.5398163397463,79.2896982832457,80.2893456851244,81.2889930870031,
82.2886404888818,83.2882878907604,84.2879352926391,84.8230016469258),
 .UNSPECIFIED.);
#6644=B_SPLINE_CURVE_WITH_KNOTS('',3,(#50730,#50731,#50732,#50733,#50734,
#50735,#50736,#50737,#50738,#50739),.UNSPECIFIED.,.F.,.F.,(4,1,1,1,1,1,
1,4),(72.2566310325663,72.5937057423558,73.5933531442345,74.5930005461132,
75.5926479479919,76.5922953498706,77.5919427517493,78.5398163397459),
 .UNSPECIFIED.);
#6645=B_SPLINE_CURVE_WITH_KNOTS('',3,(#50740,#50741,#50742,#50743,#50744,
#50745,#50746,#50747,#50748,#50749,#50750),.UNSPECIFIED.,.F.,.F.,(4,1,1,
1,1,1,1,1,4),(72.2566310325667,72.2921664700949,73.2918138719736,74.2914612738523,
75.291108675731,76.2907560776096,77.2904034794883,78.290050881367,78.5398163397463),
 .UNSPECIFIED.);
#6646=B_SPLINE_CURVE_WITH_KNOTS('',3,(#50755,#50756,#50757,#50758,#50759,
#50760,#50761,#50762,#50763,#50764),.UNSPECIFIED.,.F.,.F.,(4,1,1,1,1,1,
1,4),(65.9734457253867,66.5958213310837,67.5954687329624,68.5951161348411,
69.5947635367198,70.5944109385985,71.5940583404772,72.2566310325663),
 .UNSPECIFIED.);
#6647=B_SPLINE_CURVE_WITH_KNOTS('',3,(#50765,#50766,#50767,#50768,#50769,
#50770,#50771,#50772,#50773,#50774),.UNSPECIFIED.,.F.,.F.,(4,1,1,1,1,1,
1,4),(65.9734457253871,66.2942820588228,67.2939294607015,68.2935768625802,
69.2932242644588,70.2928716663375,71.2925190682162,72.2566310325667),
 .UNSPECIFIED.);
#6648=B_SPLINE_CURVE_WITH_KNOTS('',3,(#50779,#50780,#50781,#50782,#50783,
#50784,#50785,#50786,#50787,#50788),.UNSPECIFIED.,.F.,.F.,(4,1,1,1,1,1,
1,4),(59.6902604182071,60.5979369198116,61.5975843216903,62.597231723569,
63.5968791254477,64.5965265273264,65.5961739292051,65.9734457253867),
 .UNSPECIFIED.);
#6649=B_SPLINE_CURVE_WITH_KNOTS('',3,(#50789,#50790,#50791,#50792,#50793,
#50794,#50795,#50796,#50797,#50798),.UNSPECIFIED.,.F.,.F.,(4,1,1,1,1,1,
1,4),(59.6902604182075,60.2963976475507,61.2960450494294,62.295692451308,
63.2953398531867,64.2949872550654,65.2946346569441,65.9734457253871),
 .UNSPECIFIED.);
#6650=B_SPLINE_CURVE_WITH_KNOTS('',3,(#50803,#50804,#50805,#50806,#50807,
#50808,#50809,#50810,#50811,#50812,#50813),.UNSPECIFIED.,.F.,.F.,(4,1,1,
1,1,1,1,1,4),(53.4070751110275,53.6004051066608,54.6000525085395,55.5996999104182,
56.5993473122969,57.5989947141756,58.5986421160543,59.5982895179329,59.6902604182071),
 .UNSPECIFIED.);
#6651=B_SPLINE_CURVE_WITH_KNOTS('',3,(#50814,#50815,#50816,#50817,#50818,
#50819,#50820,#50821,#50822,#50823),.UNSPECIFIED.,.F.,.F.,(4,1,1,1,1,1,
1,4),(53.4070751110279,54.2985132362786,55.2981606381573,56.2978080400359,
57.2974554419146,58.2971028437933,59.296750245672,59.6902604182075),
 .UNSPECIFIED.);
#6652=B_SPLINE_CURVE_WITH_KNOTS('',3,(#50828,#50829,#50830,#50831,#50832,
#50833,#50834,#50835,#50836,#50837),.UNSPECIFIED.,.F.,.F.,(4,1,1,1,1,1,
1,4),(47.123889803848,47.6025206953887,48.6021680972674,49.6018154991461,
50.6014629010248,51.6011103029035,52.6007577047822,53.4070751110275),
 .UNSPECIFIED.);
#6653=B_SPLINE_CURVE_WITH_KNOTS('',3,(#50838,#50839,#50840,#50841,#50842,
#50843,#50844,#50845,#50846,#50847,#50848),.UNSPECIFIED.,.F.,.F.,(4,1,1,
1,1,1,1,1,4),(47.1238898038483,47.3009814231278,48.3006288250065,49.3002762268852,
50.2999236287638,51.2995710306425,52.2992184325212,53.2988658343999,53.4070751110279),
 .UNSPECIFIED.);
#6654=B_SPLINE_CURVE_WITH_KNOTS('',3,(#50853,#50854,#50855,#50856,#50857,
#50858,#50859,#50860,#50861,#50862),.UNSPECIFIED.,.F.,.F.,(4,1,1,1,1,1,
1,4),(40.8407044966684,41.6046362841166,42.6042836859953,43.603931087874,
44.6035784897527,45.6032258916314,46.6028732935101,47.123889803848),
 .UNSPECIFIED.);
#6655=B_SPLINE_CURVE_WITH_KNOTS('',3,(#50863,#50864,#50865,#50866,#50867,
#50868,#50869,#50870,#50871,#50872),.UNSPECIFIED.,.F.,.F.,(4,1,1,1,1,1,
1,4),(40.8407044966687,41.3030970118557,42.3027444137344,43.302391815613,
44.3020392174917,45.3016866193704,46.3013340212491,47.1238898038483),
 .UNSPECIFIED.);
#6656=B_SPLINE_CURVE_WITH_KNOTS('',3,(#50877,#50878,#50879,#50880,#50881,
#50882,#50883,#50884,#50885,#50886,#50887),.UNSPECIFIED.,.F.,.F.,(4,1,1,
1,1,1,1,1,4),(34.5575191894888,34.6071044709659,35.6067518728445,36.6063992747232,
37.6060466766019,38.6056940784806,39.6053414803593,40.604988882238,40.8407044966684),
 .UNSPECIFIED.);
#6657=B_SPLINE_CURVE_WITH_KNOTS('',3,(#50888,#50889,#50890,#50891,#50892,
#50893,#50894,#50895,#50896,#50897),.UNSPECIFIED.,.F.,.F.,(4,1,1,1,1,1,
1,4),(34.5575191894891,35.3052126005836,36.3048600024622,37.3045074043409,
38.3041548062196,39.3038022080983,40.303449609977,40.8407044966687),
 .UNSPECIFIED.);
#6658=B_SPLINE_CURVE_WITH_KNOTS('',3,(#50902,#50903,#50904,#50905,#50906,
#50907,#50908,#50909,#50910,#50911),.UNSPECIFIED.,.F.,.F.,(4,1,1,1,1,1,
1,4),(28.2743338823092,28.6092200596937,29.6088674615724,30.6085148634511,
31.6081622653298,32.6078096672085,33.6074570690872,34.5575191894888),
 .UNSPECIFIED.);
#6659=B_SPLINE_CURVE_WITH_KNOTS('',3,(#50912,#50913,#50914,#50915,#50916,
#50917,#50918,#50919,#50920,#50921,#50922),.UNSPECIFIED.,.F.,.F.,(4,1,1,
1,1,1,1,1,4),(28.2743338823096,28.3076807874328,29.3073281893115,30.3069755911901,
31.3066229930688,32.3062703949475,33.3059177968262,34.3055651987049,34.5575191894891),
 .UNSPECIFIED.);
#6660=B_SPLINE_CURVE_WITH_KNOTS('',3,(#50927,#50928,#50929,#50930,#50931,
#50932,#50933,#50934,#50935,#50936),.UNSPECIFIED.,.F.,.F.,(4,1,1,1,1,1,
1,4),(21.9911485751296,22.6113356484216,23.6109830503003,24.610630452179,
25.6102778540577,26.6099252559364,27.6095726578151,28.2743338823092),
 .UNSPECIFIED.);
#6661=B_SPLINE_CURVE_WITH_KNOTS('',3,(#50937,#50938,#50939,#50940,#50941,
#50942,#50943,#50944,#50945,#50946),.UNSPECIFIED.,.F.,.F.,(4,1,1,1,1,1,
1,4),(21.99114857513,22.3097963761607,23.3094437780394,24.309091179918,
25.3087385817967,26.3083859836754,27.3080333855541,28.2743338823096),
 .UNSPECIFIED.);
#6662=B_SPLINE_CURVE_WITH_KNOTS('',3,(#50951,#50952,#50953,#50954,#50955,
#50956,#50957,#50958,#50959,#50960),.UNSPECIFIED.,.F.,.F.,(4,1,1,1,1,1,
1,4),(15.70796326795,16.6134512371495,17.6130986390282,18.6127460409069,
19.6123934427856,20.6120408446643,21.611688246543,21.9911485751296),
 .UNSPECIFIED.);
#6663=B_SPLINE_CURVE_WITH_KNOTS('',3,(#50961,#50962,#50963,#50964,#50965,
#50966,#50967,#50968,#50969,#50970),.UNSPECIFIED.,.F.,.F.,(4,1,1,1,1,1,
1,4),(15.7079632679504,16.3119119648886,17.3115593667672,18.3112067686459,
19.3108541705246,20.3105015724033,21.310148974282,21.99114857513),
 .UNSPECIFIED.);
#6664=B_SPLINE_CURVE_WITH_KNOTS('',3,(#53196,#53197,#53198,#53199,#53200,
#53201,#53202,#53203,#53204,#53205,#53206,#53207,#53208,#53209,#53210,#53211,
#53212,#53213,#53214,#53215,#53216,#53217,#53218,#53219,#53220,#53221,#53222,
#53223,#53224,#53225,#53226,#53227,#53228,#53229,#53230,#53231,#53232,#53233,
#53234,#53235,#53236,#53237,#53238,#53239,#53240,#53241,#53242,#53243,#53244,
#53245,#53246,#53247,#53248,#53249,#53250,#53251,#53252,#53253,#53254,#53255,
#53256,#53257,#53258,#53259,#53260,#53261,#53262,#53263,#53264,#53265,#53266,
#53267,#53268,#53269,#53270,#53271,#53272,#53273,#53274,#53275,#53276,#53277,
#53278,#53279,#53280,#53281,#53282,#53283,#53284,#53285,#53286,#53287,#53288,
#53289,#53290,#53291,#53292),.UNSPECIFIED.,.F.,.F.,(4,3,3,3,3,3,3,3,3,3,
3,3,3,3,3,3,3,3,3,3,3,3,3,3,3,3,3,3,3,3,3,3,4),(-0.741270768406061,-0.71696452138596,
-0.680440927304282,-0.659057791363252,-0.642652406304131,-0.636144085542677,
-0.599356622373509,-0.567167592100486,-0.553072383076001,-0.544362289353481,
-0.537677944349364,-0.502276237676446,-0.467138641981718,-0.433041019009119,
-0.410241859304171,-0.399246154564429,-0.394829851421709,-0.361211327226496,
-0.341844380189328,-0.307582718262882,-0.273165311582215,-0.262890280829855,
-0.257095817481949,-0.2236637832585,-0.190201737698465,-0.157152119987324,
-0.137508104988908,-0.127905898067162,-0.123173244372197,-0.0909734111245149,
-0.0592276901225634,-0.0284580599725401,0.),.UNSPECIFIED.);
#6665=B_SPLINE_CURVE_WITH_KNOTS('',3,(#53293,#53294,#53295,#53296,#53297,
#53298,#53299,#53300,#53301,#53302,#53303,#53304,#53305),.UNSPECIFIED.,
 .F.,.F.,(4,3,3,3,4),(547.747166935536,547.806776229519,548.806423631398,
549.806071033277,550.743811641397),.UNSPECIFIED.);
#6666=B_SPLINE_CURVE_WITH_KNOTS('',3,(#53307,#53308,#53309,#53310,#53311,
#53312,#53313,#53314,#53315,#53316,#53317,#53318,#53319,#53320,#53321,#53322,
#53323,#53324,#53325,#53326,#53327,#53328,#53329,#53330,#53331,#53332,#53333,
#53334,#53335,#53336,#53337,#53338,#53339,#53340,#53341,#53342,#53343,#53344,
#53345,#53346,#53347,#53348,#53349,#53350,#53351,#53352,#53353,#53354,#53355,
#53356,#53357,#53358,#53359,#53360,#53361,#53362,#53363,#53364,#53365,#53366,
#53367,#53368,#53369,#53370,#53371,#53372,#53373,#53374,#53375,#53376,#53377,
#53378,#53379,#53380,#53381,#53382,#53383,#53384,#53385,#53386,#53387,#53388,
#53389,#53390,#53391,#53392,#53393,#53394,#53395,#53396,#53397,#53398,#53399,
#53400,#53401,#53402,#53403),.UNSPECIFIED.,.F.,.F.,(4,3,3,3,3,3,3,3,3,3,
3,3,3,3,3,3,3,3,3,3,3,3,3,3,3,3,3,3,3,3,3,3,4),(-0.744397949170487,-0.724177512305599,
-0.693104810887909,-0.673480410559028,-0.660865919846913,-0.655179200686015,
-0.623187078074113,-0.592677994018076,-0.579330269743559,-0.573127817992138,
-0.567887494883166,-0.534520276836344,-0.500626959353002,-0.466813781988586,
-0.444888937897893,-0.437603624926938,-0.432876525336586,-0.397960991396844,
-0.379114405625813,-0.345405658901566,-0.311054469280115,-0.300315140774403,
-0.295343553676723,-0.261000993005831,-0.225526526851419,-0.189691877406385,
-0.165980392730587,-0.15447337421228,-0.147027486947459,-0.110270615210594,
-0.0734630229077671,-0.0367315114538836,0.),.UNSPECIFIED.);
#6667=B_SPLINE_CURVE_WITH_KNOTS('',3,(#53404,#53405,#53406,#53407,#53408,
#53409,#53410,#53411,#53412),.UNSPECIFIED.,.F.,.F.,(4,1,1,1,1,1,4),(10.3759343473751,
11.3136749554951,12.3133223573738,13.3129697592525,14.3126171611312,15.3122645630099,
15.7079632679504),.UNSPECIFIED.);
#6668=B_SPLINE_CURVE_WITH_KNOTS('',3,(#53418,#53419,#53420,#53421,#53422,
#53423,#53424,#53425,#53426,#53427,#53428,#53429,#53430,#53431,#53432,#53433,
#53434,#53435,#53436,#53437,#53438,#53439,#53440,#53441,#53442,#53443,#53444,
#53445,#53446,#53447,#53448,#53449,#53450,#53451,#53452,#53453,#53454,#53455,
#53456,#53457,#53458,#53459,#53460,#53461,#53462,#53463,#53464,#53465,#53466,
#53467,#53468,#53469,#53470,#53471,#53472,#53473,#53474,#53475,#53476,#53477,
#53478,#53479,#53480,#53481,#53482,#53483,#53484,#53485,#53486,#53487,#53488,
#53489,#53490,#53491,#53492,#53493,#53494,#53495,#53496,#53497,#53498,#53499,
#53500,#53501,#53502,#53503,#53504,#53505,#53506,#53507,#53508,#53509,#53510,
#53511,#53512,#53513,#53514),.UNSPECIFIED.,.F.,.F.,(4,3,3,3,3,3,3,3,3,3,
3,3,3,3,3,3,3,3,3,3,3,3,3,3,3,3,3,3,3,3,3,3,4),(-0.741270768406467,-0.716964521386347,
-0.680440927292735,-0.659057791393028,-0.642652406228543,-0.636144086243808,
-0.599356622987026,-0.567167592637341,-0.553072383177883,-0.544362289404779,
-0.537677944378733,-0.50227623772544,-0.467138642075895,-0.433041019100885,
-0.410241859373051,-0.399246154678599,-0.394829851420893,-0.361211327215821,
-0.341844380189548,-0.307582718280384,-0.273165311644367,-0.262890280934216,
-0.25709581734905,-0.223663783123785,-0.190201737572306,-0.157152119931196,
-0.137508104939796,-0.127905897837719,-0.123173244323147,-0.0909734110776745,
-0.0592276900781323,-0.0284580599372398,0.),.UNSPECIFIED.);
#6669=B_SPLINE_CURVE_WITH_KNOTS('',3,(#53517,#53518,#53519,#53520,#53521,
#53522,#53523,#53524),.UNSPECIFIED.,.F.,.F.,(4,1,1,1,1,4),(11.6152142277561,
12.6148616296348,13.6145090315135,14.6141564333922,15.6138038352709,15.70796326795),
 .UNSPECIFIED.);
#6670=B_SPLINE_CURVE_WITH_KNOTS('',3,(#55750,#55751,#55752,#55753,#55754,
#55755,#55756,#55757,#55758,#55759,#55760,#55761,#55762,#55763,#55764,#55765,
#55766,#55767,#55768,#55769,#55770,#55771,#55772,#55773,#55774,#55775,#55776,
#55777,#55778,#55779,#55780,#55781,#55782,#55783,#55784,#55785,#55786,#55787,
#55788,#55789,#55790,#55791,#55792,#55793,#55794,#55795,#55796,#55797,#55798,
#55799,#55800,#55801,#55802,#55803,#55804,#55805,#55806,#55807,#55808,#55809,
#55810,#55811,#55812,#55813,#55814,#55815,#55816,#55817,#55818,#55819,#55820,
#55821,#55822,#55823,#55824,#55825,#55826,#55827,#55828,#55829,#55830,#55831,
#55832,#55833,#55834,#55835,#55836,#55837,#55838,#55839,#55840,#55841,#55842,
#55843,#55844,#55845,#55846),.UNSPECIFIED.,.F.,.F.,(4,3,3,3,3,3,3,3,3,3,
3,3,3,3,3,3,3,3,3,3,3,3,3,3,3,3,3,3,3,3,3,3,4),(-0.744397949170763,-0.724177512305978,
-0.693104810875057,-0.673480410546995,-0.660865919810601,-0.655179200975098,
-0.623187078406178,-0.592677994308664,-0.579330270016002,-0.573127818760234,
-0.567887496175861,-0.534520278122044,-0.500626960665077,-0.466813783274203,
-0.444888938862169,-0.437603634425512,-0.432876535092151,-0.397961001197226,
-0.379114405626065,-0.345405658896003,-0.31105446923983,-0.300315140715421,
-0.29534355375871,-0.261000992978768,-0.225526526817216,-0.189691877366772,
-0.165980392695925,-0.154473374164193,-0.147027486633724,-0.110270614975293,
-0.0734630226814967,-0.0367315113407483,0.),.UNSPECIFIED.);
#6671=B_SPLINE_CURVE_WITH_KNOTS('',3,(#55847,#55848,#55849,#55850,#55851,
#55852,#55853,#55854,#55855,#55856),.UNSPECIFIED.,.F.,.F.,(4,3,3,4),(-552.805013238912,
-551.805365837034,-550.805718435155,-550.729870764817),.UNSPECIFIED.);
#7863=VERTEX_POINT('',#44371);
#7864=VERTEX_POINT('',#44372);
#7865=VERTEX_POINT('',#44374);
#7866=VERTEX_POINT('',#44385);
#7867=VERTEX_POINT('',#44395);
#7868=VERTEX_POINT('',#44396);
#7869=VERTEX_POINT('',#44443);
#7870=VERTEX_POINT('',#44444);
#7871=VERTEX_POINT('',#44491);
#7872=VERTEX_POINT('',#44492);
#7873=VERTEX_POINT('',#44539);
#7874=VERTEX_POINT('',#44540);
#7875=VERTEX_POINT('',#44593);
#7876=VERTEX_POINT('',#44594);
#7877=VERTEX_POINT('',#44641);
#7878=VERTEX_POINT('',#44642);
#7879=VERTEX_POINT('',#44689);
#7880=VERTEX_POINT('',#44690);
#7881=VERTEX_POINT('',#44743);
#7882=VERTEX_POINT('',#44744);
#7883=VERTEX_POINT('',#44791);
#7884=VERTEX_POINT('',#44792);
#7885=VERTEX_POINT('',#44839);
#7886=VERTEX_POINT('',#44840);
#7887=VERTEX_POINT('',#44887);
#7888=VERTEX_POINT('',#44888);
#7889=VERTEX_POINT('',#44941);
#7890=VERTEX_POINT('',#44942);
#7891=VERTEX_POINT('',#44989);
#7892=VERTEX_POINT('',#44990);
#7893=VERTEX_POINT('',#45037);
#7894=VERTEX_POINT('',#45038);
#7895=VERTEX_POINT('',#45091);
#7896=VERTEX_POINT('',#45092);
#7897=VERTEX_POINT('',#45139);
#7898=VERTEX_POINT('',#45140);
#7899=VERTEX_POINT('',#45187);
#7900=VERTEX_POINT('',#45188);
#7901=VERTEX_POINT('',#45235);
#7902=VERTEX_POINT('',#45236);
#7903=VERTEX_POINT('',#45289);
#7904=VERTEX_POINT('',#45290);
#7905=VERTEX_POINT('',#45337);
#7906=VERTEX_POINT('',#45338);
#7907=VERTEX_POINT('',#45385);
#7908=VERTEX_POINT('',#45386);
#7909=VERTEX_POINT('',#45439);
#7910=VERTEX_POINT('',#45440);
#7911=VERTEX_POINT('',#45487);
#7912=VERTEX_POINT('',#45488);
#7913=VERTEX_POINT('',#45535);
#7914=VERTEX_POINT('',#45536);
#7915=VERTEX_POINT('',#45583);
#7916=VERTEX_POINT('',#45584);
#7917=VERTEX_POINT('',#45637);
#7918=VERTEX_POINT('',#45638);
#7919=VERTEX_POINT('',#45685);
#7920=VERTEX_POINT('',#45686);
#7921=VERTEX_POINT('',#45733);
#7922=VERTEX_POINT('',#45734);
#7923=VERTEX_POINT('',#45787);
#7924=VERTEX_POINT('',#45788);
#7925=VERTEX_POINT('',#45835);
#7926=VERTEX_POINT('',#45836);
#7927=VERTEX_POINT('',#45883);
#7928=VERTEX_POINT('',#45884);
#7929=VERTEX_POINT('',#45931);
#7930=VERTEX_POINT('',#45932);
#7931=VERTEX_POINT('',#45985);
#7932=VERTEX_POINT('',#45986);
#7933=VERTEX_POINT('',#46033);
#7934=VERTEX_POINT('',#46034);
#7935=VERTEX_POINT('',#46081);
#7936=VERTEX_POINT('',#46082);
#7937=VERTEX_POINT('',#46135);
#7938=VERTEX_POINT('',#46136);
#7939=VERTEX_POINT('',#46183);
#7940=VERTEX_POINT('',#46184);
#7941=VERTEX_POINT('',#46231);
#7942=VERTEX_POINT('',#46232);
#7943=VERTEX_POINT('',#46279);
#7944=VERTEX_POINT('',#46280);
#7945=VERTEX_POINT('',#46333);
#7946=VERTEX_POINT('',#46334);
#7947=VERTEX_POINT('',#46381);
#7948=VERTEX_POINT('',#46382);
#7949=VERTEX_POINT('',#46429);
#7950=VERTEX_POINT('',#46430);
#7951=VERTEX_POINT('',#46483);
#7952=VERTEX_POINT('',#46484);
#7953=VERTEX_POINT('',#46531);
#7954=VERTEX_POINT('',#46532);
#7955=VERTEX_POINT('',#46579);
#7956=VERTEX_POINT('',#46580);
#7957=VERTEX_POINT('',#46627);
#7958=VERTEX_POINT('',#46628);
#7959=VERTEX_POINT('',#46681);
#7960=VERTEX_POINT('',#46682);
#7961=VERTEX_POINT('',#46729);
#7962=VERTEX_POINT('',#46730);
#7963=VERTEX_POINT('',#46777);
#7964=VERTEX_POINT('',#46778);
#7965=VERTEX_POINT('',#46831);
#7966=VERTEX_POINT('',#46832);
#7967=VERTEX_POINT('',#46879);
#7968=VERTEX_POINT('',#46880);
#7969=VERTEX_POINT('',#46927);
#7970=VERTEX_POINT('',#46928);
#7971=VERTEX_POINT('',#46975);
#7972=VERTEX_POINT('',#46976);
#7973=VERTEX_POINT('',#47029);
#7974=VERTEX_POINT('',#47030);
#7975=VERTEX_POINT('',#47077);
#7976=VERTEX_POINT('',#47078);
#7977=VERTEX_POINT('',#47125);
#7978=VERTEX_POINT('',#47126);
#7979=VERTEX_POINT('',#47179);
#7980=VERTEX_POINT('',#47180);
#7981=VERTEX_POINT('',#47227);
#7982=VERTEX_POINT('',#47228);
#7983=VERTEX_POINT('',#47275);
#7984=VERTEX_POINT('',#47276);
#7985=VERTEX_POINT('',#47323);
#7986=VERTEX_POINT('',#47324);
#7987=VERTEX_POINT('',#47377);
#7988=VERTEX_POINT('',#47378);
#7989=VERTEX_POINT('',#47425);
#7990=VERTEX_POINT('',#47426);
#7991=VERTEX_POINT('',#47473);
#7992=VERTEX_POINT('',#47474);
#7993=VERTEX_POINT('',#47527);
#7994=VERTEX_POINT('',#47528);
#7995=VERTEX_POINT('',#47575);
#7996=VERTEX_POINT('',#47576);
#7997=VERTEX_POINT('',#47623);
#7998=VERTEX_POINT('',#47624);
#7999=VERTEX_POINT('',#47671);
#8000=VERTEX_POINT('',#47672);
#8001=VERTEX_POINT('',#47725);
#8002=VERTEX_POINT('',#47726);
#8003=VERTEX_POINT('',#47773);
#8004=VERTEX_POINT('',#47774);
#8005=VERTEX_POINT('',#47821);
#8006=VERTEX_POINT('',#47822);
#8007=VERTEX_POINT('',#47875);
#8008=VERTEX_POINT('',#47876);
#8009=VERTEX_POINT('',#47923);
#8010=VERTEX_POINT('',#47924);
#8011=VERTEX_POINT('',#47971);
#8012=VERTEX_POINT('',#47972);
#8013=VERTEX_POINT('',#48019);
#8014=VERTEX_POINT('',#48020);
#8015=VERTEX_POINT('',#48073);
#8016=VERTEX_POINT('',#48074);
#8017=VERTEX_POINT('',#48121);
#8018=VERTEX_POINT('',#48122);
#8019=VERTEX_POINT('',#48169);
#8020=VERTEX_POINT('',#48170);
#8021=VERTEX_POINT('',#48223);
#8022=VERTEX_POINT('',#48224);
#8023=VERTEX_POINT('',#48271);
#8024=VERTEX_POINT('',#48272);
#8025=VERTEX_POINT('',#48319);
#8026=VERTEX_POINT('',#48320);
#8027=VERTEX_POINT('',#48367);
#8028=VERTEX_POINT('',#48368);
#8029=VERTEX_POINT('',#48421);
#8030=VERTEX_POINT('',#48422);
#8031=VERTEX_POINT('',#48469);
#8032=VERTEX_POINT('',#48470);
#8033=VERTEX_POINT('',#48517);
#8034=VERTEX_POINT('',#48518);
#8035=VERTEX_POINT('',#48571);
#8036=VERTEX_POINT('',#48572);
#8037=VERTEX_POINT('',#48619);
#8038=VERTEX_POINT('',#48620);
#8039=VERTEX_POINT('',#48667);
#8040=VERTEX_POINT('',#48668);
#8041=VERTEX_POINT('',#48715);
#8042=VERTEX_POINT('',#48716);
#8043=VERTEX_POINT('',#48718);
#8044=VERTEX_POINT('',#48725);
#8045=VERTEX_POINT('',#48726);
#8046=VERTEX_POINT('',#48750);
#8047=VERTEX_POINT('',#48762);
#8048=VERTEX_POINT('',#48763);
#8049=VERTEX_POINT('',#48810);
#8050=VERTEX_POINT('',#48811);
#8051=VERTEX_POINT('',#48858);
#8052=VERTEX_POINT('',#48859);
#8053=VERTEX_POINT('',#48883);
#8054=VERTEX_POINT('',#48884);
#8055=VERTEX_POINT('',#48908);
#8056=VERTEX_POINT('',#48909);
#8057=VERTEX_POINT('',#48932);
#8058=VERTEX_POINT('',#48933);
#8059=VERTEX_POINT('',#48957);
#8060=VERTEX_POINT('',#48958);
#8061=VERTEX_POINT('',#48996);
#8062=VERTEX_POINT('',#48997);
#8063=VERTEX_POINT('',#49032);
#8064=VERTEX_POINT('',#49033);
#8065=VERTEX_POINT('',#49056);
#8066=VERTEX_POINT('',#49057);
#8067=VERTEX_POINT('',#49081);
#8068=VERTEX_POINT('',#49082);
#8069=VERTEX_POINT('',#49106);
#8070=VERTEX_POINT('',#49107);
#8071=VERTEX_POINT('',#49130);
#8072=VERTEX_POINT('',#49131);
#8073=VERTEX_POINT('',#49155);
#8074=VERTEX_POINT('',#49156);
#8075=VERTEX_POINT('',#49180);
#8076=VERTEX_POINT('',#49181);
#8077=VERTEX_POINT('',#49216);
#8078=VERTEX_POINT('',#49217);
#8079=VERTEX_POINT('',#49252);
#8080=VERTEX_POINT('',#49253);
#8081=VERTEX_POINT('',#49277);
#8082=VERTEX_POINT('',#49278);
#8083=VERTEX_POINT('',#49302);
#8084=VERTEX_POINT('',#49303);
#8085=VERTEX_POINT('',#49326);
#8086=VERTEX_POINT('',#49327);
#8087=VERTEX_POINT('',#49351);
#8088=VERTEX_POINT('',#49352);
#8089=VERTEX_POINT('',#49376);
#8090=VERTEX_POINT('',#49377);
#8091=VERTEX_POINT('',#49400);
#8092=VERTEX_POINT('',#49401);
#8093=VERTEX_POINT('',#49424);
#8094=VERTEX_POINT('',#49425);
#8095=VERTEX_POINT('',#49449);
#8096=VERTEX_POINT('',#49450);
#8097=VERTEX_POINT('',#49474);
#8098=VERTEX_POINT('',#49475);
#8099=VERTEX_POINT('',#49498);
#8100=VERTEX_POINT('',#49499);
#8101=VERTEX_POINT('',#49523);
#8102=VERTEX_POINT('',#49524);
#8103=VERTEX_POINT('',#49548);
#8104=VERTEX_POINT('',#49549);
#8105=VERTEX_POINT('',#49572);
#8106=VERTEX_POINT('',#49573);
#8107=VERTEX_POINT('',#49596);
#8108=VERTEX_POINT('',#49597);
#8109=VERTEX_POINT('',#49621);
#8110=VERTEX_POINT('',#49622);
#8111=VERTEX_POINT('',#49646);
#8112=VERTEX_POINT('',#49647);
#8113=VERTEX_POINT('',#49670);
#8114=VERTEX_POINT('',#49671);
#8115=VERTEX_POINT('',#49695);
#8116=VERTEX_POINT('',#49696);
#8117=VERTEX_POINT('',#49720);
#8118=VERTEX_POINT('',#49721);
#8119=VERTEX_POINT('',#49744);
#8120=VERTEX_POINT('',#49745);
#8121=VERTEX_POINT('',#49768);
#8122=VERTEX_POINT('',#49769);
#8123=VERTEX_POINT('',#49793);
#8124=VERTEX_POINT('',#49794);
#8125=VERTEX_POINT('',#49818);
#8126=VERTEX_POINT('',#49819);
#8127=VERTEX_POINT('',#49842);
#8128=VERTEX_POINT('',#49843);
#8129=VERTEX_POINT('',#49867);
#8130=VERTEX_POINT('',#49868);
#8131=VERTEX_POINT('',#49892);
#8132=VERTEX_POINT('',#49893);
#8133=VERTEX_POINT('',#49916);
#8134=VERTEX_POINT('',#49917);
#8135=VERTEX_POINT('',#49940);
#8136=VERTEX_POINT('',#49941);
#8137=VERTEX_POINT('',#49965);
#8138=VERTEX_POINT('',#49966);
#8139=VERTEX_POINT('',#49990);
#8140=VERTEX_POINT('',#49991);
#8141=VERTEX_POINT('',#50014);
#8142=VERTEX_POINT('',#50015);
#8143=VERTEX_POINT('',#50039);
#8144=VERTEX_POINT('',#50040);
#8145=VERTEX_POINT('',#50064);
#8146=VERTEX_POINT('',#50065);
#8147=VERTEX_POINT('',#50088);
#8148=VERTEX_POINT('',#50089);
#8149=VERTEX_POINT('',#50112);
#8150=VERTEX_POINT('',#50113);
#8151=VERTEX_POINT('',#50137);
#8152=VERTEX_POINT('',#50138);
#8153=VERTEX_POINT('',#50162);
#8154=VERTEX_POINT('',#50163);
#8155=VERTEX_POINT('',#50186);
#8156=VERTEX_POINT('',#50187);
#8157=VERTEX_POINT('',#50211);
#8158=VERTEX_POINT('',#50212);
#8159=VERTEX_POINT('',#50236);
#8160=VERTEX_POINT('',#50237);
#8161=VERTEX_POINT('',#50260);
#8162=VERTEX_POINT('',#50261);
#8163=VERTEX_POINT('',#50284);
#8164=VERTEX_POINT('',#50285);
#8165=VERTEX_POINT('',#50309);
#8166=VERTEX_POINT('',#50310);
#8167=VERTEX_POINT('',#50334);
#8168=VERTEX_POINT('',#50335);
#8169=VERTEX_POINT('',#50358);
#8170=VERTEX_POINT('',#50359);
#8171=VERTEX_POINT('',#50383);
#8172=VERTEX_POINT('',#50384);
#8173=VERTEX_POINT('',#50408);
#8174=VERTEX_POINT('',#50409);
#8175=VERTEX_POINT('',#50432);
#8176=VERTEX_POINT('',#50433);
#8177=VERTEX_POINT('',#50456);
#8178=VERTEX_POINT('',#50457);
#8179=VERTEX_POINT('',#50481);
#8180=VERTEX_POINT('',#50482);
#8181=VERTEX_POINT('',#50506);
#8182=VERTEX_POINT('',#50507);
#8183=VERTEX_POINT('',#50530);
#8184=VERTEX_POINT('',#50531);
#8185=VERTEX_POINT('',#50555);
#8186=VERTEX_POINT('',#50556);
#8187=VERTEX_POINT('',#50580);
#8188=VERTEX_POINT('',#50581);
#8189=VERTEX_POINT('',#50604);
#8190=VERTEX_POINT('',#50605);
#8191=VERTEX_POINT('',#50628);
#8192=VERTEX_POINT('',#50629);
#8193=VERTEX_POINT('',#50653);
#8194=VERTEX_POINT('',#50654);
#8195=VERTEX_POINT('',#50678);
#8196=VERTEX_POINT('',#50679);
#8197=VERTEX_POINT('',#50702);
#8198=VERTEX_POINT('',#50703);
#8199=VERTEX_POINT('',#50727);
#8200=VERTEX_POINT('',#50728);
#8201=VERTEX_POINT('',#50752);
#8202=VERTEX_POINT('',#50753);
#8203=VERTEX_POINT('',#50776);
#8204=VERTEX_POINT('',#50777);
#8205=VERTEX_POINT('',#50800);
#8206=VERTEX_POINT('',#50801);
#8207=VERTEX_POINT('',#50825);
#8208=VERTEX_POINT('',#50826);
#8209=VERTEX_POINT('',#50850);
#8210=VERTEX_POINT('',#50851);
#8211=VERTEX_POINT('',#50874);
#8212=VERTEX_POINT('',#50875);
#8213=VERTEX_POINT('',#50899);
#8214=VERTEX_POINT('',#50900);
#8215=VERTEX_POINT('',#50924);
#8216=VERTEX_POINT('',#50925);
#8217=VERTEX_POINT('',#50948);
#8218=VERTEX_POINT('',#50949);
#8219=VERTEX_POINT('',#53195);
#8220=VERTEX_POINT('',#53306);
#8221=VERTEX_POINT('',#53414);
#8222=VERTEX_POINT('',#53417);
#8223=VERTEX_POINT('',#55749);
#8224=VERTEX_POINT('',#55858);
#8225=VERTEX_POINT('',#55859);
#8226=VERTEX_POINT('',#55863);
#8227=VERTEX_POINT('',#55867);
#8228=VERTEX_POINT('',#55871);
#8229=VERTEX_POINT('',#55875);
#8230=VERTEX_POINT('',#55879);
#8231=VERTEX_POINT('',#55882);
#8232=VERTEX_POINT('',#55890);
#8233=VERTEX_POINT('',#55892);
#8234=VERTEX_POINT('',#55896);
#8235=VERTEX_POINT('',#55900);
#8236=VERTEX_POINT('',#55904);
#8237=VERTEX_POINT('',#55906);
#8238=VERTEX_POINT('',#55917);
#10114=EDGE_CURVE('',#7863,#7864,#4642,.T.);
#10115=EDGE_CURVE('',#7863,#7865,#6313,.T.);
#10116=EDGE_CURVE('',#7865,#7866,#1205,.T.);
#10117=EDGE_CURVE('',#7866,#7864,#6314,.T.);
#10118=EDGE_CURVE('',#7867,#7868,#4643,.T.);
#10119=EDGE_CURVE('',#7867,#7863,#6315,.T.);
#10120=EDGE_CURVE('',#7864,#7868,#6316,.T.);
#10121=EDGE_CURVE('',#7869,#7870,#4644,.T.);
#10122=EDGE_CURVE('',#7869,#7867,#6317,.T.);
#10123=EDGE_CURVE('',#7868,#7870,#6318,.T.);
#10124=EDGE_CURVE('',#7871,#7872,#4645,.T.);
#10125=EDGE_CURVE('',#7871,#7869,#6319,.T.);
#10126=EDGE_CURVE('',#7870,#7872,#6320,.T.);
#10127=EDGE_CURVE('',#7873,#7874,#4646,.T.);
#10128=EDGE_CURVE('',#7873,#7871,#6321,.T.);
#10129=EDGE_CURVE('',#7872,#7874,#6322,.T.);
#10130=EDGE_CURVE('',#7875,#7876,#4647,.T.);
#10131=EDGE_CURVE('',#7875,#7873,#6323,.T.);
#10132=EDGE_CURVE('',#7874,#7876,#6324,.T.);
#10133=EDGE_CURVE('',#7877,#7878,#4648,.T.);
#10134=EDGE_CURVE('',#7877,#7875,#6325,.T.);
#10135=EDGE_CURVE('',#7876,#7878,#6326,.T.);
#10136=EDGE_CURVE('',#7879,#7880,#4649,.T.);
#10137=EDGE_CURVE('',#7879,#7877,#6327,.T.);
#10138=EDGE_CURVE('',#7878,#7880,#6328,.T.);
#10139=EDGE_CURVE('',#7881,#7882,#4650,.T.);
#10140=EDGE_CURVE('',#7881,#7879,#6329,.T.);
#10141=EDGE_CURVE('',#7880,#7882,#6330,.T.);
#10142=EDGE_CURVE('',#7883,#7884,#4651,.T.);
#10143=EDGE_CURVE('',#7883,#7881,#6331,.T.);
#10144=EDGE_CURVE('',#7882,#7884,#6332,.T.);
#10145=EDGE_CURVE('',#7885,#7886,#4652,.T.);
#10146=EDGE_CURVE('',#7885,#7883,#6333,.T.);
#10147=EDGE_CURVE('',#7884,#7886,#6334,.T.);
#10148=EDGE_CURVE('',#7887,#7888,#4653,.T.);
#10149=EDGE_CURVE('',#7887,#7885,#6335,.T.);
#10150=EDGE_CURVE('',#7886,#7888,#6336,.T.);
#10151=EDGE_CURVE('',#7889,#7890,#4654,.T.);
#10152=EDGE_CURVE('',#7889,#7887,#6337,.T.);
#10153=EDGE_CURVE('',#7888,#7890,#6338,.T.);
#10154=EDGE_CURVE('',#7891,#7892,#4655,.T.);
#10155=EDGE_CURVE('',#7891,#7889,#6339,.T.);
#10156=EDGE_CURVE('',#7890,#7892,#6340,.T.);
#10157=EDGE_CURVE('',#7893,#7894,#4656,.T.);
#10158=EDGE_CURVE('',#7893,#7891,#6341,.T.);
#10159=EDGE_CURVE('',#7892,#7894,#6342,.T.);
#10160=EDGE_CURVE('',#7895,#7896,#4657,.T.);
#10161=EDGE_CURVE('',#7895,#7893,#6343,.T.);
#10162=EDGE_CURVE('',#7894,#7896,#6344,.T.);
#10163=EDGE_CURVE('',#7897,#7898,#4658,.T.);
#10164=EDGE_CURVE('',#7897,#7895,#6345,.T.);
#10165=EDGE_CURVE('',#7896,#7898,#6346,.T.);
#10166=EDGE_CURVE('',#7899,#7900,#4659,.T.);
#10167=EDGE_CURVE('',#7899,#7897,#6347,.T.);
#10168=EDGE_CURVE('',#7898,#7900,#6348,.T.);
#10169=EDGE_CURVE('',#7901,#7902,#4660,.T.);
#10170=EDGE_CURVE('',#7901,#7899,#6349,.T.);
#10171=EDGE_CURVE('',#7900,#7902,#6350,.T.);
#10172=EDGE_CURVE('',#7903,#7904,#4661,.T.);
#10173=EDGE_CURVE('',#7903,#7901,#6351,.T.);
#10174=EDGE_CURVE('',#7902,#7904,#6352,.T.);
#10175=EDGE_CURVE('',#7905,#7906,#4662,.T.);
#10176=EDGE_CURVE('',#7905,#7903,#6353,.T.);
#10177=EDGE_CURVE('',#7904,#7906,#6354,.T.);
#10178=EDGE_CURVE('',#7907,#7908,#4663,.T.);
#10179=EDGE_CURVE('',#7907,#7905,#6355,.T.);
#10180=EDGE_CURVE('',#7906,#7908,#6356,.T.);
#10181=EDGE_CURVE('',#7909,#7910,#4664,.T.);
#10182=EDGE_CURVE('',#7909,#7907,#6357,.T.);
#10183=EDGE_CURVE('',#7908,#7910,#6358,.T.);
#10184=EDGE_CURVE('',#7911,#7912,#4665,.T.);
#10185=EDGE_CURVE('',#7911,#7909,#6359,.T.);
#10186=EDGE_CURVE('',#7910,#7912,#6360,.T.);
#10187=EDGE_CURVE('',#7913,#7914,#4666,.T.);
#10188=EDGE_CURVE('',#7913,#7911,#6361,.T.);
#10189=EDGE_CURVE('',#7912,#7914,#6362,.T.);
#10190=EDGE_CURVE('',#7915,#7916,#4667,.T.);
#10191=EDGE_CURVE('',#7915,#7913,#6363,.T.);
#10192=EDGE_CURVE('',#7914,#7916,#6364,.T.);
#10193=EDGE_CURVE('',#7917,#7918,#4668,.T.);
#10194=EDGE_CURVE('',#7917,#7915,#6365,.T.);
#10195=EDGE_CURVE('',#7916,#7918,#6366,.T.);
#10196=EDGE_CURVE('',#7919,#7920,#4669,.T.);
#10197=EDGE_CURVE('',#7919,#7917,#6367,.T.);
#10198=EDGE_CURVE('',#7918,#7920,#6368,.T.);
#10199=EDGE_CURVE('',#7921,#7922,#4670,.T.);
#10200=EDGE_CURVE('',#7921,#7919,#6369,.T.);
#10201=EDGE_CURVE('',#7920,#7922,#6370,.T.);
#10202=EDGE_CURVE('',#7923,#7924,#4671,.T.);
#10203=EDGE_CURVE('',#7923,#7921,#6371,.T.);
#10204=EDGE_CURVE('',#7922,#7924,#6372,.T.);
#10205=EDGE_CURVE('',#7925,#7926,#4672,.T.);
#10206=EDGE_CURVE('',#7925,#7923,#6373,.T.);
#10207=EDGE_CURVE('',#7924,#7926,#6374,.T.);
#10208=EDGE_CURVE('',#7927,#7928,#4673,.T.);
#10209=EDGE_CURVE('',#7927,#7925,#6375,.T.);
#10210=EDGE_CURVE('',#7926,#7928,#6376,.T.);
#10211=EDGE_CURVE('',#7929,#7930,#4674,.T.);
#10212=EDGE_CURVE('',#7929,#7927,#6377,.T.);
#10213=EDGE_CURVE('',#7928,#7930,#6378,.T.);
#10214=EDGE_CURVE('',#7931,#7932,#4675,.T.);
#10215=EDGE_CURVE('',#7931,#7929,#6379,.T.);
#10216=EDGE_CURVE('',#7930,#7932,#6380,.T.);
#10217=EDGE_CURVE('',#7933,#7934,#4676,.T.);
#10218=EDGE_CURVE('',#7933,#7931,#6381,.T.);
#10219=EDGE_CURVE('',#7932,#7934,#6382,.T.);
#10220=EDGE_CURVE('',#7935,#7936,#4677,.T.);
#10221=EDGE_CURVE('',#7935,#7933,#6383,.T.);
#10222=EDGE_CURVE('',#7934,#7936,#6384,.T.);
#10223=EDGE_CURVE('',#7937,#7938,#4678,.T.);
#10224=EDGE_CURVE('',#7937,#7935,#6385,.T.);
#10225=EDGE_CURVE('',#7936,#7938,#6386,.T.);
#10226=EDGE_CURVE('',#7939,#7940,#4679,.T.);
#10227=EDGE_CURVE('',#7939,#7937,#6387,.T.);
#10228=EDGE_CURVE('',#7938,#7940,#6388,.T.);
#10229=EDGE_CURVE('',#7941,#7942,#4680,.T.);
#10230=EDGE_CURVE('',#7941,#7939,#6389,.T.);
#10231=EDGE_CURVE('',#7940,#7942,#6390,.T.);
#10232=EDGE_CURVE('',#7943,#7944,#4681,.T.);
#10233=EDGE_CURVE('',#7943,#7941,#6391,.T.);
#10234=EDGE_CURVE('',#7942,#7944,#6392,.T.);
#10235=EDGE_CURVE('',#7945,#7946,#4682,.T.);
#10236=EDGE_CURVE('',#7945,#7943,#6393,.T.);
#10237=EDGE_CURVE('',#7944,#7946,#6394,.T.);
#10238=EDGE_CURVE('',#7947,#7948,#4683,.T.);
#10239=EDGE_CURVE('',#7947,#7945,#6395,.T.);
#10240=EDGE_CURVE('',#7946,#7948,#6396,.T.);
#10241=EDGE_CURVE('',#7949,#7950,#4684,.T.);
#10242=EDGE_CURVE('',#7949,#7947,#6397,.T.);
#10243=EDGE_CURVE('',#7948,#7950,#6398,.T.);
#10244=EDGE_CURVE('',#7951,#7952,#4685,.T.);
#10245=EDGE_CURVE('',#7951,#7949,#6399,.T.);
#10246=EDGE_CURVE('',#7950,#7952,#6400,.T.);
#10247=EDGE_CURVE('',#7953,#7954,#4686,.T.);
#10248=EDGE_CURVE('',#7953,#7951,#6401,.T.);
#10249=EDGE_CURVE('',#7952,#7954,#6402,.T.);
#10250=EDGE_CURVE('',#7955,#7956,#4687,.T.);
#10251=EDGE_CURVE('',#7955,#7953,#6403,.T.);
#10252=EDGE_CURVE('',#7954,#7956,#6404,.T.);
#10253=EDGE_CURVE('',#7957,#7958,#4688,.T.);
#10254=EDGE_CURVE('',#7957,#7955,#6405,.T.);
#10255=EDGE_CURVE('',#7956,#7958,#6406,.T.);
#10256=EDGE_CURVE('',#7959,#7960,#4689,.T.);
#10257=EDGE_CURVE('',#7959,#7957,#6407,.T.);
#10258=EDGE_CURVE('',#7958,#7960,#6408,.T.);
#10259=EDGE_CURVE('',#7961,#7962,#4690,.T.);
#10260=EDGE_CURVE('',#7961,#7959,#6409,.T.);
#10261=EDGE_CURVE('',#7960,#7962,#6410,.T.);
#10262=EDGE_CURVE('',#7963,#7964,#4691,.T.);
#10263=EDGE_CURVE('',#7963,#7961,#6411,.T.);
#10264=EDGE_CURVE('',#7962,#7964,#6412,.T.);
#10265=EDGE_CURVE('',#7965,#7966,#4692,.T.);
#10266=EDGE_CURVE('',#7965,#7963,#6413,.T.);
#10267=EDGE_CURVE('',#7964,#7966,#6414,.T.);
#10268=EDGE_CURVE('',#7967,#7968,#4693,.T.);
#10269=EDGE_CURVE('',#7967,#7965,#6415,.T.);
#10270=EDGE_CURVE('',#7966,#7968,#6416,.T.);
#10271=EDGE_CURVE('',#7969,#7970,#4694,.T.);
#10272=EDGE_CURVE('',#7969,#7967,#6417,.T.);
#10273=EDGE_CURVE('',#7968,#7970,#6418,.T.);
#10274=EDGE_CURVE('',#7971,#7972,#4695,.T.);
#10275=EDGE_CURVE('',#7971,#7969,#6419,.T.);
#10276=EDGE_CURVE('',#7970,#7972,#6420,.T.);
#10277=EDGE_CURVE('',#7973,#7974,#4696,.T.);
#10278=EDGE_CURVE('',#7973,#7971,#6421,.T.);
#10279=EDGE_CURVE('',#7972,#7974,#6422,.T.);
#10280=EDGE_CURVE('',#7975,#7976,#4697,.T.);
#10281=EDGE_CURVE('',#7975,#7973,#6423,.T.);
#10282=EDGE_CURVE('',#7974,#7976,#6424,.T.);
#10283=EDGE_CURVE('',#7977,#7978,#4698,.T.);
#10284=EDGE_CURVE('',#7977,#7975,#6425,.T.);
#10285=EDGE_CURVE('',#7976,#7978,#6426,.T.);
#10286=EDGE_CURVE('',#7979,#7980,#4699,.T.);
#10287=EDGE_CURVE('',#7979,#7977,#6427,.T.);
#10288=EDGE_CURVE('',#7978,#7980,#6428,.T.);
#10289=EDGE_CURVE('',#7981,#7982,#4700,.T.);
#10290=EDGE_CURVE('',#7981,#7979,#6429,.T.);
#10291=EDGE_CURVE('',#7980,#7982,#6430,.T.);
#10292=EDGE_CURVE('',#7983,#7984,#4701,.T.);
#10293=EDGE_CURVE('',#7983,#7981,#6431,.T.);
#10294=EDGE_CURVE('',#7982,#7984,#6432,.T.);
#10295=EDGE_CURVE('',#7985,#7986,#4702,.T.);
#10296=EDGE_CURVE('',#7985,#7983,#6433,.T.);
#10297=EDGE_CURVE('',#7984,#7986,#6434,.T.);
#10298=EDGE_CURVE('',#7987,#7988,#4703,.T.);
#10299=EDGE_CURVE('',#7987,#7985,#6435,.T.);
#10300=EDGE_CURVE('',#7986,#7988,#6436,.T.);
#10301=EDGE_CURVE('',#7989,#7990,#4704,.T.);
#10302=EDGE_CURVE('',#7989,#7987,#6437,.T.);
#10303=EDGE_CURVE('',#7988,#7990,#6438,.T.);
#10304=EDGE_CURVE('',#7991,#7992,#4705,.T.);
#10305=EDGE_CURVE('',#7991,#7989,#6439,.T.);
#10306=EDGE_CURVE('',#7990,#7992,#6440,.T.);
#10307=EDGE_CURVE('',#7993,#7994,#4706,.T.);
#10308=EDGE_CURVE('',#7993,#7991,#6441,.T.);
#10309=EDGE_CURVE('',#7992,#7994,#6442,.T.);
#10310=EDGE_CURVE('',#7995,#7996,#4707,.T.);
#10311=EDGE_CURVE('',#7995,#7993,#6443,.T.);
#10312=EDGE_CURVE('',#7994,#7996,#6444,.T.);
#10313=EDGE_CURVE('',#7997,#7998,#4708,.T.);
#10314=EDGE_CURVE('',#7997,#7995,#6445,.T.);
#10315=EDGE_CURVE('',#7996,#7998,#6446,.T.);
#10316=EDGE_CURVE('',#7999,#8000,#4709,.T.);
#10317=EDGE_CURVE('',#7999,#7997,#6447,.T.);
#10318=EDGE_CURVE('',#7998,#8000,#6448,.T.);
#10319=EDGE_CURVE('',#8001,#8002,#4710,.T.);
#10320=EDGE_CURVE('',#8001,#7999,#6449,.T.);
#10321=EDGE_CURVE('',#8000,#8002,#6450,.T.);
#10322=EDGE_CURVE('',#8003,#8004,#4711,.T.);
#10323=EDGE_CURVE('',#8003,#8001,#6451,.T.);
#10324=EDGE_CURVE('',#8002,#8004,#6452,.T.);
#10325=EDGE_CURVE('',#8005,#8006,#4712,.T.);
#10326=EDGE_CURVE('',#8005,#8003,#6453,.T.);
#10327=EDGE_CURVE('',#8004,#8006,#6454,.T.);
#10328=EDGE_CURVE('',#8007,#8008,#4713,.T.);
#10329=EDGE_CURVE('',#8007,#8005,#6455,.T.);
#10330=EDGE_CURVE('',#8006,#8008,#6456,.T.);
#10331=EDGE_CURVE('',#8009,#8010,#4714,.T.);
#10332=EDGE_CURVE('',#8009,#8007,#6457,.T.);
#10333=EDGE_CURVE('',#8008,#8010,#6458,.T.);
#10334=EDGE_CURVE('',#8011,#8012,#4715,.T.);
#10335=EDGE_CURVE('',#8011,#8009,#6459,.T.);
#10336=EDGE_CURVE('',#8010,#8012,#6460,.T.);
#10337=EDGE_CURVE('',#8013,#8014,#4716,.T.);
#10338=EDGE_CURVE('',#8013,#8011,#6461,.T.);
#10339=EDGE_CURVE('',#8012,#8014,#6462,.T.);
#10340=EDGE_CURVE('',#8015,#8016,#4717,.T.);
#10341=EDGE_CURVE('',#8015,#8013,#6463,.T.);
#10342=EDGE_CURVE('',#8014,#8016,#6464,.T.);
#10343=EDGE_CURVE('',#8017,#8018,#4718,.T.);
#10344=EDGE_CURVE('',#8017,#8015,#6465,.T.);
#10345=EDGE_CURVE('',#8016,#8018,#6466,.T.);
#10346=EDGE_CURVE('',#8019,#8020,#4719,.T.);
#10347=EDGE_CURVE('',#8019,#8017,#6467,.T.);
#10348=EDGE_CURVE('',#8018,#8020,#6468,.T.);
#10349=EDGE_CURVE('',#8021,#8022,#4720,.T.);
#10350=EDGE_CURVE('',#8021,#8019,#6469,.T.);
#10351=EDGE_CURVE('',#8020,#8022,#6470,.T.);
#10352=EDGE_CURVE('',#8023,#8024,#4721,.T.);
#10353=EDGE_CURVE('',#8023,#8021,#6471,.T.);
#10354=EDGE_CURVE('',#8022,#8024,#6472,.T.);
#10355=EDGE_CURVE('',#8025,#8026,#4722,.T.);
#10356=EDGE_CURVE('',#8025,#8023,#6473,.T.);
#10357=EDGE_CURVE('',#8024,#8026,#6474,.T.);
#10358=EDGE_CURVE('',#8027,#8028,#4723,.T.);
#10359=EDGE_CURVE('',#8027,#8025,#6475,.T.);
#10360=EDGE_CURVE('',#8026,#8028,#6476,.T.);
#10361=EDGE_CURVE('',#8029,#8030,#4724,.T.);
#10362=EDGE_CURVE('',#8029,#8027,#6477,.T.);
#10363=EDGE_CURVE('',#8028,#8030,#6478,.T.);
#10364=EDGE_CURVE('',#8031,#8032,#4725,.T.);
#10365=EDGE_CURVE('',#8031,#8029,#6479,.T.);
#10366=EDGE_CURVE('',#8030,#8032,#6480,.T.);
#10367=EDGE_CURVE('',#8033,#8034,#4726,.T.);
#10368=EDGE_CURVE('',#8033,#8031,#6481,.T.);
#10369=EDGE_CURVE('',#8032,#8034,#6482,.T.);
#10370=EDGE_CURVE('',#8035,#8036,#4727,.T.);
#10371=EDGE_CURVE('',#8035,#8033,#6483,.T.);
#10372=EDGE_CURVE('',#8034,#8036,#6484,.T.);
#10373=EDGE_CURVE('',#8037,#8038,#4728,.T.);
#10374=EDGE_CURVE('',#8037,#8035,#6485,.T.);
#10375=EDGE_CURVE('',#8036,#8038,#6486,.T.);
#10376=EDGE_CURVE('',#8039,#8040,#4729,.T.);
#10377=EDGE_CURVE('',#8039,#8037,#6487,.T.);
#10378=EDGE_CURVE('',#8038,#8040,#6488,.T.);
#10379=EDGE_CURVE('',#8041,#8042,#4730,.T.);
#10380=EDGE_CURVE('',#8041,#8043,#6489,.T.);
#10381=EDGE_CURVE('',#8042,#8043,#1206,.T.);
#10382=EDGE_CURVE('',#8044,#8045,#4731,.T.);
#10383=EDGE_CURVE('',#8044,#8041,#6490,.T.);
#10384=EDGE_CURVE('',#8046,#8042,#1207,.T.);
#10385=EDGE_CURVE('',#8045,#8046,#6491,.T.);
#10386=EDGE_CURVE('',#8047,#8048,#4732,.T.);
#10387=EDGE_CURVE('',#8047,#8044,#6492,.T.);
#10388=EDGE_CURVE('',#8048,#8045,#6493,.T.);
#10389=EDGE_CURVE('',#8049,#8050,#4733,.T.);
#10390=EDGE_CURVE('',#8049,#8047,#6494,.T.);
#10391=EDGE_CURVE('',#8050,#8048,#6495,.T.);
#10392=EDGE_CURVE('',#8051,#8052,#4734,.T.);
#10393=EDGE_CURVE('',#8051,#8049,#6496,.T.);
#10394=EDGE_CURVE('',#8052,#8050,#6497,.T.);
#10395=EDGE_CURVE('',#8053,#8054,#4735,.T.);
#10396=EDGE_CURVE('',#8053,#8051,#6498,.T.);
#10397=EDGE_CURVE('',#8054,#8052,#6499,.T.);
#10398=EDGE_CURVE('',#8055,#8056,#4736,.T.);
#10399=EDGE_CURVE('',#8055,#8053,#6500,.T.);
#10400=EDGE_CURVE('',#8056,#8054,#6501,.T.);
#10401=EDGE_CURVE('',#8057,#8058,#4737,.T.);
#10402=EDGE_CURVE('',#8057,#8055,#6502,.T.);
#10403=EDGE_CURVE('',#8058,#8056,#6503,.T.);
#10404=EDGE_CURVE('',#8059,#8060,#4738,.T.);
#10405=EDGE_CURVE('',#8059,#8057,#6504,.T.);
#10406=EDGE_CURVE('',#8060,#8058,#6505,.T.);
#10407=EDGE_CURVE('',#8061,#8062,#4739,.T.);
#10408=EDGE_CURVE('',#8061,#8059,#6506,.T.);
#10409=EDGE_CURVE('',#8062,#8060,#6507,.T.);
#10410=EDGE_CURVE('',#8063,#8064,#4740,.T.);
#10411=EDGE_CURVE('',#8063,#8061,#6508,.T.);
#10412=EDGE_CURVE('',#8064,#8062,#6509,.T.);
#10413=EDGE_CURVE('',#8065,#8066,#4741,.T.);
#10414=EDGE_CURVE('',#8065,#8063,#6510,.T.);
#10415=EDGE_CURVE('',#8066,#8064,#6511,.T.);
#10416=EDGE_CURVE('',#8067,#8068,#4742,.T.);
#10417=EDGE_CURVE('',#8067,#8065,#6512,.T.);
#10418=EDGE_CURVE('',#8068,#8066,#6513,.T.);
#10419=EDGE_CURVE('',#8069,#8070,#4743,.T.);
#10420=EDGE_CURVE('',#8069,#8067,#6514,.T.);
#10421=EDGE_CURVE('',#8070,#8068,#6515,.T.);
#10422=EDGE_CURVE('',#8071,#8072,#4744,.T.);
#10423=EDGE_CURVE('',#8071,#8069,#6516,.T.);
#10424=EDGE_CURVE('',#8072,#8070,#6517,.T.);
#10425=EDGE_CURVE('',#8073,#8074,#4745,.T.);
#10426=EDGE_CURVE('',#8073,#8071,#6518,.T.);
#10427=EDGE_CURVE('',#8074,#8072,#6519,.T.);
#10428=EDGE_CURVE('',#8075,#8076,#4746,.T.);
#10429=EDGE_CURVE('',#8075,#8073,#6520,.T.);
#10430=EDGE_CURVE('',#8076,#8074,#6521,.T.);
#10431=EDGE_CURVE('',#8077,#8078,#4747,.T.);
#10432=EDGE_CURVE('',#8077,#8075,#6522,.T.);
#10433=EDGE_CURVE('',#8078,#8076,#6523,.T.);
#10434=EDGE_CURVE('',#8079,#8080,#4748,.T.);
#10435=EDGE_CURVE('',#8079,#8077,#6524,.T.);
#10436=EDGE_CURVE('',#8080,#8078,#6525,.T.);
#10437=EDGE_CURVE('',#8081,#8082,#4749,.T.);
#10438=EDGE_CURVE('',#8081,#8079,#6526,.T.);
#10439=EDGE_CURVE('',#8082,#8080,#6527,.T.);
#10440=EDGE_CURVE('',#8083,#8084,#4750,.T.);
#10441=EDGE_CURVE('',#8083,#8081,#6528,.T.);
#10442=EDGE_CURVE('',#8084,#8082,#6529,.T.);
#10443=EDGE_CURVE('',#8085,#8086,#4751,.T.);
#10444=EDGE_CURVE('',#8085,#8083,#6530,.T.);
#10445=EDGE_CURVE('',#8086,#8084,#6531,.T.);
#10446=EDGE_CURVE('',#8087,#8088,#4752,.T.);
#10447=EDGE_CURVE('',#8087,#8085,#6532,.T.);
#10448=EDGE_CURVE('',#8088,#8086,#6533,.T.);
#10449=EDGE_CURVE('',#8089,#8090,#4753,.T.);
#10450=EDGE_CURVE('',#8089,#8087,#6534,.T.);
#10451=EDGE_CURVE('',#8090,#8088,#6535,.T.);
#10452=EDGE_CURVE('',#8091,#8092,#4754,.T.);
#10453=EDGE_CURVE('',#8091,#8089,#6536,.T.);
#10454=EDGE_CURVE('',#8092,#8090,#6537,.T.);
#10455=EDGE_CURVE('',#8093,#8094,#4755,.T.);
#10456=EDGE_CURVE('',#8093,#8091,#6538,.T.);
#10457=EDGE_CURVE('',#8094,#8092,#6539,.T.);
#10458=EDGE_CURVE('',#8095,#8096,#4756,.T.);
#10459=EDGE_CURVE('',#8095,#8093,#6540,.T.);
#10460=EDGE_CURVE('',#8096,#8094,#6541,.T.);
#10461=EDGE_CURVE('',#8097,#8098,#4757,.T.);
#10462=EDGE_CURVE('',#8097,#8095,#6542,.T.);
#10463=EDGE_CURVE('',#8098,#8096,#6543,.T.);
#10464=EDGE_CURVE('',#8099,#8100,#4758,.T.);
#10465=EDGE_CURVE('',#8099,#8097,#6544,.T.);
#10466=EDGE_CURVE('',#8100,#8098,#6545,.T.);
#10467=EDGE_CURVE('',#8101,#8102,#4759,.T.);
#10468=EDGE_CURVE('',#8101,#8099,#6546,.T.);
#10469=EDGE_CURVE('',#8102,#8100,#6547,.T.);
#10470=EDGE_CURVE('',#8103,#8104,#4760,.T.);
#10471=EDGE_CURVE('',#8103,#8101,#6548,.T.);
#10472=EDGE_CURVE('',#8104,#8102,#6549,.T.);
#10473=EDGE_CURVE('',#8105,#8106,#4761,.T.);
#10474=EDGE_CURVE('',#8105,#8103,#6550,.T.);
#10475=EDGE_CURVE('',#8106,#8104,#6551,.T.);
#10476=EDGE_CURVE('',#8107,#8108,#4762,.T.);
#10477=EDGE_CURVE('',#8107,#8105,#6552,.T.);
#10478=EDGE_CURVE('',#8108,#8106,#6553,.T.);
#10479=EDGE_CURVE('',#8109,#8110,#4763,.T.);
#10480=EDGE_CURVE('',#8109,#8107,#6554,.T.);
#10481=EDGE_CURVE('',#8110,#8108,#6555,.T.);
#10482=EDGE_CURVE('',#8111,#8112,#4764,.T.);
#10483=EDGE_CURVE('',#8111,#8109,#6556,.T.);
#10484=EDGE_CURVE('',#8112,#8110,#6557,.T.);
#10485=EDGE_CURVE('',#8113,#8114,#4765,.T.);
#10486=EDGE_CURVE('',#8113,#8111,#6558,.T.);
#10487=EDGE_CURVE('',#8114,#8112,#6559,.T.);
#10488=EDGE_CURVE('',#8115,#8116,#4766,.T.);
#10489=EDGE_CURVE('',#8115,#8113,#6560,.T.);
#10490=EDGE_CURVE('',#8116,#8114,#6561,.T.);
#10491=EDGE_CURVE('',#8117,#8118,#4767,.T.);
#10492=EDGE_CURVE('',#8117,#8115,#6562,.T.);
#10493=EDGE_CURVE('',#8118,#8116,#6563,.T.);
#10494=EDGE_CURVE('',#8119,#8120,#4768,.T.);
#10495=EDGE_CURVE('',#8119,#8117,#6564,.T.);
#10496=EDGE_CURVE('',#8120,#8118,#6565,.T.);
#10497=EDGE_CURVE('',#8121,#8122,#4769,.T.);
#10498=EDGE_CURVE('',#8121,#8119,#6566,.T.);
#10499=EDGE_CURVE('',#8122,#8120,#6567,.T.);
#10500=EDGE_CURVE('',#8123,#8124,#4770,.T.);
#10501=EDGE_CURVE('',#8123,#8121,#6568,.T.);
#10502=EDGE_CURVE('',#8124,#8122,#6569,.T.);
#10503=EDGE_CURVE('',#8125,#8126,#4771,.T.);
#10504=EDGE_CURVE('',#8125,#8123,#6570,.T.);
#10505=EDGE_CURVE('',#8126,#8124,#6571,.T.);
#10506=EDGE_CURVE('',#8127,#8128,#4772,.T.);
#10507=EDGE_CURVE('',#8127,#8125,#6572,.T.);
#10508=EDGE_CURVE('',#8128,#8126,#6573,.T.);
#10509=EDGE_CURVE('',#8129,#8130,#4773,.T.);
#10510=EDGE_CURVE('',#8129,#8127,#6574,.T.);
#10511=EDGE_CURVE('',#8130,#8128,#6575,.T.);
#10512=EDGE_CURVE('',#8131,#8132,#4774,.T.);
#10513=EDGE_CURVE('',#8131,#8129,#6576,.T.);
#10514=EDGE_CURVE('',#8132,#8130,#6577,.T.);
#10515=EDGE_CURVE('',#8133,#8134,#4775,.T.);
#10516=EDGE_CURVE('',#8133,#8131,#6578,.T.);
#10517=EDGE_CURVE('',#8134,#8132,#6579,.T.);
#10518=EDGE_CURVE('',#8135,#8136,#4776,.T.);
#10519=EDGE_CURVE('',#8135,#8133,#6580,.T.);
#10520=EDGE_CURVE('',#8136,#8134,#6581,.T.);
#10521=EDGE_CURVE('',#8137,#8138,#4777,.T.);
#10522=EDGE_CURVE('',#8137,#8135,#6582,.T.);
#10523=EDGE_CURVE('',#8138,#8136,#6583,.T.);
#10524=EDGE_CURVE('',#8139,#8140,#4778,.T.);
#10525=EDGE_CURVE('',#8139,#8137,#6584,.T.);
#10526=EDGE_CURVE('',#8140,#8138,#6585,.T.);
#10527=EDGE_CURVE('',#8141,#8142,#4779,.T.);
#10528=EDGE_CURVE('',#8141,#8139,#6586,.T.);
#10529=EDGE_CURVE('',#8142,#8140,#6587,.T.);
#10530=EDGE_CURVE('',#8143,#8144,#4780,.T.);
#10531=EDGE_CURVE('',#8143,#8141,#6588,.T.);
#10532=EDGE_CURVE('',#8144,#8142,#6589,.T.);
#10533=EDGE_CURVE('',#8145,#8146,#4781,.T.);
#10534=EDGE_CURVE('',#8145,#8143,#6590,.T.);
#10535=EDGE_CURVE('',#8146,#8144,#6591,.T.);
#10536=EDGE_CURVE('',#8147,#8148,#4782,.T.);
#10537=EDGE_CURVE('',#8147,#8145,#6592,.T.);
#10538=EDGE_CURVE('',#8148,#8146,#6593,.T.);
#10539=EDGE_CURVE('',#8149,#8150,#4783,.T.);
#10540=EDGE_CURVE('',#8149,#8147,#6594,.T.);
#10541=EDGE_CURVE('',#8150,#8148,#6595,.T.);
#10542=EDGE_CURVE('',#8151,#8152,#4784,.T.);
#10543=EDGE_CURVE('',#8151,#8149,#6596,.T.);
#10544=EDGE_CURVE('',#8152,#8150,#6597,.T.);
#10545=EDGE_CURVE('',#8153,#8154,#4785,.T.);
#10546=EDGE_CURVE('',#8153,#8151,#6598,.T.);
#10547=EDGE_CURVE('',#8154,#8152,#6599,.T.);
#10548=EDGE_CURVE('',#8155,#8156,#4786,.T.);
#10549=EDGE_CURVE('',#8155,#8153,#6600,.T.);
#10550=EDGE_CURVE('',#8156,#8154,#6601,.T.);
#10551=EDGE_CURVE('',#8157,#8158,#4787,.T.);
#10552=EDGE_CURVE('',#8157,#8155,#6602,.T.);
#10553=EDGE_CURVE('',#8158,#8156,#6603,.T.);
#10554=EDGE_CURVE('',#8159,#8160,#4788,.T.);
#10555=EDGE_CURVE('',#8159,#8157,#6604,.T.);
#10556=EDGE_CURVE('',#8160,#8158,#6605,.T.);
#10557=EDGE_CURVE('',#8161,#8162,#4789,.T.);
#10558=EDGE_CURVE('',#8161,#8159,#6606,.T.);
#10559=EDGE_CURVE('',#8162,#8160,#6607,.T.);
#10560=EDGE_CURVE('',#8163,#8164,#4790,.T.);
#10561=EDGE_CURVE('',#8163,#8161,#6608,.T.);
#10562=EDGE_CURVE('',#8164,#8162,#6609,.T.);
#10563=EDGE_CURVE('',#8165,#8166,#4791,.T.);
#10564=EDGE_CURVE('',#8165,#8163,#6610,.T.);
#10565=EDGE_CURVE('',#8166,#8164,#6611,.T.);
#10566=EDGE_CURVE('',#8167,#8168,#4792,.T.);
#10567=EDGE_CURVE('',#8167,#8165,#6612,.T.);
#10568=EDGE_CURVE('',#8168,#8166,#6613,.T.);
#10569=EDGE_CURVE('',#8169,#8170,#4793,.T.);
#10570=EDGE_CURVE('',#8169,#8167,#6614,.T.);
#10571=EDGE_CURVE('',#8170,#8168,#6615,.T.);
#10572=EDGE_CURVE('',#8171,#8172,#4794,.T.);
#10573=EDGE_CURVE('',#8171,#8169,#6616,.T.);
#10574=EDGE_CURVE('',#8172,#8170,#6617,.T.);
#10575=EDGE_CURVE('',#8173,#8174,#4795,.T.);
#10576=EDGE_CURVE('',#8173,#8171,#6618,.T.);
#10577=EDGE_CURVE('',#8174,#8172,#6619,.T.);
#10578=EDGE_CURVE('',#8175,#8176,#4796,.T.);
#10579=EDGE_CURVE('',#8175,#8173,#6620,.T.);
#10580=EDGE_CURVE('',#8176,#8174,#6621,.T.);
#10581=EDGE_CURVE('',#8177,#8178,#4797,.T.);
#10582=EDGE_CURVE('',#8177,#8175,#6622,.T.);
#10583=EDGE_CURVE('',#8178,#8176,#6623,.T.);
#10584=EDGE_CURVE('',#8179,#8180,#4798,.T.);
#10585=EDGE_CURVE('',#8179,#8177,#6624,.T.);
#10586=EDGE_CURVE('',#8180,#8178,#6625,.T.);
#10587=EDGE_CURVE('',#8181,#8182,#4799,.T.);
#10588=EDGE_CURVE('',#8181,#8179,#6626,.T.);
#10589=EDGE_CURVE('',#8182,#8180,#6627,.T.);
#10590=EDGE_CURVE('',#8183,#8184,#4800,.T.);
#10591=EDGE_CURVE('',#8183,#8181,#6628,.T.);
#10592=EDGE_CURVE('',#8184,#8182,#6629,.T.);
#10593=EDGE_CURVE('',#8185,#8186,#4801,.T.);
#10594=EDGE_CURVE('',#8185,#8183,#6630,.T.);
#10595=EDGE_CURVE('',#8186,#8184,#6631,.T.);
#10596=EDGE_CURVE('',#8187,#8188,#4802,.T.);
#10597=EDGE_CURVE('',#8187,#8185,#6632,.T.);
#10598=EDGE_CURVE('',#8188,#8186,#6633,.T.);
#10599=EDGE_CURVE('',#8189,#8190,#4803,.T.);
#10600=EDGE_CURVE('',#8189,#8187,#6634,.T.);
#10601=EDGE_CURVE('',#8190,#8188,#6635,.T.);
#10602=EDGE_CURVE('',#8191,#8192,#4804,.T.);
#10603=EDGE_CURVE('',#8191,#8189,#6636,.T.);
#10604=EDGE_CURVE('',#8192,#8190,#6637,.T.);
#10605=EDGE_CURVE('',#8193,#8194,#4805,.T.);
#10606=EDGE_CURVE('',#8193,#8191,#6638,.T.);
#10607=EDGE_CURVE('',#8194,#8192,#6639,.T.);
#10608=EDGE_CURVE('',#8195,#8196,#4806,.T.);
#10609=EDGE_CURVE('',#8195,#8193,#6640,.T.);
#10610=EDGE_CURVE('',#8196,#8194,#6641,.T.);
#10611=EDGE_CURVE('',#8197,#8198,#4807,.T.);
#10612=EDGE_CURVE('',#8197,#8195,#6642,.T.);
#10613=EDGE_CURVE('',#8198,#8196,#6643,.T.);
#10614=EDGE_CURVE('',#8199,#8200,#4808,.T.);
#10615=EDGE_CURVE('',#8199,#8197,#6644,.T.);
#10616=EDGE_CURVE('',#8200,#8198,#6645,.T.);
#10617=EDGE_CURVE('',#8201,#8202,#4809,.T.);
#10618=EDGE_CURVE('',#8201,#8199,#6646,.T.);
#10619=EDGE_CURVE('',#8202,#8200,#6647,.T.);
#10620=EDGE_CURVE('',#8203,#8204,#4810,.T.);
#10621=EDGE_CURVE('',#8203,#8201,#6648,.T.);
#10622=EDGE_CURVE('',#8204,#8202,#6649,.T.);
#10623=EDGE_CURVE('',#8205,#8206,#4811,.T.);
#10624=EDGE_CURVE('',#8205,#8203,#6650,.T.);
#10625=EDGE_CURVE('',#8206,#8204,#6651,.T.);
#10626=EDGE_CURVE('',#8207,#8208,#4812,.T.);
#10627=EDGE_CURVE('',#8207,#8205,#6652,.T.);
#10628=EDGE_CURVE('',#8208,#8206,#6653,.T.);
#10629=EDGE_CURVE('',#8209,#8210,#4813,.T.);
#10630=EDGE_CURVE('',#8209,#8207,#6654,.T.);
#10631=EDGE_CURVE('',#8210,#8208,#6655,.T.);
#10632=EDGE_CURVE('',#8211,#8212,#4814,.T.);
#10633=EDGE_CURVE('',#8211,#8209,#6656,.T.);
#10634=EDGE_CURVE('',#8212,#8210,#6657,.T.);
#10635=EDGE_CURVE('',#8213,#8214,#4815,.T.);
#10636=EDGE_CURVE('',#8213,#8211,#6658,.T.);
#10637=EDGE_CURVE('',#8214,#8212,#6659,.T.);
#10638=EDGE_CURVE('',#8215,#8216,#4816,.T.);
#10639=EDGE_CURVE('',#8215,#8213,#6660,.T.);
#10640=EDGE_CURVE('',#8216,#8214,#6661,.T.);
#10641=EDGE_CURVE('',#8217,#8218,#4817,.T.);
#10642=EDGE_CURVE('',#8217,#8215,#6662,.T.);
#10643=EDGE_CURVE('',#8218,#8216,#6663,.T.);
#10644=EDGE_CURVE('',#8219,#8046,#6664,.T.);
#10645=EDGE_CURVE('',#8040,#8219,#6665,.T.);
#10646=EDGE_CURVE('',#8220,#7866,#6666,.T.);
#10647=EDGE_CURVE('',#8220,#8218,#6667,.T.);
#10648=EDGE_CURVE('',#7866,#8221,#1208,.T.);
#10649=EDGE_CURVE('',#8221,#7865,#1209,.T.);
#10650=EDGE_CURVE('',#7865,#8222,#6668,.T.);
#10651=EDGE_CURVE('',#8222,#8220,#1210,.T.);
#10652=EDGE_CURVE('',#8222,#8217,#6669,.T.);
#10653=EDGE_CURVE('',#8043,#8223,#6670,.T.);
#10654=EDGE_CURVE('',#8223,#8039,#6671,.T.);
#10655=EDGE_CURVE('',#8224,#8225,#1785,.T.);
#10656=EDGE_CURVE('',#8226,#8224,#1786,.T.);
#10657=EDGE_CURVE('',#8227,#8226,#1787,.T.);
#10658=EDGE_CURVE('',#8228,#8227,#1788,.T.);
#10659=EDGE_CURVE('',#8229,#8228,#1789,.T.);
#10660=EDGE_CURVE('',#8229,#8230,#4818,.T.);
#10661=EDGE_CURVE('',#8230,#8230,#1211,.T.);
#10662=EDGE_CURVE('',#8231,#8229,#1790,.T.);
#10663=EDGE_CURVE('',#8225,#8231,#1791,.T.);
#10664=EDGE_CURVE('',#8232,#8227,#4819,.T.);
#10665=EDGE_CURVE('',#8232,#8233,#4820,.T.);
#10666=EDGE_CURVE('',#8233,#8228,#4821,.T.);
#10667=EDGE_CURVE('',#8234,#8226,#4822,.T.);
#10668=EDGE_CURVE('',#8234,#8232,#4823,.T.);
#10669=EDGE_CURVE('',#8235,#8224,#4824,.T.);
#10670=EDGE_CURVE('',#8235,#8234,#4825,.T.);
#10671=EDGE_CURVE('',#8236,#8235,#4826,.T.);
#10672=EDGE_CURVE('',#8237,#8236,#4827,.T.);
#10673=EDGE_CURVE('',#8233,#8237,#4828,.T.);
#10674=EDGE_CURVE('',#8223,#8219,#1212,.F.);
#10675=EDGE_CURVE('',#8236,#8225,#4829,.T.);
#10676=EDGE_CURVE('',#8237,#8231,#4830,.T.);
#10677=EDGE_CURVE('',#8238,#8238,#1213,.T.);
#10678=EDGE_CURVE('',#8221,#8238,#4831,.T.);
#14414=ORIENTED_EDGE('',*,*,#10114,.F.);
#14415=ORIENTED_EDGE('',*,*,#10115,.T.);
#14416=ORIENTED_EDGE('',*,*,#10116,.T.);
#14417=ORIENTED_EDGE('',*,*,#10117,.T.);
#14418=ORIENTED_EDGE('',*,*,#10118,.F.);
#14419=ORIENTED_EDGE('',*,*,#10119,.T.);
#14420=ORIENTED_EDGE('',*,*,#10114,.T.);
#14421=ORIENTED_EDGE('',*,*,#10120,.T.);
#14422=ORIENTED_EDGE('',*,*,#10121,.F.);
#14423=ORIENTED_EDGE('',*,*,#10122,.T.);
#14424=ORIENTED_EDGE('',*,*,#10118,.T.);
#14425=ORIENTED_EDGE('',*,*,#10123,.T.);
#14426=ORIENTED_EDGE('',*,*,#10124,.F.);
#14427=ORIENTED_EDGE('',*,*,#10125,.T.);
#14428=ORIENTED_EDGE('',*,*,#10121,.T.);
#14429=ORIENTED_EDGE('',*,*,#10126,.T.);
#14430=ORIENTED_EDGE('',*,*,#10127,.F.);
#14431=ORIENTED_EDGE('',*,*,#10128,.T.);
#14432=ORIENTED_EDGE('',*,*,#10124,.T.);
#14433=ORIENTED_EDGE('',*,*,#10129,.T.);
#14434=ORIENTED_EDGE('',*,*,#10130,.F.);
#14435=ORIENTED_EDGE('',*,*,#10131,.T.);
#14436=ORIENTED_EDGE('',*,*,#10127,.T.);
#14437=ORIENTED_EDGE('',*,*,#10132,.T.);
#14438=ORIENTED_EDGE('',*,*,#10133,.F.);
#14439=ORIENTED_EDGE('',*,*,#10134,.T.);
#14440=ORIENTED_EDGE('',*,*,#10130,.T.);
#14441=ORIENTED_EDGE('',*,*,#10135,.T.);
#14442=ORIENTED_EDGE('',*,*,#10136,.F.);
#14443=ORIENTED_EDGE('',*,*,#10137,.T.);
#14444=ORIENTED_EDGE('',*,*,#10133,.T.);
#14445=ORIENTED_EDGE('',*,*,#10138,.T.);
#14446=ORIENTED_EDGE('',*,*,#10139,.F.);
#14447=ORIENTED_EDGE('',*,*,#10140,.T.);
#14448=ORIENTED_EDGE('',*,*,#10136,.T.);
#14449=ORIENTED_EDGE('',*,*,#10141,.T.);
#14450=ORIENTED_EDGE('',*,*,#10142,.F.);
#14451=ORIENTED_EDGE('',*,*,#10143,.T.);
#14452=ORIENTED_EDGE('',*,*,#10139,.T.);
#14453=ORIENTED_EDGE('',*,*,#10144,.T.);
#14454=ORIENTED_EDGE('',*,*,#10145,.F.);
#14455=ORIENTED_EDGE('',*,*,#10146,.T.);
#14456=ORIENTED_EDGE('',*,*,#10142,.T.);
#14457=ORIENTED_EDGE('',*,*,#10147,.T.);
#14458=ORIENTED_EDGE('',*,*,#10148,.F.);
#14459=ORIENTED_EDGE('',*,*,#10149,.T.);
#14460=ORIENTED_EDGE('',*,*,#10145,.T.);
#14461=ORIENTED_EDGE('',*,*,#10150,.T.);
#14462=ORIENTED_EDGE('',*,*,#10151,.F.);
#14463=ORIENTED_EDGE('',*,*,#10152,.T.);
#14464=ORIENTED_EDGE('',*,*,#10148,.T.);
#14465=ORIENTED_EDGE('',*,*,#10153,.T.);
#14466=ORIENTED_EDGE('',*,*,#10154,.F.);
#14467=ORIENTED_EDGE('',*,*,#10155,.T.);
#14468=ORIENTED_EDGE('',*,*,#10151,.T.);
#14469=ORIENTED_EDGE('',*,*,#10156,.T.);
#14470=ORIENTED_EDGE('',*,*,#10157,.F.);
#14471=ORIENTED_EDGE('',*,*,#10158,.T.);
#14472=ORIENTED_EDGE('',*,*,#10154,.T.);
#14473=ORIENTED_EDGE('',*,*,#10159,.T.);
#14474=ORIENTED_EDGE('',*,*,#10160,.F.);
#14475=ORIENTED_EDGE('',*,*,#10161,.T.);
#14476=ORIENTED_EDGE('',*,*,#10157,.T.);
#14477=ORIENTED_EDGE('',*,*,#10162,.T.);
#14478=ORIENTED_EDGE('',*,*,#10163,.F.);
#14479=ORIENTED_EDGE('',*,*,#10164,.T.);
#14480=ORIENTED_EDGE('',*,*,#10160,.T.);
#14481=ORIENTED_EDGE('',*,*,#10165,.T.);
#14482=ORIENTED_EDGE('',*,*,#10166,.F.);
#14483=ORIENTED_EDGE('',*,*,#10167,.T.);
#14484=ORIENTED_EDGE('',*,*,#10163,.T.);
#14485=ORIENTED_EDGE('',*,*,#10168,.T.);
#14486=ORIENTED_EDGE('',*,*,#10169,.F.);
#14487=ORIENTED_EDGE('',*,*,#10170,.T.);
#14488=ORIENTED_EDGE('',*,*,#10166,.T.);
#14489=ORIENTED_EDGE('',*,*,#10171,.T.);
#14490=ORIENTED_EDGE('',*,*,#10172,.F.);
#14491=ORIENTED_EDGE('',*,*,#10173,.T.);
#14492=ORIENTED_EDGE('',*,*,#10169,.T.);
#14493=ORIENTED_EDGE('',*,*,#10174,.T.);
#14494=ORIENTED_EDGE('',*,*,#10175,.F.);
#14495=ORIENTED_EDGE('',*,*,#10176,.T.);
#14496=ORIENTED_EDGE('',*,*,#10172,.T.);
#14497=ORIENTED_EDGE('',*,*,#10177,.T.);
#14498=ORIENTED_EDGE('',*,*,#10178,.F.);
#14499=ORIENTED_EDGE('',*,*,#10179,.T.);
#14500=ORIENTED_EDGE('',*,*,#10175,.T.);
#14501=ORIENTED_EDGE('',*,*,#10180,.T.);
#14502=ORIENTED_EDGE('',*,*,#10181,.F.);
#14503=ORIENTED_EDGE('',*,*,#10182,.T.);
#14504=ORIENTED_EDGE('',*,*,#10178,.T.);
#14505=ORIENTED_EDGE('',*,*,#10183,.T.);
#14506=ORIENTED_EDGE('',*,*,#10184,.F.);
#14507=ORIENTED_EDGE('',*,*,#10185,.T.);
#14508=ORIENTED_EDGE('',*,*,#10181,.T.);
#14509=ORIENTED_EDGE('',*,*,#10186,.T.);
#14510=ORIENTED_EDGE('',*,*,#10187,.F.);
#14511=ORIENTED_EDGE('',*,*,#10188,.T.);
#14512=ORIENTED_EDGE('',*,*,#10184,.T.);
#14513=ORIENTED_EDGE('',*,*,#10189,.T.);
#14514=ORIENTED_EDGE('',*,*,#10190,.F.);
#14515=ORIENTED_EDGE('',*,*,#10191,.T.);
#14516=ORIENTED_EDGE('',*,*,#10187,.T.);
#14517=ORIENTED_EDGE('',*,*,#10192,.T.);
#14518=ORIENTED_EDGE('',*,*,#10193,.F.);
#14519=ORIENTED_EDGE('',*,*,#10194,.T.);
#14520=ORIENTED_EDGE('',*,*,#10190,.T.);
#14521=ORIENTED_EDGE('',*,*,#10195,.T.);
#14522=ORIENTED_EDGE('',*,*,#10196,.F.);
#14523=ORIENTED_EDGE('',*,*,#10197,.T.);
#14524=ORIENTED_EDGE('',*,*,#10193,.T.);
#14525=ORIENTED_EDGE('',*,*,#10198,.T.);
#14526=ORIENTED_EDGE('',*,*,#10199,.F.);
#14527=ORIENTED_EDGE('',*,*,#10200,.T.);
#14528=ORIENTED_EDGE('',*,*,#10196,.T.);
#14529=ORIENTED_EDGE('',*,*,#10201,.T.);
#14530=ORIENTED_EDGE('',*,*,#10202,.F.);
#14531=ORIENTED_EDGE('',*,*,#10203,.T.);
#14532=ORIENTED_EDGE('',*,*,#10199,.T.);
#14533=ORIENTED_EDGE('',*,*,#10204,.T.);
#14534=ORIENTED_EDGE('',*,*,#10205,.F.);
#14535=ORIENTED_EDGE('',*,*,#10206,.T.);
#14536=ORIENTED_EDGE('',*,*,#10202,.T.);
#14537=ORIENTED_EDGE('',*,*,#10207,.T.);
#14538=ORIENTED_EDGE('',*,*,#10208,.F.);
#14539=ORIENTED_EDGE('',*,*,#10209,.T.);
#14540=ORIENTED_EDGE('',*,*,#10205,.T.);
#14541=ORIENTED_EDGE('',*,*,#10210,.T.);
#14542=ORIENTED_EDGE('',*,*,#10211,.F.);
#14543=ORIENTED_EDGE('',*,*,#10212,.T.);
#14544=ORIENTED_EDGE('',*,*,#10208,.T.);
#14545=ORIENTED_EDGE('',*,*,#10213,.T.);
#14546=ORIENTED_EDGE('',*,*,#10214,.F.);
#14547=ORIENTED_EDGE('',*,*,#10215,.T.);
#14548=ORIENTED_EDGE('',*,*,#10211,.T.);
#14549=ORIENTED_EDGE('',*,*,#10216,.T.);
#14550=ORIENTED_EDGE('',*,*,#10217,.F.);
#14551=ORIENTED_EDGE('',*,*,#10218,.T.);
#14552=ORIENTED_EDGE('',*,*,#10214,.T.);
#14553=ORIENTED_EDGE('',*,*,#10219,.T.);
#14554=ORIENTED_EDGE('',*,*,#10220,.F.);
#14555=ORIENTED_EDGE('',*,*,#10221,.T.);
#14556=ORIENTED_EDGE('',*,*,#10217,.T.);
#14557=ORIENTED_EDGE('',*,*,#10222,.T.);
#14558=ORIENTED_EDGE('',*,*,#10223,.F.);
#14559=ORIENTED_EDGE('',*,*,#10224,.T.);
#14560=ORIENTED_EDGE('',*,*,#10220,.T.);
#14561=ORIENTED_EDGE('',*,*,#10225,.T.);
#14562=ORIENTED_EDGE('',*,*,#10226,.F.);
#14563=ORIENTED_EDGE('',*,*,#10227,.T.);
#14564=ORIENTED_EDGE('',*,*,#10223,.T.);
#14565=ORIENTED_EDGE('',*,*,#10228,.T.);
#14566=ORIENTED_EDGE('',*,*,#10229,.F.);
#14567=ORIENTED_EDGE('',*,*,#10230,.T.);
#14568=ORIENTED_EDGE('',*,*,#10226,.T.);
#14569=ORIENTED_EDGE('',*,*,#10231,.T.);
#14570=ORIENTED_EDGE('',*,*,#10232,.F.);
#14571=ORIENTED_EDGE('',*,*,#10233,.T.);
#14572=ORIENTED_EDGE('',*,*,#10229,.T.);
#14573=ORIENTED_EDGE('',*,*,#10234,.T.);
#14574=ORIENTED_EDGE('',*,*,#10235,.F.);
#14575=ORIENTED_EDGE('',*,*,#10236,.T.);
#14576=ORIENTED_EDGE('',*,*,#10232,.T.);
#14577=ORIENTED_EDGE('',*,*,#10237,.T.);
#14578=ORIENTED_EDGE('',*,*,#10238,.F.);
#14579=ORIENTED_EDGE('',*,*,#10239,.T.);
#14580=ORIENTED_EDGE('',*,*,#10235,.T.);
#14581=ORIENTED_EDGE('',*,*,#10240,.T.);
#14582=ORIENTED_EDGE('',*,*,#10241,.F.);
#14583=ORIENTED_EDGE('',*,*,#10242,.T.);
#14584=ORIENTED_EDGE('',*,*,#10238,.T.);
#14585=ORIENTED_EDGE('',*,*,#10243,.T.);
#14586=ORIENTED_EDGE('',*,*,#10244,.F.);
#14587=ORIENTED_EDGE('',*,*,#10245,.T.);
#14588=ORIENTED_EDGE('',*,*,#10241,.T.);
#14589=ORIENTED_EDGE('',*,*,#10246,.T.);
#14590=ORIENTED_EDGE('',*,*,#10247,.F.);
#14591=ORIENTED_EDGE('',*,*,#10248,.T.);
#14592=ORIENTED_EDGE('',*,*,#10244,.T.);
#14593=ORIENTED_EDGE('',*,*,#10249,.T.);
#14594=ORIENTED_EDGE('',*,*,#10250,.F.);
#14595=ORIENTED_EDGE('',*,*,#10251,.T.);
#14596=ORIENTED_EDGE('',*,*,#10247,.T.);
#14597=ORIENTED_EDGE('',*,*,#10252,.T.);
#14598=ORIENTED_EDGE('',*,*,#10253,.F.);
#14599=ORIENTED_EDGE('',*,*,#10254,.T.);
#14600=ORIENTED_EDGE('',*,*,#10250,.T.);
#14601=ORIENTED_EDGE('',*,*,#10255,.T.);
#14602=ORIENTED_EDGE('',*,*,#10256,.F.);
#14603=ORIENTED_EDGE('',*,*,#10257,.T.);
#14604=ORIENTED_EDGE('',*,*,#10253,.T.);
#14605=ORIENTED_EDGE('',*,*,#10258,.T.);
#14606=ORIENTED_EDGE('',*,*,#10259,.F.);
#14607=ORIENTED_EDGE('',*,*,#10260,.T.);
#14608=ORIENTED_EDGE('',*,*,#10256,.T.);
#14609=ORIENTED_EDGE('',*,*,#10261,.T.);
#14610=ORIENTED_EDGE('',*,*,#10262,.F.);
#14611=ORIENTED_EDGE('',*,*,#10263,.T.);
#14612=ORIENTED_EDGE('',*,*,#10259,.T.);
#14613=ORIENTED_EDGE('',*,*,#10264,.T.);
#14614=ORIENTED_EDGE('',*,*,#10265,.F.);
#14615=ORIENTED_EDGE('',*,*,#10266,.T.);
#14616=ORIENTED_EDGE('',*,*,#10262,.T.);
#14617=ORIENTED_EDGE('',*,*,#10267,.T.);
#14618=ORIENTED_EDGE('',*,*,#10268,.F.);
#14619=ORIENTED_EDGE('',*,*,#10269,.T.);
#14620=ORIENTED_EDGE('',*,*,#10265,.T.);
#14621=ORIENTED_EDGE('',*,*,#10270,.T.);
#14622=ORIENTED_EDGE('',*,*,#10271,.F.);
#14623=ORIENTED_EDGE('',*,*,#10272,.T.);
#14624=ORIENTED_EDGE('',*,*,#10268,.T.);
#14625=ORIENTED_EDGE('',*,*,#10273,.T.);
#14626=ORIENTED_EDGE('',*,*,#10274,.F.);
#14627=ORIENTED_EDGE('',*,*,#10275,.T.);
#14628=ORIENTED_EDGE('',*,*,#10271,.T.);
#14629=ORIENTED_EDGE('',*,*,#10276,.T.);
#14630=ORIENTED_EDGE('',*,*,#10277,.F.);
#14631=ORIENTED_EDGE('',*,*,#10278,.T.);
#14632=ORIENTED_EDGE('',*,*,#10274,.T.);
#14633=ORIENTED_EDGE('',*,*,#10279,.T.);
#14634=ORIENTED_EDGE('',*,*,#10280,.F.);
#14635=ORIENTED_EDGE('',*,*,#10281,.T.);
#14636=ORIENTED_EDGE('',*,*,#10277,.T.);
#14637=ORIENTED_EDGE('',*,*,#10282,.T.);
#14638=ORIENTED_EDGE('',*,*,#10283,.F.);
#14639=ORIENTED_EDGE('',*,*,#10284,.T.);
#14640=ORIENTED_EDGE('',*,*,#10280,.T.);
#14641=ORIENTED_EDGE('',*,*,#10285,.T.);
#14642=ORIENTED_EDGE('',*,*,#10286,.F.);
#14643=ORIENTED_EDGE('',*,*,#10287,.T.);
#14644=ORIENTED_EDGE('',*,*,#10283,.T.);
#14645=ORIENTED_EDGE('',*,*,#10288,.T.);
#14646=ORIENTED_EDGE('',*,*,#10289,.F.);
#14647=ORIENTED_EDGE('',*,*,#10290,.T.);
#14648=ORIENTED_EDGE('',*,*,#10286,.T.);
#14649=ORIENTED_EDGE('',*,*,#10291,.T.);
#14650=ORIENTED_EDGE('',*,*,#10292,.F.);
#14651=ORIENTED_EDGE('',*,*,#10293,.T.);
#14652=ORIENTED_EDGE('',*,*,#10289,.T.);
#14653=ORIENTED_EDGE('',*,*,#10294,.T.);
#14654=ORIENTED_EDGE('',*,*,#10295,.F.);
#14655=ORIENTED_EDGE('',*,*,#10296,.T.);
#14656=ORIENTED_EDGE('',*,*,#10292,.T.);
#14657=ORIENTED_EDGE('',*,*,#10297,.T.);
#14658=ORIENTED_EDGE('',*,*,#10298,.F.);
#14659=ORIENTED_EDGE('',*,*,#10299,.T.);
#14660=ORIENTED_EDGE('',*,*,#10295,.T.);
#14661=ORIENTED_EDGE('',*,*,#10300,.T.);
#14662=ORIENTED_EDGE('',*,*,#10301,.F.);
#14663=ORIENTED_EDGE('',*,*,#10302,.T.);
#14664=ORIENTED_EDGE('',*,*,#10298,.T.);
#14665=ORIENTED_EDGE('',*,*,#10303,.T.);
#14666=ORIENTED_EDGE('',*,*,#10304,.F.);
#14667=ORIENTED_EDGE('',*,*,#10305,.T.);
#14668=ORIENTED_EDGE('',*,*,#10301,.T.);
#14669=ORIENTED_EDGE('',*,*,#10306,.T.);
#14670=ORIENTED_EDGE('',*,*,#10307,.F.);
#14671=ORIENTED_EDGE('',*,*,#10308,.T.);
#14672=ORIENTED_EDGE('',*,*,#10304,.T.);
#14673=ORIENTED_EDGE('',*,*,#10309,.T.);
#14674=ORIENTED_EDGE('',*,*,#10310,.F.);
#14675=ORIENTED_EDGE('',*,*,#10311,.T.);
#14676=ORIENTED_EDGE('',*,*,#10307,.T.);
#14677=ORIENTED_EDGE('',*,*,#10312,.T.);
#14678=ORIENTED_EDGE('',*,*,#10313,.F.);
#14679=ORIENTED_EDGE('',*,*,#10314,.T.);
#14680=ORIENTED_EDGE('',*,*,#10310,.T.);
#14681=ORIENTED_EDGE('',*,*,#10315,.T.);
#14682=ORIENTED_EDGE('',*,*,#10316,.F.);
#14683=ORIENTED_EDGE('',*,*,#10317,.T.);
#14684=ORIENTED_EDGE('',*,*,#10313,.T.);
#14685=ORIENTED_EDGE('',*,*,#10318,.T.);
#14686=ORIENTED_EDGE('',*,*,#10319,.F.);
#14687=ORIENTED_EDGE('',*,*,#10320,.T.);
#14688=ORIENTED_EDGE('',*,*,#10316,.T.);
#14689=ORIENTED_EDGE('',*,*,#10321,.T.);
#14690=ORIENTED_EDGE('',*,*,#10322,.F.);
#14691=ORIENTED_EDGE('',*,*,#10323,.T.);
#14692=ORIENTED_EDGE('',*,*,#10319,.T.);
#14693=ORIENTED_EDGE('',*,*,#10324,.T.);
#14694=ORIENTED_EDGE('',*,*,#10325,.F.);
#14695=ORIENTED_EDGE('',*,*,#10326,.T.);
#14696=ORIENTED_EDGE('',*,*,#10322,.T.);
#14697=ORIENTED_EDGE('',*,*,#10327,.T.);
#14698=ORIENTED_EDGE('',*,*,#10328,.F.);
#14699=ORIENTED_EDGE('',*,*,#10329,.T.);
#14700=ORIENTED_EDGE('',*,*,#10325,.T.);
#14701=ORIENTED_EDGE('',*,*,#10330,.T.);
#14702=ORIENTED_EDGE('',*,*,#10331,.F.);
#14703=ORIENTED_EDGE('',*,*,#10332,.T.);
#14704=ORIENTED_EDGE('',*,*,#10328,.T.);
#14705=ORIENTED_EDGE('',*,*,#10333,.T.);
#14706=ORIENTED_EDGE('',*,*,#10334,.F.);
#14707=ORIENTED_EDGE('',*,*,#10335,.T.);
#14708=ORIENTED_EDGE('',*,*,#10331,.T.);
#14709=ORIENTED_EDGE('',*,*,#10336,.T.);
#14710=ORIENTED_EDGE('',*,*,#10337,.F.);
#14711=ORIENTED_EDGE('',*,*,#10338,.T.);
#14712=ORIENTED_EDGE('',*,*,#10334,.T.);
#14713=ORIENTED_EDGE('',*,*,#10339,.T.);
#14714=ORIENTED_EDGE('',*,*,#10340,.F.);
#14715=ORIENTED_EDGE('',*,*,#10341,.T.);
#14716=ORIENTED_EDGE('',*,*,#10337,.T.);
#14717=ORIENTED_EDGE('',*,*,#10342,.T.);
#14718=ORIENTED_EDGE('',*,*,#10343,.F.);
#14719=ORIENTED_EDGE('',*,*,#10344,.T.);
#14720=ORIENTED_EDGE('',*,*,#10340,.T.);
#14721=ORIENTED_EDGE('',*,*,#10345,.T.);
#14722=ORIENTED_EDGE('',*,*,#10346,.F.);
#14723=ORIENTED_EDGE('',*,*,#10347,.T.);
#14724=ORIENTED_EDGE('',*,*,#10343,.T.);
#14725=ORIENTED_EDGE('',*,*,#10348,.T.);
#14726=ORIENTED_EDGE('',*,*,#10349,.F.);
#14727=ORIENTED_EDGE('',*,*,#10350,.T.);
#14728=ORIENTED_EDGE('',*,*,#10346,.T.);
#14729=ORIENTED_EDGE('',*,*,#10351,.T.);
#14730=ORIENTED_EDGE('',*,*,#10352,.F.);
#14731=ORIENTED_EDGE('',*,*,#10353,.T.);
#14732=ORIENTED_EDGE('',*,*,#10349,.T.);
#14733=ORIENTED_EDGE('',*,*,#10354,.T.);
#14734=ORIENTED_EDGE('',*,*,#10355,.F.);
#14735=ORIENTED_EDGE('',*,*,#10356,.T.);
#14736=ORIENTED_EDGE('',*,*,#10352,.T.);
#14737=ORIENTED_EDGE('',*,*,#10357,.T.);
#14738=ORIENTED_EDGE('',*,*,#10358,.F.);
#14739=ORIENTED_EDGE('',*,*,#10359,.T.);
#14740=ORIENTED_EDGE('',*,*,#10355,.T.);
#14741=ORIENTED_EDGE('',*,*,#10360,.T.);
#14742=ORIENTED_EDGE('',*,*,#10361,.F.);
#14743=ORIENTED_EDGE('',*,*,#10362,.T.);
#14744=ORIENTED_EDGE('',*,*,#10358,.T.);
#14745=ORIENTED_EDGE('',*,*,#10363,.T.);
#14746=ORIENTED_EDGE('',*,*,#10364,.F.);
#14747=ORIENTED_EDGE('',*,*,#10365,.T.);
#14748=ORIENTED_EDGE('',*,*,#10361,.T.);
#14749=ORIENTED_EDGE('',*,*,#10366,.T.);
#14750=ORIENTED_EDGE('',*,*,#10367,.F.);
#14751=ORIENTED_EDGE('',*,*,#10368,.T.);
#14752=ORIENTED_EDGE('',*,*,#10364,.T.);
#14753=ORIENTED_EDGE('',*,*,#10369,.T.);
#14754=ORIENTED_EDGE('',*,*,#10370,.F.);
#14755=ORIENTED_EDGE('',*,*,#10371,.T.);
#14756=ORIENTED_EDGE('',*,*,#10367,.T.);
#14757=ORIENTED_EDGE('',*,*,#10372,.T.);
#14758=ORIENTED_EDGE('',*,*,#10373,.F.);
#14759=ORIENTED_EDGE('',*,*,#10374,.T.);
#14760=ORIENTED_EDGE('',*,*,#10370,.T.);
#14761=ORIENTED_EDGE('',*,*,#10375,.T.);
#14762=ORIENTED_EDGE('',*,*,#10376,.F.);
#14763=ORIENTED_EDGE('',*,*,#10377,.T.);
#14764=ORIENTED_EDGE('',*,*,#10373,.T.);
#14765=ORIENTED_EDGE('',*,*,#10378,.T.);
#14766=ORIENTED_EDGE('',*,*,#10379,.F.);
#14767=ORIENTED_EDGE('',*,*,#10380,.T.);
#14768=ORIENTED_EDGE('',*,*,#10381,.F.);
#14769=ORIENTED_EDGE('',*,*,#10382,.F.);
#14770=ORIENTED_EDGE('',*,*,#10383,.T.);
#14771=ORIENTED_EDGE('',*,*,#10379,.T.);
#14772=ORIENTED_EDGE('',*,*,#10384,.F.);
#14773=ORIENTED_EDGE('',*,*,#10385,.F.);
#14774=ORIENTED_EDGE('',*,*,#10386,.F.);
#14775=ORIENTED_EDGE('',*,*,#10387,.T.);
#14776=ORIENTED_EDGE('',*,*,#10382,.T.);
#14777=ORIENTED_EDGE('',*,*,#10388,.F.);
#14778=ORIENTED_EDGE('',*,*,#10389,.F.);
#14779=ORIENTED_EDGE('',*,*,#10390,.T.);
#14780=ORIENTED_EDGE('',*,*,#10386,.T.);
#14781=ORIENTED_EDGE('',*,*,#10391,.F.);
#14782=ORIENTED_EDGE('',*,*,#10392,.F.);
#14783=ORIENTED_EDGE('',*,*,#10393,.T.);
#14784=ORIENTED_EDGE('',*,*,#10389,.T.);
#14785=ORIENTED_EDGE('',*,*,#10394,.F.);
#14786=ORIENTED_EDGE('',*,*,#10395,.F.);
#14787=ORIENTED_EDGE('',*,*,#10396,.T.);
#14788=ORIENTED_EDGE('',*,*,#10392,.T.);
#14789=ORIENTED_EDGE('',*,*,#10397,.F.);
#14790=ORIENTED_EDGE('',*,*,#10398,.F.);
#14791=ORIENTED_EDGE('',*,*,#10399,.T.);
#14792=ORIENTED_EDGE('',*,*,#10395,.T.);
#14793=ORIENTED_EDGE('',*,*,#10400,.F.);
#14794=ORIENTED_EDGE('',*,*,#10401,.F.);
#14795=ORIENTED_EDGE('',*,*,#10402,.T.);
#14796=ORIENTED_EDGE('',*,*,#10398,.T.);
#14797=ORIENTED_EDGE('',*,*,#10403,.F.);
#14798=ORIENTED_EDGE('',*,*,#10404,.F.);
#14799=ORIENTED_EDGE('',*,*,#10405,.T.);
#14800=ORIENTED_EDGE('',*,*,#10401,.T.);
#14801=ORIENTED_EDGE('',*,*,#10406,.F.);
#14802=ORIENTED_EDGE('',*,*,#10407,.F.);
#14803=ORIENTED_EDGE('',*,*,#10408,.T.);
#14804=ORIENTED_EDGE('',*,*,#10404,.T.);
#14805=ORIENTED_EDGE('',*,*,#10409,.F.);
#14806=ORIENTED_EDGE('',*,*,#10410,.F.);
#14807=ORIENTED_EDGE('',*,*,#10411,.T.);
#14808=ORIENTED_EDGE('',*,*,#10407,.T.);
#14809=ORIENTED_EDGE('',*,*,#10412,.F.);
#14810=ORIENTED_EDGE('',*,*,#10413,.F.);
#14811=ORIENTED_EDGE('',*,*,#10414,.T.);
#14812=ORIENTED_EDGE('',*,*,#10410,.T.);
#14813=ORIENTED_EDGE('',*,*,#10415,.F.);
#14814=ORIENTED_EDGE('',*,*,#10416,.F.);
#14815=ORIENTED_EDGE('',*,*,#10417,.T.);
#14816=ORIENTED_EDGE('',*,*,#10413,.T.);
#14817=ORIENTED_EDGE('',*,*,#10418,.F.);
#14818=ORIENTED_EDGE('',*,*,#10419,.F.);
#14819=ORIENTED_EDGE('',*,*,#10420,.T.);
#14820=ORIENTED_EDGE('',*,*,#10416,.T.);
#14821=ORIENTED_EDGE('',*,*,#10421,.F.);
#14822=ORIENTED_EDGE('',*,*,#10422,.F.);
#14823=ORIENTED_EDGE('',*,*,#10423,.T.);
#14824=ORIENTED_EDGE('',*,*,#10419,.T.);
#14825=ORIENTED_EDGE('',*,*,#10424,.F.);
#14826=ORIENTED_EDGE('',*,*,#10425,.F.);
#14827=ORIENTED_EDGE('',*,*,#10426,.T.);
#14828=ORIENTED_EDGE('',*,*,#10422,.T.);
#14829=ORIENTED_EDGE('',*,*,#10427,.F.);
#14830=ORIENTED_EDGE('',*,*,#10428,.F.);
#14831=ORIENTED_EDGE('',*,*,#10429,.T.);
#14832=ORIENTED_EDGE('',*,*,#10425,.T.);
#14833=ORIENTED_EDGE('',*,*,#10430,.F.);
#14834=ORIENTED_EDGE('',*,*,#10431,.F.);
#14835=ORIENTED_EDGE('',*,*,#10432,.T.);
#14836=ORIENTED_EDGE('',*,*,#10428,.T.);
#14837=ORIENTED_EDGE('',*,*,#10433,.F.);
#14838=ORIENTED_EDGE('',*,*,#10434,.F.);
#14839=ORIENTED_EDGE('',*,*,#10435,.T.);
#14840=ORIENTED_EDGE('',*,*,#10431,.T.);
#14841=ORIENTED_EDGE('',*,*,#10436,.F.);
#14842=ORIENTED_EDGE('',*,*,#10437,.F.);
#14843=ORIENTED_EDGE('',*,*,#10438,.T.);
#14844=ORIENTED_EDGE('',*,*,#10434,.T.);
#14845=ORIENTED_EDGE('',*,*,#10439,.F.);
#14846=ORIENTED_EDGE('',*,*,#10440,.F.);
#14847=ORIENTED_EDGE('',*,*,#10441,.T.);
#14848=ORIENTED_EDGE('',*,*,#10437,.T.);
#14849=ORIENTED_EDGE('',*,*,#10442,.F.);
#14850=ORIENTED_EDGE('',*,*,#10443,.F.);
#14851=ORIENTED_EDGE('',*,*,#10444,.T.);
#14852=ORIENTED_EDGE('',*,*,#10440,.T.);
#14853=ORIENTED_EDGE('',*,*,#10445,.F.);
#14854=ORIENTED_EDGE('',*,*,#10446,.F.);
#14855=ORIENTED_EDGE('',*,*,#10447,.T.);
#14856=ORIENTED_EDGE('',*,*,#10443,.T.);
#14857=ORIENTED_EDGE('',*,*,#10448,.F.);
#14858=ORIENTED_EDGE('',*,*,#10449,.F.);
#14859=ORIENTED_EDGE('',*,*,#10450,.T.);
#14860=ORIENTED_EDGE('',*,*,#10446,.T.);
#14861=ORIENTED_EDGE('',*,*,#10451,.F.);
#14862=ORIENTED_EDGE('',*,*,#10452,.F.);
#14863=ORIENTED_EDGE('',*,*,#10453,.T.);
#14864=ORIENTED_EDGE('',*,*,#10449,.T.);
#14865=ORIENTED_EDGE('',*,*,#10454,.F.);
#14866=ORIENTED_EDGE('',*,*,#10455,.F.);
#14867=ORIENTED_EDGE('',*,*,#10456,.T.);
#14868=ORIENTED_EDGE('',*,*,#10452,.T.);
#14869=ORIENTED_EDGE('',*,*,#10457,.F.);
#14870=ORIENTED_EDGE('',*,*,#10458,.F.);
#14871=ORIENTED_EDGE('',*,*,#10459,.T.);
#14872=ORIENTED_EDGE('',*,*,#10455,.T.);
#14873=ORIENTED_EDGE('',*,*,#10460,.F.);
#14874=ORIENTED_EDGE('',*,*,#10461,.F.);
#14875=ORIENTED_EDGE('',*,*,#10462,.T.);
#14876=ORIENTED_EDGE('',*,*,#10458,.T.);
#14877=ORIENTED_EDGE('',*,*,#10463,.F.);
#14878=ORIENTED_EDGE('',*,*,#10464,.F.);
#14879=ORIENTED_EDGE('',*,*,#10465,.T.);
#14880=ORIENTED_EDGE('',*,*,#10461,.T.);
#14881=ORIENTED_EDGE('',*,*,#10466,.F.);
#14882=ORIENTED_EDGE('',*,*,#10467,.F.);
#14883=ORIENTED_EDGE('',*,*,#10468,.T.);
#14884=ORIENTED_EDGE('',*,*,#10464,.T.);
#14885=ORIENTED_EDGE('',*,*,#10469,.F.);
#14886=ORIENTED_EDGE('',*,*,#10470,.F.);
#14887=ORIENTED_EDGE('',*,*,#10471,.T.);
#14888=ORIENTED_EDGE('',*,*,#10467,.T.);
#14889=ORIENTED_EDGE('',*,*,#10472,.F.);
#14890=ORIENTED_EDGE('',*,*,#10473,.F.);
#14891=ORIENTED_EDGE('',*,*,#10474,.T.);
#14892=ORIENTED_EDGE('',*,*,#10470,.T.);
#14893=ORIENTED_EDGE('',*,*,#10475,.F.);
#14894=ORIENTED_EDGE('',*,*,#10476,.F.);
#14895=ORIENTED_EDGE('',*,*,#10477,.T.);
#14896=ORIENTED_EDGE('',*,*,#10473,.T.);
#14897=ORIENTED_EDGE('',*,*,#10478,.F.);
#14898=ORIENTED_EDGE('',*,*,#10479,.F.);
#14899=ORIENTED_EDGE('',*,*,#10480,.T.);
#14900=ORIENTED_EDGE('',*,*,#10476,.T.);
#14901=ORIENTED_EDGE('',*,*,#10481,.F.);
#14902=ORIENTED_EDGE('',*,*,#10482,.F.);
#14903=ORIENTED_EDGE('',*,*,#10483,.T.);
#14904=ORIENTED_EDGE('',*,*,#10479,.T.);
#14905=ORIENTED_EDGE('',*,*,#10484,.F.);
#14906=ORIENTED_EDGE('',*,*,#10485,.F.);
#14907=ORIENTED_EDGE('',*,*,#10486,.T.);
#14908=ORIENTED_EDGE('',*,*,#10482,.T.);
#14909=ORIENTED_EDGE('',*,*,#10487,.F.);
#14910=ORIENTED_EDGE('',*,*,#10488,.F.);
#14911=ORIENTED_EDGE('',*,*,#10489,.T.);
#14912=ORIENTED_EDGE('',*,*,#10485,.T.);
#14913=ORIENTED_EDGE('',*,*,#10490,.F.);
#14914=ORIENTED_EDGE('',*,*,#10491,.F.);
#14915=ORIENTED_EDGE('',*,*,#10492,.T.);
#14916=ORIENTED_EDGE('',*,*,#10488,.T.);
#14917=ORIENTED_EDGE('',*,*,#10493,.F.);
#14918=ORIENTED_EDGE('',*,*,#10494,.F.);
#14919=ORIENTED_EDGE('',*,*,#10495,.T.);
#14920=ORIENTED_EDGE('',*,*,#10491,.T.);
#14921=ORIENTED_EDGE('',*,*,#10496,.F.);
#14922=ORIENTED_EDGE('',*,*,#10497,.F.);
#14923=ORIENTED_EDGE('',*,*,#10498,.T.);
#14924=ORIENTED_EDGE('',*,*,#10494,.T.);
#14925=ORIENTED_EDGE('',*,*,#10499,.F.);
#14926=ORIENTED_EDGE('',*,*,#10500,.F.);
#14927=ORIENTED_EDGE('',*,*,#10501,.T.);
#14928=ORIENTED_EDGE('',*,*,#10497,.T.);
#14929=ORIENTED_EDGE('',*,*,#10502,.F.);
#14930=ORIENTED_EDGE('',*,*,#10503,.F.);
#14931=ORIENTED_EDGE('',*,*,#10504,.T.);
#14932=ORIENTED_EDGE('',*,*,#10500,.T.);
#14933=ORIENTED_EDGE('',*,*,#10505,.F.);
#14934=ORIENTED_EDGE('',*,*,#10506,.F.);
#14935=ORIENTED_EDGE('',*,*,#10507,.T.);
#14936=ORIENTED_EDGE('',*,*,#10503,.T.);
#14937=ORIENTED_EDGE('',*,*,#10508,.F.);
#14938=ORIENTED_EDGE('',*,*,#10509,.F.);
#14939=ORIENTED_EDGE('',*,*,#10510,.T.);
#14940=ORIENTED_EDGE('',*,*,#10506,.T.);
#14941=ORIENTED_EDGE('',*,*,#10511,.F.);
#14942=ORIENTED_EDGE('',*,*,#10512,.F.);
#14943=ORIENTED_EDGE('',*,*,#10513,.T.);
#14944=ORIENTED_EDGE('',*,*,#10509,.T.);
#14945=ORIENTED_EDGE('',*,*,#10514,.F.);
#14946=ORIENTED_EDGE('',*,*,#10515,.F.);
#14947=ORIENTED_EDGE('',*,*,#10516,.T.);
#14948=ORIENTED_EDGE('',*,*,#10512,.T.);
#14949=ORIENTED_EDGE('',*,*,#10517,.F.);
#14950=ORIENTED_EDGE('',*,*,#10518,.F.);
#14951=ORIENTED_EDGE('',*,*,#10519,.T.);
#14952=ORIENTED_EDGE('',*,*,#10515,.T.);
#14953=ORIENTED_EDGE('',*,*,#10520,.F.);
#14954=ORIENTED_EDGE('',*,*,#10521,.F.);
#14955=ORIENTED_EDGE('',*,*,#10522,.T.);
#14956=ORIENTED_EDGE('',*,*,#10518,.T.);
#14957=ORIENTED_EDGE('',*,*,#10523,.F.);
#14958=ORIENTED_EDGE('',*,*,#10524,.F.);
#14959=ORIENTED_EDGE('',*,*,#10525,.T.);
#14960=ORIENTED_EDGE('',*,*,#10521,.T.);
#14961=ORIENTED_EDGE('',*,*,#10526,.F.);
#14962=ORIENTED_EDGE('',*,*,#10527,.F.);
#14963=ORIENTED_EDGE('',*,*,#10528,.T.);
#14964=ORIENTED_EDGE('',*,*,#10524,.T.);
#14965=ORIENTED_EDGE('',*,*,#10529,.F.);
#14966=ORIENTED_EDGE('',*,*,#10530,.F.);
#14967=ORIENTED_EDGE('',*,*,#10531,.T.);
#14968=ORIENTED_EDGE('',*,*,#10527,.T.);
#14969=ORIENTED_EDGE('',*,*,#10532,.F.);
#14970=ORIENTED_EDGE('',*,*,#10533,.F.);
#14971=ORIENTED_EDGE('',*,*,#10534,.T.);
#14972=ORIENTED_EDGE('',*,*,#10530,.T.);
#14973=ORIENTED_EDGE('',*,*,#10535,.F.);
#14974=ORIENTED_EDGE('',*,*,#10536,.F.);
#14975=ORIENTED_EDGE('',*,*,#10537,.T.);
#14976=ORIENTED_EDGE('',*,*,#10533,.T.);
#14977=ORIENTED_EDGE('',*,*,#10538,.F.);
#14978=ORIENTED_EDGE('',*,*,#10539,.F.);
#14979=ORIENTED_EDGE('',*,*,#10540,.T.);
#14980=ORIENTED_EDGE('',*,*,#10536,.T.);
#14981=ORIENTED_EDGE('',*,*,#10541,.F.);
#14982=ORIENTED_EDGE('',*,*,#10542,.F.);
#14983=ORIENTED_EDGE('',*,*,#10543,.T.);
#14984=ORIENTED_EDGE('',*,*,#10539,.T.);
#14985=ORIENTED_EDGE('',*,*,#10544,.F.);
#14986=ORIENTED_EDGE('',*,*,#10545,.F.);
#14987=ORIENTED_EDGE('',*,*,#10546,.T.);
#14988=ORIENTED_EDGE('',*,*,#10542,.T.);
#14989=ORIENTED_EDGE('',*,*,#10547,.F.);
#14990=ORIENTED_EDGE('',*,*,#10548,.F.);
#14991=ORIENTED_EDGE('',*,*,#10549,.T.);
#14992=ORIENTED_EDGE('',*,*,#10545,.T.);
#14993=ORIENTED_EDGE('',*,*,#10550,.F.);
#14994=ORIENTED_EDGE('',*,*,#10551,.F.);
#14995=ORIENTED_EDGE('',*,*,#10552,.T.);
#14996=ORIENTED_EDGE('',*,*,#10548,.T.);
#14997=ORIENTED_EDGE('',*,*,#10553,.F.);
#14998=ORIENTED_EDGE('',*,*,#10554,.F.);
#14999=ORIENTED_EDGE('',*,*,#10555,.T.);
#15000=ORIENTED_EDGE('',*,*,#10551,.T.);
#15001=ORIENTED_EDGE('',*,*,#10556,.F.);
#15002=ORIENTED_EDGE('',*,*,#10557,.F.);
#15003=ORIENTED_EDGE('',*,*,#10558,.T.);
#15004=ORIENTED_EDGE('',*,*,#10554,.T.);
#15005=ORIENTED_EDGE('',*,*,#10559,.F.);
#15006=ORIENTED_EDGE('',*,*,#10560,.F.);
#15007=ORIENTED_EDGE('',*,*,#10561,.T.);
#15008=ORIENTED_EDGE('',*,*,#10557,.T.);
#15009=ORIENTED_EDGE('',*,*,#10562,.F.);
#15010=ORIENTED_EDGE('',*,*,#10563,.F.);
#15011=ORIENTED_EDGE('',*,*,#10564,.T.);
#15012=ORIENTED_EDGE('',*,*,#10560,.T.);
#15013=ORIENTED_EDGE('',*,*,#10565,.F.);
#15014=ORIENTED_EDGE('',*,*,#10566,.F.);
#15015=ORIENTED_EDGE('',*,*,#10567,.T.);
#15016=ORIENTED_EDGE('',*,*,#10563,.T.);
#15017=ORIENTED_EDGE('',*,*,#10568,.F.);
#15018=ORIENTED_EDGE('',*,*,#10569,.F.);
#15019=ORIENTED_EDGE('',*,*,#10570,.T.);
#15020=ORIENTED_EDGE('',*,*,#10566,.T.);
#15021=ORIENTED_EDGE('',*,*,#10571,.F.);
#15022=ORIENTED_EDGE('',*,*,#10572,.F.);
#15023=ORIENTED_EDGE('',*,*,#10573,.T.);
#15024=ORIENTED_EDGE('',*,*,#10569,.T.);
#15025=ORIENTED_EDGE('',*,*,#10574,.F.);
#15026=ORIENTED_EDGE('',*,*,#10575,.F.);
#15027=ORIENTED_EDGE('',*,*,#10576,.T.);
#15028=ORIENTED_EDGE('',*,*,#10572,.T.);
#15029=ORIENTED_EDGE('',*,*,#10577,.F.);
#15030=ORIENTED_EDGE('',*,*,#10578,.F.);
#15031=ORIENTED_EDGE('',*,*,#10579,.T.);
#15032=ORIENTED_EDGE('',*,*,#10575,.T.);
#15033=ORIENTED_EDGE('',*,*,#10580,.F.);
#15034=ORIENTED_EDGE('',*,*,#10581,.F.);
#15035=ORIENTED_EDGE('',*,*,#10582,.T.);
#15036=ORIENTED_EDGE('',*,*,#10578,.T.);
#15037=ORIENTED_EDGE('',*,*,#10583,.F.);
#15038=ORIENTED_EDGE('',*,*,#10584,.F.);
#15039=ORIENTED_EDGE('',*,*,#10585,.T.);
#15040=ORIENTED_EDGE('',*,*,#10581,.T.);
#15041=ORIENTED_EDGE('',*,*,#10586,.F.);
#15042=ORIENTED_EDGE('',*,*,#10587,.F.);
#15043=ORIENTED_EDGE('',*,*,#10588,.T.);
#15044=ORIENTED_EDGE('',*,*,#10584,.T.);
#15045=ORIENTED_EDGE('',*,*,#10589,.F.);
#15046=ORIENTED_EDGE('',*,*,#10590,.F.);
#15047=ORIENTED_EDGE('',*,*,#10591,.T.);
#15048=ORIENTED_EDGE('',*,*,#10587,.T.);
#15049=ORIENTED_EDGE('',*,*,#10592,.F.);
#15050=ORIENTED_EDGE('',*,*,#10593,.F.);
#15051=ORIENTED_EDGE('',*,*,#10594,.T.);
#15052=ORIENTED_EDGE('',*,*,#10590,.T.);
#15053=ORIENTED_EDGE('',*,*,#10595,.F.);
#15054=ORIENTED_EDGE('',*,*,#10596,.F.);
#15055=ORIENTED_EDGE('',*,*,#10597,.T.);
#15056=ORIENTED_EDGE('',*,*,#10593,.T.);
#15057=ORIENTED_EDGE('',*,*,#10598,.F.);
#15058=ORIENTED_EDGE('',*,*,#10599,.F.);
#15059=ORIENTED_EDGE('',*,*,#10600,.T.);
#15060=ORIENTED_EDGE('',*,*,#10596,.T.);
#15061=ORIENTED_EDGE('',*,*,#10601,.F.);
#15062=ORIENTED_EDGE('',*,*,#10602,.F.);
#15063=ORIENTED_EDGE('',*,*,#10603,.T.);
#15064=ORIENTED_EDGE('',*,*,#10599,.T.);
#15065=ORIENTED_EDGE('',*,*,#10604,.F.);
#15066=ORIENTED_EDGE('',*,*,#10605,.F.);
#15067=ORIENTED_EDGE('',*,*,#10606,.T.);
#15068=ORIENTED_EDGE('',*,*,#10602,.T.);
#15069=ORIENTED_EDGE('',*,*,#10607,.F.);
#15070=ORIENTED_EDGE('',*,*,#10608,.F.);
#15071=ORIENTED_EDGE('',*,*,#10609,.T.);
#15072=ORIENTED_EDGE('',*,*,#10605,.T.);
#15073=ORIENTED_EDGE('',*,*,#10610,.F.);
#15074=ORIENTED_EDGE('',*,*,#10611,.F.);
#15075=ORIENTED_EDGE('',*,*,#10612,.T.);
#15076=ORIENTED_EDGE('',*,*,#10608,.T.);
#15077=ORIENTED_EDGE('',*,*,#10613,.F.);
#15078=ORIENTED_EDGE('',*,*,#10614,.F.);
#15079=ORIENTED_EDGE('',*,*,#10615,.T.);
#15080=ORIENTED_EDGE('',*,*,#10611,.T.);
#15081=ORIENTED_EDGE('',*,*,#10616,.F.);
#15082=ORIENTED_EDGE('',*,*,#10617,.F.);
#15083=ORIENTED_EDGE('',*,*,#10618,.T.);
#15084=ORIENTED_EDGE('',*,*,#10614,.T.);
#15085=ORIENTED_EDGE('',*,*,#10619,.F.);
#15086=ORIENTED_EDGE('',*,*,#10620,.F.);
#15087=ORIENTED_EDGE('',*,*,#10621,.T.);
#15088=ORIENTED_EDGE('',*,*,#10617,.T.);
#15089=ORIENTED_EDGE('',*,*,#10622,.F.);
#15090=ORIENTED_EDGE('',*,*,#10623,.F.);
#15091=ORIENTED_EDGE('',*,*,#10624,.T.);
#15092=ORIENTED_EDGE('',*,*,#10620,.T.);
#15093=ORIENTED_EDGE('',*,*,#10625,.F.);
#15094=ORIENTED_EDGE('',*,*,#10626,.F.);
#15095=ORIENTED_EDGE('',*,*,#10627,.T.);
#15096=ORIENTED_EDGE('',*,*,#10623,.T.);
#15097=ORIENTED_EDGE('',*,*,#10628,.F.);
#15098=ORIENTED_EDGE('',*,*,#10629,.F.);
#15099=ORIENTED_EDGE('',*,*,#10630,.T.);
#15100=ORIENTED_EDGE('',*,*,#10626,.T.);
#15101=ORIENTED_EDGE('',*,*,#10631,.F.);
#15102=ORIENTED_EDGE('',*,*,#10632,.F.);
#15103=ORIENTED_EDGE('',*,*,#10633,.T.);
#15104=ORIENTED_EDGE('',*,*,#10629,.T.);
#15105=ORIENTED_EDGE('',*,*,#10634,.F.);
#15106=ORIENTED_EDGE('',*,*,#10635,.F.);
#15107=ORIENTED_EDGE('',*,*,#10636,.T.);
#15108=ORIENTED_EDGE('',*,*,#10632,.T.);
#15109=ORIENTED_EDGE('',*,*,#10637,.F.);
#15110=ORIENTED_EDGE('',*,*,#10638,.F.);
#15111=ORIENTED_EDGE('',*,*,#10639,.T.);
#15112=ORIENTED_EDGE('',*,*,#10635,.T.);
#15113=ORIENTED_EDGE('',*,*,#10640,.F.);
#15114=ORIENTED_EDGE('',*,*,#10641,.F.);
#15115=ORIENTED_EDGE('',*,*,#10642,.T.);
#15116=ORIENTED_EDGE('',*,*,#10638,.T.);
#15117=ORIENTED_EDGE('',*,*,#10643,.F.);
#15118=ORIENTED_EDGE('',*,*,#10644,.F.);
#15119=ORIENTED_EDGE('',*,*,#10645,.F.);
#15120=ORIENTED_EDGE('',*,*,#10378,.F.);
#15121=ORIENTED_EDGE('',*,*,#10375,.F.);
#15122=ORIENTED_EDGE('',*,*,#10372,.F.);
#15123=ORIENTED_EDGE('',*,*,#10369,.F.);
#15124=ORIENTED_EDGE('',*,*,#10366,.F.);
#15125=ORIENTED_EDGE('',*,*,#10363,.F.);
#15126=ORIENTED_EDGE('',*,*,#10360,.F.);
#15127=ORIENTED_EDGE('',*,*,#10357,.F.);
#15128=ORIENTED_EDGE('',*,*,#10354,.F.);
#15129=ORIENTED_EDGE('',*,*,#10351,.F.);
#15130=ORIENTED_EDGE('',*,*,#10348,.F.);
#15131=ORIENTED_EDGE('',*,*,#10345,.F.);
#15132=ORIENTED_EDGE('',*,*,#10342,.F.);
#15133=ORIENTED_EDGE('',*,*,#10339,.F.);
#15134=ORIENTED_EDGE('',*,*,#10336,.F.);
#15135=ORIENTED_EDGE('',*,*,#10333,.F.);
#15136=ORIENTED_EDGE('',*,*,#10330,.F.);
#15137=ORIENTED_EDGE('',*,*,#10327,.F.);
#15138=ORIENTED_EDGE('',*,*,#10324,.F.);
#15139=ORIENTED_EDGE('',*,*,#10321,.F.);
#15140=ORIENTED_EDGE('',*,*,#10318,.F.);
#15141=ORIENTED_EDGE('',*,*,#10315,.F.);
#15142=ORIENTED_EDGE('',*,*,#10312,.F.);
#15143=ORIENTED_EDGE('',*,*,#10309,.F.);
#15144=ORIENTED_EDGE('',*,*,#10306,.F.);
#15145=ORIENTED_EDGE('',*,*,#10303,.F.);
#15146=ORIENTED_EDGE('',*,*,#10300,.F.);
#15147=ORIENTED_EDGE('',*,*,#10297,.F.);
#15148=ORIENTED_EDGE('',*,*,#10294,.F.);
#15149=ORIENTED_EDGE('',*,*,#10291,.F.);
#15150=ORIENTED_EDGE('',*,*,#10288,.F.);
#15151=ORIENTED_EDGE('',*,*,#10285,.F.);
#15152=ORIENTED_EDGE('',*,*,#10282,.F.);
#15153=ORIENTED_EDGE('',*,*,#10279,.F.);
#15154=ORIENTED_EDGE('',*,*,#10276,.F.);
#15155=ORIENTED_EDGE('',*,*,#10273,.F.);
#15156=ORIENTED_EDGE('',*,*,#10270,.F.);
#15157=ORIENTED_EDGE('',*,*,#10267,.F.);
#15158=ORIENTED_EDGE('',*,*,#10264,.F.);
#15159=ORIENTED_EDGE('',*,*,#10261,.F.);
#15160=ORIENTED_EDGE('',*,*,#10258,.F.);
#15161=ORIENTED_EDGE('',*,*,#10255,.F.);
#15162=ORIENTED_EDGE('',*,*,#10252,.F.);
#15163=ORIENTED_EDGE('',*,*,#10249,.F.);
#15164=ORIENTED_EDGE('',*,*,#10246,.F.);
#15165=ORIENTED_EDGE('',*,*,#10243,.F.);
#15166=ORIENTED_EDGE('',*,*,#10240,.F.);
#15167=ORIENTED_EDGE('',*,*,#10237,.F.);
#15168=ORIENTED_EDGE('',*,*,#10234,.F.);
#15169=ORIENTED_EDGE('',*,*,#10231,.F.);
#15170=ORIENTED_EDGE('',*,*,#10228,.F.);
#15171=ORIENTED_EDGE('',*,*,#10225,.F.);
#15172=ORIENTED_EDGE('',*,*,#10222,.F.);
#15173=ORIENTED_EDGE('',*,*,#10219,.F.);
#15174=ORIENTED_EDGE('',*,*,#10216,.F.);
#15175=ORIENTED_EDGE('',*,*,#10213,.F.);
#15176=ORIENTED_EDGE('',*,*,#10210,.F.);
#15177=ORIENTED_EDGE('',*,*,#10207,.F.);
#15178=ORIENTED_EDGE('',*,*,#10204,.F.);
#15179=ORIENTED_EDGE('',*,*,#10201,.F.);
#15180=ORIENTED_EDGE('',*,*,#10198,.F.);
#15181=ORIENTED_EDGE('',*,*,#10195,.F.);
#15182=ORIENTED_EDGE('',*,*,#10192,.F.);
#15183=ORIENTED_EDGE('',*,*,#10189,.F.);
#15184=ORIENTED_EDGE('',*,*,#10186,.F.);
#15185=ORIENTED_EDGE('',*,*,#10183,.F.);
#15186=ORIENTED_EDGE('',*,*,#10180,.F.);
#15187=ORIENTED_EDGE('',*,*,#10177,.F.);
#15188=ORIENTED_EDGE('',*,*,#10174,.F.);
#15189=ORIENTED_EDGE('',*,*,#10171,.F.);
#15190=ORIENTED_EDGE('',*,*,#10168,.F.);
#15191=ORIENTED_EDGE('',*,*,#10165,.F.);
#15192=ORIENTED_EDGE('',*,*,#10162,.F.);
#15193=ORIENTED_EDGE('',*,*,#10159,.F.);
#15194=ORIENTED_EDGE('',*,*,#10156,.F.);
#15195=ORIENTED_EDGE('',*,*,#10153,.F.);
#15196=ORIENTED_EDGE('',*,*,#10150,.F.);
#15197=ORIENTED_EDGE('',*,*,#10147,.F.);
#15198=ORIENTED_EDGE('',*,*,#10144,.F.);
#15199=ORIENTED_EDGE('',*,*,#10141,.F.);
#15200=ORIENTED_EDGE('',*,*,#10138,.F.);
#15201=ORIENTED_EDGE('',*,*,#10135,.F.);
#15202=ORIENTED_EDGE('',*,*,#10132,.F.);
#15203=ORIENTED_EDGE('',*,*,#10129,.F.);
#15204=ORIENTED_EDGE('',*,*,#10126,.F.);
#15205=ORIENTED_EDGE('',*,*,#10123,.F.);
#15206=ORIENTED_EDGE('',*,*,#10120,.F.);
#15207=ORIENTED_EDGE('',*,*,#10117,.F.);
#15208=ORIENTED_EDGE('',*,*,#10646,.F.);
#15209=ORIENTED_EDGE('',*,*,#10647,.T.);
#15210=ORIENTED_EDGE('',*,*,#10643,.T.);
#15211=ORIENTED_EDGE('',*,*,#10640,.T.);
#15212=ORIENTED_EDGE('',*,*,#10637,.T.);
#15213=ORIENTED_EDGE('',*,*,#10634,.T.);
#15214=ORIENTED_EDGE('',*,*,#10631,.T.);
#15215=ORIENTED_EDGE('',*,*,#10628,.T.);
#15216=ORIENTED_EDGE('',*,*,#10625,.T.);
#15217=ORIENTED_EDGE('',*,*,#10622,.T.);
#15218=ORIENTED_EDGE('',*,*,#10619,.T.);
#15219=ORIENTED_EDGE('',*,*,#10616,.T.);
#15220=ORIENTED_EDGE('',*,*,#10613,.T.);
#15221=ORIENTED_EDGE('',*,*,#10610,.T.);
#15222=ORIENTED_EDGE('',*,*,#10607,.T.);
#15223=ORIENTED_EDGE('',*,*,#10604,.T.);
#15224=ORIENTED_EDGE('',*,*,#10601,.T.);
#15225=ORIENTED_EDGE('',*,*,#10598,.T.);
#15226=ORIENTED_EDGE('',*,*,#10595,.T.);
#15227=ORIENTED_EDGE('',*,*,#10592,.T.);
#15228=ORIENTED_EDGE('',*,*,#10589,.T.);
#15229=ORIENTED_EDGE('',*,*,#10586,.T.);
#15230=ORIENTED_EDGE('',*,*,#10583,.T.);
#15231=ORIENTED_EDGE('',*,*,#10580,.T.);
#15232=ORIENTED_EDGE('',*,*,#10577,.T.);
#15233=ORIENTED_EDGE('',*,*,#10574,.T.);
#15234=ORIENTED_EDGE('',*,*,#10571,.T.);
#15235=ORIENTED_EDGE('',*,*,#10568,.T.);
#15236=ORIENTED_EDGE('',*,*,#10565,.T.);
#15237=ORIENTED_EDGE('',*,*,#10562,.T.);
#15238=ORIENTED_EDGE('',*,*,#10559,.T.);
#15239=ORIENTED_EDGE('',*,*,#10556,.T.);
#15240=ORIENTED_EDGE('',*,*,#10553,.T.);
#15241=ORIENTED_EDGE('',*,*,#10550,.T.);
#15242=ORIENTED_EDGE('',*,*,#10547,.T.);
#15243=ORIENTED_EDGE('',*,*,#10544,.T.);
#15244=ORIENTED_EDGE('',*,*,#10541,.T.);
#15245=ORIENTED_EDGE('',*,*,#10538,.T.);
#15246=ORIENTED_EDGE('',*,*,#10535,.T.);
#15247=ORIENTED_EDGE('',*,*,#10532,.T.);
#15248=ORIENTED_EDGE('',*,*,#10529,.T.);
#15249=ORIENTED_EDGE('',*,*,#10526,.T.);
#15250=ORIENTED_EDGE('',*,*,#10523,.T.);
#15251=ORIENTED_EDGE('',*,*,#10520,.T.);
#15252=ORIENTED_EDGE('',*,*,#10517,.T.);
#15253=ORIENTED_EDGE('',*,*,#10514,.T.);
#15254=ORIENTED_EDGE('',*,*,#10511,.T.);
#15255=ORIENTED_EDGE('',*,*,#10508,.T.);
#15256=ORIENTED_EDGE('',*,*,#10505,.T.);
#15257=ORIENTED_EDGE('',*,*,#10502,.T.);
#15258=ORIENTED_EDGE('',*,*,#10499,.T.);
#15259=ORIENTED_EDGE('',*,*,#10496,.T.);
#15260=ORIENTED_EDGE('',*,*,#10493,.T.);
#15261=ORIENTED_EDGE('',*,*,#10490,.T.);
#15262=ORIENTED_EDGE('',*,*,#10487,.T.);
#15263=ORIENTED_EDGE('',*,*,#10484,.T.);
#15264=ORIENTED_EDGE('',*,*,#10481,.T.);
#15265=ORIENTED_EDGE('',*,*,#10478,.T.);
#15266=ORIENTED_EDGE('',*,*,#10475,.T.);
#15267=ORIENTED_EDGE('',*,*,#10472,.T.);
#15268=ORIENTED_EDGE('',*,*,#10469,.T.);
#15269=ORIENTED_EDGE('',*,*,#10466,.T.);
#15270=ORIENTED_EDGE('',*,*,#10463,.T.);
#15271=ORIENTED_EDGE('',*,*,#10460,.T.);
#15272=ORIENTED_EDGE('',*,*,#10457,.T.);
#15273=ORIENTED_EDGE('',*,*,#10454,.T.);
#15274=ORIENTED_EDGE('',*,*,#10451,.T.);
#15275=ORIENTED_EDGE('',*,*,#10448,.T.);
#15276=ORIENTED_EDGE('',*,*,#10445,.T.);
#15277=ORIENTED_EDGE('',*,*,#10442,.T.);
#15278=ORIENTED_EDGE('',*,*,#10439,.T.);
#15279=ORIENTED_EDGE('',*,*,#10436,.T.);
#15280=ORIENTED_EDGE('',*,*,#10433,.T.);
#15281=ORIENTED_EDGE('',*,*,#10430,.T.);
#15282=ORIENTED_EDGE('',*,*,#10427,.T.);
#15283=ORIENTED_EDGE('',*,*,#10424,.T.);
#15284=ORIENTED_EDGE('',*,*,#10421,.T.);
#15285=ORIENTED_EDGE('',*,*,#10418,.T.);
#15286=ORIENTED_EDGE('',*,*,#10415,.T.);
#15287=ORIENTED_EDGE('',*,*,#10412,.T.);
#15288=ORIENTED_EDGE('',*,*,#10409,.T.);
#15289=ORIENTED_EDGE('',*,*,#10406,.T.);
#15290=ORIENTED_EDGE('',*,*,#10403,.T.);
#15291=ORIENTED_EDGE('',*,*,#10400,.T.);
#15292=ORIENTED_EDGE('',*,*,#10397,.T.);
#15293=ORIENTED_EDGE('',*,*,#10394,.T.);
#15294=ORIENTED_EDGE('',*,*,#10391,.T.);
#15295=ORIENTED_EDGE('',*,*,#10388,.T.);
#15296=ORIENTED_EDGE('',*,*,#10385,.T.);
#15297=ORIENTED_EDGE('',*,*,#10648,.T.);
#15298=ORIENTED_EDGE('',*,*,#10649,.T.);
#15299=ORIENTED_EDGE('',*,*,#10650,.T.);
#15300=ORIENTED_EDGE('',*,*,#10651,.T.);
#15301=ORIENTED_EDGE('',*,*,#10646,.T.);
#15302=ORIENTED_EDGE('',*,*,#10641,.T.);
#15303=ORIENTED_EDGE('',*,*,#10647,.F.);
#15304=ORIENTED_EDGE('',*,*,#10651,.F.);
#15305=ORIENTED_EDGE('',*,*,#10652,.T.);
#15306=ORIENTED_EDGE('',*,*,#10653,.F.);
#15307=ORIENTED_EDGE('',*,*,#10380,.F.);
#15308=ORIENTED_EDGE('',*,*,#10383,.F.);
#15309=ORIENTED_EDGE('',*,*,#10387,.F.);
#15310=ORIENTED_EDGE('',*,*,#10390,.F.);
#15311=ORIENTED_EDGE('',*,*,#10393,.F.);
#15312=ORIENTED_EDGE('',*,*,#10396,.F.);
#15313=ORIENTED_EDGE('',*,*,#10399,.F.);
#15314=ORIENTED_EDGE('',*,*,#10402,.F.);
#15315=ORIENTED_EDGE('',*,*,#10405,.F.);
#15316=ORIENTED_EDGE('',*,*,#10408,.F.);
#15317=ORIENTED_EDGE('',*,*,#10411,.F.);
#15318=ORIENTED_EDGE('',*,*,#10414,.F.);
#15319=ORIENTED_EDGE('',*,*,#10417,.F.);
#15320=ORIENTED_EDGE('',*,*,#10420,.F.);
#15321=ORIENTED_EDGE('',*,*,#10423,.F.);
#15322=ORIENTED_EDGE('',*,*,#10426,.F.);
#15323=ORIENTED_EDGE('',*,*,#10429,.F.);
#15324=ORIENTED_EDGE('',*,*,#10432,.F.);
#15325=ORIENTED_EDGE('',*,*,#10435,.F.);
#15326=ORIENTED_EDGE('',*,*,#10438,.F.);
#15327=ORIENTED_EDGE('',*,*,#10441,.F.);
#15328=ORIENTED_EDGE('',*,*,#10444,.F.);
#15329=ORIENTED_EDGE('',*,*,#10447,.F.);
#15330=ORIENTED_EDGE('',*,*,#10450,.F.);
#15331=ORIENTED_EDGE('',*,*,#10453,.F.);
#15332=ORIENTED_EDGE('',*,*,#10456,.F.);
#15333=ORIENTED_EDGE('',*,*,#10459,.F.);
#15334=ORIENTED_EDGE('',*,*,#10462,.F.);
#15335=ORIENTED_EDGE('',*,*,#10465,.F.);
#15336=ORIENTED_EDGE('',*,*,#10468,.F.);
#15337=ORIENTED_EDGE('',*,*,#10471,.F.);
#15338=ORIENTED_EDGE('',*,*,#10474,.F.);
#15339=ORIENTED_EDGE('',*,*,#10477,.F.);
#15340=ORIENTED_EDGE('',*,*,#10480,.F.);
#15341=ORIENTED_EDGE('',*,*,#10483,.F.);
#15342=ORIENTED_EDGE('',*,*,#10486,.F.);
#15343=ORIENTED_EDGE('',*,*,#10489,.F.);
#15344=ORIENTED_EDGE('',*,*,#10492,.F.);
#15345=ORIENTED_EDGE('',*,*,#10495,.F.);
#15346=ORIENTED_EDGE('',*,*,#10498,.F.);
#15347=ORIENTED_EDGE('',*,*,#10501,.F.);
#15348=ORIENTED_EDGE('',*,*,#10504,.F.);
#15349=ORIENTED_EDGE('',*,*,#10507,.F.);
#15350=ORIENTED_EDGE('',*,*,#10510,.F.);
#15351=ORIENTED_EDGE('',*,*,#10513,.F.);
#15352=ORIENTED_EDGE('',*,*,#10516,.F.);
#15353=ORIENTED_EDGE('',*,*,#10519,.F.);
#15354=ORIENTED_EDGE('',*,*,#10522,.F.);
#15355=ORIENTED_EDGE('',*,*,#10525,.F.);
#15356=ORIENTED_EDGE('',*,*,#10528,.F.);
#15357=ORIENTED_EDGE('',*,*,#10531,.F.);
#15358=ORIENTED_EDGE('',*,*,#10534,.F.);
#15359=ORIENTED_EDGE('',*,*,#10537,.F.);
#15360=ORIENTED_EDGE('',*,*,#10540,.F.);
#15361=ORIENTED_EDGE('',*,*,#10543,.F.);
#15362=ORIENTED_EDGE('',*,*,#10546,.F.);
#15363=ORIENTED_EDGE('',*,*,#10549,.F.);
#15364=ORIENTED_EDGE('',*,*,#10552,.F.);
#15365=ORIENTED_EDGE('',*,*,#10555,.F.);
#15366=ORIENTED_EDGE('',*,*,#10558,.F.);
#15367=ORIENTED_EDGE('',*,*,#10561,.F.);
#15368=ORIENTED_EDGE('',*,*,#10564,.F.);
#15369=ORIENTED_EDGE('',*,*,#10567,.F.);
#15370=ORIENTED_EDGE('',*,*,#10570,.F.);
#15371=ORIENTED_EDGE('',*,*,#10573,.F.);
#15372=ORIENTED_EDGE('',*,*,#10576,.F.);
#15373=ORIENTED_EDGE('',*,*,#10579,.F.);
#15374=ORIENTED_EDGE('',*,*,#10582,.F.);
#15375=ORIENTED_EDGE('',*,*,#10585,.F.);
#15376=ORIENTED_EDGE('',*,*,#10588,.F.);
#15377=ORIENTED_EDGE('',*,*,#10591,.F.);
#15378=ORIENTED_EDGE('',*,*,#10594,.F.);
#15379=ORIENTED_EDGE('',*,*,#10597,.F.);
#15380=ORIENTED_EDGE('',*,*,#10600,.F.);
#15381=ORIENTED_EDGE('',*,*,#10603,.F.);
#15382=ORIENTED_EDGE('',*,*,#10606,.F.);
#15383=ORIENTED_EDGE('',*,*,#10609,.F.);
#15384=ORIENTED_EDGE('',*,*,#10612,.F.);
#15385=ORIENTED_EDGE('',*,*,#10615,.F.);
#15386=ORIENTED_EDGE('',*,*,#10618,.F.);
#15387=ORIENTED_EDGE('',*,*,#10621,.F.);
#15388=ORIENTED_EDGE('',*,*,#10624,.F.);
#15389=ORIENTED_EDGE('',*,*,#10627,.F.);
#15390=ORIENTED_EDGE('',*,*,#10630,.F.);
#15391=ORIENTED_EDGE('',*,*,#10633,.F.);
#15392=ORIENTED_EDGE('',*,*,#10636,.F.);
#15393=ORIENTED_EDGE('',*,*,#10639,.F.);
#15394=ORIENTED_EDGE('',*,*,#10642,.F.);
#15395=ORIENTED_EDGE('',*,*,#10652,.F.);
#15396=ORIENTED_EDGE('',*,*,#10650,.F.);
#15397=ORIENTED_EDGE('',*,*,#10115,.F.);
#15398=ORIENTED_EDGE('',*,*,#10119,.F.);
#15399=ORIENTED_EDGE('',*,*,#10122,.F.);
#15400=ORIENTED_EDGE('',*,*,#10125,.F.);
#15401=ORIENTED_EDGE('',*,*,#10128,.F.);
#15402=ORIENTED_EDGE('',*,*,#10131,.F.);
#15403=ORIENTED_EDGE('',*,*,#10134,.F.);
#15404=ORIENTED_EDGE('',*,*,#10137,.F.);
#15405=ORIENTED_EDGE('',*,*,#10140,.F.);
#15406=ORIENTED_EDGE('',*,*,#10143,.F.);
#15407=ORIENTED_EDGE('',*,*,#10146,.F.);
#15408=ORIENTED_EDGE('',*,*,#10149,.F.);
#15409=ORIENTED_EDGE('',*,*,#10152,.F.);
#15410=ORIENTED_EDGE('',*,*,#10155,.F.);
#15411=ORIENTED_EDGE('',*,*,#10158,.F.);
#15412=ORIENTED_EDGE('',*,*,#10161,.F.);
#15413=ORIENTED_EDGE('',*,*,#10164,.F.);
#15414=ORIENTED_EDGE('',*,*,#10167,.F.);
#15415=ORIENTED_EDGE('',*,*,#10170,.F.);
#15416=ORIENTED_EDGE('',*,*,#10173,.F.);
#15417=ORIENTED_EDGE('',*,*,#10176,.F.);
#15418=ORIENTED_EDGE('',*,*,#10179,.F.);
#15419=ORIENTED_EDGE('',*,*,#10182,.F.);
#15420=ORIENTED_EDGE('',*,*,#10185,.F.);
#15421=ORIENTED_EDGE('',*,*,#10188,.F.);
#15422=ORIENTED_EDGE('',*,*,#10191,.F.);
#15423=ORIENTED_EDGE('',*,*,#10194,.F.);
#15424=ORIENTED_EDGE('',*,*,#10197,.F.);
#15425=ORIENTED_EDGE('',*,*,#10200,.F.);
#15426=ORIENTED_EDGE('',*,*,#10203,.F.);
#15427=ORIENTED_EDGE('',*,*,#10206,.F.);
#15428=ORIENTED_EDGE('',*,*,#10209,.F.);
#15429=ORIENTED_EDGE('',*,*,#10212,.F.);
#15430=ORIENTED_EDGE('',*,*,#10215,.F.);
#15431=ORIENTED_EDGE('',*,*,#10218,.F.);
#15432=ORIENTED_EDGE('',*,*,#10221,.F.);
#15433=ORIENTED_EDGE('',*,*,#10224,.F.);
#15434=ORIENTED_EDGE('',*,*,#10227,.F.);
#15435=ORIENTED_EDGE('',*,*,#10230,.F.);
#15436=ORIENTED_EDGE('',*,*,#10233,.F.);
#15437=ORIENTED_EDGE('',*,*,#10236,.F.);
#15438=ORIENTED_EDGE('',*,*,#10239,.F.);
#15439=ORIENTED_EDGE('',*,*,#10242,.F.);
#15440=ORIENTED_EDGE('',*,*,#10245,.F.);
#15441=ORIENTED_EDGE('',*,*,#10248,.F.);
#15442=ORIENTED_EDGE('',*,*,#10251,.F.);
#15443=ORIENTED_EDGE('',*,*,#10254,.F.);
#15444=ORIENTED_EDGE('',*,*,#10257,.F.);
#15445=ORIENTED_EDGE('',*,*,#10260,.F.);
#15446=ORIENTED_EDGE('',*,*,#10263,.F.);
#15447=ORIENTED_EDGE('',*,*,#10266,.F.);
#15448=ORIENTED_EDGE('',*,*,#10269,.F.);
#15449=ORIENTED_EDGE('',*,*,#10272,.F.);
#15450=ORIENTED_EDGE('',*,*,#10275,.F.);
#15451=ORIENTED_EDGE('',*,*,#10278,.F.);
#15452=ORIENTED_EDGE('',*,*,#10281,.F.);
#15453=ORIENTED_EDGE('',*,*,#10284,.F.);
#15454=ORIENTED_EDGE('',*,*,#10287,.F.);
#15455=ORIENTED_EDGE('',*,*,#10290,.F.);
#15456=ORIENTED_EDGE('',*,*,#10293,.F.);
#15457=ORIENTED_EDGE('',*,*,#10296,.F.);
#15458=ORIENTED_EDGE('',*,*,#10299,.F.);
#15459=ORIENTED_EDGE('',*,*,#10302,.F.);
#15460=ORIENTED_EDGE('',*,*,#10305,.F.);
#15461=ORIENTED_EDGE('',*,*,#10308,.F.);
#15462=ORIENTED_EDGE('',*,*,#10311,.F.);
#15463=ORIENTED_EDGE('',*,*,#10314,.F.);
#15464=ORIENTED_EDGE('',*,*,#10317,.F.);
#15465=ORIENTED_EDGE('',*,*,#10320,.F.);
#15466=ORIENTED_EDGE('',*,*,#10323,.F.);
#15467=ORIENTED_EDGE('',*,*,#10326,.F.);
#15468=ORIENTED_EDGE('',*,*,#10329,.F.);
#15469=ORIENTED_EDGE('',*,*,#10332,.F.);
#15470=ORIENTED_EDGE('',*,*,#10335,.F.);
#15471=ORIENTED_EDGE('',*,*,#10338,.F.);
#15472=ORIENTED_EDGE('',*,*,#10341,.F.);
#15473=ORIENTED_EDGE('',*,*,#10344,.F.);
#15474=ORIENTED_EDGE('',*,*,#10347,.F.);
#15475=ORIENTED_EDGE('',*,*,#10350,.F.);
#15476=ORIENTED_EDGE('',*,*,#10353,.F.);
#15477=ORIENTED_EDGE('',*,*,#10356,.F.);
#15478=ORIENTED_EDGE('',*,*,#10359,.F.);
#15479=ORIENTED_EDGE('',*,*,#10362,.F.);
#15480=ORIENTED_EDGE('',*,*,#10365,.F.);
#15481=ORIENTED_EDGE('',*,*,#10368,.F.);
#15482=ORIENTED_EDGE('',*,*,#10371,.F.);
#15483=ORIENTED_EDGE('',*,*,#10374,.F.);
#15484=ORIENTED_EDGE('',*,*,#10377,.F.);
#15485=ORIENTED_EDGE('',*,*,#10654,.F.);
#15486=ORIENTED_EDGE('',*,*,#10655,.F.);
#15487=ORIENTED_EDGE('',*,*,#10656,.F.);
#15488=ORIENTED_EDGE('',*,*,#10657,.F.);
#15489=ORIENTED_EDGE('',*,*,#10658,.F.);
#15490=ORIENTED_EDGE('',*,*,#10659,.F.);
#15491=ORIENTED_EDGE('',*,*,#10660,.T.);
#15492=ORIENTED_EDGE('',*,*,#10661,.F.);
#15493=ORIENTED_EDGE('',*,*,#10660,.F.);
#15494=ORIENTED_EDGE('',*,*,#10662,.F.);
#15495=ORIENTED_EDGE('',*,*,#10663,.F.);
#15496=ORIENTED_EDGE('',*,*,#10658,.T.);
#15497=ORIENTED_EDGE('',*,*,#10664,.F.);
#15498=ORIENTED_EDGE('',*,*,#10665,.T.);
#15499=ORIENTED_EDGE('',*,*,#10666,.T.);
#15500=ORIENTED_EDGE('',*,*,#10657,.T.);
#15501=ORIENTED_EDGE('',*,*,#10667,.F.);
#15502=ORIENTED_EDGE('',*,*,#10668,.T.);
#15503=ORIENTED_EDGE('',*,*,#10664,.T.);
#15504=ORIENTED_EDGE('',*,*,#10656,.T.);
#15505=ORIENTED_EDGE('',*,*,#10669,.F.);
#15506=ORIENTED_EDGE('',*,*,#10670,.T.);
#15507=ORIENTED_EDGE('',*,*,#10667,.T.);
#15508=ORIENTED_EDGE('',*,*,#10670,.F.);
#15509=ORIENTED_EDGE('',*,*,#10671,.F.);
#15510=ORIENTED_EDGE('',*,*,#10672,.F.);
#15511=ORIENTED_EDGE('',*,*,#10673,.F.);
#15512=ORIENTED_EDGE('',*,*,#10665,.F.);
#15513=ORIENTED_EDGE('',*,*,#10668,.F.);
#15514=ORIENTED_EDGE('',*,*,#10674,.T.);
#15515=ORIENTED_EDGE('',*,*,#10644,.T.);
#15516=ORIENTED_EDGE('',*,*,#10384,.T.);
#15517=ORIENTED_EDGE('',*,*,#10381,.T.);
#15518=ORIENTED_EDGE('',*,*,#10653,.T.);
#15519=ORIENTED_EDGE('',*,*,#10655,.T.);
#15520=ORIENTED_EDGE('',*,*,#10675,.F.);
#15521=ORIENTED_EDGE('',*,*,#10671,.T.);
#15522=ORIENTED_EDGE('',*,*,#10669,.T.);
#15523=ORIENTED_EDGE('',*,*,#10663,.T.);
#15524=ORIENTED_EDGE('',*,*,#10676,.F.);
#15525=ORIENTED_EDGE('',*,*,#10672,.T.);
#15526=ORIENTED_EDGE('',*,*,#10675,.T.);
#15527=ORIENTED_EDGE('',*,*,#10662,.T.);
#15528=ORIENTED_EDGE('',*,*,#10659,.T.);
#15529=ORIENTED_EDGE('',*,*,#10666,.F.);
#15530=ORIENTED_EDGE('',*,*,#10673,.T.);
#15531=ORIENTED_EDGE('',*,*,#10676,.T.);
#15532=ORIENTED_EDGE('',*,*,#10661,.T.);
#15533=ORIENTED_EDGE('',*,*,#10677,.F.);
#15534=ORIENTED_EDGE('',*,*,#10648,.F.);
#15535=ORIENTED_EDGE('',*,*,#10116,.F.);
#15536=ORIENTED_EDGE('',*,*,#10649,.F.);
#15537=ORIENTED_EDGE('',*,*,#10678,.T.);
#15538=ORIENTED_EDGE('',*,*,#10677,.T.);
#15539=ORIENTED_EDGE('',*,*,#10678,.F.);
#15540=ORIENTED_EDGE('',*,*,#10376,.T.);
#15541=ORIENTED_EDGE('',*,*,#10645,.T.);
#15542=ORIENTED_EDGE('',*,*,#10674,.F.);
#15543=ORIENTED_EDGE('',*,*,#10654,.T.);
#15946=PLANE('',#18667);
#15947=PLANE('',#18674);
#15948=PLANE('',#18675);
#15949=PLANE('',#18676);
#15950=PLANE('',#18677);
#15951=PLANE('',#18679);
#15952=PLANE('',#18680);
#15953=PLANE('',#18681);
#15954=PLANE('',#18682);
#15955=PLANE('',#18683);
#16720=ADVANCED_FACE('',(#2549),#1582,.T.);
#16721=ADVANCED_FACE('',(#2550),#1583,.T.);
#16722=ADVANCED_FACE('',(#2551),#1584,.T.);
#16723=ADVANCED_FACE('',(#2552),#1585,.T.);
#16724=ADVANCED_FACE('',(#2553),#1586,.T.);
#16725=ADVANCED_FACE('',(#2554),#1587,.T.);
#16726=ADVANCED_FACE('',(#2555),#1588,.T.);
#16727=ADVANCED_FACE('',(#2556),#1589,.T.);
#16728=ADVANCED_FACE('',(#2557),#1590,.T.);
#16729=ADVANCED_FACE('',(#2558),#1591,.T.);
#16730=ADVANCED_FACE('',(#2559),#1592,.T.);
#16731=ADVANCED_FACE('',(#2560),#1593,.T.);
#16732=ADVANCED_FACE('',(#2561),#1594,.T.);
#16733=ADVANCED_FACE('',(#2562),#1595,.T.);
#16734=ADVANCED_FACE('',(#2563),#1596,.T.);
#16735=ADVANCED_FACE('',(#2564),#1597,.T.);
#16736=ADVANCED_FACE('',(#2565),#1598,.T.);
#16737=ADVANCED_FACE('',(#2566),#1599,.T.);
#16738=ADVANCED_FACE('',(#2567),#1600,.T.);
#16739=ADVANCED_FACE('',(#2568),#1601,.T.);
#16740=ADVANCED_FACE('',(#2569),#1602,.T.);
#16741=ADVANCED_FACE('',(#2570),#1603,.T.);
#16742=ADVANCED_FACE('',(#2571),#1604,.T.);
#16743=ADVANCED_FACE('',(#2572),#1605,.T.);
#16744=ADVANCED_FACE('',(#2573),#1606,.T.);
#16745=ADVANCED_FACE('',(#2574),#1607,.T.);
#16746=ADVANCED_FACE('',(#2575),#1608,.T.);
#16747=ADVANCED_FACE('',(#2576),#1609,.T.);
#16748=ADVANCED_FACE('',(#2577),#1610,.T.);
#16749=ADVANCED_FACE('',(#2578),#1611,.T.);
#16750=ADVANCED_FACE('',(#2579),#1612,.T.);
#16751=ADVANCED_FACE('',(#2580),#1613,.T.);
#16752=ADVANCED_FACE('',(#2581),#1614,.T.);
#16753=ADVANCED_FACE('',(#2582),#1615,.T.);
#16754=ADVANCED_FACE('',(#2583),#1616,.T.);
#16755=ADVANCED_FACE('',(#2584),#1617,.T.);
#16756=ADVANCED_FACE('',(#2585),#1618,.T.);
#16757=ADVANCED_FACE('',(#2586),#1619,.T.);
#16758=ADVANCED_FACE('',(#2587),#1620,.T.);
#16759=ADVANCED_FACE('',(#2588),#1621,.T.);
#16760=ADVANCED_FACE('',(#2589),#1622,.T.);
#16761=ADVANCED_FACE('',(#2590),#1623,.T.);
#16762=ADVANCED_FACE('',(#2591),#1624,.T.);
#16763=ADVANCED_FACE('',(#2592),#1625,.T.);
#16764=ADVANCED_FACE('',(#2593),#1626,.T.);
#16765=ADVANCED_FACE('',(#2594),#1627,.T.);
#16766=ADVANCED_FACE('',(#2595),#1628,.T.);
#16767=ADVANCED_FACE('',(#2596),#1629,.T.);
#16768=ADVANCED_FACE('',(#2597),#1630,.T.);
#16769=ADVANCED_FACE('',(#2598),#1631,.T.);
#16770=ADVANCED_FACE('',(#2599),#1632,.T.);
#16771=ADVANCED_FACE('',(#2600),#1633,.T.);
#16772=ADVANCED_FACE('',(#2601),#1634,.T.);
#16773=ADVANCED_FACE('',(#2602),#1635,.T.);
#16774=ADVANCED_FACE('',(#2603),#1636,.T.);
#16775=ADVANCED_FACE('',(#2604),#1637,.T.);
#16776=ADVANCED_FACE('',(#2605),#1638,.T.);
#16777=ADVANCED_FACE('',(#2606),#1639,.T.);
#16778=ADVANCED_FACE('',(#2607),#1640,.T.);
#16779=ADVANCED_FACE('',(#2608),#1641,.T.);
#16780=ADVANCED_FACE('',(#2609),#1642,.T.);
#16781=ADVANCED_FACE('',(#2610),#1643,.T.);
#16782=ADVANCED_FACE('',(#2611),#1644,.T.);
#16783=ADVANCED_FACE('',(#2612),#1645,.T.);
#16784=ADVANCED_FACE('',(#2613),#1646,.T.);
#16785=ADVANCED_FACE('',(#2614),#1647,.T.);
#16786=ADVANCED_FACE('',(#2615),#1648,.T.);
#16787=ADVANCED_FACE('',(#2616),#1649,.T.);
#16788=ADVANCED_FACE('',(#2617),#1650,.T.);
#16789=ADVANCED_FACE('',(#2618),#1651,.T.);
#16790=ADVANCED_FACE('',(#2619),#1652,.T.);
#16791=ADVANCED_FACE('',(#2620),#1653,.T.);
#16792=ADVANCED_FACE('',(#2621),#1654,.T.);
#16793=ADVANCED_FACE('',(#2622),#1655,.T.);
#16794=ADVANCED_FACE('',(#2623),#1656,.T.);
#16795=ADVANCED_FACE('',(#2624),#1657,.T.);
#16796=ADVANCED_FACE('',(#2625),#1658,.T.);
#16797=ADVANCED_FACE('',(#2626),#1659,.T.);
#16798=ADVANCED_FACE('',(#2627),#1660,.T.);
#16799=ADVANCED_FACE('',(#2628),#1661,.T.);
#16800=ADVANCED_FACE('',(#2629),#1662,.T.);
#16801=ADVANCED_FACE('',(#2630),#1663,.T.);
#16802=ADVANCED_FACE('',(#2631),#1664,.T.);
#16803=ADVANCED_FACE('',(#2632),#1665,.T.);
#16804=ADVANCED_FACE('',(#2633),#1666,.T.);
#16805=ADVANCED_FACE('',(#2634),#1667,.T.);
#16806=ADVANCED_FACE('',(#2635),#1668,.T.);
#16807=ADVANCED_FACE('',(#2636),#1669,.T.);
#16808=ADVANCED_FACE('',(#2637),#1670,.T.);
#16809=ADVANCED_FACE('',(#2638),#1671,.T.);
#16810=ADVANCED_FACE('',(#2639),#1672,.T.);
#16811=ADVANCED_FACE('',(#2640),#1673,.T.);
#16812=ADVANCED_FACE('',(#2641),#1674,.T.);
#16813=ADVANCED_FACE('',(#2642),#1675,.T.);
#16814=ADVANCED_FACE('',(#2643),#1676,.T.);
#16815=ADVANCED_FACE('',(#2644),#1677,.T.);
#16816=ADVANCED_FACE('',(#2645),#1678,.T.);
#16817=ADVANCED_FACE('',(#2646),#1679,.T.);
#16818=ADVANCED_FACE('',(#2647),#1680,.T.);
#16819=ADVANCED_FACE('',(#2648),#1681,.T.);
#16820=ADVANCED_FACE('',(#2649),#1682,.T.);
#16821=ADVANCED_FACE('',(#2650),#1683,.T.);
#16822=ADVANCED_FACE('',(#2651),#1684,.T.);
#16823=ADVANCED_FACE('',(#2652),#1685,.T.);
#16824=ADVANCED_FACE('',(#2653),#1686,.T.);
#16825=ADVANCED_FACE('',(#2654),#1687,.T.);
#16826=ADVANCED_FACE('',(#2655),#1688,.T.);
#16827=ADVANCED_FACE('',(#2656),#1689,.T.);
#16828=ADVANCED_FACE('',(#2657),#1690,.T.);
#16829=ADVANCED_FACE('',(#2658),#1691,.T.);
#16830=ADVANCED_FACE('',(#2659),#1692,.T.);
#16831=ADVANCED_FACE('',(#2660),#1693,.T.);
#16832=ADVANCED_FACE('',(#2661),#1694,.T.);
#16833=ADVANCED_FACE('',(#2662),#1695,.T.);
#16834=ADVANCED_FACE('',(#2663),#1696,.T.);
#16835=ADVANCED_FACE('',(#2664),#1697,.T.);
#16836=ADVANCED_FACE('',(#2665),#1698,.T.);
#16837=ADVANCED_FACE('',(#2666),#1699,.T.);
#16838=ADVANCED_FACE('',(#2667),#1700,.T.);
#16839=ADVANCED_FACE('',(#2668),#1701,.T.);
#16840=ADVANCED_FACE('',(#2669),#1702,.T.);
#16841=ADVANCED_FACE('',(#2670),#1703,.T.);
#16842=ADVANCED_FACE('',(#2671),#1704,.T.);
#16843=ADVANCED_FACE('',(#2672),#1705,.T.);
#16844=ADVANCED_FACE('',(#2673),#1706,.T.);
#16845=ADVANCED_FACE('',(#2674),#1707,.T.);
#16846=ADVANCED_FACE('',(#2675),#1708,.T.);
#16847=ADVANCED_FACE('',(#2676),#1709,.T.);
#16848=ADVANCED_FACE('',(#2677),#1710,.T.);
#16849=ADVANCED_FACE('',(#2678),#1711,.T.);
#16850=ADVANCED_FACE('',(#2679),#1712,.T.);
#16851=ADVANCED_FACE('',(#2680),#1713,.T.);
#16852=ADVANCED_FACE('',(#2681),#1714,.T.);
#16853=ADVANCED_FACE('',(#2682),#1715,.T.);
#16854=ADVANCED_FACE('',(#2683),#1716,.T.);
#16855=ADVANCED_FACE('',(#2684),#1717,.T.);
#16856=ADVANCED_FACE('',(#2685),#1718,.T.);
#16857=ADVANCED_FACE('',(#2686),#1719,.T.);
#16858=ADVANCED_FACE('',(#2687),#1720,.T.);
#16859=ADVANCED_FACE('',(#2688),#1721,.T.);
#16860=ADVANCED_FACE('',(#2689),#1722,.T.);
#16861=ADVANCED_FACE('',(#2690),#1723,.T.);
#16862=ADVANCED_FACE('',(#2691),#1724,.T.);
#16863=ADVANCED_FACE('',(#2692),#1725,.T.);
#16864=ADVANCED_FACE('',(#2693),#1726,.T.);
#16865=ADVANCED_FACE('',(#2694),#1727,.T.);
#16866=ADVANCED_FACE('',(#2695),#1728,.T.);
#16867=ADVANCED_FACE('',(#2696),#1729,.T.);
#16868=ADVANCED_FACE('',(#2697),#1730,.T.);
#16869=ADVANCED_FACE('',(#2698),#1731,.T.);
#16870=ADVANCED_FACE('',(#2699),#1732,.T.);
#16871=ADVANCED_FACE('',(#2700),#1733,.T.);
#16872=ADVANCED_FACE('',(#2701),#1734,.T.);
#16873=ADVANCED_FACE('',(#2702),#1735,.T.);
#16874=ADVANCED_FACE('',(#2703),#1736,.T.);
#16875=ADVANCED_FACE('',(#2704),#1737,.T.);
#16876=ADVANCED_FACE('',(#2705),#1738,.T.);
#16877=ADVANCED_FACE('',(#2706),#1739,.T.);
#16878=ADVANCED_FACE('',(#2707),#1740,.T.);
#16879=ADVANCED_FACE('',(#2708),#1741,.T.);
#16880=ADVANCED_FACE('',(#2709),#1742,.T.);
#16881=ADVANCED_FACE('',(#2710),#1743,.T.);
#16882=ADVANCED_FACE('',(#2711),#1744,.T.);
#16883=ADVANCED_FACE('',(#2712),#1745,.T.);
#16884=ADVANCED_FACE('',(#2713),#1746,.T.);
#16885=ADVANCED_FACE('',(#2714),#1747,.T.);
#16886=ADVANCED_FACE('',(#2715),#1748,.T.);
#16887=ADVANCED_FACE('',(#2716),#1749,.T.);
#16888=ADVANCED_FACE('',(#2717),#1750,.T.);
#16889=ADVANCED_FACE('',(#2718),#1751,.T.);
#16890=ADVANCED_FACE('',(#2719),#1752,.T.);
#16891=ADVANCED_FACE('',(#2720),#1753,.T.);
#16892=ADVANCED_FACE('',(#2721),#1754,.T.);
#16893=ADVANCED_FACE('',(#2722),#1755,.T.);
#16894=ADVANCED_FACE('',(#2723),#1756,.T.);
#16895=ADVANCED_FACE('',(#2724),#1757,.T.);
#16896=ADVANCED_FACE('',(#2725),#359,.F.);
#16897=ADVANCED_FACE('',(#2726),#15946,.T.);
#16898=ADVANCED_FACE('',(#2727),#1758,.T.);
#16899=ADVANCED_FACE('',(#2728),#360,.F.);
#16900=ADVANCED_FACE('',(#2729),#650,.T.);
#16901=ADVANCED_FACE('',(#2730),#15947,.T.);
#16902=ADVANCED_FACE('',(#2731),#15948,.T.);
#16903=ADVANCED_FACE('',(#2732),#15949,.T.);
#16904=ADVANCED_FACE('',(#2733,#561),#15950,.F.);
#16905=ADVANCED_FACE('',(#2734),#15951,.T.);
#16906=ADVANCED_FACE('',(#2735),#15952,.T.);
#16907=ADVANCED_FACE('',(#2736),#15953,.T.);
#16908=ADVANCED_FACE('',(#2737),#15954,.T.);
#16909=ADVANCED_FACE('',(#2738),#15955,.T.);
#16910=ADVANCED_FACE('',(#2739),#651,.T.);
#16911=ADVANCED_FACE('',(#2740),#1759,.T.);
#16967=CLOSED_SHELL('',(#16720,#16721,#16722,#16723,#16724,#16725,#16726,
#16727,#16728,#16729,#16730,#16731,#16732,#16733,#16734,#16735,#16736,#16737,
#16738,#16739,#16740,#16741,#16742,#16743,#16744,#16745,#16746,#16747,#16748,
#16749,#16750,#16751,#16752,#16753,#16754,#16755,#16756,#16757,#16758,#16759,
#16760,#16761,#16762,#16763,#16764,#16765,#16766,#16767,#16768,#16769,#16770,
#16771,#16772,#16773,#16774,#16775,#16776,#16777,#16778,#16779,#16780,#16781,
#16782,#16783,#16784,#16785,#16786,#16787,#16788,#16789,#16790,#16791,#16792,
#16793,#16794,#16795,#16796,#16797,#16798,#16799,#16800,#16801,#16802,#16803,
#16804,#16805,#16806,#16807,#16808,#16809,#16810,#16811,#16812,#16813,#16814,
#16815,#16816,#16817,#16818,#16819,#16820,#16821,#16822,#16823,#16824,#16825,
#16826,#16827,#16828,#16829,#16830,#16831,#16832,#16833,#16834,#16835,#16836,
#16837,#16838,#16839,#16840,#16841,#16842,#16843,#16844,#16845,#16846,#16847,
#16848,#16849,#16850,#16851,#16852,#16853,#16854,#16855,#16856,#16857,#16858,
#16859,#16860,#16861,#16862,#16863,#16864,#16865,#16866,#16867,#16868,#16869,
#16870,#16871,#16872,#16873,#16874,#16875,#16876,#16877,#16878,#16879,#16880,
#16881,#16882,#16883,#16884,#16885,#16886,#16887,#16888,#16889,#16890,#16891,
#16892,#16893,#16894,#16895,#16896,#16897,#16898,#16899,#16900,#16901,#16902,
#16903,#16904,#16905,#16906,#16907,#16908,#16909,#16910,#16911));
#18487=AXIS2_PLACEMENT_3D('',#44369,#22124,#22125);
#18488=AXIS2_PLACEMENT_3D('',#44370,#22126,#22127);
#18489=AXIS2_PLACEMENT_3D('',#44386,#22129,#22130);
#18490=AXIS2_PLACEMENT_3D('',#44394,#22131,#22132);
#18491=AXIS2_PLACEMENT_3D('',#44442,#22134,#22135);
#18492=AXIS2_PLACEMENT_3D('',#44490,#22137,#22138);
#18493=AXIS2_PLACEMENT_3D('',#44538,#22140,#22141);
#18494=AXIS2_PLACEMENT_3D('',#44592,#22143,#22144);
#18495=AXIS2_PLACEMENT_3D('',#44640,#22146,#22147);
#18496=AXIS2_PLACEMENT_3D('',#44688,#22149,#22150);
#18497=AXIS2_PLACEMENT_3D('',#44742,#22152,#22153);
#18498=AXIS2_PLACEMENT_3D('',#44790,#22155,#22156);
#18499=AXIS2_PLACEMENT_3D('',#44838,#22158,#22159);
#18500=AXIS2_PLACEMENT_3D('',#44886,#22161,#22162);
#18501=AXIS2_PLACEMENT_3D('',#44940,#22164,#22165);
#18502=AXIS2_PLACEMENT_3D('',#44988,#22167,#22168);
#18503=AXIS2_PLACEMENT_3D('',#45036,#22170,#22171);
#18504=AXIS2_PLACEMENT_3D('',#45090,#22173,#22174);
#18505=AXIS2_PLACEMENT_3D('',#45138,#22176,#22177);
#18506=AXIS2_PLACEMENT_3D('',#45186,#22179,#22180);
#18507=AXIS2_PLACEMENT_3D('',#45234,#22182,#22183);
#18508=AXIS2_PLACEMENT_3D('',#45288,#22185,#22186);
#18509=AXIS2_PLACEMENT_3D('',#45336,#22188,#22189);
#18510=AXIS2_PLACEMENT_3D('',#45384,#22191,#22192);
#18511=AXIS2_PLACEMENT_3D('',#45438,#22194,#22195);
#18512=AXIS2_PLACEMENT_3D('',#45486,#22197,#22198);
#18513=AXIS2_PLACEMENT_3D('',#45534,#22200,#22201);
#18514=AXIS2_PLACEMENT_3D('',#45582,#22203,#22204);
#18515=AXIS2_PLACEMENT_3D('',#45636,#22206,#22207);
#18516=AXIS2_PLACEMENT_3D('',#45684,#22209,#22210);
#18517=AXIS2_PLACEMENT_3D('',#45732,#22212,#22213);
#18518=AXIS2_PLACEMENT_3D('',#45786,#22215,#22216);
#18519=AXIS2_PLACEMENT_3D('',#45834,#22218,#22219);
#18520=AXIS2_PLACEMENT_3D('',#45882,#22221,#22222);
#18521=AXIS2_PLACEMENT_3D('',#45930,#22224,#22225);
#18522=AXIS2_PLACEMENT_3D('',#45984,#22227,#22228);
#18523=AXIS2_PLACEMENT_3D('',#46032,#22230,#22231);
#18524=AXIS2_PLACEMENT_3D('',#46080,#22233,#22234);
#18525=AXIS2_PLACEMENT_3D('',#46134,#22236,#22237);
#18526=AXIS2_PLACEMENT_3D('',#46182,#22239,#22240);
#18527=AXIS2_PLACEMENT_3D('',#46230,#22242,#22243);
#18528=AXIS2_PLACEMENT_3D('',#46278,#22245,#22246);
#18529=AXIS2_PLACEMENT_3D('',#46332,#22248,#22249);
#18530=AXIS2_PLACEMENT_3D('',#46380,#22251,#22252);
#18531=AXIS2_PLACEMENT_3D('',#46428,#22254,#22255);
#18532=AXIS2_PLACEMENT_3D('',#46482,#22257,#22258);
#18533=AXIS2_PLACEMENT_3D('',#46530,#22260,#22261);
#18534=AXIS2_PLACEMENT_3D('',#46578,#22263,#22264);
#18535=AXIS2_PLACEMENT_3D('',#46626,#22266,#22267);
#18536=AXIS2_PLACEMENT_3D('',#46680,#22269,#22270);
#18537=AXIS2_PLACEMENT_3D('',#46728,#22272,#22273);
#18538=AXIS2_PLACEMENT_3D('',#46776,#22275,#22276);
#18539=AXIS2_PLACEMENT_3D('',#46830,#22278,#22279);
#18540=AXIS2_PLACEMENT_3D('',#46878,#22281,#22282);
#18541=AXIS2_PLACEMENT_3D('',#46926,#22284,#22285);
#18542=AXIS2_PLACEMENT_3D('',#46974,#22287,#22288);
#18543=AXIS2_PLACEMENT_3D('',#47028,#22290,#22291);
#18544=AXIS2_PLACEMENT_3D('',#47076,#22293,#22294);
#18545=AXIS2_PLACEMENT_3D('',#47124,#22296,#22297);
#18546=AXIS2_PLACEMENT_3D('',#47178,#22299,#22300);
#18547=AXIS2_PLACEMENT_3D('',#47226,#22302,#22303);
#18548=AXIS2_PLACEMENT_3D('',#47274,#22305,#22306);
#18549=AXIS2_PLACEMENT_3D('',#47322,#22308,#22309);
#18550=AXIS2_PLACEMENT_3D('',#47376,#22311,#22312);
#18551=AXIS2_PLACEMENT_3D('',#47424,#22314,#22315);
#18552=AXIS2_PLACEMENT_3D('',#47472,#22317,#22318);
#18553=AXIS2_PLACEMENT_3D('',#47526,#22320,#22321);
#18554=AXIS2_PLACEMENT_3D('',#47574,#22323,#22324);
#18555=AXIS2_PLACEMENT_3D('',#47622,#22326,#22327);
#18556=AXIS2_PLACEMENT_3D('',#47670,#22329,#22330);
#18557=AXIS2_PLACEMENT_3D('',#47724,#22332,#22333);
#18558=AXIS2_PLACEMENT_3D('',#47772,#22335,#22336);
#18559=AXIS2_PLACEMENT_3D('',#47820,#22338,#22339);
#18560=AXIS2_PLACEMENT_3D('',#47874,#22341,#22342);
#18561=AXIS2_PLACEMENT_3D('',#47922,#22344,#22345);
#18562=AXIS2_PLACEMENT_3D('',#47970,#22347,#22348);
#18563=AXIS2_PLACEMENT_3D('',#48018,#22350,#22351);
#18564=AXIS2_PLACEMENT_3D('',#48072,#22353,#22354);
#18565=AXIS2_PLACEMENT_3D('',#48120,#22356,#22357);
#18566=AXIS2_PLACEMENT_3D('',#48168,#22359,#22360);
#18567=AXIS2_PLACEMENT_3D('',#48222,#22362,#22363);
#18568=AXIS2_PLACEMENT_3D('',#48270,#22365,#22366);
#18569=AXIS2_PLACEMENT_3D('',#48318,#22368,#22369);
#18570=AXIS2_PLACEMENT_3D('',#48366,#22371,#22372);
#18571=AXIS2_PLACEMENT_3D('',#48420,#22374,#22375);
#18572=AXIS2_PLACEMENT_3D('',#48468,#22377,#22378);
#18573=AXIS2_PLACEMENT_3D('',#48516,#22380,#22381);
#18574=AXIS2_PLACEMENT_3D('',#48570,#22383,#22384);
#18575=AXIS2_PLACEMENT_3D('',#48618,#22386,#22387);
#18576=AXIS2_PLACEMENT_3D('',#48666,#22389,#22390);
#18577=AXIS2_PLACEMENT_3D('',#48714,#22392,#22393);
#18578=AXIS2_PLACEMENT_3D('',#48723,#22395,#22396);
#18579=AXIS2_PLACEMENT_3D('',#48724,#22397,#22398);
#18580=AXIS2_PLACEMENT_3D('',#48751,#22400,#22401);
#18581=AXIS2_PLACEMENT_3D('',#48761,#22402,#22403);
#18582=AXIS2_PLACEMENT_3D('',#48809,#22405,#22406);
#18583=AXIS2_PLACEMENT_3D('',#48857,#22408,#22409);
#18584=AXIS2_PLACEMENT_3D('',#48882,#22411,#22412);
#18585=AXIS2_PLACEMENT_3D('',#48907,#22414,#22415);
#18586=AXIS2_PLACEMENT_3D('',#48931,#22417,#22418);
#18587=AXIS2_PLACEMENT_3D('',#48956,#22420,#22421);
#18588=AXIS2_PLACEMENT_3D('',#48995,#22423,#22424);
#18589=AXIS2_PLACEMENT_3D('',#49031,#22426,#22427);
#18590=AXIS2_PLACEMENT_3D('',#49055,#22429,#22430);
#18591=AXIS2_PLACEMENT_3D('',#49080,#22432,#22433);
#18592=AXIS2_PLACEMENT_3D('',#49105,#22435,#22436);
#18593=AXIS2_PLACEMENT_3D('',#49129,#22438,#22439);
#18594=AXIS2_PLACEMENT_3D('',#49154,#22441,#22442);
#18595=AXIS2_PLACEMENT_3D('',#49179,#22444,#22445);
#18596=AXIS2_PLACEMENT_3D('',#49215,#22447,#22448);
#18597=AXIS2_PLACEMENT_3D('',#49251,#22450,#22451);
#18598=AXIS2_PLACEMENT_3D('',#49276,#22453,#22454);
#18599=AXIS2_PLACEMENT_3D('',#49301,#22456,#22457);
#18600=AXIS2_PLACEMENT_3D('',#49325,#22459,#22460);
#18601=AXIS2_PLACEMENT_3D('',#49350,#22462,#22463);
#18602=AXIS2_PLACEMENT_3D('',#49375,#22465,#22466);
#18603=AXIS2_PLACEMENT_3D('',#49399,#22468,#22469);
#18604=AXIS2_PLACEMENT_3D('',#49423,#22471,#22472);
#18605=AXIS2_PLACEMENT_3D('',#49448,#22474,#22475);
#18606=AXIS2_PLACEMENT_3D('',#49473,#22477,#22478);
#18607=AXIS2_PLACEMENT_3D('',#49497,#22480,#22481);
#18608=AXIS2_PLACEMENT_3D('',#49522,#22483,#22484);
#18609=AXIS2_PLACEMENT_3D('',#49547,#22486,#22487);
#18610=AXIS2_PLACEMENT_3D('',#49571,#22489,#22490);
#18611=AXIS2_PLACEMENT_3D('',#49595,#22492,#22493);
#18612=AXIS2_PLACEMENT_3D('',#49620,#22495,#22496);
#18613=AXIS2_PLACEMENT_3D('',#49645,#22498,#22499);
#18614=AXIS2_PLACEMENT_3D('',#49669,#22501,#22502);
#18615=AXIS2_PLACEMENT_3D('',#49694,#22504,#22505);
#18616=AXIS2_PLACEMENT_3D('',#49719,#22507,#22508);
#18617=AXIS2_PLACEMENT_3D('',#49743,#22510,#22511);
#18618=AXIS2_PLACEMENT_3D('',#49767,#22513,#22514);
#18619=AXIS2_PLACEMENT_3D('',#49792,#22516,#22517);
#18620=AXIS2_PLACEMENT_3D('',#49817,#22519,#22520);
#18621=AXIS2_PLACEMENT_3D('',#49841,#22522,#22523);
#18622=AXIS2_PLACEMENT_3D('',#49866,#22525,#22526);
#18623=AXIS2_PLACEMENT_3D('',#49891,#22528,#22529);
#18624=AXIS2_PLACEMENT_3D('',#49915,#22531,#22532);
#18625=AXIS2_PLACEMENT_3D('',#49939,#22534,#22535);
#18626=AXIS2_PLACEMENT_3D('',#49964,#22537,#22538);
#18627=AXIS2_PLACEMENT_3D('',#49989,#22540,#22541);
#18628=AXIS2_PLACEMENT_3D('',#50013,#22543,#22544);
#18629=AXIS2_PLACEMENT_3D('',#50038,#22546,#22547);
#18630=AXIS2_PLACEMENT_3D('',#50063,#22549,#22550);
#18631=AXIS2_PLACEMENT_3D('',#50087,#22552,#22553);
#18632=AXIS2_PLACEMENT_3D('',#50111,#22555,#22556);
#18633=AXIS2_PLACEMENT_3D('',#50136,#22558,#22559);
#18634=AXIS2_PLACEMENT_3D('',#50161,#22561,#22562);
#18635=AXIS2_PLACEMENT_3D('',#50185,#22564,#22565);
#18636=AXIS2_PLACEMENT_3D('',#50210,#22567,#22568);
#18637=AXIS2_PLACEMENT_3D('',#50235,#22570,#22571);
#18638=AXIS2_PLACEMENT_3D('',#50259,#22573,#22574);
#18639=AXIS2_PLACEMENT_3D('',#50283,#22576,#22577);
#18640=AXIS2_PLACEMENT_3D('',#50308,#22579,#22580);
#18641=AXIS2_PLACEMENT_3D('',#50333,#22582,#22583);
#18642=AXIS2_PLACEMENT_3D('',#50357,#22585,#22586);
#18643=AXIS2_PLACEMENT_3D('',#50382,#22588,#22589);
#18644=AXIS2_PLACEMENT_3D('',#50407,#22591,#22592);
#18645=AXIS2_PLACEMENT_3D('',#50431,#22594,#22595);
#18646=AXIS2_PLACEMENT_3D('',#50455,#22597,#22598);
#18647=AXIS2_PLACEMENT_3D('',#50480,#22600,#22601);
#18648=AXIS2_PLACEMENT_3D('',#50505,#22603,#22604);
#18649=AXIS2_PLACEMENT_3D('',#50529,#22606,#22607);
#18650=AXIS2_PLACEMENT_3D('',#50554,#22609,#22610);
#18651=AXIS2_PLACEMENT_3D('',#50579,#22612,#22613);
#18652=AXIS2_PLACEMENT_3D('',#50603,#22615,#22616);
#18653=AXIS2_PLACEMENT_3D('',#50627,#22618,#22619);
#18654=AXIS2_PLACEMENT_3D('',#50652,#22621,#22622);
#18655=AXIS2_PLACEMENT_3D('',#50677,#22624,#22625);
#18656=AXIS2_PLACEMENT_3D('',#50701,#22627,#22628);
#18657=AXIS2_PLACEMENT_3D('',#50726,#22630,#22631);
#18658=AXIS2_PLACEMENT_3D('',#50751,#22633,#22634);
#18659=AXIS2_PLACEMENT_3D('',#50775,#22636,#22637);
#18660=AXIS2_PLACEMENT_3D('',#50799,#22639,#22640);
#18661=AXIS2_PLACEMENT_3D('',#50824,#22642,#22643);
#18662=AXIS2_PLACEMENT_3D('',#50849,#22645,#22646);
#18663=AXIS2_PLACEMENT_3D('',#50873,#22648,#22649);
#18664=AXIS2_PLACEMENT_3D('',#50898,#22651,#22652);
#18665=AXIS2_PLACEMENT_3D('',#50923,#22654,#22655);
#18666=AXIS2_PLACEMENT_3D('',#50947,#22657,#22658);
#18667=AXIS2_PLACEMENT_3D('',#53413,#22660,#22661);
#18668=AXIS2_PLACEMENT_3D('',#53415,#22662,#22663);
#18669=AXIS2_PLACEMENT_3D('',#53416,#22664,#22665);
#18670=AXIS2_PLACEMENT_3D('',#53515,#22666,#22667);
#18671=AXIS2_PLACEMENT_3D('',#53516,#22668,#22669);
#18672=AXIS2_PLACEMENT_3D('',#55857,#22670,#22671);
#18673=AXIS2_PLACEMENT_3D('',#55881,#22673,#22674);
#18674=AXIS2_PLACEMENT_3D('',#55889,#22675,#22676);
#18675=AXIS2_PLACEMENT_3D('',#55895,#22680,#22681);
#18676=AXIS2_PLACEMENT_3D('',#55899,#22684,#22685);
#18677=AXIS2_PLACEMENT_3D('',#55903,#22688,#22689);
#18678=AXIS2_PLACEMENT_3D('',#55909,#22693,#22694);
#18679=AXIS2_PLACEMENT_3D('',#55910,#22695,#22696);
#18680=AXIS2_PLACEMENT_3D('',#55912,#22698,#22699);
#18681=AXIS2_PLACEMENT_3D('',#55914,#22701,#22702);
#18682=AXIS2_PLACEMENT_3D('',#55915,#22703,#22704);
#18683=AXIS2_PLACEMENT_3D('',#55916,#22705,#22706);
#18684=AXIS2_PLACEMENT_3D('',#55918,#22707,#22708);
#18685=AXIS2_PLACEMENT_3D('',#55919,#22709,#22710);
#18686=AXIS2_PLACEMENT_3D('',#55921,#22712,#22713);
#22124=DIRECTION('axis',(0.,0.,1.));
#22125=DIRECTION('refdir',(1.,0.,0.));
#22126=DIRECTION('center_axis',(1.,0.,0.));
#22127=DIRECTION('ref_axis',(0.,1.,0.));
#22128=DIRECTION('',(-1.,0.,0.));
#22129=DIRECTION('center_axis',(1.,0.,0.));
#22130=DIRECTION('ref_axis',(0.,1.,0.));
#22131=DIRECTION('center_axis',(1.,0.,0.));
#22132=DIRECTION('ref_axis',(0.,1.,0.));
#22133=DIRECTION('',(-1.,0.,0.));
#22134=DIRECTION('center_axis',(1.,0.,0.));
#22135=DIRECTION('ref_axis',(0.,1.,0.));
#22136=DIRECTION('',(-1.,0.,0.));
#22137=DIRECTION('center_axis',(1.,0.,0.));
#22138=DIRECTION('ref_axis',(0.,1.,0.));
#22139=DIRECTION('',(-1.,0.,0.));
#22140=DIRECTION('center_axis',(1.,0.,0.));
#22141=DIRECTION('ref_axis',(0.,1.,0.));
#22142=DIRECTION('',(-1.,0.,0.));
#22143=DIRECTION('center_axis',(1.,0.,0.));
#22144=DIRECTION('ref_axis',(0.,1.,0.));
#22145=DIRECTION('',(-1.,0.,0.));
#22146=DIRECTION('center_axis',(1.,0.,0.));
#22147=DIRECTION('ref_axis',(0.,1.,0.));
#22148=DIRECTION('',(-1.,0.,0.));
#22149=DIRECTION('center_axis',(1.,0.,0.));
#22150=DIRECTION('ref_axis',(0.,1.,0.));
#22151=DIRECTION('',(-1.,0.,0.));
#22152=DIRECTION('center_axis',(1.,0.,0.));
#22153=DIRECTION('ref_axis',(0.,1.,0.));
#22154=DIRECTION('',(-1.,0.,0.));
#22155=DIRECTION('center_axis',(1.,0.,0.));
#22156=DIRECTION('ref_axis',(0.,1.,0.));
#22157=DIRECTION('',(-1.,0.,0.));
#22158=DIRECTION('center_axis',(1.,0.,0.));
#22159=DIRECTION('ref_axis',(0.,1.,0.));
#22160=DIRECTION('',(-1.,0.,0.));
#22161=DIRECTION('center_axis',(1.,0.,0.));
#22162=DIRECTION('ref_axis',(0.,1.,0.));
#22163=DIRECTION('',(-1.,0.,0.));
#22164=DIRECTION('center_axis',(1.,0.,0.));
#22165=DIRECTION('ref_axis',(0.,1.,0.));
#22166=DIRECTION('',(-1.,0.,0.));
#22167=DIRECTION('center_axis',(1.,0.,0.));
#22168=DIRECTION('ref_axis',(0.,1.,0.));
#22169=DIRECTION('',(-1.,0.,0.));
#22170=DIRECTION('center_axis',(1.,0.,0.));
#22171=DIRECTION('ref_axis',(0.,1.,0.));
#22172=DIRECTION('',(-1.,0.,0.));
#22173=DIRECTION('center_axis',(1.,0.,0.));
#22174=DIRECTION('ref_axis',(0.,1.,0.));
#22175=DIRECTION('',(-1.,0.,0.));
#22176=DIRECTION('center_axis',(1.,0.,0.));
#22177=DIRECTION('ref_axis',(0.,1.,0.));
#22178=DIRECTION('',(-1.,0.,0.));
#22179=DIRECTION('center_axis',(1.,0.,0.));
#22180=DIRECTION('ref_axis',(0.,1.,0.));
#22181=DIRECTION('',(-1.,0.,0.));
#22182=DIRECTION('center_axis',(1.,0.,0.));
#22183=DIRECTION('ref_axis',(0.,1.,0.));
#22184=DIRECTION('',(-1.,0.,0.));
#22185=DIRECTION('center_axis',(1.,0.,0.));
#22186=DIRECTION('ref_axis',(0.,1.,0.));
#22187=DIRECTION('',(-1.,0.,0.));
#22188=DIRECTION('center_axis',(1.,0.,0.));
#22189=DIRECTION('ref_axis',(0.,1.,0.));
#22190=DIRECTION('',(-1.,0.,0.));
#22191=DIRECTION('center_axis',(1.,0.,0.));
#22192=DIRECTION('ref_axis',(0.,1.,0.));
#22193=DIRECTION('',(-1.,0.,0.));
#22194=DIRECTION('center_axis',(1.,0.,0.));
#22195=DIRECTION('ref_axis',(0.,1.,0.));
#22196=DIRECTION('',(-1.,0.,0.));
#22197=DIRECTION('center_axis',(1.,0.,0.));
#22198=DIRECTION('ref_axis',(0.,1.,0.));
#22199=DIRECTION('',(-1.,0.,0.));
#22200=DIRECTION('center_axis',(1.,0.,0.));
#22201=DIRECTION('ref_axis',(0.,1.,0.));
#22202=DIRECTION('',(-1.,0.,0.));
#22203=DIRECTION('center_axis',(1.,0.,0.));
#22204=DIRECTION('ref_axis',(0.,1.,0.));
#22205=DIRECTION('',(-1.,0.,0.));
#22206=DIRECTION('center_axis',(1.,0.,0.));
#22207=DIRECTION('ref_axis',(0.,1.,0.));
#22208=DIRECTION('',(-1.,0.,0.));
#22209=DIRECTION('center_axis',(1.,0.,0.));
#22210=DIRECTION('ref_axis',(0.,1.,0.));
#22211=DIRECTION('',(-1.,0.,0.));
#22212=DIRECTION('center_axis',(1.,0.,0.));
#22213=DIRECTION('ref_axis',(0.,1.,0.));
#22214=DIRECTION('',(-1.,0.,0.));
#22215=DIRECTION('center_axis',(1.,0.,0.));
#22216=DIRECTION('ref_axis',(0.,1.,0.));
#22217=DIRECTION('',(-1.,0.,0.));
#22218=DIRECTION('center_axis',(1.,0.,0.));
#22219=DIRECTION('ref_axis',(0.,1.,0.));
#22220=DIRECTION('',(-1.,0.,0.));
#22221=DIRECTION('center_axis',(1.,0.,0.));
#22222=DIRECTION('ref_axis',(0.,1.,0.));
#22223=DIRECTION('',(-1.,0.,0.));
#22224=DIRECTION('center_axis',(1.,0.,0.));
#22225=DIRECTION('ref_axis',(0.,1.,0.));
#22226=DIRECTION('',(-1.,0.,0.));
#22227=DIRECTION('center_axis',(1.,0.,0.));
#22228=DIRECTION('ref_axis',(0.,1.,0.));
#22229=DIRECTION('',(-1.,0.,0.));
#22230=DIRECTION('center_axis',(1.,0.,0.));
#22231=DIRECTION('ref_axis',(0.,1.,0.));
#22232=DIRECTION('',(-1.,0.,0.));
#22233=DIRECTION('center_axis',(1.,0.,0.));
#22234=DIRECTION('ref_axis',(0.,1.,0.));
#22235=DIRECTION('',(-1.,0.,0.));
#22236=DIRECTION('center_axis',(1.,0.,0.));
#22237=DIRECTION('ref_axis',(0.,1.,0.));
#22238=DIRECTION('',(-1.,0.,0.));
#22239=DIRECTION('center_axis',(1.,0.,0.));
#22240=DIRECTION('ref_axis',(0.,1.,0.));
#22241=DIRECTION('',(-1.,0.,0.));
#22242=DIRECTION('center_axis',(1.,0.,0.));
#22243=DIRECTION('ref_axis',(0.,1.,0.));
#22244=DIRECTION('',(-1.,0.,0.));
#22245=DIRECTION('center_axis',(1.,0.,0.));
#22246=DIRECTION('ref_axis',(0.,1.,0.));
#22247=DIRECTION('',(-1.,0.,0.));
#22248=DIRECTION('center_axis',(1.,0.,0.));
#22249=DIRECTION('ref_axis',(0.,1.,0.));
#22250=DIRECTION('',(-1.,0.,0.));
#22251=DIRECTION('center_axis',(1.,0.,0.));
#22252=DIRECTION('ref_axis',(0.,1.,0.));
#22253=DIRECTION('',(-1.,0.,0.));
#22254=DIRECTION('center_axis',(1.,0.,0.));
#22255=DIRECTION('ref_axis',(0.,1.,0.));
#22256=DIRECTION('',(-1.,0.,0.));
#22257=DIRECTION('center_axis',(1.,0.,0.));
#22258=DIRECTION('ref_axis',(0.,1.,0.));
#22259=DIRECTION('',(-1.,0.,0.));
#22260=DIRECTION('center_axis',(1.,0.,0.));
#22261=DIRECTION('ref_axis',(0.,1.,0.));
#22262=DIRECTION('',(-1.,0.,0.));
#22263=DIRECTION('center_axis',(1.,0.,0.));
#22264=DIRECTION('ref_axis',(0.,1.,0.));
#22265=DIRECTION('',(-1.,0.,0.));
#22266=DIRECTION('center_axis',(1.,0.,0.));
#22267=DIRECTION('ref_axis',(0.,1.,0.));
#22268=DIRECTION('',(-1.,0.,0.));
#22269=DIRECTION('center_axis',(1.,0.,0.));
#22270=DIRECTION('ref_axis',(0.,1.,0.));
#22271=DIRECTION('',(-1.,0.,0.));
#22272=DIRECTION('center_axis',(1.,0.,0.));
#22273=DIRECTION('ref_axis',(0.,1.,0.));
#22274=DIRECTION('',(-1.,0.,0.));
#22275=DIRECTION('center_axis',(1.,0.,0.));
#22276=DIRECTION('ref_axis',(0.,1.,0.));
#22277=DIRECTION('',(-1.,0.,0.));
#22278=DIRECTION('center_axis',(1.,0.,0.));
#22279=DIRECTION('ref_axis',(0.,1.,0.));
#22280=DIRECTION('',(-1.,0.,0.));
#22281=DIRECTION('center_axis',(1.,0.,0.));
#22282=DIRECTION('ref_axis',(0.,1.,0.));
#22283=DIRECTION('',(-1.,0.,0.));
#22284=DIRECTION('center_axis',(1.,0.,0.));
#22285=DIRECTION('ref_axis',(0.,1.,0.));
#22286=DIRECTION('',(-1.,0.,0.));
#22287=DIRECTION('center_axis',(1.,0.,0.));
#22288=DIRECTION('ref_axis',(0.,1.,0.));
#22289=DIRECTION('',(-1.,0.,0.));
#22290=DIRECTION('center_axis',(1.,0.,0.));
#22291=DIRECTION('ref_axis',(0.,1.,0.));
#22292=DIRECTION('',(-1.,0.,0.));
#22293=DIRECTION('center_axis',(1.,0.,0.));
#22294=DIRECTION('ref_axis',(0.,1.,0.));
#22295=DIRECTION('',(-1.,0.,0.));
#22296=DIRECTION('center_axis',(1.,0.,0.));
#22297=DIRECTION('ref_axis',(0.,1.,0.));
#22298=DIRECTION('',(-1.,0.,0.));
#22299=DIRECTION('center_axis',(1.,0.,0.));
#22300=DIRECTION('ref_axis',(0.,1.,0.));
#22301=DIRECTION('',(-1.,0.,0.));
#22302=DIRECTION('center_axis',(1.,0.,0.));
#22303=DIRECTION('ref_axis',(0.,1.,0.));
#22304=DIRECTION('',(-1.,0.,0.));
#22305=DIRECTION('center_axis',(1.,0.,0.));
#22306=DIRECTION('ref_axis',(0.,1.,0.));
#22307=DIRECTION('',(-1.,0.,0.));
#22308=DIRECTION('center_axis',(1.,0.,0.));
#22309=DIRECTION('ref_axis',(0.,1.,0.));
#22310=DIRECTION('',(-1.,0.,0.));
#22311=DIRECTION('center_axis',(1.,0.,0.));
#22312=DIRECTION('ref_axis',(0.,1.,0.));
#22313=DIRECTION('',(-1.,0.,0.));
#22314=DIRECTION('center_axis',(1.,0.,0.));
#22315=DIRECTION('ref_axis',(0.,1.,0.));
#22316=DIRECTION('',(-1.,0.,0.));
#22317=DIRECTION('center_axis',(1.,0.,0.));
#22318=DIRECTION('ref_axis',(0.,1.,0.));
#22319=DIRECTION('',(-1.,0.,0.));
#22320=DIRECTION('center_axis',(1.,0.,0.));
#22321=DIRECTION('ref_axis',(0.,1.,0.));
#22322=DIRECTION('',(-1.,0.,0.));
#22323=DIRECTION('center_axis',(1.,0.,0.));
#22324=DIRECTION('ref_axis',(0.,1.,0.));
#22325=DIRECTION('',(-1.,0.,0.));
#22326=DIRECTION('center_axis',(1.,0.,0.));
#22327=DIRECTION('ref_axis',(0.,1.,0.));
#22328=DIRECTION('',(-1.,0.,0.));
#22329=DIRECTION('center_axis',(1.,0.,0.));
#22330=DIRECTION('ref_axis',(0.,1.,0.));
#22331=DIRECTION('',(-1.,0.,0.));
#22332=DIRECTION('center_axis',(1.,0.,0.));
#22333=DIRECTION('ref_axis',(0.,1.,0.));
#22334=DIRECTION('',(-1.,0.,0.));
#22335=DIRECTION('center_axis',(1.,0.,0.));
#22336=DIRECTION('ref_axis',(0.,1.,0.));
#22337=DIRECTION('',(-1.,0.,0.));
#22338=DIRECTION('center_axis',(1.,0.,0.));
#22339=DIRECTION('ref_axis',(0.,1.,0.));
#22340=DIRECTION('',(-1.,0.,0.));
#22341=DIRECTION('center_axis',(1.,0.,0.));
#22342=DIRECTION('ref_axis',(0.,1.,0.));
#22343=DIRECTION('',(-1.,0.,0.));
#22344=DIRECTION('center_axis',(1.,0.,0.));
#22345=DIRECTION('ref_axis',(0.,1.,0.));
#22346=DIRECTION('',(-1.,0.,0.));
#22347=DIRECTION('center_axis',(1.,0.,0.));
#22348=DIRECTION('ref_axis',(0.,1.,0.));
#22349=DIRECTION('',(-1.,0.,0.));
#22350=DIRECTION('center_axis',(1.,0.,0.));
#22351=DIRECTION('ref_axis',(0.,1.,0.));
#22352=DIRECTION('',(-1.,0.,0.));
#22353=DIRECTION('center_axis',(1.,0.,0.));
#22354=DIRECTION('ref_axis',(0.,1.,0.));
#22355=DIRECTION('',(-1.,0.,0.));
#22356=DIRECTION('center_axis',(1.,0.,0.));
#22357=DIRECTION('ref_axis',(0.,1.,0.));
#22358=DIRECTION('',(-1.,0.,0.));
#22359=DIRECTION('center_axis',(1.,0.,0.));
#22360=DIRECTION('ref_axis',(0.,1.,0.));
#22361=DIRECTION('',(-1.,0.,0.));
#22362=DIRECTION('center_axis',(1.,0.,0.));
#22363=DIRECTION('ref_axis',(0.,1.,0.));
#22364=DIRECTION('',(-1.,0.,0.));
#22365=DIRECTION('center_axis',(1.,0.,0.));
#22366=DIRECTION('ref_axis',(0.,1.,0.));
#22367=DIRECTION('',(-1.,0.,0.));
#22368=DIRECTION('center_axis',(1.,0.,0.));
#22369=DIRECTION('ref_axis',(0.,1.,0.));
#22370=DIRECTION('',(-1.,0.,0.));
#22371=DIRECTION('center_axis',(1.,0.,0.));
#22372=DIRECTION('ref_axis',(0.,1.,0.));
#22373=DIRECTION('',(-1.,0.,0.));
#22374=DIRECTION('center_axis',(1.,0.,0.));
#22375=DIRECTION('ref_axis',(0.,1.,0.));
#22376=DIRECTION('',(-1.,0.,0.));
#22377=DIRECTION('center_axis',(1.,0.,0.));
#22378=DIRECTION('ref_axis',(0.,1.,0.));
#22379=DIRECTION('',(-1.,0.,0.));
#22380=DIRECTION('center_axis',(1.,0.,0.));
#22381=DIRECTION('ref_axis',(0.,1.,0.));
#22382=DIRECTION('',(-1.,0.,0.));
#22383=DIRECTION('center_axis',(1.,0.,0.));
#22384=DIRECTION('ref_axis',(0.,1.,0.));
#22385=DIRECTION('',(-1.,0.,0.));
#22386=DIRECTION('center_axis',(1.,0.,0.));
#22387=DIRECTION('ref_axis',(0.,1.,0.));
#22388=DIRECTION('',(-1.,0.,0.));
#22389=DIRECTION('center_axis',(1.,0.,0.));
#22390=DIRECTION('ref_axis',(0.,1.,0.));
#22391=DIRECTION('',(-1.,0.,0.));
#22392=DIRECTION('center_axis',(1.,0.,0.));
#22393=DIRECTION('ref_axis',(0.,1.,-1.69495320649391E-12));
#22394=DIRECTION('',(1.,0.,0.));
#22395=DIRECTION('center_axis',(1.,0.,0.));
#22396=DIRECTION('ref_axis',(0.,1.,-1.69495320649391E-12));
#22397=DIRECTION('center_axis',(1.,0.,0.));
#22398=DIRECTION('ref_axis',(0.,1.,-1.69495320649391E-12));
#22399=DIRECTION('',(1.,0.,0.));
#22400=DIRECTION('center_axis',(1.,0.,0.));
#22401=DIRECTION('ref_axis',(0.,1.,-1.69495320649391E-12));
#22402=DIRECTION('center_axis',(1.,0.,0.));
#22403=DIRECTION('ref_axis',(0.,1.,-1.69495320649391E-12));
#22404=DIRECTION('',(1.,0.,0.));
#22405=DIRECTION('center_axis',(1.,0.,0.));
#22406=DIRECTION('ref_axis',(0.,1.,-1.69495320649391E-12));
#22407=DIRECTION('',(1.,0.,0.));
#22408=DIRECTION('center_axis',(1.,0.,0.));
#22409=DIRECTION('ref_axis',(0.,1.,-1.69495320649391E-12));
#22410=DIRECTION('',(1.,0.,0.));
#22411=DIRECTION('center_axis',(1.,0.,0.));
#22412=DIRECTION('ref_axis',(0.,1.,-1.69495320649391E-12));
#22413=DIRECTION('',(1.,0.,0.));
#22414=DIRECTION('center_axis',(1.,0.,0.));
#22415=DIRECTION('ref_axis',(0.,1.,-1.69495320649391E-12));
#22416=DIRECTION('',(1.,0.,0.));
#22417=DIRECTION('center_axis',(1.,0.,0.));
#22418=DIRECTION('ref_axis',(0.,1.,-1.69495320649391E-12));
#22419=DIRECTION('',(1.,0.,0.));
#22420=DIRECTION('center_axis',(1.,0.,0.));
#22421=DIRECTION('ref_axis',(0.,1.,-1.69495320649391E-12));
#22422=DIRECTION('',(1.,0.,0.));
#22423=DIRECTION('center_axis',(1.,0.,0.));
#22424=DIRECTION('ref_axis',(0.,1.,-1.69495320649391E-12));
#22425=DIRECTION('',(1.,0.,0.));
#22426=DIRECTION('center_axis',(1.,0.,0.));
#22427=DIRECTION('ref_axis',(0.,1.,-1.69495320649391E-12));
#22428=DIRECTION('',(1.,0.,0.));
#22429=DIRECTION('center_axis',(1.,0.,0.));
#22430=DIRECTION('ref_axis',(0.,1.,-1.69495320649391E-12));
#22431=DIRECTION('',(1.,0.,0.));
#22432=DIRECTION('center_axis',(1.,0.,0.));
#22433=DIRECTION('ref_axis',(0.,1.,-1.69495320649391E-12));
#22434=DIRECTION('',(1.,0.,0.));
#22435=DIRECTION('center_axis',(1.,0.,0.));
#22436=DIRECTION('ref_axis',(0.,1.,-1.69495320649391E-12));
#22437=DIRECTION('',(1.,0.,0.));
#22438=DIRECTION('center_axis',(1.,0.,0.));
#22439=DIRECTION('ref_axis',(0.,1.,-1.69495320649391E-12));
#22440=DIRECTION('',(1.,0.,0.));
#22441=DIRECTION('center_axis',(1.,0.,0.));
#22442=DIRECTION('ref_axis',(0.,1.,-1.69495320649391E-12));
#22443=DIRECTION('',(1.,0.,0.));
#22444=DIRECTION('center_axis',(1.,0.,0.));
#22445=DIRECTION('ref_axis',(0.,1.,-1.69495320649391E-12));
#22446=DIRECTION('',(1.,0.,0.));
#22447=DIRECTION('center_axis',(1.,0.,0.));
#22448=DIRECTION('ref_axis',(0.,1.,-1.69495320649391E-12));
#22449=DIRECTION('',(1.,0.,0.));
#22450=DIRECTION('center_axis',(1.,0.,0.));
#22451=DIRECTION('ref_axis',(0.,1.,-1.69495320649391E-12));
#22452=DIRECTION('',(1.,0.,0.));
#22453=DIRECTION('center_axis',(1.,0.,0.));
#22454=DIRECTION('ref_axis',(0.,1.,-1.69495320649391E-12));
#22455=DIRECTION('',(1.,0.,0.));
#22456=DIRECTION('center_axis',(1.,0.,0.));
#22457=DIRECTION('ref_axis',(0.,1.,-1.69495320649391E-12));
#22458=DIRECTION('',(1.,0.,0.));
#22459=DIRECTION('center_axis',(1.,0.,0.));
#22460=DIRECTION('ref_axis',(0.,1.,-1.69495320649391E-12));
#22461=DIRECTION('',(1.,0.,0.));
#22462=DIRECTION('center_axis',(1.,0.,0.));
#22463=DIRECTION('ref_axis',(0.,1.,-1.69495320649391E-12));
#22464=DIRECTION('',(1.,0.,0.));
#22465=DIRECTION('center_axis',(1.,0.,0.));
#22466=DIRECTION('ref_axis',(0.,1.,-1.69495320649391E-12));
#22467=DIRECTION('',(1.,0.,0.));
#22468=DIRECTION('center_axis',(1.,0.,0.));
#22469=DIRECTION('ref_axis',(0.,1.,-1.69495320649391E-12));
#22470=DIRECTION('',(1.,0.,0.));
#22471=DIRECTION('center_axis',(1.,0.,0.));
#22472=DIRECTION('ref_axis',(0.,1.,-1.69495320649391E-12));
#22473=DIRECTION('',(1.,0.,0.));
#22474=DIRECTION('center_axis',(1.,0.,0.));
#22475=DIRECTION('ref_axis',(0.,1.,-1.69495320649391E-12));
#22476=DIRECTION('',(1.,0.,0.));
#22477=DIRECTION('center_axis',(1.,0.,0.));
#22478=DIRECTION('ref_axis',(0.,1.,-1.69495320649391E-12));
#22479=DIRECTION('',(1.,0.,0.));
#22480=DIRECTION('center_axis',(1.,0.,0.));
#22481=DIRECTION('ref_axis',(0.,1.,-1.69495320649391E-12));
#22482=DIRECTION('',(1.,0.,0.));
#22483=DIRECTION('center_axis',(1.,0.,0.));
#22484=DIRECTION('ref_axis',(0.,1.,-1.69495320649391E-12));
#22485=DIRECTION('',(1.,0.,0.));
#22486=DIRECTION('center_axis',(1.,0.,0.));
#22487=DIRECTION('ref_axis',(0.,1.,-1.69495320649391E-12));
#22488=DIRECTION('',(1.,0.,0.));
#22489=DIRECTION('center_axis',(1.,0.,0.));
#22490=DIRECTION('ref_axis',(0.,1.,-1.69495320649391E-12));
#22491=DIRECTION('',(1.,0.,0.));
#22492=DIRECTION('center_axis',(1.,0.,0.));
#22493=DIRECTION('ref_axis',(0.,1.,-1.69495320649391E-12));
#22494=DIRECTION('',(1.,0.,0.));
#22495=DIRECTION('center_axis',(1.,0.,0.));
#22496=DIRECTION('ref_axis',(0.,1.,-1.69495320649391E-12));
#22497=DIRECTION('',(1.,0.,0.));
#22498=DIRECTION('center_axis',(1.,0.,0.));
#22499=DIRECTION('ref_axis',(0.,1.,-1.69495320649391E-12));
#22500=DIRECTION('',(1.,0.,0.));
#22501=DIRECTION('center_axis',(1.,0.,0.));
#22502=DIRECTION('ref_axis',(0.,1.,-1.69495320649391E-12));
#22503=DIRECTION('',(1.,0.,0.));
#22504=DIRECTION('center_axis',(1.,0.,0.));
#22505=DIRECTION('ref_axis',(0.,1.,-1.69495320649391E-12));
#22506=DIRECTION('',(1.,0.,0.));
#22507=DIRECTION('center_axis',(1.,0.,0.));
#22508=DIRECTION('ref_axis',(0.,1.,-1.69495320649391E-12));
#22509=DIRECTION('',(1.,0.,0.));
#22510=DIRECTION('center_axis',(1.,0.,0.));
#22511=DIRECTION('ref_axis',(0.,1.,-1.69495320649391E-12));
#22512=DIRECTION('',(1.,0.,0.));
#22513=DIRECTION('center_axis',(1.,0.,0.));
#22514=DIRECTION('ref_axis',(0.,1.,-1.69495320649391E-12));
#22515=DIRECTION('',(1.,0.,0.));
#22516=DIRECTION('center_axis',(1.,0.,0.));
#22517=DIRECTION('ref_axis',(0.,1.,-1.69495320649391E-12));
#22518=DIRECTION('',(1.,0.,0.));
#22519=DIRECTION('center_axis',(1.,0.,0.));
#22520=DIRECTION('ref_axis',(0.,1.,-1.69495320649391E-12));
#22521=DIRECTION('',(1.,0.,0.));
#22522=DIRECTION('center_axis',(1.,0.,0.));
#22523=DIRECTION('ref_axis',(0.,1.,-1.69495320649391E-12));
#22524=DIRECTION('',(1.,0.,0.));
#22525=DIRECTION('center_axis',(1.,0.,0.));
#22526=DIRECTION('ref_axis',(0.,1.,-1.69495320649391E-12));
#22527=DIRECTION('',(1.,0.,0.));
#22528=DIRECTION('center_axis',(1.,0.,0.));
#22529=DIRECTION('ref_axis',(0.,1.,-1.69495320649391E-12));
#22530=DIRECTION('',(1.,0.,0.));
#22531=DIRECTION('center_axis',(1.,0.,0.));
#22532=DIRECTION('ref_axis',(0.,1.,-1.69495320649391E-12));
#22533=DIRECTION('',(1.,0.,0.));
#22534=DIRECTION('center_axis',(1.,0.,0.));
#22535=DIRECTION('ref_axis',(0.,1.,-1.69495320649391E-12));
#22536=DIRECTION('',(1.,0.,0.));
#22537=DIRECTION('center_axis',(1.,0.,0.));
#22538=DIRECTION('ref_axis',(0.,1.,-1.69495320649391E-12));
#22539=DIRECTION('',(1.,0.,0.));
#22540=DIRECTION('center_axis',(1.,0.,0.));
#22541=DIRECTION('ref_axis',(0.,1.,-1.69495320649391E-12));
#22542=DIRECTION('',(1.,0.,0.));
#22543=DIRECTION('center_axis',(1.,0.,0.));
#22544=DIRECTION('ref_axis',(0.,1.,-1.69495320649391E-12));
#22545=DIRECTION('',(1.,0.,0.));
#22546=DIRECTION('center_axis',(1.,0.,0.));
#22547=DIRECTION('ref_axis',(0.,1.,-1.69495320649391E-12));
#22548=DIRECTION('',(1.,0.,0.));
#22549=DIRECTION('center_axis',(1.,0.,0.));
#22550=DIRECTION('ref_axis',(0.,1.,-1.69495320649391E-12));
#22551=DIRECTION('',(1.,0.,0.));
#22552=DIRECTION('center_axis',(1.,0.,0.));
#22553=DIRECTION('ref_axis',(0.,1.,-1.69495320649391E-12));
#22554=DIRECTION('',(1.,0.,0.));
#22555=DIRECTION('center_axis',(1.,0.,0.));
#22556=DIRECTION('ref_axis',(0.,1.,-1.69495320649391E-12));
#22557=DIRECTION('',(1.,0.,0.));
#22558=DIRECTION('center_axis',(1.,0.,0.));
#22559=DIRECTION('ref_axis',(0.,1.,-1.69495320649391E-12));
#22560=DIRECTION('',(1.,0.,0.));
#22561=DIRECTION('center_axis',(1.,0.,0.));
#22562=DIRECTION('ref_axis',(0.,1.,-1.69495320649391E-12));
#22563=DIRECTION('',(1.,0.,0.));
#22564=DIRECTION('center_axis',(1.,0.,0.));
#22565=DIRECTION('ref_axis',(0.,1.,-1.69495320649391E-12));
#22566=DIRECTION('',(1.,0.,0.));
#22567=DIRECTION('center_axis',(1.,0.,0.));
#22568=DIRECTION('ref_axis',(0.,1.,-1.69495320649391E-12));
#22569=DIRECTION('',(1.,0.,0.));
#22570=DIRECTION('center_axis',(1.,0.,0.));
#22571=DIRECTION('ref_axis',(0.,1.,-1.69495320649391E-12));
#22572=DIRECTION('',(1.,0.,0.));
#22573=DIRECTION('center_axis',(1.,0.,0.));
#22574=DIRECTION('ref_axis',(0.,1.,-1.69495320649391E-12));
#22575=DIRECTION('',(1.,0.,0.));
#22576=DIRECTION('center_axis',(1.,0.,0.));
#22577=DIRECTION('ref_axis',(0.,1.,-1.69495320649391E-12));
#22578=DIRECTION('',(1.,0.,0.));
#22579=DIRECTION('center_axis',(1.,0.,0.));
#22580=DIRECTION('ref_axis',(0.,1.,-1.69495320649391E-12));
#22581=DIRECTION('',(1.,0.,0.));
#22582=DIRECTION('center_axis',(1.,0.,0.));
#22583=DIRECTION('ref_axis',(0.,1.,-1.69495320649391E-12));
#22584=DIRECTION('',(1.,0.,0.));
#22585=DIRECTION('center_axis',(1.,0.,0.));
#22586=DIRECTION('ref_axis',(0.,1.,-1.69495320649391E-12));
#22587=DIRECTION('',(1.,0.,0.));
#22588=DIRECTION('center_axis',(1.,0.,0.));
#22589=DIRECTION('ref_axis',(0.,1.,-1.69495320649391E-12));
#22590=DIRECTION('',(1.,0.,0.));
#22591=DIRECTION('center_axis',(1.,0.,0.));
#22592=DIRECTION('ref_axis',(0.,1.,-1.69495320649391E-12));
#22593=DIRECTION('',(1.,0.,0.));
#22594=DIRECTION('center_axis',(1.,0.,0.));
#22595=DIRECTION('ref_axis',(0.,1.,-1.69495320649391E-12));
#22596=DIRECTION('',(1.,0.,0.));
#22597=DIRECTION('center_axis',(1.,0.,0.));
#22598=DIRECTION('ref_axis',(0.,1.,-1.69495320649391E-12));
#22599=DIRECTION('',(1.,0.,0.));
#22600=DIRECTION('center_axis',(1.,0.,0.));
#22601=DIRECTION('ref_axis',(0.,1.,-1.69495320649391E-12));
#22602=DIRECTION('',(1.,0.,0.));
#22603=DIRECTION('center_axis',(1.,0.,0.));
#22604=DIRECTION('ref_axis',(0.,1.,-1.69495320649391E-12));
#22605=DIRECTION('',(1.,0.,0.));
#22606=DIRECTION('center_axis',(1.,0.,0.));
#22607=DIRECTION('ref_axis',(0.,1.,-1.69495320649391E-12));
#22608=DIRECTION('',(1.,0.,0.));
#22609=DIRECTION('center_axis',(1.,0.,0.));
#22610=DIRECTION('ref_axis',(0.,1.,-1.69495320649391E-12));
#22611=DIRECTION('',(1.,0.,0.));
#22612=DIRECTION('center_axis',(1.,0.,0.));
#22613=DIRECTION('ref_axis',(0.,1.,-1.69495320649391E-12));
#22614=DIRECTION('',(1.,0.,0.));
#22615=DIRECTION('center_axis',(1.,0.,0.));
#22616=DIRECTION('ref_axis',(0.,1.,-1.69495320649391E-12));
#22617=DIRECTION('',(1.,0.,0.));
#22618=DIRECTION('center_axis',(1.,0.,0.));
#22619=DIRECTION('ref_axis',(0.,1.,-1.69495320649391E-12));
#22620=DIRECTION('',(1.,0.,0.));
#22621=DIRECTION('center_axis',(1.,0.,0.));
#22622=DIRECTION('ref_axis',(0.,1.,-1.69495320649391E-12));
#22623=DIRECTION('',(1.,0.,0.));
#22624=DIRECTION('center_axis',(1.,0.,0.));
#22625=DIRECTION('ref_axis',(0.,1.,-1.69495320649391E-12));
#22626=DIRECTION('',(1.,0.,0.));
#22627=DIRECTION('center_axis',(1.,0.,0.));
#22628=DIRECTION('ref_axis',(0.,1.,-1.69495320649391E-12));
#22629=DIRECTION('',(1.,0.,0.));
#22630=DIRECTION('center_axis',(1.,0.,0.));
#22631=DIRECTION('ref_axis',(0.,1.,-1.69495320649391E-12));
#22632=DIRECTION('',(1.,0.,0.));
#22633=DIRECTION('center_axis',(1.,0.,0.));
#22634=DIRECTION('ref_axis',(0.,1.,-1.69495320649391E-12));
#22635=DIRECTION('',(1.,0.,0.));
#22636=DIRECTION('center_axis',(1.,0.,0.));
#22637=DIRECTION('ref_axis',(0.,1.,-1.69495320649391E-12));
#22638=DIRECTION('',(1.,0.,0.));
#22639=DIRECTION('center_axis',(1.,0.,0.));
#22640=DIRECTION('ref_axis',(0.,1.,-1.69495320649391E-12));
#22641=DIRECTION('',(1.,0.,0.));
#22642=DIRECTION('center_axis',(1.,0.,0.));
#22643=DIRECTION('ref_axis',(0.,1.,-1.69495320649391E-12));
#22644=DIRECTION('',(1.,0.,0.));
#22645=DIRECTION('center_axis',(1.,0.,0.));
#22646=DIRECTION('ref_axis',(0.,1.,-1.69495320649391E-12));
#22647=DIRECTION('',(1.,0.,0.));
#22648=DIRECTION('center_axis',(1.,0.,0.));
#22649=DIRECTION('ref_axis',(0.,1.,-1.69495320649391E-12));
#22650=DIRECTION('',(1.,0.,0.));
#22651=DIRECTION('center_axis',(1.,0.,0.));
#22652=DIRECTION('ref_axis',(0.,1.,-1.69495320649391E-12));
#22653=DIRECTION('',(1.,0.,0.));
#22654=DIRECTION('center_axis',(1.,0.,0.));
#22655=DIRECTION('ref_axis',(0.,1.,-1.69495320649391E-12));
#22656=DIRECTION('',(1.,0.,0.));
#22657=DIRECTION('center_axis',(1.,0.,0.));
#22658=DIRECTION('ref_axis',(0.,1.,-1.69495320649391E-12));
#22659=DIRECTION('',(1.,0.,0.));
#22660=DIRECTION('center_axis',(1.,0.,0.));
#22661=DIRECTION('ref_axis',(0.,0.,-1.));
#22662=DIRECTION('center_axis',(1.,0.,0.));
#22663=DIRECTION('ref_axis',(0.,1.,0.));
#22664=DIRECTION('center_axis',(1.,0.,0.));
#22665=DIRECTION('ref_axis',(0.,1.,0.));
#22666=DIRECTION('center_axis',(-1.,0.,0.));
#22667=DIRECTION('ref_axis',(0.,1.,-1.69495320649391E-12));
#22668=DIRECTION('center_axis',(1.,0.,0.));
#22669=DIRECTION('ref_axis',(0.,1.,-1.69495320649391E-12));
#22670=DIRECTION('center_axis',(-1.,0.,0.));
#22671=DIRECTION('ref_axis',(0.,1.,0.));
#22672=DIRECTION('',(0.500490667348524,0.865741931465162,1.06022808525646E-16));
#22673=DIRECTION('center_axis',(1.,0.,0.));
#22674=DIRECTION('ref_axis',(0.,1.,0.));
#22675=DIRECTION('center_axis',(0.,-0.5,0.866025403784439));
#22676=DIRECTION('ref_axis',(0.,-0.866025403784439,-0.5));
#22677=DIRECTION('',(1.,0.,0.));
#22678=DIRECTION('',(0.,-0.866025403784439,-0.5));
#22679=DIRECTION('',(1.,0.,0.));
#22680=DIRECTION('center_axis',(0.,0.5,0.866025403784439));
#22681=DIRECTION('ref_axis',(0.,-0.866025403784439,0.5));
#22682=DIRECTION('',(1.,0.,0.));
#22683=DIRECTION('',(0.,-0.866025403784439,0.5));
#22684=DIRECTION('center_axis',(0.,1.,-4.43760619934668E-16));
#22685=DIRECTION('ref_axis',(0.,4.43760619934668E-16,1.));
#22686=DIRECTION('',(1.,0.,0.));
#22687=DIRECTION('',(0.,4.43760619934668E-16,1.));
#22688=DIRECTION('center_axis',(1.,0.,0.));
#22689=DIRECTION('ref_axis',(0.,0.,-1.));
#22690=DIRECTION('',(0.,0.866025403784439,0.5));
#22691=DIRECTION('',(0.,0.866025403784439,-0.5));
#22692=DIRECTION('',(0.,1.4792020664489E-16,-1.));
#22693=DIRECTION('center_axis',(-1.,0.,0.));
#22694=DIRECTION('ref_axis',(0.,1.,0.));
#22695=DIRECTION('center_axis',(0.,0.5,-0.866025403784439));
#22696=DIRECTION('ref_axis',(0.,0.866025403784439,0.5));
#22697=DIRECTION('',(1.,0.,0.));
#22698=DIRECTION('center_axis',(0.,-0.5,-0.866025403784439));
#22699=DIRECTION('ref_axis',(0.,0.866025403784439,-0.5));
#22700=DIRECTION('',(1.,0.,0.));
#22701=DIRECTION('center_axis',(0.,-1.,-1.4792020664489E-16));
#22702=DIRECTION('ref_axis',(0.,1.4792020664489E-16,-1.));
#22703=DIRECTION('center_axis',(1.,0.,0.));
#22704=DIRECTION('ref_axis',(0.,0.,-1.));
#22705=DIRECTION('center_axis',(-1.,0.,0.));
#22706=DIRECTION('ref_axis',(0.,0.,1.));
#22707=DIRECTION('center_axis',(1.,0.,0.));
#22708=DIRECTION('ref_axis',(0.,0.,-1.));
#22709=DIRECTION('center_axis',(1.,0.,0.));
#22710=DIRECTION('ref_axis',(0.,1.,0.));
#22711=DIRECTION('',(-0.707106781186552,0.707106781186543,8.65956056235488E-17));
#22712=DIRECTION('center_axis',(1.,0.,0.));
#22713=DIRECTION('ref_axis',(0.,1.,0.));
#44369=CARTESIAN_POINT('',(0.,0.,0.));
#44370=CARTESIAN_POINT('Origin',(-54.75,0.,0.));
#44371=CARTESIAN_POINT('',(-109.162836477965,-3.93801241551785,0.0024295370903759));
#44372=CARTESIAN_POINT('',(-109.346163522035,-3.93703449438079,0.00416483169883862));
#44373=CARTESIAN_POINT('',(-54.75,-3.933,-4.81653586104654E-16));
#44374=CARTESIAN_POINT('',(-109.567,1.75072546723784,3.52562190316238));
#44375=CARTESIAN_POINT('Ctrl Pts',(-109.162836477965,-3.93801241551785,
0.0024295370903759));
#44376=CARTESIAN_POINT('Ctrl Pts',(-109.169080619277,-3.93882021117856,
0.125415509802713));
#44377=CARTESIAN_POINT('Ctrl Pts',(-109.17532476059,-3.93356178335156,0.248326376778116));
#44378=CARTESIAN_POINT('Ctrl Pts',(-109.181568901902,-3.92201207588029,
0.370636940123473));
#44379=CARTESIAN_POINT('Ctrl Pts',(-109.247860079135,-3.79939414225896,
1.66915195227987));
#44380=CARTESIAN_POINT('Ctrl Pts',(-109.314151256367,-2.96768025587816,
2.90000618657311));
#44381=CARTESIAN_POINT('Ctrl Pts',(-109.3804424336,-1.80872165918533,3.49932265847817));
#44382=CARTESIAN_POINT('Ctrl Pts',(-109.442628289066,-0.721535780237971,
4.06152428253533));
#44383=CARTESIAN_POINT('Ctrl Pts',(-109.504814144533,0.653618210307921,
4.06798663531537));
#44384=CARTESIAN_POINT('Ctrl Pts',(-109.567,1.75275645914439,3.52838181187396));
#44385=CARTESIAN_POINT('',(-109.567,-1.74869447532986,3.5228619944515));
#44386=CARTESIAN_POINT('Origin',(-109.567,0.,0.));
#44387=CARTESIAN_POINT('Ctrl Pts',(-109.567,-1.74869447532986,3.5228619944515));
#44388=CARTESIAN_POINT('Ctrl Pts',(-109.500708822768,-2.92256775530673,
2.9401693648038));
#44389=CARTESIAN_POINT('Ctrl Pts',(-109.434417645535,-3.77202868504578,
1.72965923743315));
#44390=CARTESIAN_POINT('Ctrl Pts',(-109.368126468303,-3.91512454167974,
0.435231098702328));
#44391=CARTESIAN_POINT('Ctrl Pts',(-109.360805486213,-3.93092758285667,
0.292278663473746));
#44392=CARTESIAN_POINT('Ctrl Pts',(-109.353484504124,-3.93811560100482,
0.148302741059963));
#44393=CARTESIAN_POINT('Ctrl Pts',(-109.346163522035,-3.93703449438079,
0.00416483169883862));
#44394=CARTESIAN_POINT('Origin',(-54.75,0.,0.));
#44395=CARTESIAN_POINT('',(-107.912836477965,-3.92799297266711,0.00241250680657806));
#44396=CARTESIAN_POINT('',(-108.096163522035,-3.92761091684392,0.00216275952952855));
#44397=CARTESIAN_POINT('',(-54.75,-3.933,-4.81653586104654E-16));
#44398=CARTESIAN_POINT('Ctrl Pts',(-107.912836477965,-3.92799297266711,
0.00241250680657806));
#44399=CARTESIAN_POINT('Ctrl Pts',(-107.938000222549,-3.93076900949478,
0.501336754196634));
#44400=CARTESIAN_POINT('Ctrl Pts',(-107.963163967133,-3.8426867303152,0.9993162840385));
#44401=CARTESIAN_POINT('Ctrl Pts',(-107.988327711717,-3.65926185083382,
1.45927211247531));
#44402=CARTESIAN_POINT('Ctrl Pts',(-108.05461888895,-3.17604874421936,2.67097624657527));
#44403=CARTESIAN_POINT('Ctrl Pts',(-108.120910066182,-2.03115577349008,
3.61879500835267));
#44404=CARTESIAN_POINT('Ctrl Pts',(-108.187201243415,-0.75054268099906,
3.8673339509319));
#44405=CARTESIAN_POINT('Ctrl Pts',(-108.253492420647,0.530070411491968,
4.11587289351112));
#44406=CARTESIAN_POINT('Ctrl Pts',(-108.31978359788,1.94640362574474,3.66513201689217));
#44407=CARTESIAN_POINT('Ctrl Pts',(-108.386074775112,2.84778208996043,2.72211706459808));
#44408=CARTESIAN_POINT('Ctrl Pts',(-108.452365952345,3.74916055417613,1.77910211230399));
#44409=CARTESIAN_POINT('Ctrl Pts',(-108.518657129577,4.13558426835475,0.343813084334772));
#44410=CARTESIAN_POINT('Ctrl Pts',(-108.58494830681,3.82954854862144,-0.924253883068262));
#44411=CARTESIAN_POINT('Ctrl Pts',(-108.651239484042,3.52351282888813,-2.1923208504713));
#44412=CARTESIAN_POINT('Ctrl Pts',(-108.717530661275,2.52501767524288,-3.29316575730815));
#44413=CARTESIAN_POINT('Ctrl Pts',(-108.783821838507,1.29273734961643,-3.72129137538108));
#44414=CARTESIAN_POINT('Ctrl Pts',(-108.85011301574,0.0604570239899871,
-4.149416993454));
#44415=CARTESIAN_POINT('Ctrl Pts',(-108.916404192972,-1.40560847361764,
-3.90482332276299));
#44416=CARTESIAN_POINT('Ctrl Pts',(-108.982695370205,-2.43188023199054,
-3.09943859240772));
#44417=CARTESIAN_POINT('Ctrl Pts',(-109.042742406125,-3.36148473912884,
-2.36991517990962));
#44418=CARTESIAN_POINT('Ctrl Pts',(-109.102789442045,-3.93024421607646,
-1.180270013047));
#44419=CARTESIAN_POINT('Ctrl Pts',(-109.162836477965,-3.93801241551785,
0.0024295370903759));
#44420=CARTESIAN_POINT('Ctrl Pts',(-109.346163522035,-3.93703449438079,
0.00416483169883862));
#44421=CARTESIAN_POINT('Ctrl Pts',(-109.287193326892,-3.92832622712764,
-1.15685981483869));
#44422=CARTESIAN_POINT('Ctrl Pts',(-109.228223131748,-3.38309787307521,
-2.32839455203784));
#44423=CARTESIAN_POINT('Ctrl Pts',(-109.169252936605,-2.48212429262528,
-3.06019835595209));
#44424=CARTESIAN_POINT('Ctrl Pts',(-109.102961759373,-1.469297403408,-3.8828535217847));
#44425=CARTESIAN_POINT('Ctrl Pts',(-109.03667058214,-0.00691284144458862,
-4.14981770335895));
#44426=CARTESIAN_POINT('Ctrl Pts',(-108.970379404908,1.23227169689118,-3.74142213250333));
#44427=CARTESIAN_POINT('Ctrl Pts',(-108.904088227675,2.47145623522696,-3.33302656164771));
#44428=CARTESIAN_POINT('Ctrl Pts',(-108.837797050443,3.48744074993509,-2.24927123836224));
#44429=CARTESIAN_POINT('Ctrl Pts',(-108.77150587321,3.81396665854964,-0.986513452623214));
#44430=CARTESIAN_POINT('Ctrl Pts',(-108.705214695978,4.14049256716419,0.276244333115812));
#44431=CARTESIAN_POINT('Ctrl Pts',(-108.638923518745,3.77755986968516,1.71800458130839));
#44432=CARTESIAN_POINT('Ctrl Pts',(-108.572632341513,2.89164421227576,2.67562232022101));
#44433=CARTESIAN_POINT('Ctrl Pts',(-108.50634116428,2.00572855486636,3.63324005913362));
#44434=CARTESIAN_POINT('Ctrl Pts',(-108.440049987048,0.596829937526585,
4.10671528876627));
#44435=CARTESIAN_POINT('Ctrl Pts',(-108.373758809815,-0.687666737997685,
3.87895524761894));
#44436=CARTESIAN_POINT('Ctrl Pts',(-108.307467632583,-1.97216341352196,
3.65119520647162));
#44437=CARTESIAN_POINT('Ctrl Pts',(-108.24117645535,-3.13225814723073,2.72219989454433));
#44438=CARTESIAN_POINT('Ctrl Pts',(-108.174885278118,-3.63507393339194,
1.51852718954578));
#44439=CARTESIAN_POINT('Ctrl Pts',(-108.148644692757,-3.8341076677211,1.04206746019844));
#44440=CARTESIAN_POINT('Ctrl Pts',(-108.122404107396,-3.9301537168598,0.522569095592642));
#44441=CARTESIAN_POINT('Ctrl Pts',(-108.096163522035,-3.92761091684392,
0.00216275952952855));
#44442=CARTESIAN_POINT('Origin',(-54.75,0.,0.));
#44443=CARTESIAN_POINT('',(-106.662836477965,-3.9292423024608,-0.00304753711075328));
#44444=CARTESIAN_POINT('',(-106.846163522035,-3.92976983246225,-0.00322859656514467));
#44445=CARTESIAN_POINT('',(-54.75,-3.933,-4.81653586104654E-16));
#44446=CARTESIAN_POINT('Ctrl Pts',(-106.662836477965,-3.9292423024608,-0.00304753711075328));
#44447=CARTESIAN_POINT('Ctrl Pts',(-106.706919825821,-3.92295993091212,
0.870298256322931));
#44448=CARTESIAN_POINT('Ctrl Pts',(-106.751003173677,-3.63576905577679,
1.74739404838634));
#44449=CARTESIAN_POINT('Ctrl Pts',(-106.795086521533,-3.10063925105004,
2.43016447487287));
#44450=CARTESIAN_POINT('Ctrl Pts',(-106.861377698765,-2.29592757526039,
3.45689355859143));
#44451=CARTESIAN_POINT('Ctrl Pts',(-106.927668875998,-0.930546250520585,
4.0441905019856));
#44452=CARTESIAN_POINT('Ctrl Pts',(-106.99396005323,0.368247256980288,3.92225124680251));
#44453=CARTESIAN_POINT('Ctrl Pts',(-107.060251230463,1.66704076448116,3.80031199161943));
#44454=CARTESIAN_POINT('Ctrl Pts',(-107.126542407695,2.8992464547431,2.96913653785908));
#44455=CARTESIAN_POINT('Ctrl Pts',(-107.192833584928,3.49878754932471,1.81056630634775));
#44456=CARTESIAN_POINT('Ctrl Pts',(-107.25912476216,4.09832864390631,0.651996074836404));
#44457=CARTESIAN_POINT('Ctrl Pts',(-107.325415939392,4.06520514280758,-0.833968934425934));
#44458=CARTESIAN_POINT('Ctrl Pts',(-107.391707116625,3.41463443053716,-1.96467215928025));
#44459=CARTESIAN_POINT('Ctrl Pts',(-107.457998293857,2.76406371826674,-3.09537538413456));
#44460=CARTESIAN_POINT('Ctrl Pts',(-107.52428947109,1.49604579482464,-3.87081682458085));
#44461=CARTESIAN_POINT('Ctrl Pts',(-107.590580648323,0.193108614131911,
-3.93476300637775));
#44462=CARTESIAN_POINT('Ctrl Pts',(-107.656871825555,-1.10982856656081,
-3.99870918817465));
#44463=CARTESIAN_POINT('Ctrl Pts',(-107.723163002787,-2.44768500450416,
-3.35116011132216));
#44464=CARTESIAN_POINT('Ctrl Pts',(-107.78945418002,-3.20584660222602,-2.28959081968466));
#44465=CARTESIAN_POINT('Ctrl Pts',(-107.830581612668,-3.6762144754277,-1.6309870451541));
#44466=CARTESIAN_POINT('Ctrl Pts',(-107.871709045317,-3.92345583920203,
-0.813025486238145));
#44467=CARTESIAN_POINT('Ctrl Pts',(-107.912836477965,-3.92799297266711,
0.00241250680657806));
#44468=CARTESIAN_POINT('Ctrl Pts',(-108.096163522035,-3.92761091684392,
0.00216275952952855));
#44469=CARTESIAN_POINT('Ctrl Pts',(-108.056112930163,-3.92372988125552,
-0.792125229330703));
#44470=CARTESIAN_POINT('Ctrl Pts',(-108.016062338292,-3.69018182508964,
-1.58852837726987));
#44471=CARTESIAN_POINT('Ctrl Pts',(-107.976011746421,-3.24260701068257,
-2.23724918584132));
#44472=CARTESIAN_POINT('Ctrl Pts',(-107.909720569188,-2.50178746319835,
-3.3110027581601));
#44473=CARTESIAN_POINT('Ctrl Pts',(-107.843429391955,-1.17461152961626,
-3.98015980472787));
#44474=CARTESIAN_POINT('Ctrl Pts',(-107.777138214723,0.129194693027765,
-3.93737157699463));
#44475=CARTESIAN_POINT('Ctrl Pts',(-107.71084703749,1.43300091567179,-3.89458334926139));
#44476=CARTESIAN_POINT('Ctrl Pts',(-107.644555860258,2.71343742737774,-3.13984984722715));
#44477=CARTESIAN_POINT('Ctrl Pts',(-107.578264683026,3.38228103075617,-2.01986321819148));
#44478=CARTESIAN_POINT('Ctrl Pts',(-107.511973505793,4.0511246341346,-0.899876589155813));
#44479=CARTESIAN_POINT('Ctrl Pts',(-107.445682328561,4.10837532918551,0.585363166881283));
#44480=CARTESIAN_POINT('Ctrl Pts',(-107.379391151328,3.52772644721466,1.75351779922835));
#44481=CARTESIAN_POINT('Ctrl Pts',(-107.313099974096,2.94707756524382,2.92167243157543));
#44482=CARTESIAN_POINT('Ctrl Pts',(-107.246808796863,1.72852910625122,3.77274194023248));
#44483=CARTESIAN_POINT('Ctrl Pts',(-107.180517619631,0.431886470594226,
3.91575343066037));
#44484=CARTESIAN_POINT('Ctrl Pts',(-107.114226442398,-0.86475616506276,
4.05876492108826));
#44485=CARTESIAN_POINT('Ctrl Pts',(-107.047935265166,-2.23949297738414,
3.49371839328699));
#44486=CARTESIAN_POINT('Ctrl Pts',(-106.981644087933,-3.06077004551541,
2.48019187083103));
#44487=CARTESIAN_POINT('Ctrl Pts',(-106.9364838993,-3.62025667503408,1.78973726058977));
#44488=CARTESIAN_POINT('Ctrl Pts',(-106.891323710667,-3.92288946057965,
0.891148613896295));
#44489=CARTESIAN_POINT('Ctrl Pts',(-106.846163522035,-3.92976983246225,
-0.00322859656514467));
#44490=CARTESIAN_POINT('Origin',(-54.75,0.,0.));
#44491=CARTESIAN_POINT('',(-105.412836477965,-3.93906449910886,-0.0011929863556448));
#44492=CARTESIAN_POINT('',(-105.596163522035,-3.93929733158332,-0.000812073971306047));
#44493=CARTESIAN_POINT('',(-54.75,-3.933,-4.81653586104654E-16));
#44494=CARTESIAN_POINT('Ctrl Pts',(-105.412836477965,-3.93906449910886,
-0.0011929863556448));
#44495=CARTESIAN_POINT('Ctrl Pts',(-105.475839429093,-3.93412821791734,
1.23897268504913));
#44496=CARTESIAN_POINT('Ctrl Pts',(-105.53884238022,-3.29985743316472,2.48348604357577));
#44497=CARTESIAN_POINT('Ctrl Pts',(-105.601845331348,-2.29134164332814,
3.20459297925897));
#44498=CARTESIAN_POINT('Ctrl Pts',(-105.66813650858,-1.2301897802929,3.96333565434574));
#44499=CARTESIAN_POINT('Ctrl Pts',(-105.734427685813,0.245291424639117,
4.14261130709347));
#44500=CARTESIAN_POINT('Ctrl Pts',(-105.800718863045,1.45726439370239,3.66006053535915));
#44501=CARTESIAN_POINT('Ctrl Pts',(-105.867010040278,2.66923736276567,3.17750976362482));
#44502=CARTESIAN_POINT('Ctrl Pts',(-105.93330121751,3.61770209596021,2.03313256740845));
#44503=CARTESIAN_POINT('Ctrl Pts',(-105.999592394743,3.86693291628907,0.752656973826566));
#44504=CARTESIAN_POINT('Ctrl Pts',(-106.065883571975,4.11616373661792,-0.527818619755315));
#44505=CARTESIAN_POINT('Ctrl Pts',(-106.132174749208,3.66616064408109,-1.9443926107027));
#44506=CARTESIAN_POINT('Ctrl Pts',(-106.19846592644,2.72365553051665,-2.84628939344151));
#44507=CARTESIAN_POINT('Ctrl Pts',(-106.264757103673,1.7811504169522,-3.74818617618033));
#44508=CARTESIAN_POINT('Ctrl Pts',(-106.331048280905,0.346143282360121,
-4.13540575071056));
#44509=CARTESIAN_POINT('Ctrl Pts',(-106.397339458138,-0.922122139650376,
-3.83005915992413));
#44510=CARTESIAN_POINT('Ctrl Pts',(-106.46363063537,-2.19038756166086,-3.52471256913771));
#44511=CARTESIAN_POINT('Ctrl Pts',(-106.529921812603,-3.29191127108978,
-2.52679981303464));
#44512=CARTESIAN_POINT('Ctrl Pts',(-106.596212989835,-3.72065211238448,
-1.29476282296164));
#44513=CARTESIAN_POINT('Ctrl Pts',(-106.618420819212,-3.86428213749116,
-0.882025134426596));
#44514=CARTESIAN_POINT('Ctrl Pts',(-106.640628648588,-3.93240716725033,
-0.443012179332428));
#44515=CARTESIAN_POINT('Ctrl Pts',(-106.662836477965,-3.9292423024608,-0.00304753711075328));
#44516=CARTESIAN_POINT('Ctrl Pts',(-106.846163522035,-3.92976983246225,
-0.00322859656514467));
#44517=CARTESIAN_POINT('Ctrl Pts',(-106.825032533435,-3.93298924017984,
-0.421718315279691));
#44518=CARTESIAN_POINT('Ctrl Pts',(-106.803901544835,-3.87145616371382,
-0.839285975727229));
#44519=CARTESIAN_POINT('Ctrl Pts',(-106.782770556236,-3.74118562589317,
-1.23417777390522));
#44520=CARTESIAN_POINT('Ctrl Pts',(-106.716479379003,-3.3325068141985,-2.47301437907483));
#44521=CARTESIAN_POINT('Ctrl Pts',(-106.650188201771,-2.24733186686799,
-3.48868107230339));
#44522=CARTESIAN_POINT('Ctrl Pts',(-106.583897024538,-0.984191712527803,
-3.81458091516079));
#44523=CARTESIAN_POINT('Ctrl Pts',(-106.517605847306,0.278948441812384,
-4.14048075801819));
#44524=CARTESIAN_POINT('Ctrl Pts',(-106.451314670073,1.72005380316225,-3.77661375050442));
#44525=CARTESIAN_POINT('Ctrl Pts',(-106.385023492841,2.67707932403443,-2.89014003690369));
#44526=CARTESIAN_POINT('Ctrl Pts',(-106.318732315608,3.63410484490661,-2.00366632330296));
#44527=CARTESIAN_POINT('Ctrl Pts',(-106.252441138376,4.1070505253011,-0.594585903615262));
#44528=CARTESIAN_POINT('Ctrl Pts',(-106.186149961143,3.87864450964041,0.689767842792736));
#44529=CARTESIAN_POINT('Ctrl Pts',(-106.119858783911,3.65023849397972,1.97412158920074));
#44530=CARTESIAN_POINT('Ctrl Pts',(-106.053567606678,2.72048078226385,3.13374866232904));
#44531=CARTESIAN_POINT('Ctrl Pts',(-105.987276429446,1.51650308769314,3.63591539972664));
#44532=CARTESIAN_POINT('Ctrl Pts',(-105.920985252213,0.312525393122438,
4.13808213712423));
#44533=CARTESIAN_POINT('Ctrl Pts',(-105.854694074981,-1.1656722843031,3.98278853879111));
#44534=CARTESIAN_POINT('Ctrl Pts',(-105.788402897748,-2.2390044489117,3.24137653441947));
#44535=CARTESIAN_POINT('Ctrl Pts',(-105.724323105844,-3.27653168291185,
2.52469704645246));
#44536=CARTESIAN_POINT('Ctrl Pts',(-105.660243313939,-3.93575441738167,
1.26035117732303));
#44537=CARTESIAN_POINT('Ctrl Pts',(-105.596163522035,-3.93929733158332,
-0.000812073971306047));
#44538=CARTESIAN_POINT('Origin',(-54.75,0.,0.));
#44539=CARTESIAN_POINT('',(-104.162836477965,-3.93287283233362,0.00363418799115139));
#44540=CARTESIAN_POINT('',(-104.346163522035,-3.93222879534157,0.0036280465933886));
#44541=CARTESIAN_POINT('',(-54.75,-3.933,-4.81653586104654E-16));
#44542=CARTESIAN_POINT('Ctrl Pts',(-104.162836477965,-3.93287283233362,
0.00363418799115139));
#44543=CARTESIAN_POINT('Ctrl Pts',(-104.178467855132,-3.93572410183324,
0.312586993871509));
#44544=CARTESIAN_POINT('Ctrl Pts',(-104.194099232299,-3.90239986290354,
0.620931697066951));
#44545=CARTESIAN_POINT('Ctrl Pts',(-104.209730609466,-3.83056314357427,
0.920026454639353));
#44546=CARTESIAN_POINT('Ctrl Pts',(-104.276021786698,-3.52591047976832,
2.18845874770064));
#44547=CARTESIAN_POINT('Ctrl Pts',(-104.342312963931,-2.52860043113539,
3.29052826488843));
#44548=CARTESIAN_POINT('Ctrl Pts',(-104.408604141163,-1.29679825792208,
3.71994313838599));
#44549=CARTESIAN_POINT('Ctrl Pts',(-104.474895318396,-0.0649960847087633,
4.14935801188356));
#44550=CARTESIAN_POINT('Ctrl Pts',(-104.541186495628,1.40129821308494,3.9061182416909));
#44551=CARTESIAN_POINT('Ctrl Pts',(-104.607477672861,2.42846752975822,3.10196842832357));
#44552=CARTESIAN_POINT('Ctrl Pts',(-104.673768850093,3.45563684643151,2.29781861495623));
#44553=CARTESIAN_POINT('Ctrl Pts',(-104.740060027326,4.04368118198438,0.932758758414215));
#44554=CARTESIAN_POINT('Ctrl Pts',(-104.806351204558,3.92245236484942,-0.366101242486227));
#44555=CARTESIAN_POINT('Ctrl Pts',(-104.872642381791,3.80122354771446,-1.66496124338667));
#44556=CARTESIAN_POINT('Ctrl Pts',(-104.938933559023,2.97072157789166,-2.89762138864554));
#44557=CARTESIAN_POINT('Ctrl Pts',(-105.005224736256,1.8124799131427,-3.4977963407172));
#44558=CARTESIAN_POINT('Ctrl Pts',(-105.071515913488,0.654238248393729,
-4.09797129278886));
#44559=CARTESIAN_POINT('Ctrl Pts',(-105.137807090721,-0.83174311128142,
-4.0656610516733));
#44560=CARTESIAN_POINT('Ctrl Pts',(-105.204098267953,-1.96280280406628,
-3.41570897780247));
#44561=CARTESIAN_POINT('Ctrl Pts',(-105.270389445186,-3.09386249685114,
-2.76575690393164));
#44562=CARTESIAN_POINT('Ctrl Pts',(-105.336680622418,-3.87000052274572,
-1.49816299730554));
#44563=CARTESIAN_POINT('Ctrl Pts',(-105.402971799651,-3.93465827512377,
-0.195261195279577));
#44564=CARTESIAN_POINT('Ctrl Pts',(-105.406260025755,-3.93786547882909,
-0.130633655140379));
#44565=CARTESIAN_POINT('Ctrl Pts',(-105.40954825186,-3.93932213162264,-0.065919242222293));
#44566=CARTESIAN_POINT('Ctrl Pts',(-105.412836477965,-3.93906449910886,
-0.0011929863556448));
#44567=CARTESIAN_POINT('Ctrl Pts',(-105.596163522035,-3.93929733158332,
-0.000812073971306047));
#44568=CARTESIAN_POINT('Ctrl Pts',(-105.593952136707,-3.93941959709403,
-0.0443346546021957));
#44569=CARTESIAN_POINT('Ctrl Pts',(-105.591740751379,-3.93876099306918,
-0.0878534449543062));
#44570=CARTESIAN_POINT('Ctrl Pts',(-105.589529366051,-3.93731011969357,
-0.131345805750395));
#44571=CARTESIAN_POINT('Ctrl Pts',(-105.523238188818,-3.8938169740752,-1.43512573113845));
#44572=CARTESIAN_POINT('Ctrl Pts',(-105.456947011586,-3.13836403104679,
-2.7151551715044));
#44573=CARTESIAN_POINT('Ctrl Pts',(-105.390655834354,-2.01800715800226,
-3.38338731833911));
#44574=CARTESIAN_POINT('Ctrl Pts',(-105.324364657121,-0.897650284957724,
-4.05161946517383));
#44575=CARTESIAN_POINT('Ctrl Pts',(-105.258073479888,0.587610518102931,
-4.10805431847731));
#44576=CARTESIAN_POINT('Ctrl Pts',(-105.191782302656,1.7554449186165,-3.52676563254053));
#44577=CARTESIAN_POINT('Ctrl Pts',(-105.125491125424,2.92327931913007,-2.94547694660376));
#44578=CARTESIAN_POINT('Ctrl Pts',(-105.059199948191,3.77368731709656,-1.72646472142674));
#44579=CARTESIAN_POINT('Ctrl Pts',(-104.992908770959,3.9159906024442,-0.429744433298131));
#44580=CARTESIAN_POINT('Ctrl Pts',(-104.926617593726,4.05829388779184,0.866975854830487));
#44581=CARTESIAN_POINT('Ctrl Pts',(-104.860326416494,3.49249246052062,2.24140420591069));
#44582=CARTESIAN_POINT('Ctrl Pts',(-104.794035239261,2.47851607864565,3.06212682895171));
#44583=CARTESIAN_POINT('Ctrl Pts',(-104.727744062029,1.46453969677069,3.88284945199272));
#44584=CARTESIAN_POINT('Ctrl Pts',(-104.661452884796,0.00238836029199191,
4.14986634699456));
#44585=CARTESIAN_POINT('Ctrl Pts',(-104.595161707564,-1.2362241064848,3.7405096758632));
#44586=CARTESIAN_POINT('Ctrl Pts',(-104.528870530331,-2.47483657326161,
3.33115300473184));
#44587=CARTESIAN_POINT('Ctrl Pts',(-104.462579353099,-3.48991017033652,
2.24542276746725));
#44588=CARTESIAN_POINT('Ctrl Pts',(-104.396288175866,-3.81511904469398,
0.982104550990416));
#44589=CARTESIAN_POINT('Ctrl Pts',(-104.379579957922,-3.89708561968762,
0.663694213830095));
#44590=CARTESIAN_POINT('Ctrl Pts',(-104.362871739978,-3.93522812177383,
0.334002493099642));
#44591=CARTESIAN_POINT('Ctrl Pts',(-104.346163522035,-3.93222879534157,
0.0036280465933886));
#44592=CARTESIAN_POINT('Origin',(-54.75,0.,0.));
#44593=CARTESIAN_POINT('',(-102.912836477965,-3.92652662675955,-0.000460690130250907));
#44594=CARTESIAN_POINT('',(-103.096163522035,-3.92662908956275,-0.000809190342590051));
#44595=CARTESIAN_POINT('',(-54.75,-3.933,-4.81653586104654E-16));
#44596=CARTESIAN_POINT('Ctrl Pts',(-102.912836477965,-3.92652662675955,
-0.000460690130250907));
#44597=CARTESIAN_POINT('Ctrl Pts',(-102.947387458404,-3.92581264510619,
0.685223319963354));
#44598=CARTESIAN_POINT('Ctrl Pts',(-102.981938438842,-3.75521499743656,
1.371239773391));
#44599=CARTESIAN_POINT('Ctrl Pts',(-103.016489419281,-3.41678238161711,
1.96093366303795));
#44600=CARTESIAN_POINT('Ctrl Pts',(-103.082780596514,-2.76744924456302,
3.09234879670921));
#44601=CARTESIAN_POINT('Ctrl Pts',(-103.149071773746,-1.50028017576009,
3.86918024857726));
#44602=CARTESIAN_POINT('Ctrl Pts',(-103.215362950979,-0.197413946338789,
3.93455085212624));
#44603=CARTESIAN_POINT('Ctrl Pts',(-103.281654128211,1.10545228308254,3.99992145567523));
#44604=CARTESIAN_POINT('Ctrl Pts',(-103.347945305443,2.44401567312224,3.35383121090512));
#44605=CARTESIAN_POINT('Ctrl Pts',(-103.414236482676,3.20333882817959,2.29309463957116));
#44606=CARTESIAN_POINT('Ctrl Pts',(-103.480527659908,3.96266198323693,1.23235806823722));
#44607=CARTESIAN_POINT('Ctrl Pts',(-103.546818837141,4.14274490331193,-0.243024829660569));
#44608=CARTESIAN_POINT('Ctrl Pts',(-103.613110014373,3.6608573100401,-1.45526163616176));
#44609=CARTESIAN_POINT('Ctrl Pts',(-103.679401191606,3.17896971676828,-2.66749844266296));
#44610=CARTESIAN_POINT('Ctrl Pts',(-103.745692368838,2.03511161014963,-3.61658915776756));
#44611=CARTESIAN_POINT('Ctrl Pts',(-103.811983546071,0.754772578695459,
-3.86652053255643));
#44612=CARTESIAN_POINT('Ctrl Pts',(-103.878274723303,-0.525566452758725,
-4.1164519073453));
#44613=CARTESIAN_POINT('Ctrl Pts',(-103.944565900536,-1.94238640904844,
-3.66722394181842));
#44614=CARTESIAN_POINT('Ctrl Pts',(-104.010857077768,-2.84479874770382,
-2.72521242458757));
#44615=CARTESIAN_POINT('Ctrl Pts',(-104.061516877834,-3.53442337893724,
-2.00532605185032));
#44616=CARTESIAN_POINT('Ctrl Pts',(-104.112176677899,-3.92363214027932,
-0.997652340282243));
#44617=CARTESIAN_POINT('Ctrl Pts',(-104.162836477965,-3.93287283233362,
0.00363418799115139));
#44618=CARTESIAN_POINT('Ctrl Pts',(-104.346163522035,-3.93222879534157,
0.0036280465933886));
#44619=CARTESIAN_POINT('Ctrl Pts',(-104.296580562746,-3.92332805674193,
-0.976784274227112));
#44620=CARTESIAN_POINT('Ctrl Pts',(-104.246997603457,-3.55211073389444,
-1.96320903737145));
#44621=CARTESIAN_POINT('Ctrl Pts',(-104.197414644169,-2.88867477093556,
-2.67866025116411));
#44622=CARTESIAN_POINT('Ctrl Pts',(-104.131123466936,-2.00167747117968,
-3.63520064115272));
#44623=CARTESIAN_POINT('Ctrl Pts',(-104.064832289704,-0.592338720027921,
-4.10737522544087));
#44624=CARTESIAN_POINT('Ctrl Pts',(-103.998541112471,0.691889813476739,
-3.87826651489836));
#44625=CARTESIAN_POINT('Ctrl Pts',(-103.932249935239,1.97611834698141,-3.64915780435585));
#44626=CARTESIAN_POINT('Ctrl Pts',(-103.865958758006,3.13523666283897,-2.71876579898269));
#44627=CARTESIAN_POINT('Ctrl Pts',(-103.799667580774,3.63674461669093,-1.51451354141037));
#44628=CARTESIAN_POINT('Ctrl Pts',(-103.733376403541,4.1382525705429,-0.310261283838064));
#44629=CARTESIAN_POINT('Ctrl Pts',(-103.667085226309,3.98215016238928,1.16785122593339));
#44630=CARTESIAN_POINT('Ctrl Pts',(-103.600794049076,3.24015099882834,2.24077758353109));
#44631=CARTESIAN_POINT('Ctrl Pts',(-103.534502871844,2.4981518352674,3.31370394112879));
#44632=CARTESIAN_POINT('Ctrl Pts',(-103.468211694611,1.17025591629913,3.98144414655273));
#44633=CARTESIAN_POINT('Ctrl Pts',(-103.401920517379,-0.1335000096533,3.93723766385185));
#44634=CARTESIAN_POINT('Ctrl Pts',(-103.335629340146,-1.43725593560575,
3.89303118115098));
#44635=CARTESIAN_POINT('Ctrl Pts',(-103.269338162914,-2.71687186854237,
3.13687801032527));
#44636=CARTESIAN_POINT('Ctrl Pts',(-103.203046985682,-3.38449093516292,
2.0161556943744));
#44637=CARTESIAN_POINT('Ctrl Pts',(-103.167419164466,-3.74329905622377,
1.41382977451589));
#44638=CARTESIAN_POINT('Ctrl Pts',(-103.13179134325,-3.92533404230202,0.706199343721507));
#44639=CARTESIAN_POINT('Ctrl Pts',(-103.096163522035,-3.92662908956275,
-0.000809190342590051));
#44640=CARTESIAN_POINT('Origin',(-54.75,0.,0.));
#44641=CARTESIAN_POINT('',(-101.662836477965,-3.93456922033058,-0.0034735344748954));
#44642=CARTESIAN_POINT('',(-101.846163522035,-3.93520758847436,-0.00334434899688729));
#44643=CARTESIAN_POINT('',(-54.75,-3.933,-4.81653586104654E-16));
#44644=CARTESIAN_POINT('Ctrl Pts',(-101.662836477965,-3.93456922033058,
-0.0034735344748954));
#44645=CARTESIAN_POINT('Ctrl Pts',(-101.716307061675,-3.92483692582627,
1.05219970964738));
#44646=CARTESIAN_POINT('Ctrl Pts',(-101.769777645386,-3.48619833240327,
2.11500422185773));
#44647=CARTESIAN_POINT('Ctrl Pts',(-101.823248229096,-2.72676850018497,
2.84330726805342));
#44648=CARTESIAN_POINT('Ctrl Pts',(-101.889539406329,-1.78525086357474,
3.74623487729314));
#44649=CARTESIAN_POINT('Ctrl Pts',(-101.955830583561,-0.350668299552551,
4.13502456406624));
#44650=CARTESIAN_POINT('Ctrl Pts',(-102.022121760794,0.917930489175272,
3.83106594712348));
#44651=CARTESIAN_POINT('Ctrl Pts',(-102.088412938026,2.18652927790309,3.52710733018071));
#44652=CARTESIAN_POINT('Ctrl Pts',(-102.154704115259,3.28914429133654,2.53040040952208));
#44653=CARTESIAN_POINT('Ctrl Pts',(-102.220995292491,3.71923306031976,1.29883336775382));
#44654=CARTESIAN_POINT('Ctrl Pts',(-102.287286469724,4.14932182930299,0.0672663259855481));
#44655=CARTESIAN_POINT('Ctrl Pts',(-102.353577646956,3.90688435383597,-1.39916083689237));
#44656=CARTESIAN_POINT('Ctrl Pts',(-102.419868824189,3.1032966590433,-2.42676997676681));
#44657=CARTESIAN_POINT('Ctrl Pts',(-102.486160001421,2.29970896425063,-3.45437911664124));
#44658=CARTESIAN_POINT('Ctrl Pts',(-102.552451178654,0.934971050132315,
-4.04317023351221));
#44659=CARTESIAN_POINT('Ctrl Pts',(-102.618742355886,-0.363955084476125,
-3.92265208381421));
#44660=CARTESIAN_POINT('Ctrl Pts',(-102.685033533119,-1.66288121908456,
-3.80213393411621));
#44661=CARTESIAN_POINT('Ctrl Pts',(-102.751324710351,-2.89599557418311,
-2.97230651784925));
#44662=CARTESIAN_POINT('Ctrl Pts',(-102.817615887584,-3.49680414907977,
-1.81439340197853));
#44663=CARTESIAN_POINT('Ctrl Pts',(-102.849356084377,-3.78447112376253,
-1.25998493161789));
#44664=CARTESIAN_POINT('Ctrl Pts',(-102.881096281171,-3.9271825247369,-0.630363087758761));
#44665=CARTESIAN_POINT('Ctrl Pts',(-102.912836477965,-3.92652662675955,
-0.000460690130250907));
#44666=CARTESIAN_POINT('Ctrl Pts',(-103.096163522035,-3.92662908956275,
-0.000809190342590051));
#44667=CARTESIAN_POINT('Ctrl Pts',(-103.065500166018,-3.92774368186336,
-0.609301476630808));
#44668=CARTESIAN_POINT('Ctrl Pts',(-103.034836810001,-3.79497849937131,
-1.21733310439087));
#44669=CARTESIAN_POINT('Ctrl Pts',(-103.004173453984,-3.52580464015748,
-1.75737426679605));
#44670=CARTESIAN_POINT('Ctrl Pts',(-102.937882276752,-2.94387707822704,
-2.92489045093963));
#44671=CARTESIAN_POINT('Ctrl Pts',(-102.871591099519,-1.72439975406168,
-3.7746313581508));
#44672=CARTESIAN_POINT('Ctrl Pts',(-102.805299922287,-0.427601802340093,
-3.91622514327406));
#44673=CARTESIAN_POINT('Ctrl Pts',(-102.739008745054,0.869196149381524,
-4.05781892839732));
#44674=CARTESIAN_POINT('Ctrl Pts',(-102.672717567822,2.24331472865938,-3.49126559143261));
#44675=CARTESIAN_POINT('Ctrl Pts',(-102.606426390589,3.06348244945187,-2.47684031702992));
#44676=CARTESIAN_POINT('Ctrl Pts',(-102.540135213357,3.88365017024434,-1.46241504262724));
#44677=CARTESIAN_POINT('Ctrl Pts',(-102.473844036124,4.14986703255148,-0.000117830786606349));
#44678=CARTESIAN_POINT('Ctrl Pts',(-102.407552858892,3.73983273652221,1.23827047812727));
#44679=CARTESIAN_POINT('Ctrl Pts',(-102.341261681659,3.32979844049294,2.47665878704114));
#44680=CARTESIAN_POINT('Ctrl Pts',(-102.274970504427,2.24351298612724,3.49113819302825));
#44681=CARTESIAN_POINT('Ctrl Pts',(-102.208679327194,0.980017026380408,
3.81565581547556));
#44682=CARTESIAN_POINT('Ctrl Pts',(-102.142388149962,-0.283478933366429,
4.14017343792287));
#44683=CARTESIAN_POINT('Ctrl Pts',(-102.076096972729,-1.72418539849439,
3.7747292768304));
#44684=CARTESIAN_POINT('Ctrl Pts',(-102.009805795497,-2.68024033984199,
2.88720875498287));
#44685=CARTESIAN_POINT('Ctrl Pts',(-101.955258371009,-3.46692624430341,
2.1569161177485));
#44686=CARTESIAN_POINT('Ctrl Pts',(-101.900710946522,-3.92546652330563,
1.07313841850271));
#44687=CARTESIAN_POINT('Ctrl Pts',(-101.846163522035,-3.93520758847436,
-0.00334434899688729));
#44688=CARTESIAN_POINT('Origin',(-54.75,0.,0.));
#44689=CARTESIAN_POINT('',(-100.412836477965,-3.93811660215707,0.00210082759382085));
#44690=CARTESIAN_POINT('',(-100.596163522035,-3.93764551384021,0.00240487699158903));
#44691=CARTESIAN_POINT('',(-54.75,-3.933,-4.81653586104654E-16));
#44692=CARTESIAN_POINT('Ctrl Pts',(-100.412836477965,-3.93811660215707,
0.00210082759382085));
#44693=CARTESIAN_POINT('Ctrl Pts',(-100.418935487715,-3.93889166556813,
0.122231846672544));
#44694=CARTESIAN_POINT('Ctrl Pts',(-100.425034497464,-3.93387331381181,
0.242297225123603));
#44695=CARTESIAN_POINT('Ctrl Pts',(-100.431133507214,-3.92285062854615,
0.361808817307622));
#44696=CARTESIAN_POINT('Ctrl Pts',(-100.497424684447,-3.80304318233601,
1.66080069696202));
#44697=CARTESIAN_POINT('Ctrl Pts',(-100.563715861679,-2.97389056792372,
2.89436889351655));
#44698=CARTESIAN_POINT('Ctrl Pts',(-100.630007038912,-1.81630634760845,
3.4958109110482));
#44699=CARTESIAN_POINT('Ctrl Pts',(-100.696298216144,-0.658722127293182,
4.09725292857986));
#44700=CARTESIAN_POINT('Ctrl Pts',(-100.762589393376,0.827293698925068,
4.06656876708864));
#44701=CARTESIAN_POINT('Ctrl Pts',(-100.828880570609,1.95906393488388,3.41785476186507));
#44702=CARTESIAN_POINT('Ctrl Pts',(-100.895171747841,3.09083417084268,2.76914075664151));
#44703=CARTESIAN_POINT('Ctrl Pts',(-100.961462925074,3.86835881654205,1.50239690768561));
#44704=CARTESIAN_POINT('Ctrl Pts',(-101.027754102307,3.93444225151268,0.199566639692902));
#44705=CARTESIAN_POINT('Ctrl Pts',(-101.094045279539,4.0005256864833,-1.10326362829981));
#44706=CARTESIAN_POINT('Ctrl Pts',(-101.160336456771,3.35516791072517,-2.44218031532932));
#44707=CARTESIAN_POINT('Ctrl Pts',(-101.226627634004,2.29484694896928,-3.20208372079382));
#44708=CARTESIAN_POINT('Ctrl Pts',(-101.292918811236,1.23452598721339,-3.96198712625833));
#44709=CARTESIAN_POINT('Ctrl Pts',(-101.359209988469,-0.240758160540255,
-4.14287725015782));
#44710=CARTESIAN_POINT('Ctrl Pts',(-101.425501165701,-1.45325844223339,
-3.6616529838645));
#44711=CARTESIAN_POINT('Ctrl Pts',(-101.491792342934,-2.6657587239265,-3.1804287175712));
#44712=CARTESIAN_POINT('Ctrl Pts',(-101.558083520166,-3.61547513955912,
-2.03709006108511));
#44713=CARTESIAN_POINT('Ctrl Pts',(-101.624374697399,-3.8661069927763,-0.756887966988903));
#44714=CARTESIAN_POINT('Ctrl Pts',(-101.637195290921,-3.91457873891088,
-0.509299202394739));
#44715=CARTESIAN_POINT('Ctrl Pts',(-101.650015884443,-3.93690272378647,
-0.256591353952766));
#44716=CARTESIAN_POINT('Ctrl Pts',(-101.662836477965,-3.93456922033058,
-0.0034735344748954));
#44717=CARTESIAN_POINT('Ctrl Pts',(-101.846163522035,-3.93520758847436,
-0.00334434899688729));
#44718=CARTESIAN_POINT('Ctrl Pts',(-101.83441976929,-3.9373047848478,-0.235105015511939));
#44719=CARTESIAN_POINT('Ctrl Pts',(-101.822676016544,-3.91859939235631,
-0.466527549826132));
#44720=CARTESIAN_POINT('Ctrl Pts',(-101.810932263799,-3.87788737855351,
-0.694011637814258));
#44721=CARTESIAN_POINT('Ctrl Pts',(-101.744641086567,-3.64807605835022,
-1.9781146261613));
#44722=CARTESIAN_POINT('Ctrl Pts',(-101.678349909334,-2.71705000037639,
-3.1367237202528));
#44723=CARTESIAN_POINT('Ctrl Pts',(-101.612058732102,-1.51252353149032,
-3.6375727127928));
#44724=CARTESIAN_POINT('Ctrl Pts',(-101.545767554869,-0.307997062604245,
-4.13842170533278));
#44725=CARTESIAN_POINT('Ctrl Pts',(-101.479476377637,1.17002981719408,-3.98151059632128));
#44726=CARTESIAN_POINT('Ctrl Pts',(-101.413185200404,2.24255004192927,-3.23892451032891));
#44727=CARTESIAN_POINT('Ctrl Pts',(-101.346894023172,3.31507026666446,-2.49633842433654));
#44728=CARTESIAN_POINT('Ctrl Pts',(-101.280602845939,3.9820838363365,-1.16807736136331));
#44729=CARTESIAN_POINT('Ctrl Pts',(-101.214311668707,3.93716403225775,0.13565418261995));
#44730=CARTESIAN_POINT('Ctrl Pts',(-101.148020491474,3.892244228179,1.43938572660321));
#44731=CARTESIAN_POINT('Ctrl Pts',(-101.081729314242,3.13539105034946,2.71858775159648));
#44732=CARTESIAN_POINT('Ctrl Pts',(-101.015438137009,2.01430362567694,3.38559353404262));
#44733=CARTESIAN_POINT('Ctrl Pts',(-100.949146959777,0.893216201004411,
4.05259931648877));
#44734=CARTESIAN_POINT('Ctrl Pts',(-100.882855782545,-0.592105470511098,
4.10740885638778));
#44735=CARTESIAN_POINT('Ctrl Pts',(-100.816564605312,-1.75930308809024,
3.52484259484059));
#44736=CARTESIAN_POINT('Ctrl Pts',(-100.75027342808,-2.92650070566936,2.94227633329342));
#44737=CARTESIAN_POINT('Ctrl Pts',(-100.683982250847,-3.77557426931215,
1.72233427030002));
#44738=CARTESIAN_POINT('Ctrl Pts',(-100.617691073615,-3.91645851219133,
0.425459042036407));
#44739=CARTESIAN_POINT('Ctrl Pts',(-100.610515223088,-3.93170887144981,
0.285075612773802));
#44740=CARTESIAN_POINT('Ctrl Pts',(-100.603339372561,-3.93866101580183,
0.143790718436667));
#44741=CARTESIAN_POINT('Ctrl Pts',(-100.596163522035,-3.93764551384021,
0.00240487699158903));
#44742=CARTESIAN_POINT('Origin',(-54.75,0.,0.));
#44743=CARTESIAN_POINT('',(-99.162836477965,-3.92804752189454,0.0024429329458453));
#44744=CARTESIAN_POINT('',(-99.3461635220346,-3.92766917194721,0.00216747763683944));
#44745=CARTESIAN_POINT('',(-54.75,-3.933,-4.81653586104654E-16));
#44746=CARTESIAN_POINT('Ctrl Pts',(-99.162836477965,-3.92804752189454,0.0024429329458453));
#44747=CARTESIAN_POINT('Ctrl Pts',(-99.1878550909865,-3.93085117530156,
0.498471328175551));
#44748=CARTESIAN_POINT('Ctrl Pts',(-99.212873704008,-3.8438135452639,0.993552004141601));
#44749=CARTESIAN_POINT('Ctrl Pts',(-99.2378923170294,-3.66244756155688,
1.45125481326075));
#44750=CARTESIAN_POINT('Ctrl Pts',(-99.3041834942619,-3.18188676629823,
2.66401820718217));
#44751=CARTESIAN_POINT('Ctrl Pts',(-99.3704746714944,-2.03906790220586,
3.61436003905749));
#44752=CARTESIAN_POINT('Ctrl Pts',(-99.4367658487269,-0.759003128703129,
3.86569229566779));
#44753=CARTESIAN_POINT('Ctrl Pts',(-99.5030570259594,0.521061644799618,
4.11702455227809));
#44754=CARTESIAN_POINT('Ctrl Pts',(-99.5693482031918,1.93837232771275,3.66934723362335));
#44755=CARTESIAN_POINT('Ctrl Pts',(-99.6356393804243,2.84181493724338,2.72832375949535));
#44756=CARTESIAN_POINT('Ctrl Pts',(-99.7019305576568,3.74525754677402,1.78730028536734));
#44757=CARTESIAN_POINT('Ctrl Pts',(-99.7682217348893,4.13483208292217,0.352930655766074));
#44758=CARTESIAN_POINT('Ctrl Pts',(-99.8345129121218,3.83156760383002,-0.915834248893745));
#44759=CARTESIAN_POINT('Ctrl Pts',(-99.9008040893543,3.52830312473787,-2.18459915355355));
#44760=CARTESIAN_POINT('Ctrl Pts',(-99.9670952665867,2.53219963040542,-3.28775933327191));
#44761=CARTESIAN_POINT('Ctrl Pts',(-100.033386443819,1.30086808876499,-3.71852186894192));
#44762=CARTESIAN_POINT('Ctrl Pts',(-100.099677621052,0.0695365471245464,
-4.14928440461195));
#44763=CARTESIAN_POINT('Ctrl Pts',(-100.165968798284,-1.39702304182386,
-3.90764929623362));
#44764=CARTESIAN_POINT('Ctrl Pts',(-100.232259975517,-2.42507169729408,
-3.10462396066732));
#44765=CARTESIAN_POINT('Ctrl Pts',(-100.292452142999,-3.35853644228551,
-2.37547963846285));
#44766=CARTESIAN_POINT('Ctrl Pts',(-100.352644310482,-3.93046736915652,
-1.18349268955144));
#44767=CARTESIAN_POINT('Ctrl Pts',(-100.412836477965,-3.93811660215707,
0.00210082759382085));
#44768=CARTESIAN_POINT('Ctrl Pts',(-100.596163522035,-3.93764551384021,
0.00240487699158903));
#44769=CARTESIAN_POINT('Ctrl Pts',(-100.537048195329,-3.92927971385468,
-1.16234488717197));
#44770=CARTESIAN_POINT('Ctrl Pts',(-100.477932868623,-3.38018017500286,
-2.33394554618446));
#44771=CARTESIAN_POINT('Ctrl Pts',(-100.418817541917,-2.47516381373419,
-3.0648371521742));
#44772=CARTESIAN_POINT('Ctrl Pts',(-100.352526364685,-1.46028995028229,
-3.88444972458731));
#44773=CARTESIAN_POINT('Ctrl Pts',(-100.286235187452,0.00215269873712037,
-4.14986647587968));
#44774=CARTESIAN_POINT('Ctrl Pts',(-100.21994401022,1.24031647896784,-3.73915467802112));
#44775=CARTESIAN_POINT('Ctrl Pts',(-100.153652832987,2.47848025919858,-3.32844288016256));
#44776=CARTESIAN_POINT('Ctrl Pts',(-100.087361655755,3.49236517064062,-2.24160253315307));
#44777=CARTESIAN_POINT('Ctrl Pts',(-100.021070478522,3.81619144408645,-0.977929208198526));
#44778=CARTESIAN_POINT('Ctrl Pts',(-99.9547793012898,4.14001771753228,0.285744116755994));
#44779=CARTESIAN_POINT('Ctrl Pts',(-99.8884881240572,3.77378535298192,1.72625041965556));
#44780=CARTESIAN_POINT('Ctrl Pts',(-99.8221969468248,2.88574187469724,2.68181962607206));
#44781=CARTESIAN_POINT('Ctrl Pts',(-99.7559057695923,1.99769839641255,3.63738883248858));
#44782=CARTESIAN_POINT('Ctrl Pts',(-99.6896145923599,0.587843804393512,
4.10802094242204));
#44783=CARTESIAN_POINT('Ctrl Pts',(-99.6233234151274,-0.69613325437843,
3.877507081401));
#44784=CARTESIAN_POINT('Ctrl Pts',(-99.5570322378949,-1.98011031315038,
3.64699322037997));
#44785=CARTESIAN_POINT('Ctrl Pts',(-99.4907410606623,-3.13820983867523,
2.71533338840444));
#44786=CARTESIAN_POINT('Ctrl Pts',(-99.4244498834298,-3.63839971997988,
1.51053306875976));
#44787=CARTESIAN_POINT('Ctrl Pts',(-99.3983544296314,-3.83529895277289,
1.03626466095421));
#44788=CARTESIAN_POINT('Ctrl Pts',(-99.372258975833,-3.93024882717627,0.519670536064647));
#44789=CARTESIAN_POINT('Ctrl Pts',(-99.3461635220346,-3.92766917194721,
0.00216747763683944));
#44790=CARTESIAN_POINT('Origin',(-54.75,0.,0.));
#44791=CARTESIAN_POINT('',(-97.912836477965,-3.92917392440496,-0.00302087060105316));
#44792=CARTESIAN_POINT('',(-98.0961635220346,-3.92969678555117,-0.00320611983441186));
#44793=CARTESIAN_POINT('',(-54.75,-3.933,-4.81653586104654E-16));
#44794=CARTESIAN_POINT('Ctrl Pts',(-97.912836477965,-3.92917392440496,-0.00302087060105316));
#44795=CARTESIAN_POINT('Ctrl Pts',(-97.9567746942582,-3.9229741941987,0.867487733808038));
#44796=CARTESIAN_POINT('Ctrl Pts',(-98.0007129105514,-3.63782776715222,
1.74168435746078));
#44797=CARTESIAN_POINT('Ctrl Pts',(-98.0446511268447,-3.10595033290786,
2.42337269186479));
#44798=CARTESIAN_POINT('Ctrl Pts',(-98.1109423040771,-2.30348759695728,
3.45186055517975));
#44799=CARTESIAN_POINT('Ctrl Pts',(-98.1772334813097,-0.939394794011104,
4.04214470581234));
#44800=CARTESIAN_POINT('Ctrl Pts',(-98.2435246585422,0.359662441830008,
3.92304799895481));
#44801=CARTESIAN_POINT('Ctrl Pts',(-98.3098158357747,1.65871967767111,3.80395129209728));
#44802=CARTESIAN_POINT('Ctrl Pts',(-98.3761070130071,2.89274134640716,2.97547372774965));
#44803=CARTESIAN_POINT('Ctrl Pts',(-98.4423981902396,3.49481662652941,1.81821874951834));
#44804=CARTESIAN_POINT('Ctrl Pts',(-98.5086893674721,4.09689190665167,0.660963771287009));
#44805=CARTESIAN_POINT('Ctrl Pts',(-98.5749805447046,4.06702079816011,-0.825068620827995));
#44806=CARTESIAN_POINT('Ctrl Pts',(-98.6412717219371,3.41892611896252,-1.95719362027428));
#44807=CARTESIAN_POINT('Ctrl Pts',(-98.7075628991696,2.77083143976494,-3.08931861972053));
#44808=CARTESIAN_POINT('Ctrl Pts',(-98.773854076402,1.50451318986137,-3.86753622649808));
#44809=CARTESIAN_POINT('Ctrl Pts',(-98.8401452536345,0.201719273305738,
-3.9343324731069));
#44810=CARTESIAN_POINT('Ctrl Pts',(-98.906436430867,-1.10107464324994,-4.00112871971572));
#44811=CARTESIAN_POINT('Ctrl Pts',(-98.9727276080995,-2.44034422645769,
-3.35650360615575));
#44812=CARTESIAN_POINT('Ctrl Pts',(-99.039018785332,-3.20082765484909,-2.29659857139199));
#44813=CARTESIAN_POINT('Ctrl Pts',(-99.080291349543,-3.67430093500554,-1.63670685682111));
#44814=CARTESIAN_POINT('Ctrl Pts',(-99.121563913754,-3.92342240677856,-0.815842388268304));
#44815=CARTESIAN_POINT('Ctrl Pts',(-99.162836477965,-3.92804752189454,0.0024429329458453));
#44816=CARTESIAN_POINT('Ctrl Pts',(-99.3461635220346,-3.92766917194721,
0.00216747763683944));
#44817=CARTESIAN_POINT('Ctrl Pts',(-99.3059677986006,-3.92369564042928,
-0.794960250952785));
#44818=CARTESIAN_POINT('Ctrl Pts',(-99.2657720751666,-3.68832063477402,
-1.5942445423951));
#44819=CARTESIAN_POINT('Ctrl Pts',(-99.2255763517325,-3.23769705223747,
-2.24432182899406));
#44820=CARTESIAN_POINT('Ctrl Pts',(-99.1592851745001,-2.49452426610597,
-3.31643559978938));
#44821=CARTESIAN_POINT('Ctrl Pts',(-99.0929939972675,-1.16589845675849,
-3.98272233406624));
#44822=CARTESIAN_POINT('Ctrl Pts',(-99.026702820035,0.137808314975248,-3.9370892220637));
#44823=CARTESIAN_POINT('Ctrl Pts',(-98.9604116428025,1.441515086709,-3.89145611006115));
#44824=CARTESIAN_POINT('Ctrl Pts',(-98.89412046557,2.72030282082902,-3.1339031517792));
#44825=CARTESIAN_POINT('Ctrl Pts',(-98.8278292883375,3.38669511943069,-2.01245095398391));
#44826=CARTESIAN_POINT('Ctrl Pts',(-98.761538111105,4.05308741803236,-0.89099875618864));
#44827=CARTESIAN_POINT('Ctrl Pts',(-98.6952469338725,4.10708428111567,0.594352681119947));
#44828=CARTESIAN_POINT('Ctrl Pts',(-98.62895575664,3.52387949434503,1.76123138272662));
#44829=CARTESIAN_POINT('Ctrl Pts',(-98.5626645794076,2.94067470757438,2.92811008433328));
#44830=CARTESIAN_POINT('Ctrl Pts',(-98.4963734021752,1.72026827094977,3.77651605023802));
#44831=CARTESIAN_POINT('Ctrl Pts',(-98.4300822249427,0.423316154370067,
3.91669070869985));
#44832=CARTESIAN_POINT('Ctrl Pts',(-98.3637910477102,-0.873635962209635,
4.05686536716169));
#44833=CARTESIAN_POINT('Ctrl Pts',(-98.2974998704777,-2.24713375874445,
3.4888087181806));
#44834=CARTESIAN_POINT('Ctrl Pts',(-98.2312086932452,-3.06619093742357,
2.47348656948608));
#44835=CARTESIAN_POINT('Ctrl Pts',(-98.186193636175,-3.62237212444157,1.78403155637298));
#44836=CARTESIAN_POINT('Ctrl Pts',(-98.1411785791048,-3.92289542988313,
0.888338135617226));
#44837=CARTESIAN_POINT('Ctrl Pts',(-98.0961635220346,-3.92969678555117,
-0.00320611983441186));
#44838=CARTESIAN_POINT('Origin',(-54.75,0.,0.));
#44839=CARTESIAN_POINT('',(-96.662836477965,-3.93902708289076,-0.00124319021292452));
#44840=CARTESIAN_POINT('',(-96.8461635220347,-3.93927071217365,-0.000864176983421456));
#44841=CARTESIAN_POINT('',(-54.75,-3.933,-4.81653586104654E-16));
#44842=CARTESIAN_POINT('Ctrl Pts',(-96.662836477965,-3.93902708289076,-0.00124319021292452));
#44843=CARTESIAN_POINT('Ctrl Pts',(-96.72569429753,-3.9339187179751,1.23609700737983));
#44844=CARTESIAN_POINT('Ctrl Pts',(-96.788552117095,-3.30296517319286,2.47792445112764));
#44845=CARTESIAN_POINT('Ctrl Pts',(-96.85140993666,-2.29834950631729,3.1995706307218));
#44846=CARTESIAN_POINT('Ctrl Pts',(-96.9177011138925,-1.23886071583314,
3.96063385438585));
#44847=CARTESIAN_POINT('Ctrl Pts',(-96.9839922911249,0.236224606744862,
4.14313822324457));
#44848=CARTESIAN_POINT('Ctrl Pts',(-97.0502834683574,1.44925074984827,3.66324104287865));
#44849=CARTESIAN_POINT('Ctrl Pts',(-97.1165746455898,2.66227689295166,3.18334386251274));
#44850=CARTESIAN_POINT('Ctrl Pts',(-97.1828658228224,3.61324385658045,2.04104513292222));
#44851=CARTESIAN_POINT('Ctrl Pts',(-97.2491570000549,3.86527644134641,0.761118063206283));
#44852=CARTESIAN_POINT('Ctrl Pts',(-97.3154481772874,4.11730902611237,-0.518809006509664));
#44853=CARTESIAN_POINT('Ctrl Pts',(-97.3817393545198,3.67040723201546,-1.93636441635105));
#44854=CARTESIAN_POINT('Ctrl Pts',(-97.4480305317523,2.72987820206941,-2.84032175572288));
#44855=CARTESIAN_POINT('Ctrl Pts',(-97.5143217089848,1.78934917212336,-3.74427909509472));
#44856=CARTESIAN_POINT('Ctrl Pts',(-97.5806128862173,0.355192906328163,
-4.13463836399704));
#44857=CARTESIAN_POINT('Ctrl Pts',(-97.6469040634498,-0.913737734453005,
-3.8320681135391));
#44858=CARTESIAN_POINT('Ctrl Pts',(-97.7131952406823,-2.18266837523417,
-3.52949786308117));
#44859=CARTESIAN_POINT('Ctrl Pts',(-97.7794864179148,-3.28637339100131,
-2.53399809326299));
#44860=CARTESIAN_POINT('Ctrl Pts',(-97.8457775951473,-3.71780956440737,
-1.30290242035523));
#44861=CARTESIAN_POINT('Ctrl Pts',(-97.8681305560865,-3.86328708245033,
-0.887784834006066));
#44862=CARTESIAN_POINT('Ctrl Pts',(-97.8904835170257,-3.93232795155548,
-0.445880105072101));
#44863=CARTESIAN_POINT('Ctrl Pts',(-97.912836477965,-3.92917392440496,-0.00302087060105316));
#44864=CARTESIAN_POINT('Ctrl Pts',(-98.0961635220346,-3.92969678555117,
-0.00320611983441186));
#44865=CARTESIAN_POINT('Ctrl Pts',(-98.0748874018724,-3.93291140905446,
-0.424589628899468));
#44866=CARTESIAN_POINT('Ctrl Pts',(-98.0536112817101,-3.87051065061225,
-0.84504624412362));
#44867=CARTESIAN_POINT('Ctrl Pts',(-98.0323351615478,-3.73847550018669,
-1.24236210851359));
#44868=CARTESIAN_POINT('Ctrl Pts',(-97.9660439843153,-3.32708632344723,
-2.48030098941083));
#44869=CARTESIAN_POINT('Ctrl Pts',(-97.8997528070828,-2.23969140914483,
-3.49359110279734));
#44870=CARTESIAN_POINT('Ctrl Pts',(-97.8334616298503,-0.975841097269099,
-3.81672593030297));
#44871=CARTESIAN_POINT('Ctrl Pts',(-97.7671704526178,0.288009214606619,
-4.1398607578086));
#44872=CARTESIAN_POINT('Ctrl Pts',(-97.7008792753852,1.72831492405566,-3.77284029943335));
#44873=CARTESIAN_POINT('Ctrl Pts',(-97.6345880981528,2.68339810948706,-2.88427413055134));
#44874=CARTESIAN_POINT('Ctrl Pts',(-97.5682969209203,3.63848129491847,-1.99570796166933));
#44875=CARTESIAN_POINT('Ctrl Pts',(-97.5020057436879,4.10834195633222,-0.585596082280521));
#44876=CARTESIAN_POINT('Ctrl Pts',(-97.4357145664554,3.87712562349882,0.698254662551813));
#44877=CARTESIAN_POINT('Ctrl Pts',(-97.3694233892229,3.64590929066542,1.98210540738416));
#44878=CARTESIAN_POINT('Ctrl Pts',(-97.3031322119904,2.71361596358488,3.13969501766003));
#44879=CARTESIAN_POINT('Ctrl Pts',(-97.2368410347579,1.50854215384415,3.63922563799522));
#44880=CARTESIAN_POINT('Ctrl Pts',(-97.1705498575254,0.303468344103431,
4.1387562583304));
#44881=CARTESIAN_POINT('Ctrl Pts',(-97.1042586802929,-1.17438594829749,
3.98022788872488));
#44882=CARTESIAN_POINT('Ctrl Pts',(-97.0379675030604,-2.24609294421075,
3.23646862492642));
#44883=CARTESIAN_POINT('Ctrl Pts',(-96.9740328427185,-3.27970293018969,
2.51914849437028));
#44884=CARTESIAN_POINT('Ctrl Pts',(-96.9100981823766,-3.93552781346536,
1.25746548024999));
#44885=CARTESIAN_POINT('Ctrl Pts',(-96.8461635220347,-3.93927071217365,
-0.000864176983421456));
#44886=CARTESIAN_POINT('Origin',(-54.75,0.,0.));
#44887=CARTESIAN_POINT('',(-95.412836477965,-3.93296026185221,0.00363216645671877));
#44888=CARTESIAN_POINT('',(-95.5961635220347,-3.93231500343917,0.00363103561394379));
#44889=CARTESIAN_POINT('',(-54.75,-3.933,-4.81653586104654E-16));
#44890=CARTESIAN_POINT('Ctrl Pts',(-95.412836477965,-3.93296026185221,0.00363216645671877));
#44891=CARTESIAN_POINT('Ctrl Pts',(-95.4283227235693,-3.93578918688,0.309699076233004));
#44892=CARTESIAN_POINT('Ctrl Pts',(-95.4438089691735,-3.90308854705616,
0.615168125721136));
#44893=CARTESIAN_POINT('Ctrl Pts',(-95.4592952147778,-3.83256747610089,
0.911640946480624));
#44894=CARTESIAN_POINT('Ctrl Pts',(-95.5255863920103,-3.53069154485299,
2.18073694352288));
#44895=CARTESIAN_POINT('Ctrl Pts',(-95.5918775692427,-2.53579579755656,
3.28498646493961));
#44896=CARTESIAN_POINT('Ctrl Pts',(-95.6581687464752,-1.30493636191566,
3.71709614692932));
#44897=CARTESIAN_POINT('Ctrl Pts',(-95.7244599237077,-0.0740769262747676,
4.14920582891902));
#44898=CARTESIAN_POINT('Ctrl Pts',(-95.7907511009402,1.39274619771061,3.90917567148172));
#44899=CARTESIAN_POINT('Ctrl Pts',(-95.8570422781727,2.42167296098772,3.10727577536778));
#44900=CARTESIAN_POINT('Ctrl Pts',(-95.9233334554052,3.45059972426483,2.30537587925383));
#44901=CARTESIAN_POINT('Ctrl Pts',(-95.9896246326377,4.0416301268337,0.941606244463238));
#44902=CARTESIAN_POINT('Ctrl Pts',(-96.0559158098702,3.92324419498091,-0.357515958685805));
#44903=CARTESIAN_POINT('Ctrl Pts',(-96.1222069871026,3.80485826312812,-1.65663816183485));
#44904=CARTESIAN_POINT('Ctrl Pts',(-96.1884981643351,2.97705599685373,-2.89111293334231));
#44905=CARTESIAN_POINT('Ctrl Pts',(-96.2547893415676,1.82013060713598,-3.49382129582113));
#44906=CARTESIAN_POINT('Ctrl Pts',(-96.3210805188001,0.663205217418252,
-4.09652965829995));
#44907=CARTESIAN_POINT('Ctrl Pts',(-96.3873716960326,-0.822843295742819,
-4.0674716117501));
#44908=CARTESIAN_POINT('Ctrl Pts',(-96.4536628732651,-1.9553227197697,-3.41999645258864));
#44909=CARTESIAN_POINT('Ctrl Pts',(-96.5199540504975,-3.0878021437966,-2.77252129342716));
#44910=CARTESIAN_POINT('Ctrl Pts',(-96.58624522773,-3.86671247868932,-1.50662902165405));
#44911=CARTESIAN_POINT('Ctrl Pts',(-96.6525364049625,-3.93422151694052,
-0.203871846532809));
#44912=CARTESIAN_POINT('Ctrl Pts',(-96.65596976263,-3.93771795015805,-0.136399348338936));
#44913=CARTESIAN_POINT('Ctrl Pts',(-96.6594031202975,-3.93930610694812,
-0.0688279630241185));
#44914=CARTESIAN_POINT('Ctrl Pts',(-96.662836477965,-3.93902708289076,-0.00124319021292452));
#44915=CARTESIAN_POINT('Ctrl Pts',(-96.8461635220347,-3.93927071217365,
-0.000864176983421456));
#44916=CARTESIAN_POINT('Ctrl Pts',(-96.8438070051441,-3.93940866870581,
-0.0472439508851525));
#44917=CARTESIAN_POINT('Ctrl Pts',(-96.8414504882536,-3.93866075402094,
-0.0936191691598041));
#44918=CARTESIAN_POINT('Ctrl Pts',(-96.839093971363,-3.93701323328378,-0.139962406076981));
#44919=CARTESIAN_POINT('Ctrl Pts',(-96.7728027941305,-3.89066682701792,
-1.44364401529055));
#44920=CARTESIAN_POINT('Ctrl Pts',(-96.706511616898,-3.13241431506057,-2.72201707572629));
#44921=CARTESIAN_POINT('Ctrl Pts',(-96.6402204396655,-2.01059767985446,
-3.38779569099589));
#44922=CARTESIAN_POINT('Ctrl Pts',(-96.573929262433,-0.888781044648358,
-4.05357430626548));
#44923=CARTESIAN_POINT('Ctrl Pts',(-96.5076380852006,0.596599713806542,
-4.1067584763689));
#44924=CARTESIAN_POINT('Ctrl Pts',(-96.4413469079681,1.76315915013021,-3.52291533895985));
#44925=CARTESIAN_POINT('Ctrl Pts',(-96.3750557307357,2.92971858645389,-2.93907220155078));
#44926=CARTESIAN_POINT('Ctrl Pts',(-96.3087645535031,3.77745670064637,-1.71820175662924));
#44927=CARTESIAN_POINT('Ctrl Pts',(-96.2424733762706,3.91692173272892,-0.421173139982053));
#44928=CARTESIAN_POINT('Ctrl Pts',(-96.1761821990382,4.05638676481147,0.875855476665131));
#44929=CARTESIAN_POINT('Ctrl Pts',(-96.1098910218057,3.48757871478409,2.24904226503793));
#44930=CARTESIAN_POINT('Ctrl Pts',(-96.0435998445732,2.47180858478833,3.06754380479451));
#44931=CARTESIAN_POINT('Ctrl Pts',(-95.9773086673407,1.45603845479257,3.88604534455109));
#44932=CARTESIAN_POINT('Ctrl Pts',(-95.9110174901082,-0.00669375517154278,
4.14986163569144));
#44933=CARTESIAN_POINT('Ctrl Pts',(-95.8447263128757,-1.24440736615255,
3.73779520322231));
#44934=CARTESIAN_POINT('Ctrl Pts',(-95.7784351356432,-2.48212097713351,
3.3257287707532));
#44935=CARTESIAN_POINT('Ctrl Pts',(-95.7121439584108,-3.4948159891314,2.23777961467462));
#44936=CARTESIAN_POINT('Ctrl Pts',(-95.6458527811783,-3.81725927396492,
0.973752694217182));
#44937=CARTESIAN_POINT('Ctrl Pts',(-95.6292896947971,-3.8978228753777,0.657931072913059));
#44938=CARTESIAN_POINT('Ctrl Pts',(-95.6127266084159,-3.93529627055665,
0.331117480300956));
#44939=CARTESIAN_POINT('Ctrl Pts',(-95.5961635220347,-3.93231500343917,
0.00363103561394379));
#44940=CARTESIAN_POINT('Origin',(-54.75,0.,0.));
#44941=CARTESIAN_POINT('',(-94.162836477965,-3.92651713604259,-0.000413326683059989));
#44942=CARTESIAN_POINT('',(-94.3461635220346,-3.92661200070631,-0.000762584109358684));
#44943=CARTESIAN_POINT('',(-54.75,-3.933,-4.81653586104654E-16));
#44944=CARTESIAN_POINT('Ctrl Pts',(-94.162836477965,-3.92651713604259,-0.000413326683059989));
#44945=CARTESIAN_POINT('Ctrl Pts',(-94.197242326841,-3.92587933456817,0.682394578314803));
#44946=CARTESIAN_POINT('Ctrl Pts',(-94.231648175717,-3.75679084115549,1.36549820367841));
#44947=CARTESIAN_POINT('Ctrl Pts',(-94.266054024593,-3.42106576242298,1.95345123393027));
#44948=CARTESIAN_POINT('Ctrl Pts',(-94.3323452018255,-2.7742103171223,3.08628474352482));
#44949=CARTESIAN_POINT('Ctrl Pts',(-94.398636379058,-1.50874440243043,3.86588757336226));
#44950=CARTESIAN_POINT('Ctrl Pts',(-94.4649275562905,-0.206024358730012,
3.93410938304673));
#44951=CARTESIAN_POINT('Ctrl Pts',(-94.531218733523,1.09669568497042,4.0023311927312));
#44952=CARTESIAN_POINT('Ctrl Pts',(-94.5975099107554,2.43666985767939,3.35917198226269));
#44953=CARTESIAN_POINT('Ctrl Pts',(-94.6638010879879,3.19831264878829,2.300099753221));
#44954=CARTESIAN_POINT('Ctrl Pts',(-94.7300922652204,3.95995543989718,1.24102752417931));
#44955=CARTESIAN_POINT('Ctrl Pts',(-94.796383442453,4.14326684940601,-0.233957723435546));
#44956=CARTESIAN_POINT('Ctrl Pts',(-94.8626746196855,3.66403342759226,-1.44724625259593));
#44957=CARTESIAN_POINT('Ctrl Pts',(-94.928965796918,3.18480000577852,-2.66053478175629));
#44958=CARTESIAN_POINT('Ctrl Pts',(-94.9952569741504,2.04302175264223,-3.61212659246219));
#44959=CARTESIAN_POINT('Ctrl Pts',(-95.0615481513829,0.763232769865172,
-3.86485942993667));
#44960=CARTESIAN_POINT('Ctrl Pts',(-95.1278393286153,-0.516556212911885,
-4.11759226741114));
#44961=CARTESIAN_POINT('Ctrl Pts',(-95.1941305058479,-1.93435592532971,
-3.67146613165418));
#44962=CARTESIAN_POINT('Ctrl Pts',(-95.2604216830804,-2.83882772393893,
-2.73143182744182));
#44963=CARTESIAN_POINT('Ctrl Pts',(-95.3112266147086,-3.53200636107257,
-2.01099842216069));
#44964=CARTESIAN_POINT('Ctrl Pts',(-95.3620315463368,-3.92367955261569,
-1.00046584556025));
#44965=CARTESIAN_POINT('Ctrl Pts',(-95.412836477965,-3.93296026185221,0.00363216645671877));
#44966=CARTESIAN_POINT('Ctrl Pts',(-95.5961635220347,-3.93231500343917,
0.00363103561394379));
#44967=CARTESIAN_POINT('Ctrl Pts',(-95.5464354311834,-3.92336421258671,
-0.979596081550714));
#44968=CARTESIAN_POINT('Ctrl Pts',(-95.4967073403321,-3.54975216954202,
-1.96888833598873));
#44969=CARTESIAN_POINT('Ctrl Pts',(-95.4469792494808,-2.88280552298465,
-2.68497578961443));
#44970=CARTESIAN_POINT('Ctrl Pts',(-95.3806880722483,-1.9937169295017,-3.63957266815216));
#44971=CARTESIAN_POINT('Ctrl Pts',(-95.3143968950158,-0.583348184866643,
-4.10866174039123));
#44972=CARTESIAN_POINT('Ctrl Pts',(-95.2481057177833,0.700375861699437,
-3.87674300496115));
#44973=CARTESIAN_POINT('Ctrl Pts',(-95.1818145405509,1.98409990826552,-3.64482426953107));
#44974=CARTESIAN_POINT('Ctrl Pts',(-95.1155233633184,3.14117925676262,-2.71189772643183));
#44975=CARTESIAN_POINT('Ctrl Pts',(-95.049232186086,3.64005046659153,-1.50655078733948));
#44976=CARTESIAN_POINT('Ctrl Pts',(-94.9829410088535,4.13892167642045,-0.30120384824712));
#44977=CARTESIAN_POINT('Ctrl Pts',(-94.916649831621,3.97958474758117,1.17656348683836));
#44978=CARTESIAN_POINT('Ctrl Pts',(-94.8503586543885,3.23523922876354,2.24786338704912));
#44979=CARTESIAN_POINT('Ctrl Pts',(-94.784067477156,2.49089370994594,3.31916328725984));
#44980=CARTESIAN_POINT('Ctrl Pts',(-94.7177762999235,1.16153960115003,3.98399575259588));
#44981=CARTESIAN_POINT('Ctrl Pts',(-94.651485122691,-0.14211645528021,3.93693606594075));
#44982=CARTESIAN_POINT('Ctrl Pts',(-94.5851939454585,-1.44577251171053,
3.88987637928562));
#44983=CARTESIAN_POINT('Ctrl Pts',(-94.5189027682261,-2.72373051577518,
3.13092454063924));
#44984=CARTESIAN_POINT('Ctrl Pts',(-94.4526115909936,-3.3888952484088,2.00874380384326));
#44985=CARTESIAN_POINT('Ctrl Pts',(-94.4171289013406,-3.74492805339839,
1.40809085905339));
#44986=CARTESIAN_POINT('Ctrl Pts',(-94.3816462116876,-3.92539680852964,
0.703373559516597));
#44987=CARTESIAN_POINT('Ctrl Pts',(-94.3461635220346,-3.92661200070631,
-0.000762584109358684));
#44988=CARTESIAN_POINT('Origin',(-54.75,0.,0.));
#44989=CARTESIAN_POINT('',(-92.912836477965,-3.93448228467576,-0.0034881012485255));
#44990=CARTESIAN_POINT('',(-93.0961635220346,-3.9351223687927,-0.00336391575034791));
#44991=CARTESIAN_POINT('',(-54.75,-3.933,-4.81653586104654E-16));
#44992=CARTESIAN_POINT('Ctrl Pts',(-92.912836477965,-3.93448228467576,-0.0034881012485255));
#44993=CARTESIAN_POINT('Ctrl Pts',(-92.9661619301128,-3.92475942763249,
1.04937969788364));
#44994=CARTESIAN_POINT('Ctrl Pts',(-93.0194873822606,-3.48876179764117,
2.10935079459708));
#44995=CARTESIAN_POINT('Ctrl Pts',(-93.0728128344084,-2.73298463514744,
2.83733284233882));
#44996=CARTESIAN_POINT('Ctrl Pts',(-93.1391040116408,-1.79344533807233,
3.74231882942762));
#44997=CARTESIAN_POINT('Ctrl Pts',(-93.2053951888733,-0.359717087789233,
4.13424721303581));
#44998=CARTESIAN_POINT('Ctrl Pts',(-93.2716863661058,0.909543885604364,
3.83306569136588));
#44999=CARTESIAN_POINT('Ctrl Pts',(-93.3379775433383,2.17880485899794,3.53188416969595));
#45000=CARTESIAN_POINT('Ctrl Pts',(-93.4042687205708,3.28359855550202,2.53759274274792));
#45001=CARTESIAN_POINT('Ctrl Pts',(-93.4705598978033,3.71638161672134,1.30696991283736));
#45002=CARTESIAN_POINT('Ctrl Pts',(-93.5368510750358,4.14916467794067,0.0763470829267855));
#45003=CARTESIAN_POINT('Ctrl Pts',(-93.6031422522682,3.90993710387521,-1.39060714994632));
#45004=CARTESIAN_POINT('Ctrl Pts',(-93.6694334295007,3.10860028765036,-2.41997250517161));
#45005=CARTESIAN_POINT('Ctrl Pts',(-93.7357246067331,2.3072634714255,-3.4493378603969));
#45006=CARTESIAN_POINT('Ctrl Pts',(-93.8020157839657,0.943817413041241,
-4.04111433797437));
#45007=CARTESIAN_POINT('Ctrl Pts',(-93.8683069611982,-0.355369368517493,
-3.92343921656573));
#45008=CARTESIAN_POINT('Ctrl Pts',(-93.9345981384307,-1.65455615007621,
-3.80576409515709));
#45009=CARTESIAN_POINT('Ctrl Pts',(-94.0008893156632,-2.8894836548094,-2.97863737476235));
#45010=CARTESIAN_POINT('Ctrl Pts',(-94.0671804928956,-3.49282491922127,
-1.82204191988916));
#45011=CARTESIAN_POINT('Ctrl Pts',(-94.0990658212521,-3.78302544257763,
-1.26573220577906));
#45012=CARTESIAN_POINT('Ctrl Pts',(-94.1309511496085,-3.92710821314438,
-0.633199755923574));
#45013=CARTESIAN_POINT('Ctrl Pts',(-94.162836477965,-3.92651713604259,-0.000413326683059989));
#45014=CARTESIAN_POINT('Ctrl Pts',(-94.3461635220346,-3.92661200070631,
-0.000762584109358684));
#45015=CARTESIAN_POINT('Ctrl Pts',(-94.3153550344551,-3.92766711331045,
-0.612141536701368));
#45016=CARTESIAN_POINT('Ctrl Pts',(-94.2845465468755,-3.79358484768176,
-1.22308236195667));
#45017=CARTESIAN_POINT('Ctrl Pts',(-94.253738059296,-3.52195012897364,-1.76508638972403));
#45018=CARTESIAN_POINT('Ctrl Pts',(-94.1874468820636,-2.93746881570228,
-2.93132621154973));
#45019=CARTESIAN_POINT('Ctrl Pts',(-94.1211557048312,-1.71613472795704,
-3.77839622025559));
#45020=CARTESIAN_POINT('Ctrl Pts',(-94.0548645275987,-0.419029999513912,
-3.91715158420935));
#45021=CARTESIAN_POINT('Ctrl Pts',(-93.9885733503663,0.878074728929215,
-4.05590694816311));
#45022=CARTESIAN_POINT('Ctrl Pts',(-93.9222821731337,2.25095009807022,-3.48634766736474));
#45023=CARTESIAN_POINT('Ctrl Pts',(-93.8559909959012,3.06889575388203,-2.47012986014325));
#45024=CARTESIAN_POINT('Ctrl Pts',(-93.7896998186686,3.88684140969384,-1.45391205292175));
#45025=CARTESIAN_POINT('Ctrl Pts',(-93.7234086414362,4.14985735217646,0.00896428072286667));
#45026=CARTESIAN_POINT('Ctrl Pts',(-93.6571174642038,3.73711378733167,1.24645225127237));
#45027=CARTESIAN_POINT('Ctrl Pts',(-93.5908262869713,3.32437022248691,2.48394022182179));
#45028=CARTESIAN_POINT('Ctrl Pts',(-93.5245351097388,2.23586715031477,3.49603982927613));
#45029=CARTESIAN_POINT('Ctrl Pts',(-93.4582439325063,0.971663999667894,
3.81779147491267));
#45030=CARTESIAN_POINT('Ctrl Pts',(-93.3919527552738,-0.292539150979056,
4.13954312054923));
#45031=CARTESIAN_POINT('Ctrl Pts',(-93.3256615780413,-1.73244238010076,
3.77094680436794));
#45032=CARTESIAN_POINT('Ctrl Pts',(-93.2593704008089,-2.68655266598184,
2.88133605243684));
#45033=CARTESIAN_POINT('Ctrl Pts',(-93.2049681078841,-3.46954958083475,
2.15127110660222));
#45034=CARTESIAN_POINT('Ctrl Pts',(-93.1505658149594,-3.92537598800762,
1.07031477828723));
#45035=CARTESIAN_POINT('Ctrl Pts',(-93.0961635220346,-3.9351223687927,-0.00336391575034791));
#45036=CARTESIAN_POINT('Origin',(-54.75,0.,0.));
#45037=CARTESIAN_POINT('',(-91.662836477965,-3.93817602267047,0.00205778069578805));
#45038=CARTESIAN_POINT('',(-91.8461635220346,-3.93771195638885,0.00236553390519242));
#45039=CARTESIAN_POINT('',(-54.75,-3.933,-4.81653586104654E-16));
#45040=CARTESIAN_POINT('Ctrl Pts',(-91.662836477965,-3.93817602267047,0.00205778069578805));
#45041=CARTESIAN_POINT('Ctrl Pts',(-91.6687903561521,-3.93892001361361,
0.11932550450386));
#45042=CARTESIAN_POINT('Ctrl Pts',(-91.6747442343391,-3.93413809733793,
0.236531698311863));
#45043=CARTESIAN_POINT('Ctrl Pts',(-91.6806981125262,-3.92363306365089,
0.353222671967719));
#45044=CARTESIAN_POINT('Ctrl Pts',(-91.7469892897586,-3.80666878791298,
1.65247364301858));
#45045=CARTESIAN_POINT('Ctrl Pts',(-91.8132804669911,-2.9802178610021,2.88785351129623));
#45046=CARTESIAN_POINT('Ctrl Pts',(-91.8795716442236,-1.82395268720563,
3.49182749702814));
#45047=CARTESIAN_POINT('Ctrl Pts',(-91.9458628214561,-0.667687513409183,
4.09580148276003));
#45048=CARTESIAN_POINT('Ctrl Pts',(-92.0121539986886,0.818391907272832,
4.06836958594621));
#45049=CARTESIAN_POINT('Ctrl Pts',(-92.0784451759211,1.95157916331609,3.42213404814553));
#45050=CARTESIAN_POINT('Ctrl Pts',(-92.1447363531536,3.0847664193594,2.77589851034481));
#45051=CARTESIAN_POINT('Ctrl Pts',(-92.2110275303861,3.8650615107639,1.51085933155719));
#45052=CARTESIAN_POINT('Ctrl Pts',(-92.2773187076185,3.93399607145912,0.208176809252815));
#45053=CARTESIAN_POINT('Ctrl Pts',(-92.343609884851,4.00293063215433,-1.09450571305151));
#45054=CARTESIAN_POINT('Ctrl Pts',(-92.4099010620835,3.36050466214028,-2.43483157887261));
#45055=CARTESIAN_POINT('Ctrl Pts',(-92.476192239316,2.30184931157926,-3.19705370942506));
#45056=CARTESIAN_POINT('Ctrl Pts',(-92.5424834165485,1.24319396101821,-3.95927583997753));
#45057=CARTESIAN_POINT('Ctrl Pts',(-92.608774593781,-0.231690770089837,
-4.14339423526136));
#45058=CARTESIAN_POINT('Ctrl Pts',(-92.6750657710135,-1.44524132210368,
-3.66482471546054));
#45059=CARTESIAN_POINT('Ctrl Pts',(-92.741356948246,-2.6587918741175,-3.18625519565973));
#45060=CARTESIAN_POINT('Ctrl Pts',(-92.8076481254784,-3.61100824703711,
-2.04499776077428));
#45061=CARTESIAN_POINT('Ctrl Pts',(-92.8739393027109,-3.86444126156338,
-0.765347248046856));
#45062=CARTESIAN_POINT('Ctrl Pts',(-92.8869050277956,-3.91400958921899,
-0.515063613856148));
#45063=CARTESIAN_POINT('Ctrl Pts',(-92.8998707528803,-3.93684633198119,
-0.259485826242128));
#45064=CARTESIAN_POINT('Ctrl Pts',(-92.912836477965,-3.93448228467576,-0.0034881012485255));
#45065=CARTESIAN_POINT('Ctrl Pts',(-93.0961635220346,-3.9351223687927,-0.00336391575034791));
#45066=CARTESIAN_POINT('Ctrl Pts',(-93.0842746377269,-3.93725230831076,
-0.238001852698556));
#45067=CARTESIAN_POINT('Ctrl Pts',(-93.0723857534191,-3.91807827642478,
-0.472292223059233));
#45068=CARTESIAN_POINT('Ctrl Pts',(-93.0604968691114,-3.87635922590254,
-0.702496851186307));
#45069=CARTESIAN_POINT('Ctrl Pts',(-92.9942056918789,-3.64373815730172,
-1.98609381519739));
#45070=CARTESIAN_POINT('Ctrl Pts',(-92.9279145146464,-2.71017867745966,
-3.14266255553868));
#45071=CARTESIAN_POINT('Ctrl Pts',(-92.8616233374139,-1.50455896984186,
-3.64087420552191));
#45072=CARTESIAN_POINT('Ctrl Pts',(-92.7953321601814,-0.29893926222404,
-4.13908585550516));
#45073=CARTESIAN_POINT('Ctrl Pts',(-92.729040982949,1.17874067316951,-3.97894041513037));
#45074=CARTESIAN_POINT('Ctrl Pts',(-92.6627498057165,2.24963315697919,-3.23400886411684));
#45075=CARTESIAN_POINT('Ctrl Pts',(-92.596458628484,3.32052564078884,-2.48907731310333));
#45076=CARTESIAN_POINT('Ctrl Pts',(-92.5301674512514,3.98463067301462,-1.15935965145112));
#45077=CARTESIAN_POINT('Ctrl Pts',(-92.463876274019,3.9368577200577,0.144270461940386));
#45078=CARTESIAN_POINT('Ctrl Pts',(-92.3975850967865,3.88908476710079,1.44790057533193));
#45079=CARTESIAN_POINT('Ctrl Pts',(-92.3312939195541,3.12943382896112,2.72544314046279));
#45080=CARTESIAN_POINT('Ctrl Pts',(-92.2650027423216,2.0068893265053,3.38999379134027));
#45081=CARTESIAN_POINT('Ctrl Pts',(-92.1987115650892,0.88434482404947,4.05454444221775));
#45082=CARTESIAN_POINT('Ctrl Pts',(-92.1324203878566,-0.601093242722498,
4.10610317884187));
#45083=CARTESIAN_POINT('Ctrl Pts',(-92.0661292106241,-1.76701310093099,
3.52098386467543));
#45084=CARTESIAN_POINT('Ctrl Pts',(-91.9998380333916,-2.93293295913946,
2.93586455050899));
#45085=CARTESIAN_POINT('Ctrl Pts',(-91.9335468561591,-3.77933460878443,
1.71406718555199));
#45086=CARTESIAN_POINT('Ctrl Pts',(-91.8672556789267,-3.91738026307234,
0.416886733607205));
#45087=CARTESIAN_POINT('Ctrl Pts',(-91.8602249599626,-3.93202112841853,
0.279310187466734));
#45088=CARTESIAN_POINT('Ctrl Pts',(-91.8531942409986,-3.93869417241828,
0.140885707556243));
#45089=CARTESIAN_POINT('Ctrl Pts',(-91.8461635220346,-3.93771195638885,
0.00236553390519242));
#45090=CARTESIAN_POINT('Origin',(-54.75,0.,0.));
#45091=CARTESIAN_POINT('',(-90.412836477965,-3.92810207392459,0.00247836248652517));
#45092=CARTESIAN_POINT('',(-90.5961635220346,-3.92771739568111,0.00220584221594762));
#45093=CARTESIAN_POINT('',(-54.75,-3.933,-4.81653586104654E-16));
#45094=CARTESIAN_POINT('Ctrl Pts',(-90.412836477965,-3.92810207392459,0.00247836248652517));
#45095=CARTESIAN_POINT('Ctrl Pts',(-90.4377099594238,-3.93093227664902,
0.495612161623221));
#45096=CARTESIAN_POINT('Ctrl Pts',(-90.4625834408826,-3.84493247844779,
0.98779472531452));
#45097=CARTESIAN_POINT('Ctrl Pts',(-90.4874569223414,-3.66561490624659,
1.44323595897181));
#45098=CARTESIAN_POINT('Ctrl Pts',(-90.5537480995739,-3.18770943172068,
2.65704817055711));
#45099=CARTESIAN_POINT('Ctrl Pts',(-90.6200392768065,-2.04697315672674,
3.60988882064005));
#45100=CARTESIAN_POINT('Ctrl Pts',(-90.6863304540389,-0.767461497118248,
3.86402193635174));
#45101=CARTESIAN_POINT('Ctrl Pts',(-90.7526216312714,0.512050162490266,
4.11815505206344));
#45102=CARTESIAN_POINT('Ctrl Pts',(-90.8189128085039,1.93033720671331,3.6735806334039));
#45103=CARTESIAN_POINT('Ctrl Pts',(-90.8852039857364,2.83583711136996,2.73453662472151));
#45104=CARTESIAN_POINT('Ctrl Pts',(-90.9514951629689,3.7413370160266,1.79549261603915));
#45105=CARTESIAN_POINT('Ctrl Pts',(-91.0177863402014,4.1340497811168,0.361979017333895));
#45106=CARTESIAN_POINT('Ctrl Pts',(-91.0840775174339,3.83356275918494,-0.907446552451885));
#45107=CARTESIAN_POINT('Ctrl Pts',(-91.1503686946663,3.53307573725307,-2.17687212223768));
#45108=CARTESIAN_POINT('Ctrl Pts',(-91.2166598718987,2.53938892829914,-3.28220966310406));
#45109=CARTESIAN_POINT('Ctrl Pts',(-91.2829510491312,1.30900307251152,-3.71566597399737));
#45110=CARTESIAN_POINT('Ctrl Pts',(-91.3492422263637,0.0786172167238791,
-4.14912228489069));
#45111=CARTESIAN_POINT('Ctrl Pts',(-91.4155334035962,-1.3884676858974,-3.91069736581095));
#45112=CARTESIAN_POINT('Ctrl Pts',(-91.4818245808287,-2.41827132492559,
-3.10992386935904));
#45113=CARTESIAN_POINT('Ctrl Pts',(-91.5421618798742,-3.3555841427113,-2.3810710726494));
#45114=CARTESIAN_POINT('Ctrl Pts',(-91.6024991789196,-3.930636331294,-1.18634707030812));
#45115=CARTESIAN_POINT('Ctrl Pts',(-91.662836477965,-3.93817602267047,0.00205778069578805));
#45116=CARTESIAN_POINT('Ctrl Pts',(-91.8461635220346,-3.93771195638885,
0.00236553390519242));
#45117=CARTESIAN_POINT('Ctrl Pts',(-91.7869030637662,-3.92943306310346,
-1.16519201063766));
#45118=CARTESIAN_POINT('Ctrl Pts',(-91.7276426054977,-3.37728995814469,
-2.33954807026313));
#45119=CARTESIAN_POINT('Ctrl Pts',(-91.6683821472292,-2.46845039605334,
-3.07024678428145));
#45120=CARTESIAN_POINT('Ctrl Pts',(-91.6020909699967,-1.4517852158156,-3.88763631129265));
#45121=CARTESIAN_POINT('Ctrl Pts',(-91.5357997927642,0.0112348035907324,
-4.14985182638249));
#45122=CARTESIAN_POINT('Ctrl Pts',(-91.4695086155317,1.24849676326094,-3.73643125271875));
#45123=CARTESIAN_POINT('Ctrl Pts',(-91.4032174382992,2.48575872293114,-3.32301067905501));
#45124=CARTESIAN_POINT('Ctrl Pts',(-91.3369262610668,3.49726262286522,-2.23395401663771));
#45125=CARTESIAN_POINT('Ctrl Pts',(-91.2706350838343,3.81832253298691,-0.969575014246389));
#45126=CARTESIAN_POINT('Ctrl Pts',(-91.2043439066018,4.1393824431086,0.294803988144949));
#45127=CARTESIAN_POINT('Ctrl Pts',(-91.1380527293693,3.76999836341785,1.7345053305103));
#45128=CARTESIAN_POINT('Ctrl Pts',(-91.0717615521368,2.87986571934768,2.68812873811737));
#45129=CARTESIAN_POINT('Ctrl Pts',(-91.0054703749043,1.9897330752775,3.64175214572446));
#45130=CARTESIAN_POINT('Ctrl Pts',(-90.9391791976719,0.578851866827931,
4.10929761857325));
#45131=CARTESIAN_POINT('Ctrl Pts',(-90.8728880204394,-0.704617630377498,
3.87597428643788));
#45132=CARTESIAN_POINT('Ctrl Pts',(-90.8065968432069,-1.98808712758291,
3.64265095430252));
#45133=CARTESIAN_POINT('Ctrl Pts',(-90.7403056659744,-3.14414491354417,
2.70845881718298));
#45134=CARTESIAN_POINT('Ctrl Pts',(-90.6740144887419,-3.64169685453977,
1.50256670194756));
#45135=CARTESIAN_POINT('Ctrl Pts',(-90.6480641665061,-3.83646837221226,
1.03050857478256));
#45136=CARTESIAN_POINT('Ctrl Pts',(-90.6221138442704,-3.9303300118642,0.516814960462088));
#45137=CARTESIAN_POINT('Ctrl Pts',(-90.5961635220346,-3.92771739568111,
0.00220584221594762));
#45138=CARTESIAN_POINT('Origin',(-54.75,0.,0.));
#45139=CARTESIAN_POINT('',(-89.162836477965,-3.92910621855356,-0.00299364777908595));
#45140=CARTESIAN_POINT('',(-89.3461635220346,-3.92962428827605,-0.00318291295316376));
#45141=CARTESIAN_POINT('',(-54.75,-3.933,-4.81653586104654E-16));
#45142=CARTESIAN_POINT('Ctrl Pts',(-89.162836477965,-3.92910621855356,-0.00299364777908595));
#45143=CARTESIAN_POINT('Ctrl Pts',(-89.2066295626955,-3.92298954530611,
0.864677208853277));
#45144=CARTESIAN_POINT('Ctrl Pts',(-89.2504226474261,-3.63987888166823,
1.73597420126334));
#45145=CARTESIAN_POINT('Ctrl Pts',(-89.2942157321567,-3.11124652009766,
2.41656942075883));
#45146=CARTESIAN_POINT('Ctrl Pts',(-89.3605069093892,-2.31103658313397,
3.44681103531342));
#45147=CARTESIAN_POINT('Ctrl Pts',(-89.4267980866217,-0.948238901927029,
4.04007913123173));
#45148=CARTESIAN_POINT('Ctrl Pts',(-89.4930892638542,0.351075869679159,
3.92382573617834));
#45149=CARTESIAN_POINT('Ctrl Pts',(-89.5593804410867,1.65039064128533,3.80757234112494));
#45150=CARTESIAN_POINT('Ctrl Pts',(-89.6256716183192,2.88622250329074,2.98179745509986));
#45151=CARTESIAN_POINT('Ctrl Pts',(-89.6919627955516,3.49082902954029,1.82586290851347));
#45152=CARTESIAN_POINT('Ctrl Pts',(-89.7582539727841,4.09543555578984,0.669928361927062));
#45153=CARTESIAN_POINT('Ctrl Pts',(-89.8245451500166,4.06881674628351,-0.816165845220666));
#45154=CARTESIAN_POINT('Ctrl Pts',(-89.8908363272491,3.42320130943634,-1.94970650848781));
#45155=CARTESIAN_POINT('Ctrl Pts',(-89.9571275044816,2.77758587258919,-3.08324717175494));
#45156=CARTESIAN_POINT('Ctrl Pts',(-90.0234186817141,1.5129738084012,-3.8642342911415));
#45157=CARTESIAN_POINT('Ctrl Pts',(-90.0897098589465,0.210329197456982,
-3.93388158221159));
#45158=CARTESIAN_POINT('Ctrl Pts',(-90.156001036179,-1.09231541348726,-4.00352887328168));
#45159=CARTESIAN_POINT('Ctrl Pts',(-90.2222922134115,-2.43299257118775,
-3.36183633603528));
#45160=CARTESIAN_POINT('Ctrl Pts',(-90.288583390644,-3.19579381300906,-2.30359818086824));
#45161=CARTESIAN_POINT('Ctrl Pts',(-90.3300010864176,-3.67238015659939,
-1.64242745202328));
#45162=CARTESIAN_POINT('Ctrl Pts',(-90.3714187821913,-3.92338940530952,
-0.818655812163256));
#45163=CARTESIAN_POINT('Ctrl Pts',(-90.412836477965,-3.92810207392459,0.00247836248652517));
#45164=CARTESIAN_POINT('Ctrl Pts',(-90.5961635220346,-3.92771739568111,
0.00220584221594762));
#45165=CARTESIAN_POINT('Ctrl Pts',(-90.5558226670379,-3.92365597518519,
-0.797775430869884));
#45166=CARTESIAN_POINT('Ctrl Pts',(-90.5154818120412,-3.68645491319269,
-1.599969110314));
#45167=CARTESIAN_POINT('Ctrl Pts',(-90.4751409570445,-3.23277753135463,
-2.25140225347118));
#45168=CARTESIAN_POINT('Ctrl Pts',(-90.408849779812,-2.48726017114393,-3.32188700030313));
#45169=CARTESIAN_POINT('Ctrl Pts',(-90.3425586025795,-1.15717935469258,
-3.98526440061574));
#45170=CARTESIAN_POINT('Ctrl Pts',(-90.276267425347,0.146424425412479,-3.9367781956581));
#45171=CARTESIAN_POINT('Ctrl Pts',(-90.2099762481145,1.45002820551758,-3.88829199070047));
#45172=CARTESIAN_POINT('Ctrl Pts',(-90.1436850708821,2.72715494927636,-3.12794218047255));
#45173=CARTESIAN_POINT('Ctrl Pts',(-90.0773938936496,3.39109131946141,-2.00503424839575));
#45174=CARTESIAN_POINT('Ctrl Pts',(-90.0111027164171,4.05502768964645,-0.88212631631897));
#45175=CARTESIAN_POINT('Ctrl Pts',(-89.9448115391846,4.10577368625775,0.603339737606724));
#45176=CARTESIAN_POINT('Ctrl Pts',(-89.8785203619521,3.52001654635439,1.76893928317445));
#45177=CARTESIAN_POINT('Ctrl Pts',(-89.8122291847196,2.93425940645103,2.93453882874219));
#45178=CARTESIAN_POINT('Ctrl Pts',(-89.7459380074871,1.71199913003302,3.78027186595199));
#45179=CARTESIAN_POINT('Ctrl Pts',(-89.6796468302546,0.414743342903526,
3.91760776924945));
#45180=CARTESIAN_POINT('Ctrl Pts',(-89.6133556530222,-0.882512444225967,
4.05494367254691));
#45181=CARTESIAN_POINT('Ctrl Pts',(-89.5470644757897,-2.25476374206692,
3.48388244193204));
#45182=CARTESIAN_POINT('Ctrl Pts',(-89.4807732985572,-3.07159689558824,
2.46677019302147));
#45183=CARTESIAN_POINT('Ctrl Pts',(-89.4359033730497,-3.62447956083405,
1.77832637973155));
#45184=CARTESIAN_POINT('Ctrl Pts',(-89.3910334475421,-3.92290235831991,
0.885528271771005));
#45185=CARTESIAN_POINT('Ctrl Pts',(-89.3461635220346,-3.92962428827605,
-0.00318291295316376));
#45186=CARTESIAN_POINT('Origin',(-54.75,0.,0.));
#45187=CARTESIAN_POINT('',(-87.912836477965,-3.93898829629484,-0.00129309091083552));
#45188=CARTESIAN_POINT('',(-88.0961635220347,-3.93924257493437,-0.000916068792095346));
#45189=CARTESIAN_POINT('',(-54.75,-3.933,-4.81653586104654E-16));
#45190=CARTESIAN_POINT('Ctrl Pts',(-87.912836477965,-3.93898829629484,-0.00129309091083552));
#45191=CARTESIAN_POINT('Ctrl Pts',(-87.9755491659674,-3.93371149202149,
1.2332226163925));
#45192=CARTESIAN_POINT('Ctrl Pts',(-88.0382618539697,-3.30606438542729,
2.47236114778859));
#45193=CARTESIAN_POINT('Ctrl Pts',(-88.1009745419721,-2.30534636056446,
3.19453295991741));
#45194=CARTESIAN_POINT('Ctrl Pts',(-88.1672657192045,-1.24752571757992,
3.95791308465947));
#45195=CARTESIAN_POINT('Ctrl Pts',(-88.2335568964369,0.227156656004045,
4.14364528590165));
#45196=CARTESIAN_POINT('Ctrl Pts',(-88.2998480736694,1.44123016380054,3.66640399971388));
#45197=CARTESIAN_POINT('Ctrl Pts',(-88.3661392509019,2.65530367159704,3.1891627135261));
#45198=CARTESIAN_POINT('Ctrl Pts',(-88.4324304281344,3.60876831360607,2.04894793990836));
#45199=CARTESIAN_POINT('Ctrl Pts',(-88.4987216053669,3.86360145442727,0.769575516446496));
#45200=CARTESIAN_POINT('Ctrl Pts',(-88.5650127825994,4.11843459524847,-0.509796907015349));
#45201=CARTESIAN_POINT('Ctrl Pts',(-88.6313039598319,3.67463623488187,-1.92832698032131));
#45202=CARTESIAN_POINT('Ctrl Pts',(-88.6975951370643,2.73608779569937,-2.83434053148019));
#45203=CARTESIAN_POINT('Ctrl Pts',(-88.7638863142968,1.79753935651686,-3.74035408263909));
#45204=CARTESIAN_POINT('Ctrl Pts',(-88.8301774915293,0.364240838518444,
-4.13385111165089));
#45205=CARTESIAN_POINT('Ctrl Pts',(-88.8964686687618,-0.905348947651138,
-3.83405867940925));
#45206=CARTESIAN_POINT('Ctrl Pts',(-88.9627598459943,-2.1749387338207,-3.53426624716762));
#45207=CARTESIAN_POINT('Ctrl Pts',(-89.0290510232268,-3.28081978816143,
-2.54118435367256));
#45208=CARTESIAN_POINT('Ctrl Pts',(-89.0953422004593,-3.7149492189716,-1.31103584032961));
#45209=CARTESIAN_POINT('Ctrl Pts',(-89.1178402929612,-3.86228532763525,
-0.89354446063647));
#45210=CARTESIAN_POINT('Ctrl Pts',(-89.1403383854631,-3.93224857496374,
-0.448747567920103));
#45211=CARTESIAN_POINT('Ctrl Pts',(-89.162836477965,-3.92910621855356,-0.00299364777908595));
#45212=CARTESIAN_POINT('Ctrl Pts',(-89.3461635220346,-3.92962428827605,
-0.00318291295316376));
#45213=CARTESIAN_POINT('Ctrl Pts',(-89.3247422703097,-3.93283338996363,
-0.427460550667744));
#45214=CARTESIAN_POINT('Ctrl Pts',(-89.3033210185847,-3.86955855712855,
-0.850806704224785));
#45215=CARTESIAN_POINT('Ctrl Pts',(-89.2818997668597,-3.73574759958786,
-1.25054090150623));
#45216=CARTESIAN_POINT('Ctrl Pts',(-89.2156085896273,-3.32165014086451,
-2.48757647991708));
#45217=CARTESIAN_POINT('Ctrl Pts',(-89.1493174123949,-2.23204021421619,
-3.49848436953255));
#45218=CARTESIAN_POINT('Ctrl Pts',(-89.0830262351624,-0.967485738578175,
-3.81885244802863));
#45219=CARTESIAN_POINT('Ctrl Pts',(-89.0167350579299,0.297068737059861,
-4.13922052652472));
#45220=CARTESIAN_POINT('Ctrl Pts',(-88.9504438806973,1.73656776168761,-3.76904879390135));
#45221=CARTESIAN_POINT('Ctrl Pts',(-88.8841527034648,2.6897040055491,-2.87839452415744));
#45222=CARTESIAN_POINT('Ctrl Pts',(-88.8178615262323,3.6428402494106,-1.98774025441354));
#45223=CARTESIAN_POINT('Ctrl Pts',(-88.7515703489999,4.10961371250589,-0.576603447549069));
#45224=CARTESIAN_POINT('Ctrl Pts',(-88.6852791717675,3.8755881866824,0.706738198638142));
#45225=CARTESIAN_POINT('Ctrl Pts',(-88.618987994535,3.6415626608589,1.99007984482537));
#45226=CARTESIAN_POINT('Ctrl Pts',(-88.5526968173024,2.70673814611665,3.14562633033533));
#45227=CARTESIAN_POINT('Ctrl Pts',(-88.4864056400699,1.50057398425297,3.64251841339884));
#45228=CARTESIAN_POINT('Ctrl Pts',(-88.4201144628374,0.294409822389292,
4.13941049646235));
#45229=CARTESIAN_POINT('Ctrl Pts',(-88.353823285605,-1.18309398659577,3.97764817707937));
#45230=CARTESIAN_POINT('Ctrl Pts',(-88.2875321083725,-2.25317067599549,
3.23154523084553));
#45231=CARTESIAN_POINT('Ctrl Pts',(-88.2237425795933,-3.28286558600009,
2.5135981774363));
#45232=CARTESIAN_POINT('Ctrl Pts',(-88.159953050814,-3.93530353798598,1.25458118357524));
#45233=CARTESIAN_POINT('Ctrl Pts',(-88.0961635220347,-3.93924257493437,
-0.000916068792095346));
#45234=CARTESIAN_POINT('Origin',(-54.75,0.,0.));
#45235=CARTESIAN_POINT('',(-86.662836477965,-3.93304779575148,0.00362946431549549));
#45236=CARTESIAN_POINT('',(-86.8461635220346,-3.93240142136994,0.00363335402696072));
#45237=CARTESIAN_POINT('',(-54.75,-3.933,-4.81653586104654E-16));
#45238=CARTESIAN_POINT('Ctrl Pts',(-86.662836477965,-3.93304779575148,0.00362946431549549));
#45239=CARTESIAN_POINT('Ctrl Pts',(-86.6781775920066,-3.93585383828323,
0.306810777743879));
#45240=CARTESIAN_POINT('Ctrl Pts',(-86.6935187060482,-3.90377069809062,
0.609404500676993));
#45241=CARTESIAN_POINT('Ctrl Pts',(-86.7088598200898,-3.83455345189039,
0.903251071829943));
#45242=CARTESIAN_POINT('Ctrl Pts',(-86.7751509973223,-3.53545569908325,
2.17300469432574));
#45243=CARTESIAN_POINT('Ctrl Pts',(-86.8414421745548,-2.54297901833069,
3.27942893109026));
#45244=CARTESIAN_POINT('Ctrl Pts',(-86.9077333517873,-1.31306821568301,
3.71423135185862));
#45245=CARTESIAN_POINT('Ctrl Pts',(-86.9740245290198,-0.0831574130353308,
4.14903377262697));
#45246=CARTESIAN_POINT('Ctrl Pts',(-87.0403157062523,1.38418751150747,3.91221437739916));
#45247=CARTESIAN_POINT('Ctrl Pts',(-87.1066068834848,2.41486679318088,3.11256823947022));
#45248=CARTESIAN_POINT('Ctrl Pts',(-87.1728980607172,3.44554607485426,2.31292210154131));
#45249=CARTESIAN_POINT('Ctrl Pts',(-87.2391892379497,4.03955971365827,0.950449220911299));
#45250=CARTESIAN_POINT('Ctrl Pts',(-87.3054804151822,3.92401723409042,-0.348928962294304));
#45251=CARTESIAN_POINT('Ctrl Pts',(-87.3717715924147,3.80847475452257,-1.64830714549996));
#45252=CARTESIAN_POINT('Ctrl Pts',(-87.4380627696472,2.98337615658278,-2.88459063128121));
#45253=CARTESIAN_POINT('Ctrl Pts',(-87.5043539468797,1.82777258324076,-3.48982951705665));
#45254=CARTESIAN_POINT('Ctrl Pts',(-87.5706451241122,0.672169009898779,
-4.09506840283207));
#45255=CARTESIAN_POINT('Ctrl Pts',(-87.6369363013446,-0.813939538845411,
-4.06926268860171));
#45256=CARTESIAN_POINT('Ctrl Pts',(-87.7032274785771,-1.94783327000578,
-3.42426754597608));
#45257=CARTESIAN_POINT('Ctrl Pts',(-87.7695186558095,-3.08172700116616,
-2.77927240335044));
#45258=CARTESIAN_POINT('Ctrl Pts',(-87.8358098330421,-3.86340591474271,
-1.51508783232952));
#45259=CARTESIAN_POINT('Ctrl Pts',(-87.9021010102746,-3.93376591533843,
-0.212481522698077));
#45260=CARTESIAN_POINT('Ctrl Pts',(-87.9056794995047,-3.93756404526878,
-0.142165036481684));
#45261=CARTESIAN_POINT('Ctrl Pts',(-87.9092579887349,-3.93928939943462,
-0.0717365897266798));
#45262=CARTESIAN_POINT('Ctrl Pts',(-87.912836477965,-3.93898829629484,-0.00129309091083552));
#45263=CARTESIAN_POINT('Ctrl Pts',(-88.0961635220347,-3.93924257493437,
-0.000916068792095346));
#45264=CARTESIAN_POINT('Ctrl Pts',(-88.0936618735815,-3.93939705304194,
-0.0501531899855988));
#45265=CARTESIAN_POINT('Ctrl Pts',(-88.0911602251283,-3.93855414570549,
-0.0993848978486387));
#45266=CARTESIAN_POINT('Ctrl Pts',(-88.0886585766751,-3.93669749276575,
-0.148578345051743));
#45267=CARTESIAN_POINT('Ctrl Pts',(-88.0223673994425,-3.88749805032196,
-1.45215540163056));
#45268=CARTESIAN_POINT('Ctrl Pts',(-87.95607622221,-3.12644959562002,-2.72886594170351));
#45269=CARTESIAN_POINT('Ctrl Pts',(-87.8897850449775,-2.00317857006993,
-3.39218783244369));
#45270=CARTESIAN_POINT('Ctrl Pts',(-87.8234938677451,-0.879907544519845,
-4.05550972318388));
#45271=CARTESIAN_POINT('Ctrl Pts',(-87.7572026905126,0.605586051878377,
-4.10544296459131));
#45272=CARTESIAN_POINT('Ctrl Pts',(-87.6909115132801,1.77086493587776,-3.51904817430013));
#45273=CARTESIAN_POINT('Ctrl Pts',(-87.6246203360477,2.93614381987714,-2.93265338400896));
#45274=CARTESIAN_POINT('Ctrl Pts',(-87.5583291588152,3.78120799147769,-1.70993056201918));
#45275=CARTESIAN_POINT('Ctrl Pts',(-87.4920379815827,3.91783410267256,-0.412599828044509));
#45276=CARTESIAN_POINT('Ctrl Pts',(-87.4257468043502,4.05446021386743,0.884730905930157));
#45277=CARTESIAN_POINT('Ctrl Pts',(-87.3594556271177,3.48264826465663,2.25666955188971));
#45278=CARTESIAN_POINT('Ctrl Pts',(-87.2931644498852,2.4650892515505,3.07294608739832));
#45279=CARTESIAN_POINT('Ctrl Pts',(-87.2268732726527,1.44753023844436,3.88922262290694));
#45280=CARTESIAN_POINT('Ctrl Pts',(-87.1605820954203,-0.0157758385571052,
4.14983704796462));
#45281=CARTESIAN_POINT('Ctrl Pts',(-87.0942909181878,-1.25258466539632,
3.73506282814365));
#45282=CARTESIAN_POINT('Ctrl Pts',(-87.0279997409553,-2.48939349223549,
3.32028860832269));
#45283=CARTESIAN_POINT('Ctrl Pts',(-86.9617085637227,-3.49970506891242,
2.23012574362311));
#45284=CARTESIAN_POINT('Ctrl Pts',(-86.8954173864903,-3.81938121987922,
0.965396173288631));
#45285=CARTESIAN_POINT('Ctrl Pts',(-86.8789994316717,-3.89855357466691,
0.652167870363411));
#45286=CARTESIAN_POINT('Ctrl Pts',(-86.8625814768532,-3.93536402261767,
0.328232067872365));
#45287=CARTESIAN_POINT('Ctrl Pts',(-86.8461635220346,-3.93240142136994,
0.00363335402696072));
#45288=CARTESIAN_POINT('Origin',(-54.75,0.,0.));
#45289=CARTESIAN_POINT('',(-85.412836477965,-3.92650867564805,-0.000365894358481667));
#45290=CARTESIAN_POINT('',(-85.5961635220347,-3.92659593005969,-0.000715850624292737));
#45291=CARTESIAN_POINT('',(-54.75,-3.933,-4.81653586104654E-16));
#45292=CARTESIAN_POINT('Ctrl Pts',(-85.412836477965,-3.92650867564805,-0.000365894358481667));
#45293=CARTESIAN_POINT('Ctrl Pts',(-85.4470971952784,-3.92594651516599,
0.679565426024714));
#45294=CARTESIAN_POINT('Ctrl Pts',(-85.4813579125918,-3.7583595467037,1.35975629231021));
#45295=CARTESIAN_POINT('Ctrl Pts',(-85.5156186299051,-3.42533275744544,
1.94595944843094));
#45296=CARTESIAN_POINT('Ctrl Pts',(-85.5819098071376,-2.78095810212358,
3.08020590804822));
#45297=CARTESIAN_POINT('Ctrl Pts',(-85.64820098437,-1.51720140270921,3.86257638181553));
#45298=CARTESIAN_POINT('Ctrl Pts',(-85.7144921616025,-0.214633784331787,
3.93364907087425));
#45299=CARTESIAN_POINT('Ctrl Pts',(-85.780783338835,1.0879338340456,4.00472175993298));
#45300=CARTESIAN_POINT('Ctrl Pts',(-85.8470745160675,2.42931237138605,3.36449666428316));
#45301=CARTESIAN_POINT('Ctrl Pts',(-85.9133656933,3.19327115052751,2.30709385014463));
#45302=CARTESIAN_POINT('Ctrl Pts',(-85.9796568705325,3.95722992966898,1.24969103600607));
#45303=CARTESIAN_POINT('Ctrl Pts',(-86.045948047765,4.14376895061143,-0.224889496621225));
#45304=CARTESIAN_POINT('Ctrl Pts',(-86.1122392249975,3.66719199562616,-1.4392239371904));
#45305=CARTESIAN_POINT('Ctrl Pts',(-86.17853040223,3.1906150406409,-2.65355837775957));
#45306=CARTESIAN_POINT('Ctrl Pts',(-86.2448215794625,2.05092210972791,-3.60764672627063));
#45307=CARTESIAN_POINT('Ctrl Pts',(-86.311112756695,0.771689305398751,-3.86317981591585));
#45308=CARTESIAN_POINT('Ctrl Pts',(-86.3774039339274,-0.507543498930407,
-4.11871290556108));
#45309=CARTESIAN_POINT('Ctrl Pts',(-86.4436951111599,-1.92631617667573,
-3.67569073634049));
#45310=CARTESIAN_POINT('Ctrl Pts',(-86.5099862883923,-2.83284310311752,
-2.73763814761665));
#45311=CARTESIAN_POINT('Ctrl Pts',(-86.5609363515832,-3.52958143413936,
-2.01666982774167));
#45312=CARTESIAN_POINT('Ctrl Pts',(-86.6118864147741,-3.92372852181079,
-1.00327961905144));
#45313=CARTESIAN_POINT('Ctrl Pts',(-86.662836477965,-3.93304779575148,0.00362946431549549));
#45314=CARTESIAN_POINT('Ctrl Pts',(-86.8461635220346,-3.93240142136994,
0.00363335402696072));
#45315=CARTESIAN_POINT('Ctrl Pts',(-86.7962902996207,-3.92340185518861,
-0.982408088393583));
#45316=CARTESIAN_POINT('Ctrl Pts',(-86.7464170772068,-3.54738575066246,
-1.97456672412491));
#45317=CARTESIAN_POINT('Ctrl Pts',(-86.6965438547929,-2.87692246730654,
-2.69127846780546));
#45318=CARTESIAN_POINT('Ctrl Pts',(-86.6302526775604,-1.98574683851036,
-3.64392726259569));
#45319=CARTESIAN_POINT('Ctrl Pts',(-86.5639615003279,-0.57435485566134,
-4.10992857620667));
#45320=CARTESIAN_POINT('Ctrl Pts',(-86.4976703230954,0.70885855533344,-3.87520092675168));
#45321=CARTESIAN_POINT('Ctrl Pts',(-86.4313791458629,1.9920719663282,-3.64047327729668));
#45322=CARTESIAN_POINT('Ctrl Pts',(-86.3650879686304,3.14710680546873,-2.70501666477572));
#45323=CARTESIAN_POINT('Ctrl Pts',(-86.298796791398,3.64333888185318,-1.49858081735462));
#45324=CARTESIAN_POINT('Ctrl Pts',(-86.2325056141655,4.13957095823763,-0.29214496993353));
#45325=CARTESIAN_POINT('Ctrl Pts',(-86.166214436933,3.97700027186602,1.18527011238769));
#45326=CARTESIAN_POINT('Ctrl Pts',(-86.0999232597005,3.23031196295841,2.25493842402275));
#45327=CARTESIAN_POINT('Ctrl Pts',(-86.033632082468,2.48362365405083,3.32460673565777));
#45328=CARTESIAN_POINT('Ctrl Pts',(-85.9673409052355,1.1528177226073,3.98652827660665));
#45329=CARTESIAN_POINT('Ctrl Pts',(-85.901049728003,-0.150732220213392,
3.9366156114048));
#45330=CARTESIAN_POINT('Ctrl Pts',(-85.8347585507705,-1.45428216303412,
3.88670294620295));
#45331=CARTESIAN_POINT('Ctrl Pts',(-85.768467373538,-2.73057611723201,3.12495607485035));
#45332=CARTESIAN_POINT('Ctrl Pts',(-85.7021761963055,-3.39328332995887,
2.00132229208334));
#45333=CARTESIAN_POINT('Ctrl Pts',(-85.6668386382152,-3.74654986714039,
1.40235157337791));
#45334=CARTESIAN_POINT('Ctrl Pts',(-85.6315010801249,-3.92546013234001,
0.700547386331901));
#45335=CARTESIAN_POINT('Ctrl Pts',(-85.5961635220347,-3.92659593005969,
-0.000715850624292737));
#45336=CARTESIAN_POINT('Origin',(-54.75,0.,0.));
#45337=CARTESIAN_POINT('',(-84.162836477965,-3.93439518658889,-0.00350198815590452));
#45338=CARTESIAN_POINT('',(-84.3461635220346,-3.93503686469963,-0.00338281421578225));
#45339=CARTESIAN_POINT('',(-54.75,-3.933,-4.81653586104654E-16));
#45340=CARTESIAN_POINT('Ctrl Pts',(-84.162836477965,-3.93439518658889,-0.00350198815590452));
#45341=CARTESIAN_POINT('Ctrl Pts',(-84.2160167985501,-3.92468364801176,
1.04656012953353));
#45342=CARTESIAN_POINT('Ctrl Pts',(-84.2691971191353,-3.49131722508058,
2.10369626757898));
#45343=CARTESIAN_POINT('Ctrl Pts',(-84.3223774397204,-2.73918768000938,
2.83134482673009));
#45344=CARTESIAN_POINT('Ctrl Pts',(-84.3886686169529,-1.80163122255463,
3.73838485708176));
#45345=CARTESIAN_POINT('Ctrl Pts',(-84.4549597941853,-0.368764153098906,
4.13345006031658));
#45346=CARTESIAN_POINT('Ctrl Pts',(-84.5212509714178,0.901152925616475,
3.8350470764802));
#45347=CARTESIAN_POINT('Ctrl Pts',(-84.5875421486503,2.17107000433186,3.53664409264381));
#45348=CARTESIAN_POINT('Ctrl Pts',(-84.6538333258829,3.27803709230692,2.54477292173622));
#45349=CARTESIAN_POINT('Ctrl Pts',(-84.7201245031154,3.71351237287333,1.31510019796331));
#45350=CARTESIAN_POINT('Ctrl Pts',(-84.7864156803478,4.14898765343973,0.0854274741904251));
#45351=CARTESIAN_POINT('Ctrl Pts',(-84.8527068575802,3.91297112659752,-1.38204680244773));
#45352=CARTESIAN_POINT('Ctrl Pts',(-84.9189980348127,3.11388902708113,-2.41316344270134));
#45353=CARTESIAN_POINT('Ctrl Pts',(-84.9852892120452,2.31480692756472,-3.44428008295497));
#45354=CARTESIAN_POINT('Ctrl Pts',(-85.0515803892777,0.9526592553741,-4.03903908682399));
#45355=CARTESIAN_POINT('Ctrl Pts',(-85.1178715665102,-0.346781950456118,
-3.9242075573298));
#45356=CARTESIAN_POINT('Ctrl Pts',(-85.1841627437427,-1.64622315628634,
-3.80937602783561));
#45357=CARTESIAN_POINT('Ctrl Pts',(-85.2504539209751,-2.88295789575617,
-2.98495396497819));
#45358=CARTESIAN_POINT('Ctrl Pts',(-85.3167450982076,-3.48882895987641,
-1.82968171081588));
#45359=CARTESIAN_POINT('Ctrl Pts',(-85.3487755581267,-3.78157272527062,
-1.27147919914778));
#45360=CARTESIAN_POINT('Ctrl Pts',(-85.3808060180458,-3.92703424137465,
-0.636035974061732));
#45361=CARTESIAN_POINT('Ctrl Pts',(-85.412836477965,-3.92650867564805,-0.000365894358481667));
#45362=CARTESIAN_POINT('Ctrl Pts',(-85.5961635220347,-3.92659593005969,
-0.000715850624292737));
#45363=CARTESIAN_POINT('Ctrl Pts',(-85.5652099028925,-3.92759082195199,
-0.614981134594069));
#45364=CARTESIAN_POINT('Ctrl Pts',(-85.5342562837504,-3.79218420171298,
-1.22883136227772));
#45365=CARTESIAN_POINT('Ctrl Pts',(-85.5033026646082,-3.51807874880253,
-1.77279005846446));
#45366=CARTESIAN_POINT('Ctrl Pts',(-85.4370114873757,-2.93104648366353,
-2.93774793206387));
#45367=CARTESIAN_POINT('Ctrl Pts',(-85.3707203101432,-1.7078614821297,-3.78214298508129));
#45368=CARTESIAN_POINT('Ctrl Pts',(-85.3044291329107,-0.410456189671825,
-3.91805926327392));
#45369=CARTESIAN_POINT('Ctrl Pts',(-85.2381379556782,0.886949102786071,
-4.05397554146654));
#45370=CARTESIAN_POINT('Ctrl Pts',(-85.1718467784457,2.25857468616802,-3.48141304483438));
#45371=CARTESIAN_POINT('Ctrl Pts',(-85.1055556012133,3.07429435930779,-2.46340757214366));
#45372=CARTESIAN_POINT('Ctrl Pts',(-85.0392644239808,3.89001403244753,-1.44540209945299));
#45373=CARTESIAN_POINT('Ctrl Pts',(-84.9729732467483,4.14982779534511,0.0180463492962202));
#45374=CARTESIAN_POINT('Ctrl Pts',(-84.9066820695158,3.73437693859115,1.25462805431929));
#45375=CARTESIAN_POINT('Ctrl Pts',(-84.8403908922833,3.31892608183717,2.49120975934241));
#45376=CARTESIAN_POINT('Ctrl Pts',(-84.7740997150508,2.22821060543163,3.50092472063938));
#45377=CARTESIAN_POINT('Ctrl Pts',(-84.7078085378183,0.963306319003282,
3.81990884838039));
#45378=CARTESIAN_POINT('Ctrl Pts',(-84.6415173605858,-0.301597967425049,
4.13889297612139));
#45379=CARTESIAN_POINT('Ctrl Pts',(-84.5752261833534,-1.74069106387619,
3.76714627030641));
#45380=CARTESIAN_POINT('Ctrl Pts',(-84.5089350061209,-2.69285212441525,
2.87544954923551));
#45381=CARTESIAN_POINT('Ctrl Pts',(-84.4546778447588,-3.47216482425126,
2.14562493454348));
#45382=CARTESIAN_POINT('Ctrl Pts',(-84.4004206833967,-3.92528723901599,
1.06749166239896));
#45383=CARTESIAN_POINT('Ctrl Pts',(-84.3461635220346,-3.93503686469963,
-0.00338281421578225));
#45384=CARTESIAN_POINT('Origin',(-54.75,0.,0.));
#45385=CARTESIAN_POINT('',(-82.912836477965,-3.93823441574634,0.00201426645151499));
#45386=CARTESIAN_POINT('',(-83.0961635220346,-3.93777751392323,0.00232566860396301));
#45387=CARTESIAN_POINT('',(-54.75,-3.933,-4.81653586104654E-16));
#45388=CARTESIAN_POINT('Ctrl Pts',(-82.912836477965,-3.93823441574634,0.00201426645151499));
#45389=CARTESIAN_POINT('Ctrl Pts',(-82.9186452245895,-3.93894770498266,
0.11641899894547));
#45390=CARTESIAN_POINT('Ctrl Pts',(-82.9244539712139,-3.93439648798973,
0.230766159426596));
#45391=CARTESIAN_POINT('Ctrl Pts',(-82.9302627178383,-3.92439670583951,
0.34463483480704));
#45392=CARTESIAN_POINT('Ctrl Pts',(-82.9965538950707,-3.81027616079436,
1.64413867426808));
#45393=CARTESIAN_POINT('Ctrl Pts',(-83.0628450723031,-2.98653087981396,
2.88132429720423));
#45394=CARTESIAN_POINT('Ctrl Pts',(-83.1291362495356,-1.83159029066747,
3.48782735829902));
#45395=CARTESIAN_POINT('Ctrl Pts',(-83.195427426768,-0.676649701520935,
4.09433041939382));
#45396=CARTESIAN_POINT('Ctrl Pts',(-83.2617186040007,0.809486195791681,
4.0701509186472));
#45397=CARTESIAN_POINT('Ctrl Pts',(-83.3280097812332,1.94408504432396,3.42639694352571));
#45398=CARTESIAN_POINT('Ctrl Pts',(-83.3943009584657,3.07868389285625,2.78264296840423));
#45399=CARTESIAN_POINT('Ctrl Pts',(-83.4605921356981,3.86174569260815,1.51931451890789));
#45400=CARTESIAN_POINT('Ctrl Pts',(-83.5268833129305,3.93353104885403,0.216785981714108));
#45401=CARTESIAN_POINT('Ctrl Pts',(-83.593174490163,4.00531640509991,-1.08574255547963));
#45402=CARTESIAN_POINT('Ctrl Pts',(-83.6594656673956,3.36582531783971,-2.42747118037085));
#45403=CARTESIAN_POINT('Ctrl Pts',(-83.7257568446281,2.30884064908559,-3.19200838521713));
#45404=CARTESIAN_POINT('Ctrl Pts',(-83.7920480218606,1.25185598033144,-3.95654559006343));
#45405=CARTESIAN_POINT('Ctrl Pts',(-83.858339199093,-0.222622269916648,
-4.14389137486483));
#45406=CARTESIAN_POINT('Ctrl Pts',(-83.9246303763255,-1.43721727974187,
-3.66797889374759));
#45407=CARTESIAN_POINT('Ctrl Pts',(-83.990921553558,-2.6518122895671,-3.19206641263036));
#45408=CARTESIAN_POINT('Ctrl Pts',(-84.0572127307905,-3.60652405896942,
-2.0528956655945));
#45409=CARTESIAN_POINT('Ctrl Pts',(-84.1235039080229,-3.86275702094368,
-0.773802863342302));
#45410=CARTESIAN_POINT('Ctrl Pts',(-84.1366147646703,-3.91343395523601,
-0.520827986909221));
#45411=CARTESIAN_POINT('Ctrl Pts',(-84.1497256213176,-3.93678942920926,
-0.26237996678345));
#45412=CARTESIAN_POINT('Ctrl Pts',(-84.162836477965,-3.93439518658889,-0.00350198815590452));
#45413=CARTESIAN_POINT('Ctrl Pts',(-84.3461635220346,-3.93503686469963,
-0.00338281421578225));
#45414=CARTESIAN_POINT('Ctrl Pts',(-84.3341295061642,-3.93719929169106,
-0.240898381253968));
#45415=CARTESIAN_POINT('Ctrl Pts',(-84.3220954902938,-3.91755069453226,
-0.478056863309719));
#45416=CARTESIAN_POINT('Ctrl Pts',(-84.3100614744233,-3.87481250676164,
-0.710978699828652));
#45417=CARTESIAN_POINT('Ctrl Pts',(-84.2437702971909,-3.63938280394195,
-1.99406349149509));
#45418=CARTESIAN_POINT('Ctrl Pts',(-84.1774791199585,-2.70329437367554,
-3.14858633850115));
#45419=CARTESIAN_POINT('Ctrl Pts',(-84.111187942726,-1.49658720184918,-3.64415825965719));
#45420=CARTESIAN_POINT('Ctrl Pts',(-84.0448967654935,-0.289880030022867,
-4.1397301808132));
#45421=CARTESIAN_POINT('Ctrl Pts',(-83.978605588261,1.18744588336335,-3.97635117611928));
#45422=CARTESIAN_POINT('Ctrl Pts',(-83.9123144110285,2.25670549702358,-3.22907772806261));
#45423=CARTESIAN_POINT('Ctrl Pts',(-83.846023233796,3.32596511068386,-2.48180428000591));
#45424=CARTESIAN_POINT('Ctrl Pts',(-83.7797320565636,3.98715842461806,-1.15063638858639));
#45425=CARTESIAN_POINT('Ctrl Pts',(-83.7134408793311,3.93653255159977,0.152886050252543));
#45426=CARTESIAN_POINT('Ctrl Pts',(-83.6471497020986,3.88590667858149,1.45640848909151));
#45427=CARTESIAN_POINT('Ctrl Pts',(-83.580858524866,3.12346161861065,2.73228547534992));
#45428=CARTESIAN_POINT('Ctrl Pts',(-83.5145673476336,1.99946541499167,3.39437781167899));
#45429=CARTESIAN_POINT('Ctrl Pts',(-83.4482761704011,0.875469211372724,
4.05647014800804));
#45430=CARTESIAN_POINT('Ctrl Pts',(-83.3819849931687,-0.610078135894369,
4.1047778344078));
#45431=CARTESIAN_POINT('Ctrl Pts',(-83.3156938159362,-1.77471465035827,
3.5171082701518));
#45432=CARTESIAN_POINT('Ctrl Pts',(-83.2494026387037,-2.93935116482217,
2.9294387058958));
#45433=CARTESIAN_POINT('Ctrl Pts',(-83.1831114614712,-3.7830768464829,1.70579189098402));
#45434=CARTESIAN_POINT('Ctrl Pts',(-83.1168202842387,-3.91828325098612,
0.408312428427184));
#45435=CARTESIAN_POINT('Ctrl Pts',(-83.1099346968373,-3.93232698281131,
0.273544747208272));
#45436=CARTESIAN_POINT('Ctrl Pts',(-83.1030491094359,-3.93872668788066,
0.137980505116214));
#45437=CARTESIAN_POINT('Ctrl Pts',(-83.0961635220346,-3.93777751392323,
0.00232566860396301));
#45438=CARTESIAN_POINT('Origin',(-54.75,0.,0.));
#45439=CARTESIAN_POINT('',(-81.662836477965,-3.92815744923983,0.00251336901012894));
#45440=CARTESIAN_POINT('',(-81.8461635220347,-3.92776649390124,0.00224383255729018));
#45441=CARTESIAN_POINT('',(-54.75,-3.933,-4.81653586104654E-16));
#45442=CARTESIAN_POINT('Ctrl Pts',(-81.662836477965,-3.92815744923983,0.00251336901012894));
#45443=CARTESIAN_POINT('Ctrl Pts',(-81.6875648278611,-3.93101333610238,
0.492752512294545));
#45444=CARTESIAN_POINT('Ctrl Pts',(-81.7122931777573,-3.84604462728733,
0.982037294908663));
#45445=CARTESIAN_POINT('Ctrl Pts',(-81.7370215276534,-3.66876469384258,
1.43521019205571));
#45446=CARTESIAN_POINT('Ctrl Pts',(-81.8033127048859,-3.19351682905999,
2.65006540754234));
#45447=CARTESIAN_POINT('Ctrl Pts',(-81.8696038821185,-2.05486860691728,
3.60540031203857));
#45448=CARTESIAN_POINT('Ctrl Pts',(-81.935895059351,-0.775916189644389,
3.86233306963734));
#45449=CARTESIAN_POINT('Ctrl Pts',(-82.0021862365835,0.503036227628501,
4.11926582723611));
#45450=CARTESIAN_POINT('Ctrl Pts',(-82.0684774138159,1.92229284003157,3.67779643793744));
#45451=CARTESIAN_POINT('Ctrl Pts',(-82.1347685910484,2.8298457027665,2.74073639241362));
#45452=CARTESIAN_POINT('Ctrl Pts',(-82.2010597682809,3.73739856550144,1.8036763468898));
#45453=CARTESIAN_POINT('Ctrl Pts',(-82.2673509455133,4.13324767856824,0.371025645140833));
#45454=CARTESIAN_POINT('Ctrl Pts',(-82.3336421227458,3.83553955303096,-0.899054509638602));
#45455=CARTESIAN_POINT('Ctrl Pts',(-82.3999332999783,3.53783142749368,-2.16913466441804));
#45456=CARTESIAN_POINT('Ctrl Pts',(-82.4662244772108,2.54656606335231,-3.27664427222795));
#45457=CARTESIAN_POINT('Ctrl Pts',(-82.5325156544433,1.3171317865624,-3.71279228223091));
#45458=CARTESIAN_POINT('Ctrl Pts',(-82.5988068316758,0.0876975097725195,
-4.14894029223385));
#45459=CARTESIAN_POINT('Ctrl Pts',(-82.6650980089082,-1.37990567966589,
-3.91372670442989));
#45460=CARTESIAN_POINT('Ctrl Pts',(-82.7313891861407,-2.41145936983018,
-3.11520888253495));
#45461=CARTESIAN_POINT('Ctrl Pts',(-82.7918716167488,-3.35262344457671,
-2.38666097060545));
#45462=CARTESIAN_POINT('Ctrl Pts',(-82.852354047357,-3.93080743200468,-1.18920248678531));
#45463=CARTESIAN_POINT('Ctrl Pts',(-82.912836477965,-3.93823441574634,0.00201426645151499));
#45464=CARTESIAN_POINT('Ctrl Pts',(-83.0961635220346,-3.93777751392323,
0.00232566860396301));
#45465=CARTESIAN_POINT('Ctrl Pts',(-83.0367579322034,-3.92958849016864,
-1.16804006880197));
#45466=CARTESIAN_POINT('Ctrl Pts',(-82.9773523423723,-3.37439139798938,
-2.34514913109041));
#45467=CARTESIAN_POINT('Ctrl Pts',(-82.9179467525412,-2.46172515530447,
-3.07564171091296));
#45468=CARTESIAN_POINT('Ctrl Pts',(-82.8516555753088,-1.44327352777386,
-3.89080427749445));
#45469=CARTESIAN_POINT('Ctrl Pts',(-82.7853643980763,0.0203168546331192,
-4.14981730045549));
#45470=CARTESIAN_POINT('Ctrl Pts',(-82.7190732208438,1.25667106766366,-3.73368993113562));
#45471=CARTESIAN_POINT('Ctrl Pts',(-82.6527820436113,2.49302528069421,-3.31756256181575));
#45472=CARTESIAN_POINT('Ctrl Pts',(-82.5864908663788,3.50214332434836,-2.22629480021494));
#45473=CARTESIAN_POINT('Ctrl Pts',(-82.5201996891463,3.82043533337418,-0.961216176347729));
#45474=CARTESIAN_POINT('Ctrl Pts',(-82.4539085119138,4.13872734240001,0.303862447519519));
#45475=CARTESIAN_POINT('Ctrl Pts',(-82.3876173346814,3.76619331679752,1.74275193365313));
#45476=CARTESIAN_POINT('Ctrl Pts',(-82.321326157449,2.87397577038541,2.69442497490727));
#45477=CARTESIAN_POINT('Ctrl Pts',(-82.2550349802165,1.98175822397333,3.64609801616138));
#45478=CARTESIAN_POINT('Ctrl Pts',(-82.1887438029839,0.569857156751641,
4.11055461253598));
#45479=CARTESIAN_POINT('Ctrl Pts',(-82.1224526257514,-0.713098631489105,
3.87442292682856));
#45480=CARTESIAN_POINT('Ctrl Pts',(-82.0561614485189,-1.99605441972978,
3.63829124112116));
#45481=CARTESIAN_POINT('Ctrl Pts',(-81.9898702712864,-3.15006492898956,
2.70157127333181));
#45482=CARTESIAN_POINT('Ctrl Pts',(-81.923579094054,-3.64497654656548,1.49459313833364));
#45483=CARTESIAN_POINT('Ctrl Pts',(-81.8977739033809,-3.83763097195148,
1.02475232071357));
#45484=CARTESIAN_POINT('Ctrl Pts',(-81.8719687127078,-3.93041120894692,
0.513958900310409));
#45485=CARTESIAN_POINT('Ctrl Pts',(-81.8461635220347,-3.92776649390124,
0.00224383255729018));
#45486=CARTESIAN_POINT('Origin',(-54.75,0.,0.));
#45487=CARTESIAN_POINT('',(-80.412836477965,-3.92903919912688,-0.0029659054929293));
#45488=CARTESIAN_POINT('',(-80.5961635220346,-3.92955240483563,-0.0031591487905448));
#45489=CARTESIAN_POINT('',(-54.75,-3.933,-4.81653586104654E-16));
#45490=CARTESIAN_POINT('Ctrl Pts',(-80.412836477965,-3.92903919912688,-0.0029659054929293));
#45491=CARTESIAN_POINT('Ctrl Pts',(-80.4564844311329,-3.92300599112755,
0.861866566955545));
#45492=CARTESIAN_POINT('Ctrl Pts',(-80.5001323843009,-3.64192243487377,
1.73026339850602));
#45493=CARTESIAN_POINT('Ctrl Pts',(-80.5437803374688,-3.11652780543653,
2.40975457507759));
#45494=CARTESIAN_POINT('Ctrl Pts',(-80.6100715147012,-2.31857450020302,
3.44174500635217));
#45495=CARTESIAN_POINT('Ctrl Pts',(-80.6763626919337,-0.957078468089482,
4.0379942059965));
#45496=CARTESIAN_POINT('Ctrl Pts',(-80.7426538691662,0.342487615989928,
3.92458467956292));
#45497=CARTESIAN_POINT('Ctrl Pts',(-80.8089450463987,1.64205370006938,3.81117515312933));
#45498=CARTESIAN_POINT('Ctrl Pts',(-80.8752362236312,2.87968983611469,2.98810690061779));
#45499=CARTESIAN_POINT('Ctrl Pts',(-80.9415274008637,3.48682471262449,1.83349832222383));
#45500=CARTESIAN_POINT('Ctrl Pts',(-81.0078185780962,4.0939595891343,0.678889743829845));
#45501=CARTESIAN_POINT('Ctrl Pts',(-81.0741097553286,4.07059320610855,-0.807259160446579));
#45502=CARTESIAN_POINT('Ctrl Pts',(-81.1404009325611,3.42746010389805,-1.94221005824642));
#45503=CARTESIAN_POINT('Ctrl Pts',(-81.2066921097936,2.78432700168757,-3.07716095604624));
#45504=CARTESIAN_POINT('Ctrl Pts',(-81.2729832870261,1.52142718029238,-3.8609138473695));
#45505=CARTESIAN_POINT('Ctrl Pts',(-81.3392744642586,0.218938114200209,
-3.93341184931313));
#45506=CARTESIAN_POINT('Ctrl Pts',(-81.4055656414911,-1.08355095189193,
-4.00590985125675));
#45507=CARTESIAN_POINT('Ctrl Pts',(-81.4718568187236,-2.42562926268104,
-3.36715296382081));
#45508=CARTESIAN_POINT('Ctrl Pts',(-81.5381479959561,-3.19074466436435,
-2.31058675686434));
#45509=CARTESIAN_POINT('Ctrl Pts',(-81.5797108232923,-3.67045192949554,
-1.64814749024648));
#45510=CARTESIAN_POINT('Ctrl Pts',(-81.6212736506287,-3.9233573419517,-0.821469021703119));
#45511=CARTESIAN_POINT('Ctrl Pts',(-81.662836477965,-3.92815744923983,0.00251336901012894));
#45512=CARTESIAN_POINT('Ctrl Pts',(-81.8461635220347,-3.92776649390124,
0.00224383255729018));
#45513=CARTESIAN_POINT('Ctrl Pts',(-81.8056775354753,-3.9236171776203,-0.800590357575939));
#45514=CARTESIAN_POINT('Ctrl Pts',(-81.7651915489159,-3.68458179285588,
-1.60569315898882));
#45515=CARTESIAN_POINT('Ctrl Pts',(-81.7247055623565,-3.22784252652727,
-2.25847189446946));
#45516=CARTESIAN_POINT('Ctrl Pts',(-81.658414385124,-2.47998416302114,-3.32732249006709));
#45517=CARTESIAN_POINT('Ctrl Pts',(-81.5921232078915,-1.14845471011691,
-3.98778737905524));
#45518=CARTESIAN_POINT('Ctrl Pts',(-81.525832030659,0.155039834524771,-3.93644831337552));
#45519=CARTESIAN_POINT('Ctrl Pts',(-81.4595408534265,1.45853437916645,-3.88510924769581));
#45520=CARTESIAN_POINT('Ctrl Pts',(-81.393249676194,2.73399401554557,-3.12196622734823));
#45521=CARTESIAN_POINT('Ctrl Pts',(-81.3269584989616,3.39547127727642,-1.99760793935079));
#45522=CARTESIAN_POINT('Ctrl Pts',(-81.2606673217291,4.05694853900726,-0.873249651353348));
#45523=CARTESIAN_POINT('Ctrl Pts',(-81.1943761444967,4.10444342608984,0.612323904293962));
#45524=CARTESIAN_POINT('Ctrl Pts',(-81.1280849672642,3.51613673863844,1.77663871098304));
#45525=CARTESIAN_POINT('Ctrl Pts',(-81.0617937900317,2.92783005118702,2.94095351767216));
#45526=CARTESIAN_POINT('Ctrl Pts',(-80.9955026127992,1.70372178920158,3.78400957540303));
#45527=CARTESIAN_POINT('Ctrl Pts',(-80.9292114355667,0.406168544952221,
3.91850606574213));
#45528=CARTESIAN_POINT('Ctrl Pts',(-80.8629202583342,-0.89138469929703,
4.05300255608121));
#45529=CARTESIAN_POINT('Ctrl Pts',(-80.7966290811017,-2.26238292581019,
3.47893947902867));
#45530=CARTESIAN_POINT('Ctrl Pts',(-80.7303379038692,-3.07698814181064,
2.46004200153638));
#45531=CARTESIAN_POINT('Ctrl Pts',(-80.6856131099244,-3.62657938385882,
1.77262051297274));
#45532=CARTESIAN_POINT('Ctrl Pts',(-80.6408883159795,-3.92291045278412,
0.882718340543989));
#45533=CARTESIAN_POINT('Ctrl Pts',(-80.5961635220346,-3.92955240483563,
-0.0031591487905448));
#45534=CARTESIAN_POINT('Origin',(-54.75,0.,0.));
#45535=CARTESIAN_POINT('',(-79.1628364779651,-3.9389481592111,-0.0013426765242408));
#45536=CARTESIAN_POINT('',(-79.3461635220346,-3.93921293753935,-0.000967729229624012));
#45537=CARTESIAN_POINT('',(-54.75,-3.933,-4.81653586104654E-16));
#45538=CARTESIAN_POINT('Ctrl Pts',(-79.1628364779651,-3.9389481592111,-0.0013426765242408));
#45539=CARTESIAN_POINT('Ctrl Pts',(-79.2254040344047,-3.93350653257731,
1.23034949682626));
#45540=CARTESIAN_POINT('Ctrl Pts',(-79.2879715908444,-3.30915507795444,
2.46679613944863));
#45541=CARTESIAN_POINT('Ctrl Pts',(-79.350539147284,-2.31233217295835,3.18947998834734));
#45542=CARTESIAN_POINT('Ctrl Pts',(-79.4168303245165,-1.25618474408748,
3.95517335782692));
#45543=CARTESIAN_POINT('Ctrl Pts',(-79.483121501749,0.218087617257299,4.14413250185621));
#45544=CARTESIAN_POINT('Ctrl Pts',(-79.5494126789815,1.43320267473284,3.66954939567586));
#45545=CARTESIAN_POINT('Ctrl Pts',(-79.615703856214,2.64831773220827,3.19496628949555));
#45546=CARTESIAN_POINT('Ctrl Pts',(-79.6819950334464,3.60427548581447,2.05684093310556));
#45547=CARTESIAN_POINT('Ctrl Pts',(-79.7482862106789,3.86190796212373,0.778029283672377));
#45548=CARTESIAN_POINT('Ctrl Pts',(-79.8145773879114,4.11954043843302,-0.500782365760914));
#45549=CARTESIAN_POINT('Ctrl Pts',(-79.8808685651439,3.67884763744538,-1.92028030823745));
#45550=CARTESIAN_POINT('Ctrl Pts',(-79.9471597423764,2.74228428436574,-2.82834573167552));
#45551=CARTESIAN_POINT('Ctrl Pts',(-80.0134509196089,1.80572093128612,-3.73641115511357));
#45552=CARTESIAN_POINT('Ctrl Pts',(-80.0797420968414,0.373287026114508,
-4.1330440595131));
#45553=CARTESIAN_POINT('Ctrl Pts',(-80.1460332740738,-0.896955824524606,
-3.83603088139523));
#45554=CARTESIAN_POINT('Ctrl Pts',(-80.2123244513063,-2.16719867516372,
-3.53901770327735));
#45555=CARTESIAN_POINT('Ctrl Pts',(-80.2786156285388,-3.27525047127037,
-2.54835844264207));
#45556=CARTESIAN_POINT('Ctrl Pts',(-80.3449068057713,-3.71207108014695,
-1.319162980872));
#45557=CARTESIAN_POINT('Ctrl Pts',(-80.3675500298359,-3.86127686190769,
-0.899303967622076));
#45558=CARTESIAN_POINT('Ctrl Pts',(-80.3901932539004,-3.93216904304033,
-0.45161455979811));
#45559=CARTESIAN_POINT('Ctrl Pts',(-80.412836477965,-3.92903919912688,-0.0029659054929293));
#45560=CARTESIAN_POINT('Ctrl Pts',(-80.5961635220346,-3.92955240483563,
-0.0031591487905448));
#45561=CARTESIAN_POINT('Ctrl Pts',(-80.574597138747,-3.93275516713114,-0.430331010206185));
#45562=CARTESIAN_POINT('Ctrl Pts',(-80.5530307554594,-3.86859978389275,
-0.856567057420322));
#45563=CARTESIAN_POINT('Ctrl Pts',(-80.5314643721718,-3.73300180598275,
-1.25871370481774));
#45564=CARTESIAN_POINT('Ctrl Pts',(-80.4651731949393,-3.31619804866662,
-2.4948400557474));
#45565=CARTESIAN_POINT('Ctrl Pts',(-80.3988820177068,-2.22437832854666,
-3.50336087967453));
#45566=CARTESIAN_POINT('Ctrl Pts',(-80.3325908404744,-0.959125745947673,
-3.82096067470299));
#45567=CARTESIAN_POINT('Ctrl Pts',(-80.2662996632419,0.306126836651311,
-4.13856046973145));
#45568=CARTESIAN_POINT('Ctrl Pts',(-80.2000084860094,1.74481228172936,-3.76523923586116));
#45569=CARTESIAN_POINT('Ctrl Pts',(-80.1337173087769,2.69599701881079,-2.8725011311973));
#45570=CARTESIAN_POINT('Ctrl Pts',(-80.0674261315444,3.6471817558922,-1.97976302653346));
#45571=CARTESIAN_POINT('Ctrl Pts',(-80.0011349543119,4.1108657849771,-0.567608051076111));
#45572=CARTESIAN_POINT('Ctrl Pts',(-79.9348437770794,3.87403218706907,0.715218349680184));
#45573=CARTESIAN_POINT('Ctrl Pts',(-79.868552599847,3.63719858916104,1.99804475043648));
#45574=CARTESIAN_POINT('Ctrl Pts',(-79.8022614226145,2.69984736426009,3.15154257649167));
#45575=CARTESIAN_POINT('Ctrl Pts',(-79.735970245382,1.49259862740443,3.64579374233333));
#45576=CARTESIAN_POINT('Ctrl Pts',(-79.6696790681495,0.285349890548748,
4.140044908175));
#45577=CARTESIAN_POINT('Ctrl Pts',(-79.603387890917,-1.19179635826171,3.97504941380306));
#45578=CARTESIAN_POINT('Ctrl Pts',(-79.5370967136845,-2.26023761583134,
3.22660635872235));
#45579=CARTESIAN_POINT('Ctrl Pts',(-79.4734523164678,-3.28601966765575,
2.50804607543565));
#45580=CARTESIAN_POINT('Ctrl Pts',(-79.4098079192513,-3.93508158397175,
1.25169827097145));
#45581=CARTESIAN_POINT('Ctrl Pts',(-79.3461635220346,-3.93921293753935,
-0.000967729229624012));
#45582=CARTESIAN_POINT('Origin',(-54.75,0.,0.));
#45583=CARTESIAN_POINT('',(-77.912836477965,-3.93313541941523,0.00362608069297291));
#45584=CARTESIAN_POINT('',(-78.0961635220346,-3.93248803517055,0.00363500034747385));
#45585=CARTESIAN_POINT('',(-54.75,-3.933,-4.81653586104654E-16));
#45586=CARTESIAN_POINT('Ctrl Pts',(-77.912836477965,-3.93313541941523,0.00362608069297291));
#45587=CARTESIAN_POINT('Ctrl Pts',(-77.9280324604439,-3.93591805124307,
0.303922101060753));
#45588=CARTESIAN_POINT('Ctrl Pts',(-77.9432284429229,-3.90444631903579,
0.603640822955118));
#45589=CARTESIAN_POINT('Ctrl Pts',(-77.9584244254018,-3.83652106142591,
0.894856870902738));
#45590=CARTESIAN_POINT('Ctrl Pts',(-78.0247156026343,-3.54020291963971,
2.16526203714848));
#45591=CARTESIAN_POINT('Ctrl Pts',(-78.0910067798669,-2.55015005906897,
3.27385568985141));
#45592=CARTESIAN_POINT('Ctrl Pts',(-78.1572979570994,-1.32119378028406,
3.71134876683736));
#45593=CARTESIAN_POINT('Ctrl Pts',(-78.2235891343319,-0.092237501499141,
4.1488418438233));
#45594=CARTESIAN_POINT('Ctrl Pts',(-78.2898803115643,1.37562219549991,3.91523434509225));
#45595=CARTESIAN_POINT('Ctrl Pts',(-78.3561714887968,2.40804905895374,3.11784579539117));
#45596=CARTESIAN_POINT('Ctrl Pts',(-78.4224626660292,3.44047592240755,2.32045724569012));
#45597=CARTESIAN_POINT('Ctrl Pts',(-78.4887538432617,4.03746995231615,0.959287645018993));
#45598=CARTESIAN_POINT('Ctrl Pts',(-78.5550450204942,3.92477147844376,-0.340340294647681));
#45599=CARTESIAN_POINT('Ctrl Pts',(-78.6213361977267,3.81207300457136,-1.63996823431439));
#45600=CARTESIAN_POINT('Ctrl Pts',(-78.6876273749592,2.98968202691799,-2.87805451297669));
#45601=CARTESIAN_POINT('Ctrl Pts',(-78.7539185521917,1.835405804914,-3.48582102315285));
#45602=CARTESIAN_POINT('Ctrl Pts',(-78.8202097294241,0.681129582910052,
-4.093587533329));
#45603=CARTESIAN_POINT('Ctrl Pts',(-78.8865009066566,-0.805031883444454,
-4.07103427501903));
#45604=CARTESIAN_POINT('Ctrl Pts',(-78.9527920838891,-1.94033449075904,
-3.42852223824453));
#45605=CARTESIAN_POINT('Ctrl Pts',(-79.0190832611216,-3.07563709807365,
-2.78601020147002));
#45606=CARTESIAN_POINT('Ctrl Pts',(-79.0853744383542,-3.86008084634829,
-1.52353938623096));
#45607=CARTESIAN_POINT('Ctrl Pts',(-79.1516656155866,-3.93329147228718,
-0.221090181146506));
#45608=CARTESIAN_POINT('Ctrl Pts',(-79.1553892363794,-3.93740376324929,
-0.147930717940411));
#45609=CARTESIAN_POINT('Ctrl Pts',(-79.1591128571723,-3.93927201002505,
-0.0746451170862052));
#45610=CARTESIAN_POINT('Ctrl Pts',(-79.1628364779651,-3.9389481592111,-0.0013426765242408));
#45611=CARTESIAN_POINT('Ctrl Pts',(-79.3461635220346,-3.93921293753935,
-0.000967729229624012));
#45612=CARTESIAN_POINT('Ctrl Pts',(-79.3435167420188,-3.9393847481706,-0.0530623594071839));
#45613=CARTESIAN_POINT('Ctrl Pts',(-79.3408699620029,-3.93844116481995,
-0.105150621980919));
#45614=CARTESIAN_POINT('Ctrl Pts',(-79.3382231819871,-3.93636289675727,
-0.157193572384996));
#45615=CARTESIAN_POINT('Ctrl Pts',(-79.2719320047546,-3.88431065378475,
-1.46065983262229));
#45616=CARTESIAN_POINT('Ctrl Pts',(-79.2056408275221,-3.12046990151082,
-2.73570173730745));
#45617=CARTESIAN_POINT('Ctrl Pts',(-79.1393496502896,-1.99574986571674,
-3.39656372642382));
#45618=CARTESIAN_POINT('Ctrl Pts',(-79.0730584730571,-0.871029829922625,
-4.05742571554021));
#45619=CARTESIAN_POINT('Ctrl Pts',(-79.0067672958246,0.614569489391649,
-4.10410778908778));
#45620=CARTESIAN_POINT('Ctrl Pts',(-78.9404761185922,1.7785622397629,-3.51516415455325));
#45621=CARTESIAN_POINT('Ctrl Pts',(-78.8741849413597,2.94255499013405,-2.92622052001877));
#45622=CARTESIAN_POINT('Ctrl Pts',(-78.8078937641272,3.78494117156225,-1.70165117740231));
#45623=CARTESIAN_POINT('Ctrl Pts',(-78.7416025868947,3.91872770747519,-0.404024539889156));
#45624=CARTESIAN_POINT('Ctrl Pts',(-78.6753114096622,4.05251424338815,0.893602097624076));
#45625=CARTESIAN_POINT('Ctrl Pts',(-78.6090202324297,3.47770113378575,2.26428603003402));
#45626=CARTESIAN_POINT('Ctrl Pts',(-78.5427290551972,2.45835811134335,3.07833365159769));
#45627=CARTESIAN_POINT('Ctrl Pts',(-78.4764378779647,1.43901508890095,3.89238127316137));
#45628=CARTESIAN_POINT('Ctrl Pts',(-78.4101467007323,-0.0248578463814547,
4.14979258387876));
#45629=CARTESIAN_POINT('Ctrl Pts',(-78.3438555234998,-1.26075596517005,
3.73231256333852));
#45630=CARTESIAN_POINT('Ctrl Pts',(-78.2775643462673,-2.49665408395865,
3.31483254279828));
#45631=CARTESIAN_POINT('Ctrl Pts',(-78.2112731690348,-3.50457738625344,
2.2224611910004));
#45632=CARTESIAN_POINT('Ctrl Pts',(-78.1449819918023,-3.82148487220956,
0.95703502842889));
#45633=CARTESIAN_POINT('Ctrl Pts',(-78.1287091685464,-3.8992777207111,0.646404607510269));
#45634=CARTESIAN_POINT('Ctrl Pts',(-78.1124363452905,-3.93543137278026,
0.325346258476264));
#45635=CARTESIAN_POINT('Ctrl Pts',(-78.0961635220346,-3.93248803517055,
0.00363500034747385));
#45636=CARTESIAN_POINT('Origin',(-54.75,0.,0.));
#45637=CARTESIAN_POINT('',(-76.662836477965,-3.92650124665457,-0.000318401066521645));
#45638=CARTESIAN_POINT('',(-76.8461635220347,-3.92658087967646,-0.000668997711400442));
#45639=CARTESIAN_POINT('',(-54.75,-3.933,-4.81653586104654E-16));
#45640=CARTESIAN_POINT('Ctrl Pts',(-76.662836477965,-3.92650124665457,-0.000318401066521645));
#45641=CARTESIAN_POINT('Ctrl Pts',(-76.6969520637157,-3.92601417802138,
0.676735860399884));
#45642=CARTESIAN_POINT('Ctrl Pts',(-76.7310676494664,-3.75992112010715,
1.35401404301683));
#45643=CARTESIAN_POINT('Ctrl Pts',(-76.7651832352171,-3.42958334624692,
1.93845834242374));
#45644=CARTESIAN_POINT('Ctrl Pts',(-76.8314744124496,-2.78769256724728,
3.074112319395));
#45645=CARTESIAN_POINT('Ctrl Pts',(-76.8977655896821,-1.52565113609083,
3.85924668979409));
#45646=CARTESIAN_POINT('Ctrl Pts',(-76.9640567669146,-0.223242181908324,
3.93316991781225));
#45647=CARTESIAN_POINT('Ctrl Pts',(-77.0303479441471,1.07916677227421,4.00709314583042));
#45648=CARTESIAN_POINT('Ctrl Pts',(-77.0966391213795,2.4219432494828,3.36980523146763));
#45649=CARTESIAN_POINT('Ctrl Pts',(-77.162930298612,3.18821435754475,2.31407689684504));
#45650=CARTESIAN_POINT('Ctrl Pts',(-77.2292214758445,3.95448546560672,1.25834856222242));
#45651=CARTESIAN_POINT('Ctrl Pts',(-77.2955126530771,4.14425120452202,-0.215820192660025));
#45652=CARTESIAN_POINT('Ctrl Pts',(-77.3618038303095,3.67033299901256,-1.43119472837413));
#45653=CARTESIAN_POINT('Ctrl Pts',(-77.428095007542,3.19641479350313,-2.64656926408816));
#45654=CARTESIAN_POINT('Ctrl Pts',(-77.4943861847744,2.05881264356902,-3.60314958063389));
#45655=CARTESIAN_POINT('Ctrl Pts',(-77.5606773620069,0.780142144793593,
-3.86148169853015));
#45656=CARTESIAN_POINT('Ctrl Pts',(-77.6269685392394,-0.498528353981874,
-4.11981381642642));
#45657=CARTESIAN_POINT('Ctrl Pts',(-77.693259716472,-1.91826720159868,-3.67989773567319));
#45658=CARTESIAN_POINT('Ctrl Pts',(-77.7595508937044,-2.82684491390624,
-2.74383135540231));
#45659=CARTESIAN_POINT('Ctrl Pts',(-77.810646088458,-3.52714859076301,-2.02234026112835));
#45660=CARTESIAN_POINT('Ctrl Pts',(-77.8617412832115,-3.92377905727359,
-1.00609367027775));
#45661=CARTESIAN_POINT('Ctrl Pts',(-77.912836477965,-3.93313541941523,0.00362608069297291));
#45662=CARTESIAN_POINT('Ctrl Pts',(-78.0961635220346,-3.93248803517055,
0.00363500034747385));
#45663=CARTESIAN_POINT('Ctrl Pts',(-78.0461451680581,-3.92344099397065,
-0.985220303633294));
#45664=CARTESIAN_POINT('Ctrl Pts',(-77.9961268140815,-3.54501146993409,
-1.98024419461987));
#45665=CARTESIAN_POINT('Ctrl Pts',(-77.946108460105,-2.87102563211285,-2.69756825565498));
#45666=CARTESIAN_POINT('Ctrl Pts',(-77.8798172828725,-1.97776723644254,
-3.64826440382224));
#45667=CARTESIAN_POINT('Ctrl Pts',(-77.8135261056399,-0.565358775484557,
-4.11117572681156));
#45668=CARTESIAN_POINT('Ctrl Pts',(-77.7472349284074,0.717337853767346,
-3.87364028760014));
#45669=CARTESIAN_POINT('Ctrl Pts',(-77.6809437511749,2.00003448301918,-3.63610484838873));
#45670=CARTESIAN_POINT('Ctrl Pts',(-77.6146525739425,3.15301928056487,-2.69812264697659));
#45671=CARTESIAN_POINT('Ctrl Pts',(-77.54836139671,3.64660984671592,-1.49060366965903));
#45672=CARTESIAN_POINT('Ctrl Pts',(-77.4820702194775,4.14020041286697,-0.283084692341431));
#45673=CARTESIAN_POINT('Ctrl Pts',(-77.415779042245,3.97439674762335,1.19397106088165));
#45674=CARTESIAN_POINT('Ctrl Pts',(-77.3494878650125,3.22536922501803,2.26200266058046));
#45675=CARTESIAN_POINT('Ctrl Pts',(-77.28319668778,2.47634170241269,3.33003426027929));
#45676=CARTESIAN_POINT('Ctrl Pts',(-77.2169055105476,1.14409032244569,3.98904170645383));
#45677=CARTESIAN_POINT('Ctrl Pts',(-77.1506143333151,-0.159347263188599,
3.93627630177059));
#45678=CARTESIAN_POINT('Ctrl Pts',(-77.0843231560826,-1.46278484882285,
3.88351089708735));
#45679=CARTESIAN_POINT('Ctrl Pts',(-77.0180319788501,-2.73740864012438,
3.1189726415463));
#45680=CARTESIAN_POINT('Ctrl Pts',(-76.9517408016176,-3.39765515879417,
1.99389119464573));
#45681=CARTESIAN_POINT('Ctrl Pts',(-76.9165483750899,-3.74816450360395,
1.39661192143539));
#45682=CARTESIAN_POINT('Ctrl Pts',(-76.8813559485623,-3.92552400471929,
0.697720821079181));
#45683=CARTESIAN_POINT('Ctrl Pts',(-76.8461635220347,-3.92658087967646,
-0.000668997711400442));
#45684=CARTESIAN_POINT('Origin',(-54.75,0.,0.));
#45685=CARTESIAN_POINT('',(-75.412836477965,-3.93430794215879,-0.00351519416923518));
#45686=CARTESIAN_POINT('',(-75.5961635220347,-3.93495109289722,-0.00340104241912089));
#45687=CARTESIAN_POINT('',(-54.75,-3.933,-4.81653586104654E-16));
#45688=CARTESIAN_POINT('Ctrl Pts',(-75.412836477965,-3.93430794215879,-0.00351519416923518));
#45689=CARTESIAN_POINT('Ctrl Pts',(-75.4658716669875,-3.92460957776598,
1.04374099397056));
#45690=CARTESIAN_POINT('Ctrl Pts',(-75.51890685601,-3.49386462216488,2.09804064888604));
#45691=CARTESIAN_POINT('Ctrl Pts',(-75.5719420450325,-2.74537760506035,
2.82534324990779));
#45692=CARTESIAN_POINT('Ctrl Pts',(-75.638233222265,-1.80980847781403,3.73443297909794));
#45693=CARTESIAN_POINT('Ctrl Pts',(-75.7045243994974,-0.37780945214924,
4.1326331097266));
#45694=CARTESIAN_POINT('Ctrl Pts',(-75.7708155767298,0.892757649401435,
3.83701009297626));
#45695=CARTESIAN_POINT('Ctrl Pts',(-75.8371067539623,2.16332475095207,3.54138707622592));
#45696=CARTESIAN_POINT('Ctrl Pts',(-75.9033979311948,3.27245992838864,2.5519409120966));
#45697=CARTESIAN_POINT('Ctrl Pts',(-75.9696891084273,3.71062534251835,1.32322418419065));
#45698=CARTESIAN_POINT('Ctrl Pts',(-76.0359802856598,4.14879075664809,0.094507456284634));
#45699=CARTESIAN_POINT('Ctrl Pts',(-76.1022714628923,3.91598640747094,-1.37347983539797));
#45700=CARTESIAN_POINT('Ctrl Pts',(-76.1685626401248,3.11916285200426,-2.40634282196928));
#45701=CARTESIAN_POINT('Ctrl Pts',(-76.2348538173573,2.32233929653761,-3.43920580854055));
#45702=CARTESIAN_POINT('Ctrl Pts',(-76.3011449945897,0.961496534781437,
-4.03694449000047));
#45703=CARTESIAN_POINT('Ctrl Pts',(-76.3674361718222,-0.33819287142288,
-3.92495710242611));
#45704=CARTESIAN_POINT('Ctrl Pts',(-76.4337273490547,-1.6378822776272,-3.81296971485175));
#45705=CARTESIAN_POINT('Ctrl Pts',(-76.5000185262872,-2.8764183282797,-2.99125625824311));
#45706=CARTESIAN_POINT('Ctrl Pts',(-76.5663097035197,-3.48481629018454,
-1.83731273816706));
#45707=CARTESIAN_POINT('Ctrl Pts',(-76.5984852950015,-3.78011296611989,
-1.27722590844014));
#45708=CARTESIAN_POINT('Ctrl Pts',(-76.6306608864832,-3.92696061796596,
-0.638871744020152));
#45709=CARTESIAN_POINT('Ctrl Pts',(-76.662836477965,-3.92650124665457,-0.000318401066521645));
#45710=CARTESIAN_POINT('Ctrl Pts',(-76.8461635220347,-3.92658087967646,
-0.000668997711400442));
#45711=CARTESIAN_POINT('Ctrl Pts',(-76.8150647713298,-3.92751481615262,
-0.617820271787113));
#45712=CARTESIAN_POINT('Ctrl Pts',(-76.783966020625,-3.79077655588946,-1.2345801022648));
#45713=CARTESIAN_POINT('Ctrl Pts',(-76.7528672699202,-3.51419051818756,
-1.78048523612163));
#45714=CARTESIAN_POINT('Ctrl Pts',(-76.6865760926877,-2.92461011287302,
-2.94415558172847));
#45715=CARTESIAN_POINT('Ctrl Pts',(-76.6202849154552,-1.69958005620581,
-3.78587163468196));
#45716=CARTESIAN_POINT('Ctrl Pts',(-76.5539937382227,-0.401880413879147,
-3.91894817611904));
#45717=CARTESIAN_POINT('Ctrl Pts',(-76.4877025609902,0.89581922844744,-4.05202471755611));
#45718=CARTESIAN_POINT('Ctrl Pts',(-76.4214113837578,2.26618845643342,-3.47646174747684));
#45719=CARTESIAN_POINT('Ctrl Pts',(-76.3551202065253,3.07967823987134,-2.45667348522945));
#45720=CARTESIAN_POINT('Ctrl Pts',(-76.2888290292928,3.89316802330925,-1.43688522298207));
#45721=CARTESIAN_POINT('Ctrl Pts',(-76.2225378520603,4.14977836219906,0.0271283314335248));
#45722=CARTESIAN_POINT('Ctrl Pts',(-76.1562466748278,3.73162220340928,1.26279784810924));
#45723=CARTESIAN_POINT('Ctrl Pts',(-76.0899554975953,3.31346604461948,2.49846736478502));
#45724=CARTESIAN_POINT('Ctrl Pts',(-76.0236643203629,2.22054338815007,3.50579284372096));
#45725=CARTESIAN_POINT('Ctrl Pts',(-75.9573731431304,0.954944024417141,
3.822007925737));
#45726=CARTESIAN_POINT('Ctrl Pts',(-75.8910819658979,-0.31065533931575,
4.13822300775303));
#45727=CARTESIAN_POINT('Ctrl Pts',(-75.8247907886653,-1.7489314103121,3.7633276928492));
#45728=CARTESIAN_POINT('Ctrl Pts',(-75.7584996114329,-2.69913868496981,
2.86954927357345));
#45729=CARTESIAN_POINT('Ctrl Pts',(-75.7043875816335,-3.47477198201586,
2.13997760993702));
#45730=CARTESIAN_POINT('Ctrl Pts',(-75.6502755518341,-3.92520026725676,
1.06466905972103));
#45731=CARTESIAN_POINT('Ctrl Pts',(-75.5961635220347,-3.93495109289722,
-0.0034010424191209));
#45732=CARTESIAN_POINT('Origin',(-54.75,0.,0.));
#45733=CARTESIAN_POINT('',(-74.162836477965,-3.93829176197897,0.00197029291977097));
#45734=CARTESIAN_POINT('',(-74.3461635220347,-3.93784216741542,0.00228528798276027));
#45735=CARTESIAN_POINT('',(-54.75,-3.933,-4.81653586104654E-16));
#45736=CARTESIAN_POINT('Ctrl Pts',(-74.162836477965,-3.93829176197897,0.00197029291977097));
#45737=CARTESIAN_POINT('Ctrl Pts',(-74.1685000930268,-3.9389747377774,0.113512333841672));
#45738=CARTESIAN_POINT('Ctrl Pts',(-74.1741637080885,-3.93464848695273,
0.225000608832605));
#45739=CARTESIAN_POINT('Ctrl Pts',(-74.1798273231502,-3.92514155145442,
0.336045346958482));
#45740=CARTESIAN_POINT('Ctrl Pts',(-74.2461185003827,-3.81386528370203,
1.6357958306324));
#45741=CARTESIAN_POINT('Ctrl Pts',(-74.3124096776152,-2.99282959412186,
2.87478128251356));
#45742=CARTESIAN_POINT('Ctrl Pts',(-74.3787008548477,-1.83921912141205,
3.48381051402035));
#45743=CARTESIAN_POINT('Ctrl Pts',(-74.4449920320802,-0.685608648702251,
4.09283974552713));
#45744=CARTESIAN_POINT('Ctrl Pts',(-74.5112832093127,0.800576607137177,
4.07191275665953));
#45745=CARTESIAN_POINT('Ctrl Pts',(-74.5775743865452,1.93658161380189,3.43064342758774));
#45746=CARTESIAN_POINT('Ctrl Pts',(-74.6438655637776,3.07258662046659,2.78937409851594));
#45747=CARTESIAN_POINT('Ctrl Pts',(-74.7101567410101,3.85841137795658,1.52776242923994));
#45748=CARTESIAN_POINT('Ctrl Pts',(-74.7764479182426,3.93304718592474,0.22539411584145));
#45749=CARTESIAN_POINT('Ctrl Pts',(-74.8427390954751,4.00768299389289,-1.076974197557));
#45750=CARTESIAN_POINT('Ctrl Pts',(-74.9090302727075,3.37112985233926,-2.42009915507794));
#45751=CARTESIAN_POINT('Ctrl Pts',(-74.9753214499401,2.31582092800211,-3.18694777233545));
#45752=CARTESIAN_POINT('Ctrl Pts',(-75.0416126271726,1.26051200366493,-3.95379638959298));
#45753=CARTESIAN_POINT('Ctrl Pts',(-75.1079038044051,-0.213552703455776,
-4.14436866658707));
#45754=CARTESIAN_POINT('Ctrl Pts',(-75.1741949816376,-1.42918635358045,
-3.67111550361819));
#45755=CARTESIAN_POINT('Ctrl Pts',(-75.24048615887,-2.64482000370512,-3.19786234064932));
#45756=CARTESIAN_POINT('Ctrl Pts',(-75.3067773361024,-3.60202259683376,
-2.0607837377175));
#45757=CARTESIAN_POINT('Ctrl Pts',(-75.3730685133349,-3.86105427898415,
-0.78225477237576));
#45758=CARTESIAN_POINT('Ctrl Pts',(-75.3863245015449,-3.91285183437474,
-0.526592320775261));
#45759=CARTESIAN_POINT('Ctrl Pts',(-75.399580489755,-3.93673201957639,-0.265273772553341));
#45760=CARTESIAN_POINT('Ctrl Pts',(-75.412836477965,-3.93430794215879,-0.00351519416923518));
#45761=CARTESIAN_POINT('Ctrl Pts',(-75.5961635220347,-3.93495109289722,
-0.0034010424191209));
#45762=CARTESIAN_POINT('Ctrl Pts',(-75.5839843746017,-3.93714573877374,
-0.243794597993349));
#45763=CARTESIAN_POINT('Ctrl Pts',(-75.5718052271686,-3.9170166442977,-0.483821469881175));
#45764=CARTESIAN_POINT('Ctrl Pts',(-75.5596260797355,-3.87324722853908,
-0.719457143116103));
#45765=CARTESIAN_POINT('Ctrl Pts',(-75.493334902503,-3.63501001913161,-2.00202361688233));
#45766=CARTESIAN_POINT('Ctrl Pts',(-75.4270437252704,-2.69639712199763,
-3.15449504076718));
#45767=CARTESIAN_POINT('Ctrl Pts',(-75.3607525480379,-1.48860826569452,
-3.64742485946899));
#45768=CARTESIAN_POINT('Ctrl Pts',(-75.2944613708054,-0.280819409391409,
-4.1403546781708));
#45769=CARTESIAN_POINT('Ctrl Pts',(-75.228170193573,1.19614540608083,-3.97374289168959));
#45770=CARTESIAN_POINT('Ctrl Pts',(-75.1618790163406,2.26376702818862,-3.22413112578451));
#45771=CARTESIAN_POINT('Ctrl Pts',(-75.0955878391081,3.3313886502965,-2.47451935987938));
#45772=CARTESIAN_POINT('Ctrl Pts',(-75.0292966618756,3.98966707903983,-1.14190761455027));
#45773=CARTESIAN_POINT('Ctrl Pts',(-74.9630054846431,3.93618852844139,0.161500906290973));
#45774=CARTESIAN_POINT('Ctrl Pts',(-74.8967143074106,3.88270997784296,1.46490942713211));
#45775=CARTESIAN_POINT('Ctrl Pts',(-74.8304231301781,3.11747444790289,2.73911472348538));
#45776=CARTESIAN_POINT('Ctrl Pts',(-74.7641319529456,1.99203192669418,3.39874557406075));
#45777=CARTESIAN_POINT('Ctrl Pts',(-74.6978407757132,0.866589405485442,
4.05837642463612));
#45778=CARTESIAN_POINT('Ctrl Pts',(-74.6315495984807,-0.619060106991951,
4.10343282943355));
#45779=CARTESIAN_POINT('Ctrl Pts',(-74.5652584212482,-1.78240769948418,
3.51321582983254));
#45780=CARTESIAN_POINT('Ctrl Pts',(-74.4989672440157,-2.9457552919764,2.92299883023154));
#45781=CARTESIAN_POINT('Ctrl Pts',(-74.4326760667832,-3.78680096448347,
1.6975084262321));
#45782=CARTESIAN_POINT('Ctrl Pts',(-74.3663848895507,-3.91916747160762,
0.399736167564488));
#45783=CARTESIAN_POINT('Ctrl Pts',(-74.359644433712,-3.93262643602852,0.267779292405271));
#45784=CARTESIAN_POINT('Ctrl Pts',(-74.3529039778734,-3.93875855994925,
0.135075114875559));
#45785=CARTESIAN_POINT('Ctrl Pts',(-74.3461635220347,-3.93784216741542,
0.00228528798276027));
#45786=CARTESIAN_POINT('Origin',(-54.75,0.,0.));
#45787=CARTESIAN_POINT('',(-72.912836477965,-3.92821364041606,0.00254794616387777));
#45788=CARTESIAN_POINT('',(-73.0961635220347,-3.92781646010829,0.00228144192526316));
#45789=CARTESIAN_POINT('',(-54.75,-3.933,-4.81653586104654E-16));
#45790=CARTESIAN_POINT('Ctrl Pts',(-72.912836477965,-3.92821364041606,0.00254794616387777));
#45791=CARTESIAN_POINT('Ctrl Pts',(-72.9374196962985,-3.93109434647776,
0.48989238060394));
#45792=CARTESIAN_POINT('Ctrl Pts',(-72.962002914632,-3.84714999645044,0.976279715033341));
#45793=CARTESIAN_POINT('Ctrl Pts',(-72.9865861329655,-3.67189690925834,
1.42717755095344));
#45794=CARTESIAN_POINT('Ctrl Pts',(-73.052877310198,-3.1993089305005,2.64306995158314));
#45795=CARTESIAN_POINT('Ctrl Pts',(-73.1191684874305,-2.06275421496071,
3.60089453475158));
#45796=CARTESIAN_POINT('Ctrl Pts',(-73.185459664663,-0.784367165786236,
3.86062570361371));
#45797=CARTESIAN_POINT('Ctrl Pts',(-73.2517508418955,0.494019883388161,
4.12035687247583));
#45798=CARTESIAN_POINT('Ctrl Pts',(-73.3180420191279,1.91423926619718,3.68199462703174));
#45799=CARTESIAN_POINT('Ctrl Pts',(-73.3843331963604,2.8238407401297,2.746923032877));
#45800=CARTESIAN_POINT('Ctrl Pts',(-73.4506243735929,3.73344221406231,1.81185143872218));
#45801=CARTESIAN_POINT('Ctrl Pts',(-73.5169155508254,4.13242577911829,0.380070495856531));
#45802=CARTESIAN_POINT('Ctrl Pts',(-73.5832067280579,3.83749797589989,-0.890658160649008));
#45803=CARTESIAN_POINT('Ctrl Pts',(-73.6494979052904,3.54257017268151,-2.16138681715447));
#45804=CARTESIAN_POINT('Ctrl Pts',(-73.7157890825228,2.55373100118889,-3.27106318729991));
#45805=CARTESIAN_POINT('Ctrl Pts',(-73.7820802597553,1.32525419198386,-3.70990080740653));
#45806=CARTESIAN_POINT('Ctrl Pts',(-73.8483714369878,0.0967773827788009,
-4.14873842751317));
#45807=CARTESIAN_POINT('Ctrl Pts',(-73.9146626142203,-1.37133706413864,
-3.91673729758093));
#45808=CARTESIAN_POINT('Ctrl Pts',(-73.9809537914528,-2.40463586463505,
-3.12047897488147));
#45809=CARTESIAN_POINT('Ctrl Pts',(-74.0415813536236,-3.34965434044744,
-2.39224932232706));
#45810=CARTESIAN_POINT('Ctrl Pts',(-74.1022089157943,-3.93098067935254,
-1.19205895287587));
#45811=CARTESIAN_POINT('Ctrl Pts',(-74.162836477965,-3.93829176197897,0.00197029291977097));
#45812=CARTESIAN_POINT('Ctrl Pts',(-74.3461635220347,-3.93784216741542,
0.00228528798276027));
#45813=CARTESIAN_POINT('Ctrl Pts',(-74.2866128006409,-3.92974600333162,
-1.17088907506766));
#45814=CARTESIAN_POINT('Ctrl Pts',(-74.227062079247,-3.37148448707964,-2.35074871895834));
#45815=CARTESIAN_POINT('Ctrl Pts',(-74.1675113578533,-2.45498812369899,
-3.08102190622906));
#45816=CARTESIAN_POINT('Ctrl Pts',(-74.1012201806208,-1.4347549269249,-3.89395360801932));
#45817=CARTESIAN_POINT('Ctrl Pts',(-74.0349290033883,0.0293988083645495,
-4.14976289826403));
#45818=CARTESIAN_POINT('Ctrl Pts',(-73.9686378261559,1.26483935302405,-3.73093072640168));
#45819=CARTESIAN_POINT('Ctrl Pts',(-73.9023466489234,2.50027989768352,-3.31209855453934));
#45820=CARTESIAN_POINT('Ctrl Pts',(-73.8360554716908,3.50700725171301,-2.21862492056999));
#45821=CARTESIAN_POINT('Ctrl Pts',(-73.7697642944583,3.82252983512861,-0.952852734538805));
#45822=CARTESIAN_POINT('Ctrl Pts',(-73.7034731172259,4.13805241854422,0.312919451492413));
#45823=CARTESIAN_POINT('Ctrl Pts',(-73.6371819399934,3.76237023134582,1.75099018958553));
#45824=CARTESIAN_POINT('Ctrl Pts',(-73.5708907627609,2.86807205602136,2.70070830628483));
#45825=CARTESIAN_POINT('Ctrl Pts',(-73.5045995855285,1.97377388069691,3.65042642298412));
#45826=CARTESIAN_POINT('Ctrl Pts',(-73.4383084082959,0.560859717246415,
4.11179191828967));
#45827=CARTESIAN_POINT('Ctrl Pts',(-73.3720172310634,-0.721576217092039,
3.87285301000355));
#45828=CARTESIAN_POINT('Ctrl Pts',(-73.3057260538309,-2.00401215143046,
3.63391410171745));
#45829=CARTESIAN_POINT('Ctrl Pts',(-73.2394348765985,-3.15596985665681,
2.69467078983973));
#45830=CARTESIAN_POINT('Ctrl Pts',(-73.173143699366,-3.64823878034857,1.48661241610825));
#45831=CARTESIAN_POINT('Ctrl Pts',(-73.1474836402556,-3.83878675682919,
1.01899590101592));
#45832=CARTESIAN_POINT('Ctrl Pts',(-73.1218235811451,-3.93049241100765,
0.511102355713064));
#45833=CARTESIAN_POINT('Ctrl Pts',(-73.0961635220347,-3.92781646010829,
0.00228144192526316));
#45834=CARTESIAN_POINT('Origin',(-54.75,0.,0.));
#45835=CARTESIAN_POINT('',(-71.662836477965,-3.92897287541266,-0.00293764914132633));
#45836=CARTESIAN_POINT('',(-71.8461635220347,-3.92948114538815,-0.00313483220630379));
#45837=CARTESIAN_POINT('',(-54.75,-3.933,-4.81653586104654E-16));
#45838=CARTESIAN_POINT('Ctrl Pts',(-71.662836477965,-3.92897287541266,-0.00293764914132633));
#45839=CARTESIAN_POINT('Ctrl Pts',(-71.7063392995703,-3.92302352206136,
0.859055801694659));
#45840=CARTESIAN_POINT('Ctrl Pts',(-71.7498421211755,-3.64395843373945,
1.72455195491687));
#45841=CARTESIAN_POINT('Ctrl Pts',(-71.7933449427808,-3.12179416362893,
2.40292818746188));
#45842=CARTESIAN_POINT('Ctrl Pts',(-71.8596361200133,-2.3261013120603,3.43666249256066));
#45843=CARTESIAN_POINT('Ctrl Pts',(-71.9259272972458,-0.965913450159726,
4.03588994009282));
#45844=CARTESIAN_POINT('Ctrl Pts',(-71.9922184744783,0.333897721897463,
3.92532482547344));
#45845=CARTESIAN_POINT('Ctrl Pts',(-72.0585096517108,1.63370889395462,3.81475971085407));
#45846=CARTESIAN_POINT('Ctrl Pts',(-72.1248008289432,2.87314337616838,2.9944020340832));
#45847=CARTESIAN_POINT('Ctrl Pts',(-72.1910920061757,3.48280369496138,1.8411249540783));
#45848=CARTESIAN_POINT('Ctrl Pts',(-72.2573831834082,4.09246401375438,0.687847874073377));
#45849=CARTESIAN_POINT('Ctrl Pts',(-72.3236743606407,4.07235016912658,-0.798348609165588));
#45850=CARTESIAN_POINT('Ctrl Pts',(-72.3899655378732,3.43170248194958,-1.93470430545537));
#45851=CARTESIAN_POINT('Ctrl Pts',(-72.4562567151057,2.79105479477258,-3.07106000174515));
#45852=CARTESIAN_POINT('Ctrl Pts',(-72.5225478923381,1.52987326504638,-3.85757491108575));
#45853=CARTESIAN_POINT('Ctrl Pts',(-72.5888390695706,0.22754598230192,-3.93292327666135));
#45854=CARTESIAN_POINT('Ctrl Pts',(-72.6551302468031,-1.07478130044254,
-4.00827164223696));
#45855=CARTESIAN_POINT('Ctrl Pts',(-72.7214214240356,-2.41825433620526,
-3.37245346404756));
#45856=CARTESIAN_POINT('Ctrl Pts',(-72.7877126012681,-3.18568023309867,
-2.31756426590739));
#45857=CARTESIAN_POINT('Ctrl Pts',(-72.8294205601671,-3.6685162469078,-1.65386696626954));
#45858=CARTESIAN_POINT('Ctrl Pts',(-72.871128519066,-3.92332622623003,-0.824282022375144));
#45859=CARTESIAN_POINT('Ctrl Pts',(-72.912836477965,-3.92821364041606,0.00254794616387777));
#45860=CARTESIAN_POINT('Ctrl Pts',(-73.0961635220347,-3.92781646010829,
0.00228144192526316));
#45861=CARTESIAN_POINT('Ctrl Pts',(-73.0555324039126,-3.92357925720035,
-0.803405036117873));
#45862=CARTESIAN_POINT('Ctrl Pts',(-73.0149012857906,-3.6827012670755,-1.61141668343669));
#45863=CARTESIAN_POINT('Ctrl Pts',(-72.9742701676685,-3.22289206139225,
-2.26553071812793));
#45864=CARTESIAN_POINT('Ctrl Pts',(-72.907978990436,-2.47269627658706,-3.33274204304717));
#45865=CARTESIAN_POINT('Ctrl Pts',(-72.8416878132035,-1.13972456481958,
-3.99029125730048));
#45866=CARTESIAN_POINT('Ctrl Pts',(-72.7753966359711,0.163654501047081,
-3.93609957679598));
#45867=CARTESIAN_POINT('Ctrl Pts',(-72.7091054587386,1.46703356691378,-3.88190789629148));
#45868=CARTESIAN_POINT('Ctrl Pts',(-72.6428142815062,2.74081998687971,-3.11597532102913));
#45869=CARTESIAN_POINT('Ctrl Pts',(-72.5765231042737,3.39983497189712,-1.99017206241866));
#45870=CARTESIAN_POINT('Ctrl Pts',(-72.5102319270412,4.05884995691455,-0.86436880380816));
#45871=CARTESIAN_POINT('Ctrl Pts',(-72.4439407498086,4.10309350698347,0.621305138150414));
#45872=CARTESIAN_POINT('Ctrl Pts',(-72.3776495725761,3.51224008978018,1.78432962927463));
#45873=CARTESIAN_POINT('Ctrl Pts',(-72.3113583953437,2.92138667257693,2.94735412039879));
#45874=CARTESIAN_POINT('Ctrl Pts',(-72.2450672181112,1.6954362881015,3.78772916068855));
#45875=CARTESIAN_POINT('Ctrl Pts',(-72.1787760408787,0.397591801587071,
3.91938559387529));
#45876=CARTESIAN_POINT('Ctrl Pts',(-72.1124848636463,-0.900252684927396,
4.05104202706204));
#45877=CARTESIAN_POINT('Ctrl Pts',(-72.0461936864137,-2.26999127348092,
3.47397985314572));
#45878=CARTESIAN_POINT('Ctrl Pts',(-71.9799025091813,-3.08236465026863,
2.45330202725648));
#45879=CARTESIAN_POINT('Ctrl Pts',(-71.9353228467991,-3.62867160056579,
1.76691396207597));
#45880=CARTESIAN_POINT('Ctrl Pts',(-71.8907431844169,-3.92291970365932,
0.879908335057426));
#45881=CARTESIAN_POINT('Ctrl Pts',(-71.8461635220347,-3.92948114538815,
-0.00313483220630379));
#45882=CARTESIAN_POINT('Origin',(-54.75,0.,0.));
#45883=CARTESIAN_POINT('',(-70.412836477965,-3.93890669167694,-0.00139193648397762));
#45884=CARTESIAN_POINT('',(-70.5961635220346,-3.93918182025515,-0.0010191464650001));
#45885=CARTESIAN_POINT('',(-54.75,-3.933,-4.81653586104654E-16));
#45886=CARTESIAN_POINT('Ctrl Pts',(-70.412836477965,-3.93890669167694,-0.00139193648397762));
#45887=CARTESIAN_POINT('Ctrl Pts',(-70.475258902842,-3.93330383208432,1.22747763377414));
#45888=CARTESIAN_POINT('Ctrl Pts',(-70.5376813277191,-3.31223725813826,
2.46122943672829));
#45889=CARTESIAN_POINT('Ctrl Pts',(-70.6001037525961,-2.31930691003918,
3.18441174021372));
#45890=CARTESIAN_POINT('Ctrl Pts',(-70.6663949298286,-1.26483775388198,
3.95241468701055));
#45891=CARTESIAN_POINT('Ctrl Pts',(-70.7326861070611,0.209017533942394,
4.14459986877461));
#45892=CARTESIAN_POINT('Ctrl Pts',(-70.7989772842936,1.42516832109412,3.67267721569922));
#45893=CARTESIAN_POINT('Ctrl Pts',(-70.865268461526,2.64131910824584,3.20075456262383));
#45894=CARTESIAN_POINT('Ctrl Pts',(-70.9315596387585,3.59976539472492,2.06472407470899));
#45895=CARTESIAN_POINT('Ctrl Pts',(-70.997850815991,3.86019597254711,0.786479324392882));
#45896=CARTESIAN_POINT('Ctrl Pts',(-71.0641419932234,4.1206265503693,-0.491765425923184));
#45897=CARTESIAN_POINT('Ctrl Pts',(-71.130433170456,3.68304141953466,-1.9122244386405));
#45898=CARTESIAN_POINT('Ctrl Pts',(-71.1967243476885,2.74846763838938,-2.82233738502199));
#45899=CARTESIAN_POINT('Ctrl Pts',(-71.263015524921,1.8138938572441,-3.73245033140348));
#45900=CARTESIAN_POINT('Ctrl Pts',(-71.3293067021534,0.382331425788183,
-4.13221721144915));
#45901=CARTESIAN_POINT('Ctrl Pts',(-71.3955978793859,-0.888558405273612,
-3.83798471005084));
#45902=CARTESIAN_POINT('Ctrl Pts',(-71.4618890566184,-2.15944823633548,
-3.54375220865252));
#45903=CARTESIAN_POINT('Ctrl Pts',(-71.5281802338509,-3.2696654670032,-2.55552032581013));
#45904=CARTESIAN_POINT('Ctrl Pts',(-71.5944714110833,-3.70917516171872,
-1.32728380305621));
#45905=CARTESIAN_POINT('Ctrl Pts',(-71.6172597667106,-3.86026168096495,
-0.905063353165785));
#45906=CARTESIAN_POINT('Ctrl Pts',(-71.6400481223378,-3.93208936245692,
-0.454481079685571));
#45907=CARTESIAN_POINT('Ctrl Pts',(-71.662836477965,-3.92897287541266,-0.00293764914132633));
#45908=CARTESIAN_POINT('Ctrl Pts',(-71.8461635220347,-3.92948114538815,
-0.00313483220630379));
#45909=CARTESIAN_POINT('Ctrl Pts',(-71.8244520071844,-3.93267674696794,
-0.433201006218865));
#45910=CARTESIAN_POINT('Ctrl Pts',(-71.8027404923342,-3.86763432678414,
-0.862327302053894));
#45911=CARTESIAN_POINT('Ctrl Pts',(-71.7810289774839,-3.73023813252271,
-1.26688047930335));
#45912=CARTESIAN_POINT('Ctrl Pts',(-71.7147378002514,-3.31073007296715,
-2.50209168211176));
#45913=CARTESIAN_POINT('Ctrl Pts',(-71.6484466230188,-2.21670578883407,
-3.50822060986641));
#45914=CARTESIAN_POINT('Ctrl Pts',(-71.5821554457863,-0.950761159419275,
-3.82305060022833));
#45915=CARTESIAN_POINT('Ctrl Pts',(-71.5158642685538,0.315183469995524,
-4.13788059059025));
#45916=CARTESIAN_POINT('Ctrl Pts',(-71.4495730913214,1.75304844469209,-3.76141164355944));
#45917=CARTESIAN_POINT('Ctrl Pts',(-71.3832819140889,2.70227711913041,-2.86659397989856));
#45918=CARTESIAN_POINT('Ctrl Pts',(-71.3169907368564,3.65150579356876,-1.97177631623766));
#45919=CARTESIAN_POINT('Ctrl Pts',(-71.2506995596239,4.11209816774887,-0.558609935946732));
#45920=CARTESIAN_POINT('Ctrl Pts',(-71.1844083823915,3.87245763211158,0.723695075060797));
#45921=CARTESIAN_POINT('Ctrl Pts',(-71.118117205159,3.6328170964743,2.00600008606825));
#45922=CARTESIAN_POINT('Ctrl Pts',(-71.0518260279265,2.69294365101965,3.15744372779227));
#45923=CARTESIAN_POINT('Ctrl Pts',(-70.985534850694,1.48461612149768,3.64905160911101));
#45924=CARTESIAN_POINT('Ctrl Pts',(-70.9192436734615,0.276288591975673,
4.14065949042975));
#45925=CARTESIAN_POINT('Ctrl Pts',(-70.8529524962291,-1.2004930216137,3.97243161134319));
#45926=CARTESIAN_POINT('Ctrl Pts',(-70.7866613189966,-2.26729372986987,
3.22165203221254));
#45927=CARTESIAN_POINT('Ctrl Pts',(-70.7231620533426,-3.28916518247389,
2.50249219928951));
#45928=CARTESIAN_POINT('Ctrl Pts',(-70.6596627876886,-3.93486194413388,
1.24881672704683));
#45929=CARTESIAN_POINT('Ctrl Pts',(-70.5961635220346,-3.93918182025515,
-0.0010191464650001));
#45930=CARTESIAN_POINT('Origin',(-54.75,0.,0.));
#45931=CARTESIAN_POINT('',(-69.162836477965,-3.93322311813782,0.00362201478885243));
#45932=CARTESIAN_POINT('',(-69.3461635220347,-3.93257483085417,0.00363597296250955));
#45933=CARTESIAN_POINT('',(-54.75,-3.933,-4.81653586104654E-16));
#45934=CARTESIAN_POINT('Ctrl Pts',(-69.162836477965,-3.93322311813782,0.00362201478885243));
#45935=CARTESIAN_POINT('Ctrl Pts',(-69.1778873288813,-3.93598182100683,
0.301033048827567));
#45936=CARTESIAN_POINT('Ctrl Pts',(-69.1929381797976,-3.90511541289923,
0.597877093525298));
#45937=CARTESIAN_POINT('Ctrl Pts',(-69.2079890307139,-3.83847029528325,
0.886458383904474));
#45938=CARTESIAN_POINT('Ctrl Pts',(-69.2742802079464,-3.54493318378476,
2.15750900907587));
#45939=CARTESIAN_POINT('Ctrl Pts',(-69.3405713851789,-2.55730888542445,
3.26826676791706));
#45940=CARTESIAN_POINT('Ctrl Pts',(-69.4068625624114,-1.32931301680002,
3.70844840567217));
#45941=CARTESIAN_POINT('Ctrl Pts',(-69.4731537396439,-0.101317148175545,
4.1486300434273));
#45942=CARTESIAN_POINT('Ctrl Pts',(-69.5394449168763,1.36705029071311,3.91823556009631));
#45943=CARTESIAN_POINT('Ctrl Pts',(-69.6057360941088,2.40121979096113,3.1231084178528));
#45944=CARTESIAN_POINT('Ctrl Pts',(-69.6720272713413,3.43538929120911,2.32798127560932));
#45945=CARTESIAN_POINT('Ctrl Pts',(-69.7383184485738,4.0353608528165,0.96812147445346));
#45946=CARTESIAN_POINT('Ctrl Pts',(-69.8046096258063,3.92550692442834,-0.331749996882508));
#45947=CARTESIAN_POINT('Ctrl Pts',(-69.8709008030388,3.81565299604018,-1.63162146821851));
#45948=CARTESIAN_POINT('Ctrl Pts',(-69.9371919802712,2.99597357765637,-2.87150460973458));
#45949=CARTESIAN_POINT('Ctrl Pts',(-70.0034831575037,1.84303023559508,-3.48179583330912));
#45950=CARTESIAN_POINT('Ctrl Pts',(-70.0697743347362,0.690086893533902,
-4.09208705688362));
#45951=CARTESIAN_POINT('Ctrl Pts',(-70.1360655119687,-0.796120372204718,
-4.07278636251674));
#45952=CARTESIAN_POINT('Ctrl Pts',(-70.2023566892012,-1.93282641794617,
-3.43276050901542));
#45953=CARTESIAN_POINT('Ctrl Pts',(-70.2686478664337,-3.06953246368769,
-2.79273465551406));
#45954=CARTESIAN_POINT('Ctrl Pts',(-70.3349390436661,-3.85673728943204,
-1.53198364287817));
#45955=CARTESIAN_POINT('Ctrl Pts',(-70.4012302208986,-3.93279819005921,
-0.229697780645444));
#45956=CARTESIAN_POINT('Ctrl Pts',(-70.4050989732541,-3.93723710336179,
-0.153696392416323));
#45957=CARTESIAN_POINT('Ctrl Pts',(-70.4089677256096,-3.93925393990206,
-0.0775535411296101));
#45958=CARTESIAN_POINT('Ctrl Pts',(-70.412836477965,-3.93890669167694,-0.00139193648397762));
#45959=CARTESIAN_POINT('Ctrl Pts',(-70.5961635220346,-3.93918182025515,
-0.0010191464650001));
#45960=CARTESIAN_POINT('Ctrl Pts',(-70.5933716104561,-3.93937175492662,
-0.055971455134686));
#45961=CARTESIAN_POINT('Ctrl Pts',(-70.5905796988776,-3.93832181084376,
-0.110916341277931));
#45962=CARTESIAN_POINT('Ctrl Pts',(-70.587787787299,-3.93600944686095,-0.165808046812569));
#45963=CARTESIAN_POINT('Ctrl Pts',(-70.5214966100666,-3.88110465267288,
-1.4691572675323));
#45964=CARTESIAN_POINT('Ctrl Pts',(-70.4552054328341,-3.1144752613737,-2.74252442979698));
#45965=CARTESIAN_POINT('Ctrl Pts',(-70.3889142556016,-1.98831160237584,
-3.40092335197723));
#45966=CARTESIAN_POINT('Ctrl Pts',(-70.3226230783692,-0.862147943378008,
-4.05932227415747));
#45967=CARTESIAN_POINT('Ctrl Pts',(-70.2563319011367,0.623549983318482,
-4.10275295625333));
#45968=CARTESIAN_POINT('Ctrl Pts',(-70.1900407239042,1.78625102491787,-3.51126329832246));
#45969=CARTESIAN_POINT('Ctrl Pts',(-70.1237495466717,2.94895206651719,-2.91977364039161));
#45970=CARTESIAN_POINT('Ctrl Pts',(-70.0574583694392,3.78865622301945,-1.69336364243412));
#45971=CARTESIAN_POINT('Ctrl Pts',(-69.9911671922067,3.91960254285678,-0.395447316588599));
#45972=CARTESIAN_POINT('Ctrl Pts',(-69.9248760149742,4.05054886269412,0.902469009256999));
#45973=CARTESIAN_POINT('Ctrl Pts',(-69.8585848377417,3.47273734586645,2.27189166299064));
#45974=CARTESIAN_POINT('Ctrl Pts',(-69.7922936605093,2.45161519640667,3.0837064715881));
#45975=CARTESIAN_POINT('Ctrl Pts',(-69.7260024832768,1.43049304694693,3.89552128018553));
#45976=CARTESIAN_POINT('Ctrl Pts',(-69.6597113060443,-0.0339397351450109,
4.14972824364682));
#45977=CARTESIAN_POINT('Ctrl Pts',(-69.5934201288118,-1.26892122633613,
3.72954442197972));
#45978=CARTESIAN_POINT('Ctrl Pts',(-69.5271289515793,-2.50390271752731,
3.3093606003126));
#45979=CARTESIAN_POINT('Ctrl Pts',(-69.4608377743468,-3.50943291781767,
2.21478599351716));
#45980=CARTESIAN_POINT('Ctrl Pts',(-69.3945465971143,-3.82357022088014,
0.948669299685104));
#45981=CARTESIAN_POINT('Ctrl Pts',(-69.3784189054211,-3.89999531671704,
0.640641285426741));
#45982=CARTESIAN_POINT('Ctrl Pts',(-69.3622912137279,-3.93549831598826,
0.322460054554594));
#45983=CARTESIAN_POINT('Ctrl Pts',(-69.3461635220347,-3.93257483085417,
0.00363597296250955));
#45984=CARTESIAN_POINT('Origin',(-54.75,0.,0.));
#45985=CARTESIAN_POINT('',(-67.912836477965,-3.92649485000913,-0.000270854727073278));
#45986=CARTESIAN_POINT('',(-68.0961635220347,-3.92656685147973,-0.000622033211550006));
#45987=CARTESIAN_POINT('',(-54.75,-3.933,-4.81653586104654E-16));
#45988=CARTESIAN_POINT('Ctrl Pts',(-67.912836477965,-3.92649485000913,-0.000270854727073278));
#45989=CARTESIAN_POINT('Ctrl Pts',(-67.9468069321531,-3.92608231427559,
0.673905878798062));
#45990=CARTESIAN_POINT('Ctrl Pts',(-67.9807773863412,-3.76147556737439,
1.3482714594993));
#45991=CARTESIAN_POINT('Ctrl Pts',(-68.0147478405292,-3.43381750846848,
1.93094795183655));
#45992=CARTESIAN_POINT('Ctrl Pts',(-68.0810390177617,-2.79441368023744,
3.06800400675157));
#45993=CARTESIAN_POINT('Ctrl Pts',(-68.1473301949941,-1.53409356210357,
3.8558985132462));
#45994=CARTESIAN_POINT('Ctrl Pts',(-68.2136213722266,-0.231849510227881,
3.93267192615574));
#45995=CARTESIAN_POINT('Ctrl Pts',(-68.279912549459,1.07039454164785,4.0094453390653));
#45996=CARTESIAN_POINT('Ctrl Pts',(-68.3462037266916,2.41456252726537,3.37509765838973));
#45997=CARTESIAN_POINT('Ctrl Pts',(-68.4124949039241,3.18314229406039,2.32104885987572));
#45998=CARTESIAN_POINT('Ctrl Pts',(-68.4787860811566,3.95172206085539,1.26700006136175));
#45999=CARTESIAN_POINT('Ctrl Pts',(-68.545077258389,4.1447136088279,-0.206749854990709));
#46000=CARTESIAN_POINT('Ctrl Pts',(-68.6113684356215,3.6734564227072,-1.42315866460408));
#46001=CARTESIAN_POINT('Ctrl Pts',(-68.677659612854,3.20219923658649,-2.63956747421748));
#46002=CARTESIAN_POINT('Ctrl Pts',(-68.7439507900865,2.06669331637259,-3.59863517709184));
#46003=CARTESIAN_POINT('Ctrl Pts',(-68.810241967319,0.78859124756331,-3.859765085913));
#46004=CARTESIAN_POINT('Ctrl Pts',(-68.8765331445515,-0.489510821245967,
-4.12089499473416));
#46005=CARTESIAN_POINT('Ctrl Pts',(-68.942824321784,-1.91020903865058,-3.6840871095021));
#46006=CARTESIAN_POINT('Ctrl Pts',(-69.0091154990165,-2.82083318503453,
-2.75001142113526));
#46007=CARTESIAN_POINT('Ctrl Pts',(-69.0603558253326,-3.52470782356272,
-2.02800971481332));
#46008=CARTESIAN_POINT('Ctrl Pts',(-69.1115961516488,-3.9238311684066,-1.00890800885872));
#46009=CARTESIAN_POINT('Ctrl Pts',(-69.162836477965,-3.93322311813782,0.00362201478885243));
#46010=CARTESIAN_POINT('Ctrl Pts',(-69.3461635220347,-3.93257483085417,
0.00363597296250955));
#46011=CARTESIAN_POINT('Ctrl Pts',(-69.2960000364954,-3.92348163840994,
-0.988032736405674));
#46012=CARTESIAN_POINT('Ctrl Pts',(-69.2458365509562,-3.54262932001757,
-1.98592074023852));
#46013=CARTESIAN_POINT('Ctrl Pts',(-69.195673065417,-2.86511504564769,-2.70384512303677));
#46014=CARTESIAN_POINT('Ctrl Pts',(-69.1293818881845,-1.96977816151819,
-3.65258407105819));
#46015=CARTESIAN_POINT('Ctrl Pts',(-69.063090710952,-0.556359987424546,
-4.11240318623246));
#46016=CARTESIAN_POINT('Ctrl Pts',(-68.9967995337195,0.725813716388092,
-3.8720610949815));
#46017=CARTESIAN_POINT('Ctrl Pts',(-68.930508356487,2.00798742020073,-3.63171900373054));
#46018=CARTESIAN_POINT('Ctrl Pts',(-68.8642171792545,3.15891665373242,-2.69121570605441));
#46019=CARTESIAN_POINT('Ctrl Pts',(-68.797926002022,3.64986334551302,-1.4826193824603));
#46020=CARTESIAN_POINT('Ctrl Pts',(-68.7316348247895,4.14081003729361,-0.274023058866195));
#46021=CARTESIAN_POINT('Ctrl Pts',(-68.6653436475571,3.97177418732311,1.20266629064584));
#46022=CARTESIAN_POINT('Ctrl Pts',(-68.5990524703246,3.22041103861628,2.26905606288714));
#46023=CARTESIAN_POINT('Ctrl Pts',(-68.5327612930921,2.46904788990946,3.33544583512841));
#46024=CARTESIAN_POINT('Ctrl Pts',(-68.4664701158596,1.13535744246639,3.99153603009894));
#46025=CARTESIAN_POINT('Ctrl Pts',(-68.4001789386271,-0.167961542942652,
3.9359181386633));
#46026=CARTESIAN_POINT('Ctrl Pts',(-68.3338877613946,-1.47128052835169,
3.88030024722765));
#46027=CARTESIAN_POINT('Ctrl Pts',(-68.2675965841621,-2.74422805172676,
3.11297426938576));
#46028=CARTESIAN_POINT('Ctrl Pts',(-68.2013054069296,-3.40201071397511,
1.98645054712294));
#46029=CARTESIAN_POINT('Ctrl Pts',(-68.1662581119647,-3.74977196892805,
1.39087190713674));
#46030=CARTESIAN_POINT('Ctrl Pts',(-68.1312108169997,-3.9255884166725,0.694893860719782));
#46031=CARTESIAN_POINT('Ctrl Pts',(-68.0961635220347,-3.92656685147973,
-0.000622033211550006));
#46032=CARTESIAN_POINT('Origin',(-54.75,0.,0.));
#46033=CARTESIAN_POINT('',(-66.6628364779651,-3.93422056738883,-0.0035277183879312));
#46034=CARTESIAN_POINT('',(-66.8461635220347,-3.93486507000708,-0.00341859851677232));
#46035=CARTESIAN_POINT('',(-54.75,-3.933,-4.81653586104654E-16));
#46036=CARTESIAN_POINT('Ctrl Pts',(-66.6628364779651,-3.93422056738883,
-0.0035277183879312));
#46037=CARTESIAN_POINT('Ctrl Pts',(-66.7157265354249,-3.92453720768234,
1.04092228063237));
#46038=CARTESIAN_POINT('Ctrl Pts',(-66.7686165928847,-3.49640399633483,
2.09238394656257));
#46039=CARTESIAN_POINT('Ctrl Pts',(-66.8215066503445,-2.75155438065251,
2.81932814061762));
#46040=CARTESIAN_POINT('Ctrl Pts',(-66.8877978275769,-1.81797706468404,
3.73046321440442));
#46041=CARTESIAN_POINT('Ctrl Pts',(-66.9540890048094,-0.386852941616121,
4.13179636517881));
#46042=CARTESIAN_POINT('Ctrl Pts',(-67.0203801820419,0.884358097169925,
3.83895473145184));
#46043=CARTESIAN_POINT('Ctrl Pts',(-67.0866713592744,2.15556913595601,3.54611309772486));
#46044=CARTESIAN_POINT('Ctrl Pts',(-67.1529625365069,3.26686709046021,2.55909667949649));
#46045=CARTESIAN_POINT('Ctrl Pts',(-67.2192537137394,3.70772053948449,1.33134183260772));
#46046=CARTESIAN_POINT('Ctrl Pts',(-67.2855448909718,4.14857398850876,0.103586985718978));
#46047=CARTESIAN_POINT('Ctrl Pts',(-67.3518360682043,3.91898293205315,-1.36490628983015));
#46048=CARTESIAN_POINT('Ctrl Pts',(-67.4181272454368,3.12442173715988,-2.39951067564395));
#46049=CARTESIAN_POINT('Ctrl Pts',(-67.4844184226693,2.32986054226658,-3.43411506145778));
#46050=CARTESIAN_POINT('Ctrl Pts',(-67.5507095999018,0.970329208935581,
-4.03483055753626));
#46051=CARTESIAN_POINT('Ctrl Pts',(-67.6170007771343,-0.329602172556657,
-3.92568784826461));
#46052=CARTESIAN_POINT('Ctrl Pts',(-67.6832919543668,-1.6295335540489,-3.81654513899295));
#46053=CARTESIAN_POINT('Ctrl Pts',(-67.7495831315992,-2.86986498370238,
-2.99754422437115));
#46054=CARTESIAN_POINT('Ctrl Pts',(-67.8158743088317,-3.48078692936503,
-1.84493496539254));
#46055=CARTESIAN_POINT('Ctrl Pts',(-67.8481950318761,-3.77864615938421,
-1.28297233034601));
#46056=CARTESIAN_POINT('Ctrl Pts',(-67.8805157549206,-3.92688735147866,
-0.641707067697644));
#46057=CARTESIAN_POINT('Ctrl Pts',(-67.912836477965,-3.92649485000913,-0.000270854727073278));
#46058=CARTESIAN_POINT('Ctrl Pts',(-68.0961635220347,-3.92656685147973,
-0.000622033211550006));
#46059=CARTESIAN_POINT('Ctrl Pts',(-68.0649196397672,-3.92743910430135,
-0.620658949808565));
#46060=CARTESIAN_POINT('Ctrl Pts',(-68.0336757574997,-3.78936190461529,
-1.24032857880161));
#46061=CARTESIAN_POINT('Ctrl Pts',(-68.0024318752322,-3.51028545575193,
-1.7881718858384));
#46062=CARTESIAN_POINT('Ctrl Pts',(-67.9361406979997,-2.91815973415871,
-2.95054912985305));
#46063=CARTESIAN_POINT('Ctrl Pts',(-67.8698495207672,-1.69129048985058,
-3.78958215119858));
#46064=CARTESIAN_POINT('Ctrl Pts',(-67.8035583435347,-0.393302713211145,
-3.91981831848712));
#46065=CARTESIAN_POINT('Ctrl Pts',(-67.7372671663022,0.904685063428323,
-4.05005448577567));
#46066=CARTESIAN_POINT('Ctrl Pts',(-67.6709759890698,2.27379137239909,-3.47149379900719));
#46067=CARTESIAN_POINT('Ctrl Pts',(-67.6046848118373,3.08504736978577,-2.44992763165452));
#46068=CARTESIAN_POINT('Ctrl Pts',(-67.5383936346048,3.89630336717245,-1.42836146430185));
#46069=CARTESIAN_POINT('Ctrl Pts',(-67.4721024573723,4.14970905297504,0.0362101836350086));
#46070=CARTESIAN_POINT('Ctrl Pts',(-67.4058112801398,3.72884959498036,1.27096159351147));
#46071=CARTESIAN_POINT('Ctrl Pts',(-67.3395201029073,3.30799013698569,2.50571300338793));
#46072=CARTESIAN_POINT('Ctrl Pts',(-67.2732289256748,2.21286553519374,3.51064417520398));
#46073=CARTESIAN_POINT('Ctrl Pts',(-67.2069377484424,0.946577155962392,
3.82408869692854));
#46074=CARTESIAN_POINT('Ctrl Pts',(-67.1406465712099,-0.319711223268989,
4.1375332186531));
#46075=CARTESIAN_POINT('Ctrl Pts',(-67.0743553939774,-1.75716337993967,
3.75949109028616));
#46076=CARTESIAN_POINT('Ctrl Pts',(-67.008064216745,-2.70541231753474,2.86363525371122));
#46077=CARTESIAN_POINT('Ctrl Pts',(-66.9540973185082,-3.47737106158938,
2.13432914110926));
#46078=CARTESIAN_POINT('Ctrl Pts',(-66.9001304202714,-3.92511506363844,
1.06184695920244));
#46079=CARTESIAN_POINT('Ctrl Pts',(-66.8461635220347,-3.93486507000708,
-0.00341859851677232));
#46080=CARTESIAN_POINT('Origin',(-54.75,0.,0.));
#46081=CARTESIAN_POINT('',(-65.412836477965,-3.93834804191526,0.00192586831589278));
#46082=CARTESIAN_POINT('',(-65.5961635220347,-3.93790589778391,0.0022443990911959));
#46083=CARTESIAN_POINT('',(-54.75,-3.933,-4.81653586104654E-16));
#46084=CARTESIAN_POINT('Ctrl Pts',(-65.412836477965,-3.93834804191526,0.00192586831589278));
#46085=CARTESIAN_POINT('Ctrl Pts',(-65.4183549614641,-3.93900111014635,
0.110605513045279));
#46086=CARTESIAN_POINT('Ctrl Pts',(-65.4238734449632,-3.93489409538351,
0.21923504688863));
#46087=CARTESIAN_POINT('Ctrl Pts',(-65.4293919284623,-3.92586759692805,
0.327454249562873));
#46088=CARTESIAN_POINT('Ctrl Pts',(-65.4956831056947,-3.81743613944527,
1.62744515207093));
#46089=CARTESIAN_POINT('Ctrl Pts',(-65.5619742829273,-2.99911397375712,
2.86822449856297));
#46090=CARTESIAN_POINT('Ctrl Pts',(-65.6282654601598,-1.84683914289999,
3.47977698343139));
#46091=CARTESIAN_POINT('Ctrl Pts',(-65.6945566373923,-0.694564312042931,
4.09132946829977));
#46092=CARTESIAN_POINT('Ctrl Pts',(-65.7608478146247,0.791663183983091,
4.07365509154464));
#46093=CARTESIAN_POINT('Ctrl Pts',(-65.8271389918572,1.92906890768864,3.43487347999244));
#46094=CARTESIAN_POINT('Ctrl Pts',(-65.8934301690896,3.06647463139425,2.79609186844021));
#46095=CARTESIAN_POINT('Ctrl Pts',(-65.9597213463221,3.85505858277934,1.53620302209095));
#46096=CARTESIAN_POINT('Ctrl Pts',(-66.0260125235546,3.93254448498876,0.234001170404978));
#46097=CARTESIAN_POINT('Ctrl Pts',(-66.0923037007871,4.01003038719819,-1.06820068128095));
#46098=CARTESIAN_POINT('Ctrl Pts',(-66.1585948780196,3.37641824023196,-2.41271553830341));
#46099=CARTESIAN_POINT('Ctrl Pts',(-66.2248860552521,2.32279011489556,-3.1818718950187));
#46100=CARTESIAN_POINT('Ctrl Pts',(-66.2911772324846,1.26916198955922,-3.95102825173394));
#46101=CARTESIAN_POINT('Ctrl Pts',(-66.3574684097171,-0.20448211414741,
-4.14482610814199));
#46102=CARTESIAN_POINT('Ctrl Pts',(-66.4237595869495,-1.42114858208481,
-3.67423453004905));
#46103=CARTESIAN_POINT('Ctrl Pts',(-66.490050764182,-2.63781505002231,-3.20364295195607));
#46104=CARTESIAN_POINT('Ctrl Pts',(-66.5563419414145,-3.59750388219069,
-2.068661939362));
#46105=CARTESIAN_POINT('Ctrl Pts',(-66.622633118647,-3.85933304384037,-0.790702934665299));
#46106=CARTESIAN_POINT('Ctrl Pts',(-66.6360342384197,-3.91226322402019,
-0.532356614664742));
#46107=CARTESIAN_POINT('Ctrl Pts',(-66.6494353581924,-3.93667410723093,
-0.268167240553048));
#46108=CARTESIAN_POINT('Ctrl Pts',(-66.6628364779651,-3.93422056738883,
-0.0035277183879312));
#46109=CARTESIAN_POINT('Ctrl Pts',(-66.8461635220347,-3.93486507000708,
-0.00341859851677232));
#46110=CARTESIAN_POINT('Ctrl Pts',(-66.8338392430389,-3.93709165338732,
-0.246690499753148));
#46111=CARTESIAN_POINT('Ctrl Pts',(-66.8215149640432,-3.91647612331212,
-0.489586042066614));
#46112=CARTESIAN_POINT('Ctrl Pts',(-66.8091906850475,-3.87166339873204,
-0.727932140439692));
#46113=CARTESIAN_POINT('Ctrl Pts',(-66.742899507815,-3.63061982381493,-2.00997415323278));
#46114=CARTESIAN_POINT('Ctrl Pts',(-66.6766083305825,-2.68948695546139,
-3.16038863403615));
#46115=CARTESIAN_POINT('Ctrl Pts',(-66.6103171533501,-1.48062219959417,
-3.65067398931148));
#46116=CARTESIAN_POINT('Ctrl Pts',(-66.5440259761176,-0.271757443726919,
-4.14095934458682));
#46117=CARTESIAN_POINT('Ctrl Pts',(-66.4777347988851,1.20483919965406,-3.9711155743341));
#46118=CARTESIAN_POINT('Ctrl Pts',(-66.4114436216526,2.2708177166518,-3.2191690809752));
#46119=CARTESIAN_POINT('Ctrl Pts',(-66.3451524444201,3.33679623364958,-2.46722258761628));
#46120=CARTESIAN_POINT('Ctrl Pts',(-66.2788612671875,3.9921566242641,-1.13317337115124));
#46121=CARTESIAN_POINT('Ctrl Pts',(-66.2125700899551,3.93582565223036,0.170114988792669));
#46122=CARTESIAN_POINT('Ctrl Pts',(-66.1462789127226,3.87949468019661,1.47340334873654));
#46123=CARTESIAN_POINT('Ctrl Pts',(-66.0799877354902,3.11147234551458,2.74593085215923));
#46124=CARTESIAN_POINT('Ctrl Pts',(-66.0136965582577,1.98458889721679,3.4030970575654));
#46125=CARTESIAN_POINT('Ctrl Pts',(-65.9474053810252,0.857705448919006,
4.06026326297157));
#46126=CARTESIAN_POINT('Ctrl Pts',(-65.8811142037926,-0.628039112994567,
4.10206817036125));
#46127=CARTESIAN_POINT('Ctrl Pts',(-65.8148230265601,-1.79009221146151,
3.50930656236118));
#46128=CARTESIAN_POINT('Ctrl Pts',(-65.7485318493276,-2.95214530992843,
2.91654495436113));
#46129=CARTESIAN_POINT('Ctrl Pts',(-65.6822406720953,-3.79050694494877,
1.68921683097136));
#46130=CARTESIAN_POINT('Ctrl Pts',(-65.6159494948628,-3.92003292070173,
0.391157992096705));
#46131=CARTESIAN_POINT('Ctrl Pts',(-65.6093541705868,-3.93291948944168,
0.262013823458523));
#46132=CARTESIAN_POINT('Ctrl Pts',(-65.6027588463107,-3.93878978643022,
0.132169540605536));
#46133=CARTESIAN_POINT('Ctrl Pts',(-65.5961635220347,-3.93790589778391,
0.0022443990911959));
#46134=CARTESIAN_POINT('Origin',(-54.75,0.,0.));
#46135=CARTESIAN_POINT('',(-64.1628364779651,-3.92827063990554,0.00258208764951584));
#46136=CARTESIAN_POINT('',(-64.3461635220347,-3.92786728767746,0.00231866363322961));
#46137=CARTESIAN_POINT('',(-54.75,-3.933,-4.81653586104654E-16));
#46138=CARTESIAN_POINT('Ctrl Pts',(-64.1628364779651,-3.92827063990554,
0.00258208764951584));
#46139=CARTESIAN_POINT('Ctrl Pts',(-64.1872745647359,-3.93117530062354,
0.487031767005991));
#46140=CARTESIAN_POINT('Ctrl Pts',(-64.2117126515067,-3.84824859058194,
0.970521987776141));
#46141=CARTESIAN_POINT('Ctrl Pts',(-64.2361507382776,-3.67501153749169,
1.41913807413845));
#46142=CARTESIAN_POINT('Ctrl Pts',(-64.3024419155101,-3.20508570830013,
2.6360618361852));
#46143=CARTESIAN_POINT('Ctrl Pts',(-64.3687330927425,-2.07062994308782,
3.59637151036013));
#46144=CARTESIAN_POINT('Ctrl Pts',(-64.435024269975,-0.792814385066712,
3.85889984645854));
#46145=CARTESIAN_POINT('Ctrl Pts',(-64.5013154472075,0.485001172954427,
4.12142818255696));
#46146=CARTESIAN_POINT('Ctrl Pts',(-64.56760662444,1.90617652378437,3.68617518057882));
#46147=CARTESIAN_POINT('Ctrl Pts',(-64.6338978016725,2.81782225222164,2.7530965164794));
#46148=CARTESIAN_POINT('Ctrl Pts',(-64.7001889789049,3.72946798065891,1.82001785237999));
#46149=CARTESIAN_POINT('Ctrl Pts',(-64.7664801561375,4.13158408670352,0.389113526159296));
#46150=CARTESIAN_POINT('Ctrl Pts',(-64.8327713333699,3.83943801841159,-0.882257545698581));
#46151=CARTESIAN_POINT('Ctrl Pts',(-64.8990625106024,3.54729195011966,-2.15362861755646));
#46152=CARTESIAN_POINT('Ctrl Pts',(-64.9653536878349,2.56088370749119,-3.26546643505152));
#46153=CARTESIAN_POINT('Ctrl Pts',(-65.0316448650673,1.3333702498722,-3.70699156337349));
#46154=CARTESIAN_POINT('Ctrl Pts',(-65.0979360422998,0.105856792253199,
-4.14851669169545));
#46155=CARTESIAN_POINT('Ctrl Pts',(-65.1642272195323,-1.36276188035633,
-3.91972913084432));
#46156=CARTESIAN_POINT('Ctrl Pts',(-65.2305183967648,-2.39780084202234,
-3.12573412115672));
#46157=CARTESIAN_POINT('Ctrl Pts',(-65.2912910904982,-3.34667682289195,
-2.39783611777122));
#46158=CARTESIAN_POINT('Ctrl Pts',(-65.3520637842316,-3.93115608137005,
-1.19491648254071));
#46159=CARTESIAN_POINT('Ctrl Pts',(-65.412836477965,-3.93834804191526,0.00192586831589278));
#46160=CARTESIAN_POINT('Ctrl Pts',(-65.5961635220347,-3.93790589778391,
0.0022443990911959));
#46161=CARTESIAN_POINT('Ctrl Pts',(-65.5364676690782,-3.92990561084547,
-1.17373904290349));
#46162=CARTESIAN_POINT('Ctrl Pts',(-65.4767718161217,-3.36856921796084,
-2.356346824119));
#46163=CARTESIAN_POINT('Ctrl Pts',(-65.4170759631653,-2.44823933350512,
-3.08638734446033));
#46164=CARTESIAN_POINT('Ctrl Pts',(-65.3507847859328,-1.4262294540701,-3.89708428778295));
#46165=CARTESIAN_POINT('Ctrl Pts',(-65.2844936087003,0.0384806212853624,
-4.14968862006866));
#46166=CARTESIAN_POINT('Ctrl Pts',(-65.2182024314679,1.27300158021858,-3.72815365173264));
#46167=CARTESIAN_POINT('Ctrl Pts',(-65.1519112542354,2.50752253915183,-3.30661868339661));
#46168=CARTESIAN_POINT('Ctrl Pts',(-65.0856200770029,3.51185438166279,-2.21094441443874));
#46169=CARTESIAN_POINT('Ctrl Pts',(-65.0193288997704,3.82460602821833,-0.944484728877324));
#46170=CARTESIAN_POINT('Ctrl Pts',(-64.9530377225379,4.13735767477386,0.321974956684055));
#46171=CARTESIAN_POINT('Ctrl Pts',(-64.8867465453054,3.75852912537409,1.75922005884896));
#46172=CARTESIAN_POINT('Ctrl Pts',(-64.8204553680729,2.86215460453238,2.70697870215496));
#46173=CARTESIAN_POINT('Ctrl Pts',(-64.7541641908405,1.96578008369065,3.65473734546098));
#46174=CARTESIAN_POINT('Ctrl Pts',(-64.687873013608,0.551859591406997,4.113009529908));
#46175=CARTESIAN_POINT('Ctrl Pts',(-64.6215818363755,-0.730050346581443,
3.87126454348224));
#46176=CARTESIAN_POINT('Ctrl Pts',(-64.555290659143,-2.01196028456981,3.62951955705649));
#46177=CARTESIAN_POINT('Ctrl Pts',(-64.4889994819105,-3.16185966826298,
2.68775739975796));
#46178=CARTESIAN_POINT('Ctrl Pts',(-64.422708304678,-3.65148354026384,1.47862457349683));
#46179=CARTESIAN_POINT('Ctrl Pts',(-64.3971933771303,-3.83993573166107,
1.01323931793717));
#46180=CARTESIAN_POINT('Ctrl Pts',(-64.3716784495825,-3.93057361066039,
0.508245326816594));
#46181=CARTESIAN_POINT('Ctrl Pts',(-64.3461635220347,-3.92786728767746,
0.00231866363322961));
#46182=CARTESIAN_POINT('Origin',(-54.75,0.,0.));
#46183=CARTESIAN_POINT('',(-62.9128364779651,-3.92890725657977,-0.00290888419126417));
#46184=CARTESIAN_POINT('',(-63.0961635220347,-3.92941051997575,-0.00310996813596078));
#46185=CARTESIAN_POINT('',(-54.75,-3.933,-4.81653586104654E-16));
#46186=CARTESIAN_POINT('Ctrl Pts',(-62.9128364779651,-3.92890725657977,
-0.00290888419126417));
#46187=CARTESIAN_POINT('Ctrl Pts',(-62.9561941680077,-3.92304212850891,
0.85624490671229));
#46188=CARTESIAN_POINT('Ctrl Pts',(-62.9995518580503,-3.64598688522449,
1.71883987619063));
#46189=CARTESIAN_POINT('Ctrl Pts',(-63.0429095480929,-3.12704556945061,
2.39609029060797));
#46190=CARTESIAN_POINT('Ctrl Pts',(-63.1092007253254,-2.33361698265479,
3.43156351828243));
#46191=CARTESIAN_POINT('Ctrl Pts',(-63.1754919025578,-0.974743805821233,
4.03376634359936));
#46192=CARTESIAN_POINT('Ctrl Pts',(-63.2417830797903,0.325306228544258,
3.92604617036488));
#46193=CARTESIAN_POINT('Ctrl Pts',(-63.3080742570227,1.62535626290979,3.8183259971304));
#46194=CARTESIAN_POINT('Ctrl Pts',(-63.3743654342553,2.86658315480724,3.00068282534447));
#46195=CARTESIAN_POINT('Ctrl Pts',(-63.4406566114877,3.47876599581036,1.8487427675477));
#46196=CARTESIAN_POINT('Ctrl Pts',(-63.5069477887202,4.09094883681349,0.696802709750933));
#46197=CARTESIAN_POINT('Ctrl Pts',(-63.5732389659527,4.07408762692229,-0.789434234056675));
#46198=CARTESIAN_POINT('Ctrl Pts',(-63.6395301431852,3.4359284232711,-1.92718928606513));
#46199=CARTESIAN_POINT('Ctrl Pts',(-63.7058213204177,2.79776921961993,-3.06494433807355));
#46200=CARTESIAN_POINT('Ctrl Pts',(-63.7721124976502,1.53831202220882,-3.85421749828284));
#46201=CARTESIAN_POINT('Ctrl Pts',(-63.8384036748827,0.236152760532859,
-3.9324158665964));
#46202=CARTESIAN_POINT('Ctrl Pts',(-63.9046948521151,-1.06600650114314,
-4.01061423490997));
#46203=CARTESIAN_POINT('Ctrl Pts',(-63.9709860293476,-2.41086782708398,
-3.37773781132776));
#46204=CARTESIAN_POINT('Ctrl Pts',(-64.0372772065801,-3.18060054346902,
-2.32453067457735));
#46205=CARTESIAN_POINT('Ctrl Pts',(-64.0791302970417,-3.66657310203702,
-1.65958587483903));
#46206=CARTESIAN_POINT('Ctrl Pts',(-64.1209833875034,-3.9232960676761,-0.827094819727051));
#46207=CARTESIAN_POINT('Ctrl Pts',(-64.1628364779651,-3.92827063990554,
0.00258208764951584));
#46208=CARTESIAN_POINT('Ctrl Pts',(-64.3461635220347,-3.92786728767746,
0.00231866363322961));
#46209=CARTESIAN_POINT('Ctrl Pts',(-64.30538727235,-3.92354222339997,-0.806219471601042));
#46210=CARTESIAN_POINT('Ctrl Pts',(-64.2646110226653,-3.68081332915015,
-1.6171396786422));
#46211=CARTESIAN_POINT('Ctrl Pts',(-64.2238347729806,-3.21792615966099,
-2.27257869063668));
#46212=CARTESIAN_POINT('Ctrl Pts',(-64.1575435957481,-2.46539654674866,
-3.33814563328531));
#46213=CARTESIAN_POINT('Ctrl Pts',(-64.0912524185156,-1.13098896061534,
-3.99277602335871));
#46214=CARTESIAN_POINT('Ctrl Pts',(-64.0249612412831,0.172268383717981,
-3.93573198758981));
#46215=CARTESIAN_POINT('Ctrl Pts',(-63.9586700640506,1.47552572805126,-3.87868795182091));
#46216=CARTESIAN_POINT('Ctrl Pts',(-63.8923788868182,2.74763283058462,-3.10996949020974));
#46217=CARTESIAN_POINT('Ctrl Pts',(-63.8260877095857,3.40418238242286,-1.98272665321478));
#46218=CARTESIAN_POINT('Ctrl Pts',(-63.7597965323532,4.06073193426111,-0.855483816219792));
#46219=CARTESIAN_POINT('Ctrl Pts',(-63.6935053551207,4.10172393540427,0.630283396158968));
#46220=CARTESIAN_POINT('Ctrl Pts',(-63.6272141778882,3.50832661844329,1.79201200121225));
#46221=CARTESIAN_POINT('Ctrl Pts',(-63.5609230006557,2.91492930148232,2.9537406062655));
#46222=CARTESIAN_POINT('Ctrl Pts',(-63.4946318234233,1.6871426664172,3.79143060399324));
#46223=CARTESIAN_POINT('Ctrl Pts',(-63.4283406461908,0.3890131538872,3.92024634943637));
#46224=CARTESIAN_POINT('Ctrl Pts',(-63.3620494689583,-0.909116358642765,
4.04906209487949));
#46225=CARTESIAN_POINT('Ctrl Pts',(-63.2957582917257,-2.27758874863767,
3.46900358803805));
#46226=CARTESIAN_POINT('Ctrl Pts',(-63.2294671144933,-3.08772639521042,
2.44655030246413));
#46227=CARTESIAN_POINT('Ctrl Pts',(-63.1850325836737,-3.63075621799453,
1.76120673298667));
#46228=CARTESIAN_POINT('Ctrl Pts',(-63.1405980528542,-3.92293010133024,
0.877098248494651));
#46229=CARTESIAN_POINT('Ctrl Pts',(-63.0961635220347,-3.92941051997575,
-0.00310996813596078));
#46230=CARTESIAN_POINT('Origin',(-54.75,0.,0.));
#46231=CARTESIAN_POINT('',(-61.6628364779651,-3.93886391369501,-0.00144086038807723));
#46232=CARTESIAN_POINT('',(-61.8461635220346,-3.93914924332037,-0.00107030884100855));
#46233=CARTESIAN_POINT('',(-54.75,-3.933,-4.81653586104654E-16));
#46234=CARTESIAN_POINT('Ctrl Pts',(-61.6628364779651,-3.93886391369501,
-0.00144086038807723));
#46235=CARTESIAN_POINT('Ctrl Pts',(-61.7251137712794,-3.93310338294905,
1.22460701239503));
#46236=CARTESIAN_POINT('Ctrl Pts',(-61.7873910645938,-3.31531093334815,
2.45566105020782));
#46237=CARTESIAN_POINT('Ctrl Pts',(-61.8496683579081,-2.32627053840023,
3.17932823979179));
#46238=CARTESIAN_POINT('Ctrl Pts',(-61.9159595351406,-1.2734847055183,3.94963708542352));
#46239=CARTESIAN_POINT('Ctrl Pts',(-61.9822507123731,0.199946449501902,
4.14504738441835));
#46240=CARTESIAN_POINT('Ctrl Pts',(-62.0485418896056,1.41712714136624,3.67578744480276));
#46241=CARTESIAN_POINT('Ctrl Pts',(-62.1148330668381,2.63430783323069,3.20652750518713));
#46242=CARTESIAN_POINT('Ctrl Pts',(-62.1811242440705,3.59523806193922,2.07259732696095));
#46243=CARTESIAN_POINT('Ctrl Pts',(-62.247415421303,3.85846549389725,0.794925598135253));
#46244=CARTESIAN_POINT('Ctrl Pts',(-62.3137065985355,4.12169292585525,-0.482746130690301));
#46245=CARTESIAN_POINT('Ctrl Pts',(-62.379997775768,3.68721756106294,-1.90415941011534));
#46246=CARTESIAN_POINT('Ctrl Pts',(-62.4462889530005,2.75463782815404,-2.81631552029761));
#46247=CARTESIAN_POINT('Ctrl Pts',(-62.512580130233,1.82205809524509,-3.72847163047994));
#46248=CARTESIAN_POINT('Ctrl Pts',(-62.5788713074655,0.391373994219499,
-4.13137057141944));
#46249=CARTESIAN_POINT('Ctrl Pts',(-62.6451624846979,-0.880156730119362,
-3.83992015601784));
#46250=CARTESIAN_POINT('Ctrl Pts',(-62.7114536619304,-2.15168745445822,
-3.54846974061623));
#46251=CARTESIAN_POINT('Ctrl Pts',(-62.7777448391629,-3.26406480211035,
-2.56266996887352));
#46252=CARTESIAN_POINT('Ctrl Pts',(-62.8440360163953,-3.70626147755742,
-1.33539826798612));
#46253=CARTESIAN_POINT('Ctrl Pts',(-62.8669695035852,-3.8592397804802,-0.910822615450734));
#46254=CARTESIAN_POINT('Ctrl Pts',(-62.8899029907751,-3.93200953991977,
-0.457347126599487));
#46255=CARTESIAN_POINT('Ctrl Pts',(-62.9128364779651,-3.92890725657977,
-0.00290888419126417));
#46256=CARTESIAN_POINT('Ctrl Pts',(-63.0961635220347,-3.92941051997575,
-0.00310996813596078));
#46257=CARTESIAN_POINT('Ctrl Pts',(-63.0743068756218,-3.93259813592061,
-0.436070537446338));
#46258=CARTESIAN_POINT('Ctrl Pts',(-63.0524502292088,-3.86666218165736,
-0.86808743645036));
#46259=CARTESIAN_POINT('Ctrl Pts',(-63.0305935827959,-3.72745659244489,
-1.27504118584678));
#46260=CARTESIAN_POINT('Ctrl Pts',(-62.9643024055634,-3.30524623995596,
-2.50933132427722));
#46261=CARTESIAN_POINT('Ctrl Pts',(-62.8980112283309,-2.20902263182746,
-3.51306353683163));
#46262=CARTESIAN_POINT('Ctrl Pts',(-62.8317200510984,-0.942392019056605,
-3.82512221459457));
#46263=CARTESIAN_POINT('Ctrl Pts',(-62.7654288738659,0.324238593714291,
-4.13718089235752));
#46264=CARTESIAN_POINT('Ctrl Pts',(-62.6991376966334,1.76127621112752,-3.75756603532902));
#46265=CARTESIAN_POINT('Ctrl Pts',(-62.632846519401,2.70854427642858,-2.86067309855433));
#46266=CARTESIAN_POINT('Ctrl Pts',(-62.5665553421685,3.65581234172959,-1.96378016177969));
#46267=CARTESIAN_POINT('Ctrl Pts',(-62.500264164936,4.11331085491841,-0.54960914525888));
#46268=CARTESIAN_POINT('Ctrl Pts',(-62.4339729877035,3.87086452935152,0.732168334179135));
#46269=CARTESIAN_POINT('Ctrl Pts',(-62.367681810471,3.62841820378463,2.01394581361719));
#46270=CARTESIAN_POINT('Ctrl Pts',(-62.3013906332385,2.68602703946198,3.1633297559725));
#46271=CARTESIAN_POINT('Ctrl Pts',(-62.235099456006,1.47662650476639,3.65229199812773));
#46272=CARTESIAN_POINT('Ctrl Pts',(-62.1688082787735,0.267225970070802,
4.14125424028296));
#46273=CARTESIAN_POINT('Ctrl Pts',(-62.1025171015411,-1.20918393499766,
3.96979478223817));
#46274=CARTESIAN_POINT('Ctrl Pts',(-62.0362259243086,-2.27433898431471,
3.21668227504563));
#46275=CARTESIAN_POINT('Ctrl Pts',(-61.9728717902173,-3.2923021377792,2.49693655987786));
#46276=CARTESIAN_POINT('Ctrl Pts',(-61.9095176561259,-3.93464461114698,
1.24593653647341));
#46277=CARTESIAN_POINT('Ctrl Pts',(-61.8461635220346,-3.93914924332037,
-0.00107030884100855));
#46278=CARTESIAN_POINT('Origin',(-54.75,0.,0.));
#46279=CARTESIAN_POINT('',(-60.412836477965,-3.93331087711921,0.00361726591575254));
#46280=CARTESIAN_POINT('',(-60.5961635220347,-3.93266179433523,0.00363627036369697));
#46281=CARTESIAN_POINT('',(-54.75,-3.933,-4.81653586104654E-16));
#46282=CARTESIAN_POINT('Ctrl Pts',(-60.412836477965,-3.93331087711921,0.00361726591575254));
#46283=CARTESIAN_POINT('Ctrl Pts',(-60.4277421973187,-3.93604514286324,
0.298143623714554));
#46284=CARTESIAN_POINT('Ctrl Pts',(-60.4426479166723,-3.9057779826615,0.59211331334404));
#46285=CARTESIAN_POINT('Ctrl Pts',(-60.4575536360259,-3.84040114412618,
0.878055651061374));
#46286=CARTESIAN_POINT('Ctrl Pts',(-60.5238448132584,-3.54964646886187,
2.14974564724254));
#46287=CARTESIAN_POINT('Ctrl Pts',(-60.5901359904909,-2.56445546310868,
3.26266219205633));
#46288=CARTESIAN_POINT('Ctrl Pts',(-60.6564271677234,-1.3374258863424,3.70553028225484));
#46289=CARTESIAN_POINT('Ctrl Pts',(-60.7227183449559,-0.110396309576058,
4.14839837245339));
#46290=CARTESIAN_POINT('Ctrl Pts',(-60.7890095221883,1.35847183820337,3.92121800803657));
#46291=CARTESIAN_POINT('Ctrl Pts',(-60.8553006994208,2.39437902191271,3.12835608164908));
#46292=CARTESIAN_POINT('Ctrl Pts',(-60.9215918766533,3.43028620562202,2.33549415526161));
#46293=CARTESIAN_POINT('Ctrl Pts',(-60.9878830538858,4.03323242526126,0.976950666903413));
#46294=CARTESIAN_POINT('Ctrl Pts',(-61.0541742311183,3.92622356852165,-0.323158110143606));
#46295=CARTESIAN_POINT('Ctrl Pts',(-61.1204654083508,3.81921471178203,-1.62326688719066));
#46296=CARTESIAN_POINT('Ctrl Pts',(-61.1867565855833,3.00225077866358,-2.86494095292658));
#46297=CARTESIAN_POINT('Ctrl Pts',(-61.2530477628157,1.85064583876572,-3.47775396680466));
#46298=CARTESIAN_POINT('Ctrl Pts',(-61.3193389400482,0.699040898867858,
-4.09056698068275));
#46299=CARTESIAN_POINT('Ctrl Pts',(-61.3856301172807,-0.787205047809493,
-4.07451894270296));
#46300=CARTESIAN_POINT('Ctrl Pts',(-61.4519212945132,-1.92530908752859,
-3.4369823379887));
#46301=CARTESIAN_POINT('Ctrl Pts',(-61.5182124717457,-3.06341312724766,
-2.79944573327446));
#46302=CARTESIAN_POINT('Ctrl Pts',(-61.5845036489782,-3.85337526000851,
-1.54042056182595));
#46303=CARTESIAN_POINT('Ctrl Pts',(-61.6507948262107,-3.93228607101718,
-0.238304279967317));
#46304=CARTESIAN_POINT('Ctrl Pts',(-61.6548087101288,-3.93706406483925,
-0.159462059607168));
#46305=CARTESIAN_POINT('Ctrl Pts',(-61.6588225940469,-3.93923519029504,
-0.0804618578901768));
#46306=CARTESIAN_POINT('Ctrl Pts',(-61.6628364779651,-3.93886391369501,
-0.00144086038807723));
#46307=CARTESIAN_POINT('Ctrl Pts',(-61.8461635220346,-3.93914924332037,
-0.00107030884100855));
#46308=CARTESIAN_POINT('Ctrl Pts',(-61.8432264788935,-3.93935807419176,
-0.0588804731591042));
#46309=CARTESIAN_POINT('Ctrl Pts',(-61.8402894357523,-3.93819608322699,
-0.116682055459375));
#46310=CARTESIAN_POINT('Ctrl Pts',(-61.8373523926111,-3.9356371447697,-0.174421727073953));
#46311=CARTESIAN_POINT('Ctrl Pts',(-61.7710612153786,-3.87788006234203,
-1.47764766566053));
#46312=CARTESIAN_POINT('Ctrl Pts',(-61.7047700381462,-3.10846570392124,
-2.74933398649333));
#46313=CARTESIAN_POINT('Ctrl Pts',(-61.6384788609137,-1.98086381567448,
-3.40526668822253));
#46314=CARTESIAN_POINT('Ctrl Pts',(-61.5721876836812,-0.853261927427686,
-4.06119938995174));
#46315=CARTESIAN_POINT('Ctrl Pts',(-61.5058965064487,0.632527490645155,
-4.10137847257725));
#46316=CARTESIAN_POINT('Ctrl Pts',(-61.4396053292162,1.7939312545159,-3.5073456242916));
#46317=CARTESIAN_POINT('Ctrl Pts',(-61.3733141519837,2.95533501838662,-2.91331277600597));
#46318=CARTESIAN_POINT('Ctrl Pts',(-61.3070229747513,3.79235312805534,-1.68506799680926));
#46319=CARTESIAN_POINT('Ctrl Pts',(-61.2407317975188,3.92045860462712,-0.386868199225031));
#46320=CARTESIAN_POINT('Ctrl Pts',(-61.1744406202863,4.04856408119891,0.911331598359233));
#46321=CARTESIAN_POINT('Ctrl Pts',(-61.1081494430538,3.46775692467366,2.27948641433106));
#46322=CARTESIAN_POINT('Ctrl Pts',(-61.0418582658213,2.44486053903682,3.08906452163548));
#46323=CARTESIAN_POINT('Ctrl Pts',(-60.9755670885888,1.4219641534,3.89864262893988));
#46324=CARTESIAN_POINT('Ctrl Pts',(-60.9092759113564,-0.0430214613483292,
4.14964402757698));
#46325=CARTESIAN_POINT('Ctrl Pts',(-60.8429847341239,-1.27708040978551,
3.72675841732577));
#46326=CARTESIAN_POINT('Ctrl Pts',(-60.7766935568914,-2.51113935822273,
3.30387280707455));
#46327=CARTESIAN_POINT('Ctrl Pts',(-60.7104023796589,-3.51427164034871,
2.20710018793501));
#46328=CARTESIAN_POINT('Ctrl Pts',(-60.6441112024264,-3.82563725590282,
0.940299027126366));
#46329=CARTESIAN_POINT('Ctrl Pts',(-60.6281286422958,-3.90070636586495,
0.634877905170875));
#46330=CARTESIAN_POINT('Ctrl Pts',(-60.6121460821653,-3.93556484722619,
0.319573458575761));
#46331=CARTESIAN_POINT('Ctrl Pts',(-60.5961635220347,-3.93266179433523,
0.00363627036369697));
#46332=CARTESIAN_POINT('Origin',(-54.75,0.,0.));
#46333=CARTESIAN_POINT('',(-59.1628364779651,-3.92648948652695,-0.00022326326588662));
#46334=CARTESIAN_POINT('',(-59.3461635220347,-3.92655384726127,-0.000574964978985582));
#46335=CARTESIAN_POINT('',(-54.75,-3.933,-4.81653586104654E-16));
#46336=CARTESIAN_POINT('Ctrl Pts',(-59.1628364779651,-3.92648948652695,
-0.00022326326588662));
#46337=CARTESIAN_POINT('Ctrl Pts',(-59.1966618005905,-3.92615091508906,
0.671075478630216));
#46338=CARTESIAN_POINT('Ctrl Pts',(-59.2304871232159,-3.76302289449586,
1.34252854543093));
#46339=CARTESIAN_POINT('Ctrl Pts',(-59.2643124458412,-3.43803522382986,
1.92342831264168));
#46340=CARTESIAN_POINT('Ctrl Pts',(-59.3306036230737,-2.80112140890214,
3.06188099937473));
#46341=CARTESIAN_POINT('Ctrl Pts',(-59.3968948003062,-1.54252864031098,
3.85253186820853));
#46342=CARTESIAN_POINT('Ctrl Pts',(-59.4631859775387,-0.240455728064175,
3.93215509828994));
#46343=CARTESIAN_POINT('Ctrl Pts',(-59.5294771547712,1.06161718418263,4.01177832837136));
#46344=CARTESIAN_POINT('Ctrl Pts',(-59.5957683320036,2.40717024008509,3.3803739197004));
#46345=CARTESIAN_POINT('Ctrl Pts',(-59.6620595092361,3.17805498436802,2.32800970584318));
#46346=CARTESIAN_POINT('Ctrl Pts',(-59.7283506864686,3.94893972865099,1.2756454919859));
#46347=CARTESIAN_POINT('Ctrl Pts',(-59.7946418637011,4.14515616131437,-0.197678527057687));
#46348=CARTESIAN_POINT('Ctrl Pts',(-59.8609330409336,3.67656225174966,-1.41511578437099));
#46349=CARTESIAN_POINT('Ctrl Pts',(-59.9272242181661,3.207968342185,-2.63255304168415));
#46350=CARTESIAN_POINT('Ctrl Pts',(-59.9935153953985,2.07456409039245,-3.5941035372671));
#46351=CARTESIAN_POINT('Ctrl Pts',(-60.059806572631,0.797036573239359,-3.85802998628644));
#46352=CARTESIAN_POINT('Ctrl Pts',(-60.1260977498635,-0.480490943913802,
-4.12195643530578));
#46353=CARTESIAN_POINT('Ctrl Pts',(-60.1923889270961,-1.90214172642751,
-3.68825883776143));
#46354=CARTESIAN_POINT('Ctrl Pts',(-60.2586801043285,-2.81480794529668,
-2.75617831521495));
#46355=CARTESIAN_POINT('Ctrl Pts',(-60.3100655622074,-3.52225912515261,
-2.03367818125222));
#46356=CARTESIAN_POINT('Ctrl Pts',(-60.3614510200862,-3.92388486460105,
-1.01172264447929));
#46357=CARTESIAN_POINT('Ctrl Pts',(-60.412836477965,-3.93331087711921,0.00361726591575254));
#46358=CARTESIAN_POINT('Ctrl Pts',(-60.5961635220347,-3.93266179433523,
0.00363627036369697));
#46359=CARTESIAN_POINT('Ctrl Pts',(-60.5458549049328,-3.9235237979739,-0.990845395913261));
#46360=CARTESIAN_POINT('Ctrl Pts',(-60.4955462878309,-3.5402392935668,-1.99159635371037));
#46361=CARTESIAN_POINT('Ctrl Pts',(-60.445237670729,-2.85919073622048,-2.71010903988703));
#46362=CARTESIAN_POINT('Ctrl Pts',(-60.3789464934965,-1.96177965200193,
-3.65688624361394));
#46363=CARTESIAN_POINT('Ctrl Pts',(-60.312655316264,-0.547358534582749,
-4.11361094859019));
#46364=CARTESIAN_POINT('Ctrl Pts',(-60.2463641390315,0.734286102598856,
-3.87046335645961));
#46365=CARTESIAN_POINT('Ctrl Pts',(-60.180072961799,2.01593073978061,-3.62731576432901));
#46366=CARTESIAN_POINT('Ctrl Pts',(-60.1137817845665,3.16479889672468,-2.68429587509133));
#46367=CARTESIAN_POINT('Ctrl Pts',(-60.0474906073341,3.65309936266116,-1.47462799400088));
#46368=CARTESIAN_POINT('Ctrl Pts',(-59.9811994301016,4.14139982859761,-0.264960112910496));
#46369=CARTESIAN_POINT('Ctrl Pts',(-59.9149082528691,3.96913260352656,1.21135576003267));
#46370=CARTESIAN_POINT('Ctrl Pts',(-59.8486170756366,3.21543742750144,2.27609859715904));
#46371=CARTESIAN_POINT('Ctrl Pts',(-59.7823258984041,2.4617422514763,3.34084143428544));
#46372=CARTESIAN_POINT('Ctrl Pts',(-59.7160347211716,1.12661912449713,3.99401123559503));
#46373=CARTESIAN_POINT('Ctrl Pts',(-59.6497435439392,-0.176575018216088,
3.93554112379841));
#46374=CARTESIAN_POINT('Ctrl Pts',(-59.5834523667067,-1.47976916092926,
3.87707101200179));
#46375=CARTESIAN_POINT('Ctrl Pts',(-59.5171611894742,-2.75103431937646,
3.10696098709893));
#46376=CARTESIAN_POINT('Ctrl Pts',(-59.4508700122417,-3.40634997464003,
1.97900038515314));
#46377=CARTESIAN_POINT('Ctrl Pts',(-59.4159678488394,-3.75137226923431,
1.38513153436435));
#46378=CARTESIAN_POINT('Ctrl Pts',(-59.381065685437,-3.92565335922222,0.692066502269124));
#46379=CARTESIAN_POINT('Ctrl Pts',(-59.3461635220347,-3.92655384726127,
-0.000574964978985582));
#46380=CARTESIAN_POINT('Origin',(-54.75,0.,0.));
#46381=CARTESIAN_POINT('',(-57.9128364779651,-3.93413307819626,-0.00353956003321609));
#46382=CARTESIAN_POINT('',(-58.0961635220347,-3.93477881256964,-0.00343548079462405));
#46383=CARTESIAN_POINT('',(-54.75,-3.933,-4.81653586104654E-16));
#46384=CARTESIAN_POINT('Ctrl Pts',(-57.9128364779651,-3.93413307819626,
-0.00353956003321609));
#46385=CARTESIAN_POINT('Ctrl Pts',(-57.9655814038622,-3.92446652853235,
1.03810397902358));
#46386=CARTESIAN_POINT('Ctrl Pts',(-58.0183263297594,-3.49893535502753,
2.08672616861535));
#46387=CARTESIAN_POINT('Ctrl Pts',(-58.0710712556565,-2.7577179772013,2.81329952766982));
#46388=CARTESIAN_POINT('Ctrl Pts',(-58.137362432889,-1.82613694403996,3.72647558201504));
#46389=CARTESIAN_POINT('Ctrl Pts',(-58.2036536101215,-0.395894578184176,
4.13093983068094));
#46390=CARTESIAN_POINT('Ctrl Pts',(-58.269944787354,0.875954309153151,3.84088098259272));
#46391=CARTESIAN_POINT('Ctrl Pts',(-58.3362359645864,2.14780319649048,3.55082213450451));
#46392=CARTESIAN_POINT('Ctrl Pts',(-58.4025271418189,3.26125860530939,2.56624018966217));
#46393=CARTESIAN_POINT('Ctrl Pts',(-58.4688183190514,3.70479797768473,1.33945310433386));
#46394=CARTESIAN_POINT('Ctrl Pts',(-58.5351094962839,4.14833735006006,0.11266601900554));
#46395=CARTESIAN_POINT('Ctrl Pts',(-58.6014006735164,3.92196068599184,-1.35632620680879));
#46396=CARTESIAN_POINT('Ctrl Pts',(-58.6676918507489,3.12966565735949,-2.39266703644929));
#46397=CARTESIAN_POINT('Ctrl Pts',(-58.7339830279814,2.33737062872715,-3.42900786608978));
#46398=CARTESIAN_POINT('Ctrl Pts',(-58.8002742052139,0.979157235530679,
-4.03269729955644));
#46399=CARTESIAN_POINT('Ctrl Pts',(-58.8665653824463,-0.321009895004302,
-3.92639979134522));
#46400=CARTESIAN_POINT('Ctrl Pts',(-58.9328565596788,-1.62117702553925,
-3.82010228313399));
#46401=CARTESIAN_POINT('Ctrl Pts',(-58.9991477369113,-2.86329789341262,
-3.00381783324499));
#46402=CARTESIAN_POINT('Ctrl Pts',(-59.0654389141437,-3.47674089671723,
-1.85254835598435));
#46403=CARTESIAN_POINT('Ctrl Pts',(-59.0979047687509,-3.77717229930323,
-1.28871846152857));
#46404=CARTESIAN_POINT('Ctrl Pts',(-59.130370623358,-3.92681445049547,-0.644541947043256));
#46405=CARTESIAN_POINT('Ctrl Pts',(-59.1628364779651,-3.92648948652695,
-0.00022326326588662));
#46406=CARTESIAN_POINT('Ctrl Pts',(-59.3461635220347,-3.92655384726127,
-0.000574964978985582));
#46407=CARTESIAN_POINT('Ctrl Pts',(-59.3147745082045,-3.927363694811,-0.623497170235501));
#46408=CARTESIAN_POINT('Ctrl Pts',(-59.2833854943744,-3.78794024227485,
-1.24607678874562));
#46409=CARTESIAN_POINT('Ctrl Pts',(-59.2519964805442,-3.50636358019973,
-1.79584997079805));
#46410=CARTESIAN_POINT('Ctrl Pts',(-59.1857053033117,-2.9116953784159,-2.9569285458146));
#46411=CARTESIAN_POINT('Ctrl Pts',(-59.1194141260793,-1.68299282276828,
-3.79327451685904));
#46412=CARTESIAN_POINT('Ctrl Pts',(-59.0531229488468,-0.384723128751967,
-3.92066968621047));
#46413=CARTESIAN_POINT('Ctrl Pts',(-58.9868317716143,0.913546565264345,
-4.0480648555619));
#46414=CARTESIAN_POINT('Ctrl Pts',(-58.9205405943818,2.28138339764935,-3.46650922322033));
#46415=CARTESIAN_POINT('Ctrl Pts',(-58.8542494171493,3.09040172333452,-2.44317004372955));
#46416=CARTESIAN_POINT('Ctrl Pts',(-58.7879582399168,3.89942004901979,-1.41983086423867));
#46417=CARTESIAN_POINT('Ctrl Pts',(-58.7216670626844,4.14961986800506,0.0452918624015372));
#46418=CARTESIAN_POINT('Ctrl Pts',(-58.6553758854519,3.7260591265843,1.27911925142432));
#46419=CARTESIAN_POINT('Ctrl Pts',(-58.5890847082194,3.30249838516356,2.51294664044703));
#46420=CARTESIAN_POINT('Ctrl Pts',(-58.5227935309869,2.20517708333687,3.51547869185234));
#46421=CARTESIAN_POINT('Ctrl Pts',(-58.4565023537544,0.938205753713269,
3.82615115198887));
#46422=CARTESIAN_POINT('Ctrl Pts',(-58.3902111765219,-0.328765575910331,
4.1368236121254));
#46423=CARTESIAN_POINT('Ctrl Pts',(-58.3239199992895,-1.76538693333084,
3.75563648099315));
#46424=CARTESIAN_POINT('Ctrl Pts',(-58.257628822057,-2.71167299206166,2.85770751797482));
#46425=CARTESIAN_POINT('Ctrl Pts',(-58.2038070553829,-3.47996207043064,
2.12867953634796));
#46426=CARTESIAN_POINT('Ctrl Pts',(-58.1499852887088,-3.92503161905221,
1.05902534985808));
#46427=CARTESIAN_POINT('Ctrl Pts',(-58.0961635220347,-3.93477881256964,
-0.00343548079462405));
#46428=CARTESIAN_POINT('Origin',(-54.75,0.,0.));
#46429=CARTESIAN_POINT('',(-56.6628364779651,-3.93840323605561,0.00188100101654563));
#46430=CARTESIAN_POINT('',(-56.8461635220347,-3.93796868589441,0.00220300913379331));
#46431=CARTESIAN_POINT('',(-54.75,-3.933,-4.81653586104654E-16));
#46432=CARTESIAN_POINT('Ctrl Pts',(-56.6628364779651,-3.93840323605561,
0.00188100101654563));
#46433=CARTESIAN_POINT('Ctrl Pts',(-56.6682098299015,-3.93902682028425,
0.107698540420122));
#46434=CARTESIAN_POINT('Ctrl Pts',(-56.6735831818379,-3.93513331440954,
0.213469473948844));
#46435=CARTESIAN_POINT('Ctrl Pts',(-56.6789565337743,-3.9265748387829,0.318861583768759));
#46436=CARTESIAN_POINT('Ctrl Pts',(-56.7452477110068,-3.82098871092086,
1.61908667858072));
#46437=CARTESIAN_POINT('Ctrl Pts',(-56.8115388882393,-3.00538398861963,
2.86165397675729));
#46438=CARTESIAN_POINT('Ctrl Pts',(-56.8778300654718,-1.85445031863387,
3.47572678585144));
#46439=CARTESIAN_POINT('Ctrl Pts',(-56.9441212427042,-0.703516648648172,
4.08979959494555));
#46440=CARTESIAN_POINT('Ctrl Pts',(-57.0104124199367,0.782745969022029,
4.0753779149573));
#46441=CARTESIAN_POINT('Ctrl Pts',(-57.0767035971692,1.92154696196791,3.43908708047911));
#46442=CARTESIAN_POINT('Ctrl Pts',(-57.1429947744017,3.06034795491373,2.80279624600096));
#46443=CARTESIAN_POINT('Ctrl Pts',(-57.2092859516342,3.85168732313528,1.54463625703294));
#46444=CARTESIAN_POINT('Ctrl Pts',(-57.2755771288667,3.93202294845389,0.242607104179611));
#46445=CARTESIAN_POINT('Ctrl Pts',(-57.3418683060992,4.01235857377251,-1.05942204867379));
#46446=CARTESIAN_POINT('Ctrl Pts',(-57.4081594833316,3.38169045618811,-2.40532036541251));
#46447=CARTESIAN_POINT('Ctrl Pts',(-57.4744506605641,2.32974817638575,-3.17678077757873));
#46448=CARTESIAN_POINT('Ctrl Pts',(-57.5407418377966,1.27780589658338,-3.94824118974495));
#46449=CARTESIAN_POINT('Ctrl Pts',(-57.6070330150291,-0.195410545436957,
-4.14526369733868));
#46450=CARTESIAN_POINT('Ctrl Pts',(-57.6733241922616,-1.41310400375366,
-3.6773359581009));
#46451=CARTESIAN_POINT('Ctrl Pts',(-57.7396153694941,-2.63079746207036,
-3.20940821886311));
#46452=CARTESIAN_POINT('Ctrl Pts',(-57.8059065467266,-3.59296793668343,
-2.07653023279381));
#46453=CARTESIAN_POINT('Ctrl Pts',(-57.872197723959,-3.85759332375651,-0.799147309746884));
#46454=CARTESIAN_POINT('Ctrl Pts',(-57.8857439752944,-3.91166812152987,
-0.53812086777579));
#46455=CARTESIAN_POINT('Ctrl Pts',(-57.8992902266297,-3.93661569636409,
-0.271060367805669));
#46456=CARTESIAN_POINT('Ctrl Pts',(-57.9128364779651,-3.93413307819626,
-0.00353956003321609));
#46457=CARTESIAN_POINT('Ctrl Pts',(-58.0961635220347,-3.93477881256964,
-0.00343548079462405));
#46458=CARTESIAN_POINT('Ctrl Pts',(-58.0836941114763,-3.93703703940372,
-0.249586083391217));
#46459=CARTESIAN_POINT('Ctrl Pts',(-58.0712247009179,-3.91592912913868,
-0.495350579148307));
#46460=CARTESIAN_POINT('Ctrl Pts',(-58.0587552903595,-3.87006102492655,
-0.736403651206962));
#46461=CARTESIAN_POINT('Ctrl Pts',(-57.992464113127,-3.62621223901949,-2.017915062466));
#46462=CARTESIAN_POINT('Ctrl Pts',(-57.9261729358945,-2.68256390716426,
-3.16626709007967));
#46463=CARTESIAN_POINT('Ctrl Pts',(-57.8598817586621,-1.47262904179876,
-3.65390563362237));
#46464=CARTESIAN_POINT('Ctrl Pts',(-57.7935905814296,-0.262694176433262,
-4.14154417716508));
#46465=CARTESIAN_POINT('Ctrl Pts',(-57.7272994041971,1.2135272224425,-3.96846923663683));
#46466=CARTESIAN_POINT('Ctrl Pts',(-57.6610082269646,2.27785752864255,-3.21419161740132));
#46467=CARTESIAN_POINT('Ctrl Pts',(-57.5947170497321,3.3421878348426,-2.45991399816581));
#46468=CARTESIAN_POINT('Ctrl Pts',(-57.5284258724996,3.99462704836693,-1.12443370022303));
#46469=CARTESIAN_POINT('Ctrl Pts',(-57.4621346952671,3.93544392470469,0.178728256499565));
#46470=CARTESIAN_POINT('Ctrl Pts',(-57.3958435180347,3.87626080104246,1.48189021322216));
#46471=CARTESIAN_POINT('Ctrl Pts',(-57.3295523408022,3.10545534019366,2.75273382872457));
#46472=CARTESIAN_POINT('Ctrl Pts',(-57.2632611635697,1.97713636220909,3.40743224135082));
#46473=CARTESIAN_POINT('Ctrl Pts',(-57.1969699863372,0.848817384224515,
4.06213065397707));
#46474=CARTESIAN_POINT('Ctrl Pts',(-57.1306788091047,-0.637015110895826,
4.10068386372716));
#46475=CARTESIAN_POINT('Ctrl Pts',(-57.0643876318722,-1.7977681494841,3.50538048646177));
#46476=CARTESIAN_POINT('Ctrl Pts',(-56.9980964546397,-2.95852118807237,
2.91007710919639));
#46477=CARTESIAN_POINT('Ctrl Pts',(-56.9318052774073,-3.79419477012857,
1.68091714491552));
#46478=CARTESIAN_POINT('Ctrl Pts',(-56.8655141001748,-3.92087959412325,
0.382577943110031));
#46479=CARTESIAN_POINT('Ctrl Pts',(-56.8590639074614,-3.93320614439339,
0.256248340762304));
#46480=CARTESIAN_POINT('Ctrl Pts',(-56.8526137147481,-3.93882036517576,
0.12926378608889));
#46481=CARTESIAN_POINT('Ctrl Pts',(-56.8461635220347,-3.93796868589441,
0.00220300913379331));
#46482=CARTESIAN_POINT('Origin',(-54.75,0.,0.));
#46483=CARTESIAN_POINT('',(-55.4128364779651,-3.92832844003735,0.00261578722564659));
#46484=CARTESIAN_POINT('',(-55.5961635220347,-3.92791896985871,0.00235549104295047));
#46485=CARTESIAN_POINT('',(-54.75,-3.933,-4.81653586104654E-16));
#46486=CARTESIAN_POINT('Ctrl Pts',(-55.4128364779651,-3.92832844003735,
0.00261578722564659));
#46487=CARTESIAN_POINT('Ctrl Pts',(-55.4371294331733,-3.93125619142034,
0.484170671996506));
#46488=CARTESIAN_POINT('Ctrl Pts',(-55.4614223883815,-3.84934041430319,
0.964764115204058));
#46489=CARTESIAN_POINT('Ctrl Pts',(-55.4857153435896,-3.67810856362453,
1.41109180011732));
#46490=CARTESIAN_POINT('Ctrl Pts',(-55.5520065208221,-3.21084713478989,
2.6290410949153));
#46491=CARTESIAN_POINT('Ctrl Pts',(-55.6182976980545,-2.07849575357617,
3.59183126052822));
#46492=CARTESIAN_POINT('Ctrl Pts',(-55.684588875287,-0.801257807025967,
3.85715550643818));
#46493=CARTESIAN_POINT('Ctrl Pts',(-55.7508800525195,0.475980139524241,
4.12247975234815));
#46494=CARTESIAN_POINT('Ctrl Pts',(-55.817171229752,1.89810465141093,3.69033807855515));
#46495=CARTESIAN_POINT('Ctrl Pts',(-55.8834624069845,2.81179026786874,2.75925681365202));
#46496=CARTESIAN_POINT('Ctrl Pts',(-55.949753584217,3.72547588432654,1.82817554874889));
#46497=CARTESIAN_POINT('Ctrl Pts',(-56.0160447614495,4.13072260535545,0.398154692735642));
#46498=CARTESIAN_POINT('Ctrl Pts',(-56.082335938682,3.8413596712738,-0.873852705023954));
#46499=CARTESIAN_POINT('Ctrl Pts',(-56.1486271159144,3.55199673719215,-2.14586010278355));
#46500=CARTESIAN_POINT('Ctrl Pts',(-56.2149182931469,2.56802414799994,-3.25985404228949));
#46501=CARTESIAN_POINT('Ctrl Pts',(-56.2812094703794,1.34147992135404,-3.70406456406613));
#46502=CARTESIAN_POINT('Ctrl Pts',(-56.3475006476119,0.114935694708133,
-4.14827508584278));
#46503=CARTESIAN_POINT('Ctrl Pts',(-56.4137918248444,-1.35418016939147,
-3.92270218989013));
#46504=CARTESIAN_POINT('Ctrl Pts',(-56.4800830020769,-2.39095433472975,
-3.13097429619016));
#46505=CARTESIAN_POINT('Ctrl Pts',(-56.541000827373,-3.34369088448296,-2.4034213468543));
#46506=CARTESIAN_POINT('Ctrl Pts',(-56.601918652669,-3.93133364605914,-1.19777508980574));
#46507=CARTESIAN_POINT('Ctrl Pts',(-56.6628364779651,-3.93840323605561,
0.00188100101654563));
#46508=CARTESIAN_POINT('Ctrl Pts',(-56.8461635220347,-3.93796868589441,
0.00220300913379331));
#46509=CARTESIAN_POINT('Ctrl Pts',(-56.7863225375156,-3.93006732093442,
-1.17658998584482));
#46510=CARTESIAN_POINT('Ctrl Pts',(-56.7264815529964,-3.36564558318113,
-2.36194343678467));
#46511=CARTESIAN_POINT('Ctrl Pts',(-56.6666405684773,-2.44147881704743,
-3.091737999908));
#46512=CARTESIAN_POINT('Ctrl Pts',(-56.6003493912448,-1.4176971500438,-3.90019630179039));
#46513=CARTESIAN_POINT('Ctrl Pts',(-56.5340582140124,0.0475622498966481,
-4.14959446622516));
#46514=CARTESIAN_POINT('Ctrl Pts',(-56.4677670367799,1.28115771015286,-3.72535872042979));
#46515=CARTESIAN_POINT('Ctrl Pts',(-56.4014758595474,2.51475317040914,-3.3011229746344));
#46516=CARTESIAN_POINT('Ctrl Pts',(-56.3351846823149,3.51668469098117,-2.20325331860879));
#46517=CARTESIAN_POINT('Ctrl Pts',(-56.2688935050824,3.82666390269889,-0.936112199443943));
#46518=CARTESIAN_POINT('Ctrl Pts',(-56.2026023278499,4.13664311441661,0.331028919720903));
#46519=CARTESIAN_POINT('Ctrl Pts',(-56.1363111506175,3.75467001728003,1.76744150202498));
#46520=CARTESIAN_POINT('Ctrl Pts',(-56.070019973385,2.85622344426113,2.71323613248452));
#46521=CARTESIAN_POINT('Ctrl Pts',(-56.0037287961525,1.95777687124224,3.65903076294405));
#46522=CARTESIAN_POINT('Ctrl Pts',(-55.93743761892,0.542856822341028,4.11420744155904));
#46523=CARTESIAN_POINT('Ctrl Pts',(-55.8711464416875,-0.738520979369014,
3.86965753487286));
#46524=CARTESIAN_POINT('Ctrl Pts',(-55.804855264455,-2.01989878107906,3.62510762818668));
#46525=CARTESIAN_POINT('Ctrl Pts',(-55.7385640872225,-3.16773433559793,
2.68083113619934));
#46526=CARTESIAN_POINT('Ctrl Pts',(-55.67227290999,-3.65471081077004,1.47062964875833));
#46527=CARTESIAN_POINT('Ctrl Pts',(-55.6469031140049,-3.84107790124023,
1.00748257370225));
#46528=CARTESIAN_POINT('Ctrl Pts',(-55.6215333180198,-3.93065480055029,
0.50538781380894));
#46529=CARTESIAN_POINT('Ctrl Pts',(-55.5961635220347,-3.92791896985871,
0.00235549104295047));
#46530=CARTESIAN_POINT('Origin',(-54.75,0.,0.));
#46531=CARTESIAN_POINT('',(-54.1628364779651,-3.92884235167783,-0.00287961617827709));
#46532=CARTESIAN_POINT('',(-54.3461635220347,-3.92934053852407,-0.00308456158941818));
#46533=CARTESIAN_POINT('',(-54.75,-3.933,-4.81653586104654E-16));
#46534=CARTESIAN_POINT('Ctrl Pts',(-54.1628364779651,-3.92884235167783,
-0.00287961617827709));
#46535=CARTESIAN_POINT('Ctrl Pts',(-54.206049036445,-3.92306180087508,0.853433875710847));
#46536=CARTESIAN_POINT('Ctrl Pts',(-54.249261594925,-3.64800779627708,1.71312716798816));
#46537=CARTESIAN_POINT('Ctrl Pts',(-54.2924741534049,-3.1322819977492,2.38924091726697));
#46538=CARTESIAN_POINT('Ctrl Pts',(-54.3587653306374,-2.34112147598905,
3.42644810793985));
#46539=CARTESIAN_POINT('Ctrl Pts',(-54.4250565078698,-0.983569492779588,
4.03162342668745));
#46540=CARTESIAN_POINT('Ctrl Pts',(-54.4913476851023,0.316713177080749,
3.92674871078222));
#46541=CARTESIAN_POINT('Ctrl Pts',(-54.5576388623348,1.61699584694123,3.82187399487699));
#46542=CARTESIAN_POINT('Ctrl Pts',(-54.6239300395673,2.8600092034525,3.00694924431876));
#46543=CARTESIAN_POINT('Ctrl Pts',(-54.6902212167998,3.47471163451067,1.85635172614531));
#46544=CARTESIAN_POINT('Ctrl Pts',(-54.7565123940323,4.08941406556879,0.705754207971926));
#46545=CARTESIAN_POINT('Ctrl Pts',(-54.8228035712648,4.07580557117382,-0.780516077816789));
#46546=CARTESIAN_POINT('Ctrl Pts',(-54.8890947484972,3.44013790762175,-1.91966503607018));
#46547=CARTESIAN_POINT('Ctrl Pts',(-54.9553859257297,2.80447024406971,-3.0588139943235));
#46548=CARTESIAN_POINT('Ctrl Pts',(-55.0216771029623,1.54674341136077,-3.8508416250417));
#46549=CARTESIAN_POINT('Ctrl Pts',(-55.0879682801947,0.24475840766927,-3.93188962154861));
#46550=CARTESIAN_POINT('Ctrl Pts',(-55.1542594574272,-1.05722659602223,
-4.01293761805551));
#46551=CARTESIAN_POINT('Ctrl Pts',(-55.2205506346596,-2.4034697706962,-3.3830059803511));
#46552=CARTESIAN_POINT('Ctrl Pts',(-55.2868418118921,-3.17550561980544,
-2.33148594950742));
#46553=CARTESIAN_POINT('Ctrl Pts',(-55.3288400339164,-3.66462248807148,
-1.6653042106689));
#46554=CARTESIAN_POINT('Ctrl Pts',(-55.3708382559408,-3.92326687582826,
-0.829907419366287));
#46555=CARTESIAN_POINT('Ctrl Pts',(-55.4128364779651,-3.92832844003735,
0.00261578722564659));
#46556=CARTESIAN_POINT('Ctrl Pts',(-55.5961635220347,-3.92791896985871,
0.00235549104295047));
#46557=CARTESIAN_POINT('Ctrl Pts',(-55.5552421407873,-3.92350608570213,
-0.809033669191091));
#46558=CARTESIAN_POINT('Ctrl Pts',(-55.51432075954,-3.67891797236441,-1.62286213955943));
#46559=CARTESIAN_POINT('Ctrl Pts',(-55.4733993782926,-3.21294484511795,
-2.27961577823905));
#46560=CARTESIAN_POINT('Ctrl Pts',(-55.4071082010601,-2.45808500846852,
-3.34353323490047));
#46561=CARTESIAN_POINT('Ctrl Pts',(-55.3408170238277,-1.12224793934446,
-3.99524166532875));
#46562=CARTESIAN_POINT('Ctrl Pts',(-55.2745258465952,0.180881441279908,
-3.93534554751764));
#46563=CARTESIAN_POINT('Ctrl Pts',(-55.2082346693627,1.48401082190435,-3.87544942970653));
#46564=CARTESIAN_POINT('Ctrl Pts',(-55.1419434921302,2.75443251402909,-3.10394876365596));
#46565=CARTESIAN_POINT('Ctrl Pts',(-55.0756523148977,3.40851348803101,-1.97527174740012));
#46566=CARTESIAN_POINT('Ctrl Pts',(-55.0093611376652,4.06259446203293,-0.846594731144286));
#46567=CARTESIAN_POINT('Ctrl Pts',(-54.9430699604327,4.10033471791204,0.639258635316805));
#46568=CARTESIAN_POINT('Ctrl Pts',(-54.8767787832002,3.50439634337196,1.79968578999994));
#46569=CARTESIAN_POINT('Ctrl Pts',(-54.8104876059678,2.90845796883184,2.96011294468314));
#46570=CARTESIAN_POINT('Ctrl Pts',(-54.7441964287352,1.67884096387245,3.79511388758835));
#46571=CARTESIAN_POINT('Ctrl Pts',(-54.6779052515028,0.380432642941623,
3.9210883283026));
#46572=CARTESIAN_POINT('Ctrl Pts',(-54.6116140742703,-0.917975677989054,
4.04706276901683));
#46573=CARTESIAN_POINT('Ctrl Pts',(-54.5453228970378,-2.28517531489115,
3.4640107075403));
#46574=CARTESIAN_POINT('Ctrl Pts',(-54.4790317198053,-3.09307335095514,
2.43978685949768));
#46575=CARTESIAN_POINT('Ctrl Pts',(-54.4347423205485,-3.63283324317415,
1.75549883161612));
#46576=CARTESIAN_POINT('Ctrl Pts',(-54.3904529212916,-3.92294163618298,
0.874288074100991));
#46577=CARTESIAN_POINT('Ctrl Pts',(-54.3461635220347,-3.92934053852407,
-0.00308456158941818));
#46578=CARTESIAN_POINT('Origin',(-54.75,0.,0.));
#46579=CARTESIAN_POINT('',(-52.9128364779651,-3.93881984523232,-0.00148943800153567));
#46580=CARTESIAN_POINT('',(-53.0961635220347,-3.93911522694479,-0.00112120486990875));
#46581=CARTESIAN_POINT('',(-54.75,-3.933,-4.81653586104654E-16));
#46582=CARTESIAN_POINT('Ctrl Pts',(-52.9128364779651,-3.93881984523232,
-0.00148943800153567));
#46583=CARTESIAN_POINT('Ctrl Pts',(-52.9749686397168,-3.93290517754326,
1.22173761791364));
#46584=CARTESIAN_POINT('Ctrl Pts',(-53.0371008014685,-3.31837611095895,
2.45009099042727));
#46585=CARTESIAN_POINT('Ctrl Pts',(-53.0992329632202,-2.33322302468783,
3.17422951142998));
#46586=CARTESIAN_POINT('Ctrl Pts',(-53.1655241404527,-1.28212555758009,
3.94684056636974));
#46587=CARTESIAN_POINT('Ctrl Pts',(-53.2318153176851,0.190874407383879,
4.14547504664396));
#46588=CARTESIAN_POINT('Ctrl Pts',(-53.2981064949176,1.40907917406434,3.67888006808928));
#46589=CARTESIAN_POINT('Ctrl Pts',(-53.3643976721501,2.62728394074473,3.21228508953463));
#46590=CARTESIAN_POINT('Ctrl Pts',(-53.4306888493826,3.59069350914173,2.08046065215113));
#46591=CARTESIAN_POINT('Ctrl Pts',(-53.496980026615,3.85671653446252,0.803368064444818));
#46592=CARTESIAN_POINT('Ctrl Pts',(-53.5632712038475,4.12273955978333,-0.473724523261566));
#46593=CARTESIAN_POINT('Ctrl Pts',(-53.62956238108,3.69137604202797,-1.89608526129067));
#46594=CARTESIAN_POINT('Ctrl Pts',(-53.6958535583125,2.76079482410662,-2.81028016634508));
#46595=CARTESIAN_POINT('Ctrl Pts',(-53.762144735545,1.83021360618522,-3.72447507139954));
#46596=CARTESIAN_POINT('Ctrl Pts',(-53.8284359127775,0.400414688097706,
-4.13050414347906));
#46597=CARTESIAN_POINT('Ctrl Pts',(-53.89472709001,-0.871750839302914,-3.8418372100261));
#46598=CARTESIAN_POINT('Ctrl Pts',(-53.9610182672425,-2.14391636670339,
-3.55317027657317));
#46599=CARTESIAN_POINT('Ctrl Pts',(-54.0273094444749,-3.25844850341708,
-2.5698073375879));
#46600=CARTESIAN_POINT('Ctrl Pts',(-54.0936006217074,-3.70333004161861,
-1.34350633679621));
#46601=CARTESIAN_POINT('Ctrl Pts',(-54.11667924046,-3.85821115610231,-0.916581752640813));
#46602=CARTESIAN_POINT('Ctrl Pts',(-54.1397578592125,-3.93192958216936,
-0.460212699595579));
#46603=CARTESIAN_POINT('Ctrl Pts',(-54.1628364779651,-3.92884235167783,
-0.00287961617827709));
#46604=CARTESIAN_POINT('Ctrl Pts',(-54.3461635220347,-3.92934053852407,
-0.00308456158941818));
#46605=CARTESIAN_POINT('Ctrl Pts',(-54.3241617440591,-3.93251934047123,
-0.438939602665642));
#46606=CARTESIAN_POINT('Ctrl Pts',(-54.3021599660835,-3.86568334434236,
-0.873847458915858));
#46607=CARTESIAN_POINT('Ctrl Pts',(-54.2801581881079,-3.72465719907194,
-1.28319578536092));
#46608=CARTESIAN_POINT('Ctrl Pts',(-54.2138670108754,-3.29974657589884,
-2.51655894756822));
#46609=CARTESIAN_POINT('Ctrl Pts',(-54.147575833643,-2.20132889432679,-3.51788963737405));
#46610=CARTESIAN_POINT('Ctrl Pts',(-54.0812846564105,-0.934018364945315,
-3.82717550787932));
#46611=CARTESIAN_POINT('Ctrl Pts',(-54.014993479178,0.333292164436233,-4.13646137838461));
#46612=CARTESIAN_POINT('Ctrl Pts',(-53.9487023019454,1.76949554162732,-3.75370242958909));
#46613=CARTESIAN_POINT('Ctrl Pts',(-53.8824111247129,2.71479846068759,-2.85473851552375));
#46614=CARTESIAN_POINT('Ctrl Pts',(-53.8161199474805,3.66010137974786,-1.95577460145841));
#46615=CARTESIAN_POINT('Ctrl Pts',(-53.749828770248,4.11450384067746,-0.540605722123302));
#46616=CARTESIAN_POINT('Ctrl Pts',(-53.6835375930156,3.8692528864193,0.740638086451396));
#46617=CARTESIAN_POINT('Ctrl Pts',(-53.6172464157831,3.62400193216114,2.02188189502609));
#46618=CARTESIAN_POINT('Ctrl Pts',(-53.5509552385505,2.67909756271524,3.16920063284027));
#46619=CARTESIAN_POINT('Ctrl Pts',(-53.484664061318,1.46862981547812,3.65551489386313));
#46620=CARTESIAN_POINT('Ctrl Pts',(-53.4183728840855,0.258162068241059,
4.14182915488595));
#46621=CARTESIAN_POINT('Ctrl Pts',(-53.3520817068531,-1.21786905678733,
3.96713893911743));
#46622=CARTESIAN_POINT('Ctrl Pts',(-53.2857905296207,-2.28137334542168,
3.21169711102494));
#46623=CARTESIAN_POINT('Ctrl Pts',(-53.222581527092,-3.29543054090254,2.49137916804033));
#46624=CARTESIAN_POINT('Ctrl Pts',(-53.1593725245633,-3.93442957764801,
1.24305768398959));
#46625=CARTESIAN_POINT('Ctrl Pts',(-53.0961635220347,-3.93911522694479,
-0.00112120486990875));
#46626=CARTESIAN_POINT('Origin',(-54.75,0.,0.));
#46627=CARTESIAN_POINT('',(-51.6628364779651,-3.93339868146552,0.0036118335011201));
#46628=CARTESIAN_POINT('',(-51.8461635220348,-3.93274891143005,0.00363589115318885));
#46629=CARTESIAN_POINT('',(-54.75,-3.933,-4.81653586104654E-16));
#46630=CARTESIAN_POINT('Ctrl Pts',(-51.6628364779651,-3.93339868146552,
0.0036118335011201));
#46631=CARTESIAN_POINT('Ctrl Pts',(-51.677597065756,-3.93610801214239,0.295253828418355));
#46632=CARTESIAN_POINT('Ctrl Pts',(-51.692357653547,-3.90643403127602,0.586349483354395));
#46633=CARTESIAN_POINT('Ctrl Pts',(-51.707118241338,-3.84231359870667,0.869648712619224));
#46634=CARTESIAN_POINT('Ctrl Pts',(-51.7734094185705,-3.5543427522962,2.14197198883212));
#46635=CARTESIAN_POINT('Ctrl Pts',(-51.8397005958029,-2.57158975789195,
3.2570419891133));
#46636=CARTESIAN_POINT('Ctrl Pts',(-51.9059917730354,-1.34553235005313,
3.70259441056227));
#46637=CARTESIAN_POINT('Ctrl Pts',(-51.9722829502679,-0.119474942214315,
4.14814683201123));
#46638=CARTESIAN_POINT('Ctrl Pts',(-52.0385741275004,1.34988687905908,3.92418167462798));
#46639=CARTESIAN_POINT('Ctrl Pts',(-52.1048653047329,2.38752678457389,3.13358876164514));
#46640=CARTESIAN_POINT('Ctrl Pts',(-52.1711564819654,3.4251666900887,2.34299584866229));
#46641=CARTESIAN_POINT('Ctrl Pts',(-52.2374476591978,4.03108467984492,0.985775180079861));
#46642=CARTESIAN_POINT('Ctrl Pts',(-52.3037388364303,3.92692140729116,-0.314564675583407));
#46643=CARTESIAN_POINT('Ctrl Pts',(-52.3700300136628,3.82275813473739,-1.61490453124667));
#46644=CARTESIAN_POINT('Ctrl Pts',(-52.4363211908953,3.00851359987363,-2.85836357399078));
#46645=CARTESIAN_POINT('Ctrl Pts',(-52.5026123681278,1.85825257794928,-3.4736954429989));
#46646=CARTESIAN_POINT('Ctrl Pts',(-52.5689035453603,0.70799155602493,-4.08902731200702));
#46647=CARTESIAN_POINT('Ctrl Pts',(-52.6351947225927,-0.778285952960015,
-4.07623200727915));
#46648=CARTESIAN_POINT('Ctrl Pts',(-52.7014858998252,-1.91778253551145,
-3.44118770494342));
#46649=CARTESIAN_POINT('Ctrl Pts',(-52.7677770770577,-3.05727911806288,
-2.80614340260768));
#46650=CARTESIAN_POINT('Ctrl Pts',(-52.8340682542902,-3.8499947741808,-1.54885010266406));
#46651=CARTESIAN_POINT('Ctrl Pts',(-52.9003594315227,-3.93175511761398,
-0.246909637889587));
#46652=CARTESIAN_POINT('Ctrl Pts',(-52.9045184470035,-3.93688464688544,
-0.16522771920707));
#46653=CARTESIAN_POINT('Ctrl Pts',(-52.9086774624843,-3.93921576248015,
-0.0833700634079406));
#46654=CARTESIAN_POINT('Ctrl Pts',(-52.9128364779651,-3.93881984523232,
-0.00148943800153567));
#46655=CARTESIAN_POINT('Ctrl Pts',(-53.0961635220347,-3.93911522694479,
-0.00112120486990875));
#46656=CARTESIAN_POINT('Ctrl Pts',(-53.0930813473308,-3.93934370689473,
-0.0617894094753985));
#46657=CARTESIAN_POINT('Ctrl Pts',(-53.089999172627,-3.93806398139047,-0.122447764242017));
#46658=CARTESIAN_POINT('Ctrl Pts',(-53.0869169979231,-3.93524599226671,
-0.183034571912559));
#46659=CARTESIAN_POINT('Ctrl Pts',(-53.0206258206906,-3.87463689823691,
-1.48613098634102));
#46660=CARTESIAN_POINT('Ctrl Pts',(-52.9543346434582,-3.10244125793682,
-2.75613037478151));
#46661=CARTESIAN_POINT('Ctrl Pts',(-52.8880434662257,-1.97340654128442,
-3.40959371435693));
#46662=CARTESIAN_POINT('Ctrl Pts',(-52.8217522889933,-0.844371824631968,
-4.06305705393239));
#46663=CARTESIAN_POINT('Ctrl Pts',(-52.7554611117607,0.641501968372705,
-4.0999843446428));
#46664=CARTESIAN_POINT('Ctrl Pts',(-52.6891699345282,1.80160289177152,-3.50341115122489));
#46665=CARTESIAN_POINT('Ctrl Pts',(-52.6228787572957,2.96170381517028,-2.90683795780702));
#46666=CARTESIAN_POINT('Ctrl Pts',(-52.5565875800633,3.79603186896307,-1.67676428026083));
#46667=CARTESIAN_POINT('Ctrl Pts',(-52.4902964028308,3.92129588868599,-0.378287228889388));
#46668=CARTESIAN_POINT('Ctrl Pts',(-52.4240052255983,4.04655990840891,0.920189822482053));
#46669=CARTESIAN_POINT('Ctrl Pts',(-52.3577140483658,3.46275989406197,2.28707024767885));
#46670=CARTESIAN_POINT('Ctrl Pts',(-52.2914228711333,2.43809417158646,3.09440777607648));
#46671=CARTESIAN_POINT('Ctrl Pts',(-52.2251316939008,1.41342844911096,3.9017453044741));
#46672=CARTESIAN_POINT('Ctrl Pts',(-52.1588405166684,-0.0521029814929644,
4.1495399360726));
#46673=CARTESIAN_POINT('Ctrl Pts',(-52.0925493394359,-1.28523347643839,
3.72395456272073));
#46674=CARTESIAN_POINT('Ctrl Pts',(-52.0262581622034,-2.51836397138382,
3.29836918936886));
#46675=CARTESIAN_POINT('Ctrl Pts',(-51.959966984971,-3.51909353067066,2.19940381106649));
#46676=CARTESIAN_POINT('Ctrl Pts',(-51.8936758077385,-3.82768596737718,
0.931924250843543));
#46677=CARTESIAN_POINT('Ctrl Pts',(-51.8778383791706,-3.9014108713081,0.629114467787446));
#46678=CARTESIAN_POINT('Ctrl Pts',(-51.8620009506027,-3.93563096151905,
0.31668647303777));
#46679=CARTESIAN_POINT('Ctrl Pts',(-51.8461635220348,-3.93274891143005,
0.00363589115318885));
#46680=CARTESIAN_POINT('Origin',(-54.75,0.,0.));
#46681=CARTESIAN_POINT('',(-50.4128364779651,-3.92648515689148,-0.000175634614104081));
#46682=CARTESIAN_POINT('',(-50.5961635220347,-3.92654186868141,-0.000527800881415484));
#46683=CARTESIAN_POINT('',(-54.75,-3.933,-4.81653586104654E-16));
#46684=CARTESIAN_POINT('Ctrl Pts',(-50.4128364779651,-3.92648515689148,
-0.000175634614104081));
#46685=CARTESIAN_POINT('Ctrl Pts',(-50.4465166690278,-3.92621997164172,
0.668244657360119));
#46686=CARTESIAN_POINT('Ctrl Pts',(-50.4801968600906,-3.76456310744387,
1.33678530445738));
#46687=CARTESIAN_POINT('Ctrl Pts',(-50.5138770511533,-3.44223647212953,
1.91589946085585));
#46688=CARTESIAN_POINT('Ctrl Pts',(-50.5801682283858,-2.80781572111349,
3.05574332659173));
#46689=CARTESIAN_POINT('Ctrl Pts',(-50.6464594056182,-1.55095633031185,
3.84914677080616));
#46690=CARTESIAN_POINT('Ctrl Pts',(-50.7127505828507,-0.249060794196362,
3.93161943669027));
#46691=CARTESIAN_POINT('Ctrl Pts',(-50.7790417600832,1.05283474191913,4.01409210257438));
#46692=CARTESIAN_POINT('Ctrl Pts',(-50.8453329373157,2.39976642334848,3.38563399012816));
#46693=CARTESIAN_POINT('Ctrl Pts',(-50.9116241145482,3.17295245283412,2.33495940140731));
#46694=CARTESIAN_POINT('Ctrl Pts',(-50.9779152917807,3.94613848231975,1.28428481268647));
#46695=CARTESIAN_POINT('Ctrl Pts',(-51.0442064690132,4.14557885986166,-0.188606252309012));
#46696=CARTESIAN_POINT('Ctrl Pts',(-51.1104976462456,3.67965047126436,-1.40706612619678));
#46697=CARTESIAN_POINT('Ctrl Pts',(-51.1767888234781,3.21372208266706,-2.62552600008455));
#46698=CARTESIAN_POINT('Ctrl Pts',(-51.2430800007106,2.08242492793056,-3.58955468286462));
#46699=CARTESIAN_POINT('Ctrl Pts',(-51.3093711779431,0.805478081371511,
-3.85627640796099));
#46700=CARTESIAN_POINT('Ctrl Pts',(-51.3756623551755,-0.471468765187465,
-4.12299813305734));
#46701=CARTESIAN_POINT('Ctrl Pts',(-51.441953532408,-1.89406530356897,-3.69241290047008));
#46702=CARTESIAN_POINT('Ctrl Pts',(-51.5082447096405,-2.80876922355138,
-2.76233200810421));
#46703=CARTESIAN_POINT('Ctrl Pts',(-51.5597752990821,-3.51980248814202,
-2.0393456528637));
#46704=CARTESIAN_POINT('Ctrl Pts',(-51.6113058885236,-3.92394015523687,
-1.01453758688934));
#46705=CARTESIAN_POINT('Ctrl Pts',(-51.6628364779651,-3.93339868146552,
0.0036118335011201));
#46706=CARTESIAN_POINT('Ctrl Pts',(-51.8461635220348,-3.93274891143005,
0.00363589115318885));
#46707=CARTESIAN_POINT('Ctrl Pts',(-51.7957097733702,-3.92356748212124,
-0.993658291421522));
#46708=CARTESIAN_POINT('Ctrl Pts',(-51.7452560247056,-3.53784138323085,
-1.99727102772681));
#46709=CARTESIAN_POINT('Ctrl Pts',(-51.694802276041,-2.85325273220719,-2.7163599762032));
#46710=CARTESIAN_POINT('Ctrl Pts',(-51.6285110988085,-1.95377174620445,
-3.66117090088337));
#46711=CARTESIAN_POINT('Ctrl Pts',(-51.562219921576,-0.538354460072711,
-4.11479900810012));
#46712=CARTESIAN_POINT('Ctrl Pts',(-51.4959287443436,0.742754971820343,
-3.868847079687));
#46713=CARTESIAN_POINT('Ctrl Pts',(-51.4296375671111,2.0238644037134,-3.62289515127387));
#46714=CARTESIAN_POINT('Ctrl Pts',(-51.3633463898786,3.17066598136777,-2.67736318723087));
#46715=CARTESIAN_POINT('Ctrl Pts',(-51.2970552126461,3.65631788266093,-1.46662954255678));
#46716=CARTESIAN_POINT('Ctrl Pts',(-51.2307640354136,4.14196978395412,-0.255895897882616));
#46717=CARTESIAN_POINT('Ctrl Pts',(-51.1644728581811,3.96647200888603,1.22003942742267));
#46718=CARTESIAN_POINT('Ctrl Pts',(-51.0981816809486,3.2104484154953,2.283130229665));
#46719=CARTESIAN_POINT('Ctrl Pts',(-51.0318905037161,2.45442482210466,3.34622103190721));
#46720=CARTESIAN_POINT('Ctrl Pts',(-50.9655993264837,1.11787541039155,3.99646731108659));
#46721=CARTESIAN_POINT('Ctrl Pts',(-50.8993081492512,-0.185187647752963,
3.9351452589817));
#46722=CARTESIAN_POINT('Ctrl Pts',(-50.8330169720187,-1.48825070589748,
3.87382320687682));
#46723=CARTESIAN_POINT('Ctrl Pts',(-50.7667257947862,-2.7578274104734,3.10093282348768));
#46724=CARTESIAN_POINT('Ctrl Pts',(-50.7004346175537,-3.4106729200051,1.97154074442055));
#46725=CARTESIAN_POINT('Ctrl Pts',(-50.665677585714,-3.75296541062707,1.37939080697223));
#46726=CARTESIAN_POINT('Ctrl Pts',(-50.6309205538744,-3.92571882340902,
0.689238742796217));
#46727=CARTESIAN_POINT('Ctrl Pts',(-50.5961635220347,-3.92654186868141,
-0.000527800881415484));
#46728=CARTESIAN_POINT('Origin',(-54.75,0.,0.));
#46729=CARTESIAN_POINT('',(-49.1628364779651,-3.93404549041159,-0.00355071844980182));
#46730=CARTESIAN_POINT('',(-49.3461635220347,-3.9346923370435,-0.00345168766750323));
#46731=CARTESIAN_POINT('',(-54.75,-3.933,-4.81653586104654E-16));
#46732=CARTESIAN_POINT('Ctrl Pts',(-49.1628364779651,-3.93404549041159,
-0.00355071844980182));
#46733=CARTESIAN_POINT('Ctrl Pts',(-49.2154362722996,-3.92439753107285,
1.03528607871439));
#46734=CARTESIAN_POINT('Ctrl Pts',(-49.2680360666341,-3.50145870567672,
2.0810673230136));
#46735=CARTESIAN_POINT('Ctrl Pts',(-49.3206358609685,-2.76386836518494,
2.80725743993962));
#46736=CARTESIAN_POINT('Ctrl Pts',(-49.386927038201,-1.83428807679852,3.72247010102922));
#46737=CARTESIAN_POINT('Ctrl Pts',(-49.4532182154335,-0.404934318547125,
4.13006351033546));
#46738=CARTESIAN_POINT('Ctrl Pts',(-49.519509392666,0.867546325602179,3.84278883717289));
#46739=CARTESIAN_POINT('Ctrl Pts',(-49.5858005698985,2.14002696975155,3.5555141640103));
#46740=CARTESIAN_POINT('Ctrl Pts',(-49.652091747131,3.25563449979882,2.57337140837882));
#46741=CARTESIAN_POINT('Ctrl Pts',(-49.7183829243635,3.70185767111709,1.34755796051894));
#46742=CARTESIAN_POINT('Ctrl Pts',(-49.784674101596,4.14808084243537,0.121744512659055));
#46743=CARTESIAN_POINT('Ctrl Pts',(-49.8509652788283,3.92491965502465,-1.34773962742924));
#46744=CARTESIAN_POINT('Ctrl Pts',(-49.9172564560608,3.1348945874868,-2.38581193716362));
#46745=CARTESIAN_POINT('Ctrl Pts',(-49.9835476332933,2.34486951994894,-3.42388424689801));
#46746=CARTESIAN_POINT('Ctrl Pts',(-50.0498388105259,0.987980572283947,
-4.0305447262785));
#46747=CARTESIAN_POINT('Ctrl Pts',(-50.1161299877584,-0.312416079919453,
-3.92709292825803));
#46748=CARTESIAN_POINT('Ctrl Pts',(-50.1824211649909,-1.61281273212285,
-3.82364113023756));
#46749=CARTESIAN_POINT('Ctrl Pts',(-50.2487123422233,-2.85671708886466,
-3.01007705481613));
#46750=CARTESIAN_POINT('Ctrl Pts',(-50.3150035194558,-3.47267821162034,
-1.86015287347675));
#46751=CARTESIAN_POINT('Ctrl Pts',(-50.3476145056255,-3.77569138009754,
-1.29446429862426));
#46752=CARTESIAN_POINT('Ctrl Pts',(-50.3802254917953,-3.9267419236211,-0.647376384056746));
#46753=CARTESIAN_POINT('Ctrl Pts',(-50.4128364779651,-3.92648515689148,
-0.000175634614104081));
#46754=CARTESIAN_POINT('Ctrl Pts',(-50.5961635220347,-3.92654186868141,
-0.000527800881415484));
#46755=CARTESIAN_POINT('Ctrl Pts',(-50.5646293766419,-3.92728859611787,
-0.626334934695071));
#46756=CARTESIAN_POINT('Ctrl Pts',(-50.5330952312491,-3.78651156323261,
-1.25182472892874));
#46757=CARTESIAN_POINT('Ctrl Pts',(-50.5015610858563,-3.50242491031551,
-1.80351945422495));
#46758=CARTESIAN_POINT('Ctrl Pts',(-50.4352699086238,-2.90521707660678,
-2.96329379905778));
#46759=CARTESIAN_POINT('Ctrl Pts',(-50.3689787313913,-1.67468709470198,
-3.79694871397818));
#46760=CARTESIAN_POINT('Ctrl Pts',(-50.3026875541588,-0.3761417015949,-3.92150227521134));
#46761=CARTESIAN_POINT('Ctrl Pts',(-50.2363963769263,0.922403691512177,
-4.0460558364445));
#46762=CARTESIAN_POINT('Ctrl Pts',(-50.1701051996938,2.28896449582153,-3.46150804399042));
#46763=CARTESIAN_POINT('Ctrl Pts',(-50.1038140224614,3.09574127487254,-2.43640075382048));
#46764=CARTESIAN_POINT('Ctrl Pts',(-50.0375228452289,3.9025180539235,-1.41129346365059));
#46765=CARTESIAN_POINT('Ctrl Pts',(-49.9712316679964,4.14951080771618,0.0543733242351024));
#46766=CARTESIAN_POINT('Ctrl Pts',(-49.9049404907639,3.7232508115865,1.28727078277528));
#46767=CARTESIAN_POINT('Ctrl Pts',(-49.8386493135314,3.29699081545681,2.52016824131552));
#46768=CARTESIAN_POINT('Ctrl Pts',(-49.7723581362989,2.19747806940468,3.52029637051022));
#46769=CARTESIAN_POINT('Ctrl Pts',(-49.7060669590665,0.929829857766153,
3.82819528103949));
#46770=CARTESIAN_POINT('Ctrl Pts',(-49.639775781834,-0.337818353872377,
4.13609419156877));
#46771=CARTESIAN_POINT('Ctrl Pts',(-49.5734846046015,-1.77360203109731,
3.75176388343262));
#46772=CARTESIAN_POINT('Ctrl Pts',(-49.507193427369,-2.71792067856389,2.85176609475624));
#46773=CARTESIAN_POINT('Ctrl Pts',(-49.4535167922576,-3.48254501599575,
2.12302880390319));
#46774=CARTESIAN_POINT('Ctrl Pts',(-49.3998401571462,-3.9249499243723,1.05620422076861));
#46775=CARTESIAN_POINT('Ctrl Pts',(-49.3461635220347,-3.9346923370435,-0.00345168766750323));
#46776=CARTESIAN_POINT('Origin',(-54.75,0.,0.));
#46777=CARTESIAN_POINT('',(-47.9128364779652,-3.93845732485478,0.00183569955874766));
#46778=CARTESIAN_POINT('',(-48.0961635220348,-3.93803051256068,0.00216112547147041));
#46779=CARTESIAN_POINT('',(-54.75,-3.933,-4.81653586104654E-16));
#46780=CARTESIAN_POINT('Ctrl Pts',(-47.9128364779652,-3.93845732485478,
0.00183569955874766));
#46781=CARTESIAN_POINT('Ctrl Pts',(-47.9180646983389,-3.93905186643222,
0.104791419839774));
#46782=CARTESIAN_POINT('Ctrl Pts',(-47.9232929187127,-3.93536614512923,
0.207703890362527));
#46783=CARTESIAN_POINT('Ctrl Pts',(-47.9285211390864,-3.92726327363148,
0.310267390732299));
#46784=CARTESIAN_POINT('Ctrl Pts',(-47.9948123163189,-3.82452298111308,
1.61072045019609));
#46785=CARTESIAN_POINT('Ctrl Pts',(-48.0611034935513,-3.01163960867816,
2.85506974856707));
#46786=CARTESIAN_POINT('Ctrl Pts',(-48.1273946707838,-1.86205261215886,
3.47165994067951));
#46787=CARTESIAN_POINT('Ctrl Pts',(-48.1936858480162,-0.712465615639556,
4.08825013279194));
#46788=CARTESIAN_POINT('Ctrl Pts',(-48.2599770252488,0.773825004964064,
4.0770812186458));
#46789=CARTESIAN_POINT('Ctrl Pts',(-48.3262682024813,1.91401581266688,3.44328420886624));
#46790=CARTESIAN_POINT('Ctrl Pts',(-48.3925593797138,3.0542066203697,2.80948719908667));
#46791=CARTESIAN_POINT('Ctrl Pts',(-48.4588505569462,3.84829761517164,1.55306209367373));
#46792=CARTESIAN_POINT('Ctrl Pts',(-48.5251417341787,3.93148257881811,0.251211875945639));
#46793=CARTESIAN_POINT('Ctrl Pts',(-48.5914329114112,4.01466754246458,-1.05063834178238));
#46794=CARTESIAN_POINT('Ctrl Pts',(-48.6577240886437,3.38694647495551,-2.39791367182562));
#46795=CARTESIAN_POINT('Ctrl Pts',(-48.7240152658762,2.33669507914591,-3.17167444440027));
#46796=CARTESIAN_POINT('Ctrl Pts',(-48.7903064431087,1.28644368333625,-3.94543521697496));
#46797=CARTESIAN_POINT('Ctrl Pts',(-48.8565976203412,-0.186338040773995,
-4.14568143208116));
#46798=CARTESIAN_POINT('Ctrl Pts',(-48.9228887975736,-1.40505265711748,
-3.68041977291906));
#46799=CARTESIAN_POINT('Ctrl Pts',(-48.9891799748061,-2.62376727346096,
-3.21515811375696));
#46800=CARTESIAN_POINT('Ctrl Pts',(-49.0554711520386,-3.58841478203762,
-2.08438858032658));
#46801=CARTESIAN_POINT('Ctrl Pts',(-49.1217623292711,-3.85583512706524,
-0.807587857174833));
#46802=CARTESIAN_POINT('Ctrl Pts',(-49.1354537121691,-3.91106652423369,
-0.54388507929504));
#46803=CARTESIAN_POINT('Ctrl Pts',(-49.1491450950671,-3.93655679120968,
-0.273953151358113));
#46804=CARTESIAN_POINT('Ctrl Pts',(-49.1628364779651,-3.93404549041159,
-0.00355071844980182));
#46805=CARTESIAN_POINT('Ctrl Pts',(-49.3461635220347,-3.9346923370435,-0.00345168766750323));
#46806=CARTESIAN_POINT('Ctrl Pts',(-49.3335489799137,-3.93698190073814,
-0.252481345787259));
#46807=CARTESIAN_POINT('Ctrl Pts',(-49.3209344377926,-3.91537565931263,
-0.501115080397896));
#46808=CARTESIAN_POINT('Ctrl Pts',(-49.3083198956715,-3.8684401147974,-0.744871634842373));
#46809=CARTESIAN_POINT('Ctrl Pts',(-49.242028718439,-3.62178728585608,-2.02584630654768));
#46810=CARTESIAN_POINT('Ctrl Pts',(-49.1757375412066,-2.6756280102654,-3.17213038074177));
#46811=CARTESIAN_POINT('Ctrl Pts',(-49.1094463639741,-1.46462883059311,
-3.65711977692308));
#46812=CARTESIAN_POINT('Ctrl Pts',(-49.0431551867416,-0.253629650920743,
-4.14210917310442));
#46813=CARTESIAN_POINT('Ctrl Pts',(-48.9768640095091,1.22220943283327,-3.9658038912729));
#46814=CARTESIAN_POINT('Ctrl Pts',(-48.9105728322766,2.28488643044238,-3.20919875890334));
#46815=CARTESIAN_POINT('Ctrl Pts',(-48.8442816550441,3.34756342805149,-2.45259362653377));
#46816=CARTESIAN_POINT('Ctrl Pts',(-48.7779904778117,3.99707833951569,-1.11568864362615));
#46817=CARTESIAN_POINT('Ctrl Pts',(-48.7116993005792,3.93504334769276,0.187340668156589));
#46818=CARTESIAN_POINT('Ctrl Pts',(-48.6454081233467,3.87300835586984,1.49036997993933));
#46819=CARTESIAN_POINT('Ctrl Pts',(-48.5791169461142,3.09942346075977,2.7595236205972));
#46820=CARTESIAN_POINT('Ctrl Pts',(-48.5128257688817,1.96967435736646,3.41175110465278));
#46821=CARTESIAN_POINT('Ctrl Pts',(-48.4465345916492,0.83992525397314,4.06397858870837));
#46822=CARTESIAN_POINT('Ctrl Pts',(-48.3802434144167,-0.645988057703424,
4.09927991616168));
#46823=CARTESIAN_POINT('Ctrl Pts',(-48.3139522371843,-1.8054354767865,3.50143762093903));
#46824=CARTESIAN_POINT('Ctrl Pts',(-48.2476610599518,-2.96488289586957,
2.90359532571638));
#46825=CARTESIAN_POINT('Ctrl Pts',(-48.1813698827193,-3.79786442235915,
1.67260940781778));
#46826=CARTESIAN_POINT('Ctrl Pts',(-48.1150787054868,-3.92170748781686,
0.373996061700655));
#46827=CARTESIAN_POINT('Ctrl Pts',(-48.1087736443361,-3.93348640219728,
0.250482844705844));
#46828=CARTESIAN_POINT('Ctrl Pts',(-48.1024685831855,-3.93885029408403,
0.1263578551207));
#46829=CARTESIAN_POINT('Ctrl Pts',(-48.0961635220348,-3.93803051256068,
0.00216112547147041));
#46830=CARTESIAN_POINT('Origin',(-54.75,0.,0.));
#46831=CARTESIAN_POINT('',(-46.6628364779651,-3.92838703301762,0.00264903870899197));
#46832=CARTESIAN_POINT('',(-46.8461635220347,-3.92797149977701,0.00239191756703917));
#46833=CARTESIAN_POINT('',(-54.75,-3.933,-4.81653586104654E-16));
#46834=CARTESIAN_POINT('Ctrl Pts',(-46.6628364779651,-3.92838703301762,
0.00264903870899197));
#46835=CARTESIAN_POINT('Ctrl Pts',(-46.6869843016106,-3.93133701178113,
0.481309096112364));
#46836=CARTESIAN_POINT('Ctrl Pts',(-46.7111321252561,-3.85042547221201,
0.959006099363471));
#46837=CARTESIAN_POINT('Ctrl Pts',(-46.7352799489016,-3.68118797282308,
1.40303876742916));
#46838=CARTESIAN_POINT('Ctrl Pts',(-46.8015711261341,-3.21659318237439,
2.62200776140054));
#46839=CARTESIAN_POINT('Ctrl Pts',(-46.8678623033666,-2.08635160875129,
3.58727380700206));
#46840=CARTESIAN_POINT('Ctrl Pts',(-46.9341534805991,-0.809697391222998,
3.85539269190742));
#46841=CARTESIAN_POINT('Ctrl Pts',(-47.0004446578316,0.466956826305223,
4.12351157681276));
#46842=CARTESIAN_POINT('Ctrl Pts',(-47.0667358350641,1.89002368773869,3.69448330102175));
#46843=CARTESIAN_POINT('Ctrl Pts',(-47.1330270122966,2.80574481596238,2.7654038948889));
#46844=CARTESIAN_POINT('Ctrl Pts',(-47.1993181895291,3.72146594418606,1.83632448875605));
#46845=CARTESIAN_POINT('Ctrl Pts',(-47.2656093667615,4.12984133920024,0.407193952281507));
#46846=CARTESIAN_POINT('Ctrl Pts',(-47.331900543994,3.84326292528247,-0.865443678881344));
#46847=CARTESIAN_POINT('Ctrl Pts',(-47.3981917212265,3.5566845113647,-2.1380813100442));
#46848=CARTESIAN_POINT('Ctrl Pts',(-47.464482898459,2.57515228851486,-3.25422603589525));
#46849=CARTESIAN_POINT('Ctrl Pts',(-47.5307740756915,1.34958316758683,-3.70111982350379));
#46850=CARTESIAN_POINT('Ctrl Pts',(-47.597065252924,0.124014046658786,-4.14801361111233));
#46851=CARTESIAN_POINT('Ctrl Pts',(-47.6633564301564,-1.34559197234754,
-3.9256564604784));
#46852=CARTESIAN_POINT('Ctrl Pts',(-47.7296476073889,-2.3840963755497,-3.13619947488313));
#46853=CARTESIAN_POINT('Ctrl Pts',(-47.7907105642476,-3.34069651779697,
-2.40900499945294));
#46854=CARTESIAN_POINT('Ctrl Pts',(-47.8517735211064,-3.93151338139049,
-1.20063478876308));
#46855=CARTESIAN_POINT('Ctrl Pts',(-47.9128364779652,-3.93845732485478,
0.00183569955874766));
#46856=CARTESIAN_POINT('Ctrl Pts',(-48.0961635220348,-3.93803051256068,
0.00216112547147041));
#46857=CARTESIAN_POINT('Ctrl Pts',(-48.036177405953,-3.93023114179386,-1.17944191749285));
#46858=CARTESIAN_POINT('Ctrl Pts',(-47.9761912898711,-3.36271357529152,
-2.36753854712791));
#46859=CARTESIAN_POINT('Ctrl Pts',(-47.9162051737893,-2.43470660670667,
-3.09707384694413));
#46860=CARTESIAN_POINT('Ctrl Pts',(-47.8499139965569,-1.40915805571296,
-3.90328963513612));
#46861=CARTESIAN_POINT('Ctrl Pts',(-47.7836228193244,0.0566436507002789,
-4.14948043718453));
#46862=CARTESIAN_POINT('Ctrl Pts',(-47.7173316420919,1.28930770376171,-3.72254594587994));
#46863=CARTESIAN_POINT('Ctrl Pts',(-47.6510404648594,2.52197175682313,-3.29561145457534));
#46864=CARTESIAN_POINT('Ctrl Pts',(-47.5847492876269,3.52149815653267,-2.19555166991778));
#46865=CARTESIAN_POINT('Ctrl Pts',(-47.5184581103945,3.8287034487138,-0.927735186340111));
#46866=CARTESIAN_POINT('Ctrl Pts',(-47.452166933162,4.13590874089496,0.340081297237703));
#46867=CARTESIAN_POINT('Ctrl Pts',(-47.3858757559295,3.75079292554741,1.77565447973578));
#46868=CARTESIAN_POINT('Ctrl Pts',(-47.319584578697,2.85027860361577,2.71948056730262));
#46869=CARTESIAN_POINT('Ctrl Pts',(-47.2532934014645,1.94976428168418,3.66330665486941));
#46870=CARTESIAN_POINT('Ctrl Pts',(-47.187002224232,0.533851453168638,4.11538564750519));
#46871=CARTESIAN_POINT('Ctrl Pts',(-47.1207110469995,-0.746988074883418,
3.8680319918724));
#46872=CARTESIAN_POINT('Ctrl Pts',(-47.054419869767,-2.0278276029354,3.62067833623963));
#46873=CARTESIAN_POINT('Ctrl Pts',(-46.9881286925346,-3.17359383052384,
2.6738920323384));
#46874=CARTESIAN_POINT('Ctrl Pts',(-46.9218375153021,-3.65792057640951,
1.46262768018602));
#46875=CARTESIAN_POINT('Ctrl Pts',(-46.8966128508797,-3.84221327033675,
1.00172567051489));
#46876=CARTESIAN_POINT('Ctrl Pts',(-46.8713881864572,-3.93073597335362,
0.50252981692053));
#46877=CARTESIAN_POINT('Ctrl Pts',(-46.8461635220347,-3.92797149977701,
0.00239191756703917));
#46878=CARTESIAN_POINT('Origin',(-54.75,0.,0.));
#46879=CARTESIAN_POINT('',(-45.4128364779651,-3.92877816963689,-0.00284985070313576));
#46880=CARTESIAN_POINT('',(-45.5961635220348,-3.92927121084188,-0.0030586176504822));
#46881=CARTESIAN_POINT('',(-54.75,-3.933,-4.81653586104654E-16));
#46882=CARTESIAN_POINT('Ctrl Pts',(-45.4128364779651,-3.92877816963689,
-0.00284985070313576));
#46883=CARTESIAN_POINT('Ctrl Pts',(-45.4559039048824,-3.92308252956803,
0.850622702455208));
#46884=CARTESIAN_POINT('Ctrl Pts',(-45.4989713317997,-3.65002117383353,
1.70741383593766));
#46885=CARTESIAN_POINT('Ctrl Pts',(-45.542038758717,-3.13750342344379,2.38238010024533));
#46886=CARTESIAN_POINT('Ctrl Pts',(-45.6083299359494,-2.3486147561188,3.42131628603418));
#46887=CARTESIAN_POINT('Ctrl Pts',(-45.6746211131819,-0.992390468762286,
4.02946119962105));
#46888=CARTESIAN_POINT('Ctrl Pts',(-45.7409122904143,0.308118608665171,
3.9274324433605));
#46889=CARTESIAN_POINT('Ctrl Pts',(-45.8072034676468,1.6086276860927,3.82540368709996));
#46890=CARTESIAN_POINT('Ctrl Pts',(-45.8734946448794,2.85342155359117,3.01320126099192));
#46891=CARTESIAN_POINT('Ctrl Pts',(-45.9397858221119,3.47064063048122,1.86395179342691));
#46892=CARTESIAN_POINT('Ctrl Pts',(-46.0060769993443,4.08785970737127,0.714702325861893));
#46893=CARTESIAN_POINT('Ctrl Pts',(-46.0723681765768,4.07750399365291,-0.771594183160101));
#46894=CARTESIAN_POINT('Ctrl Pts',(-46.1386593538093,3.4443309148399,-1.91213159150844));
#46895=CARTESIAN_POINT('Ctrl Pts',(-46.2049505310417,2.81115783602689,-3.05266899985677));
#46896=CARTESIAN_POINT('Ctrl Pts',(-46.2712417082743,1.55516739211924,-3.84744730753145));
#46897=CARTESIAN_POINT('Ctrl Pts',(-46.3375328855068,0.253362882493478,
-3.93134454403847));
#46898=CARTESIAN_POINT('Ctrl Pts',(-46.4038240627392,-1.04844162713228,
-4.01524178054549));
#46899=CARTESIAN_POINT('Ctrl Pts',(-46.4701152399717,-2.39606020247614,
-3.38825794588486));
#46900=CARTESIAN_POINT('Ctrl Pts',(-46.5364064172042,-3.17039548651101,
-2.33843005738403));
#46901=CARTESIAN_POINT('Ctrl Pts',(-46.5785497707911,-3.66266439818702,
-1.67102196844027));
#46902=CARTESIAN_POINT('Ctrl Pts',(-46.6206931243781,-3.92323866023133,
-0.832719826959837));
#46903=CARTESIAN_POINT('Ctrl Pts',(-46.6628364779651,-3.92838703301762,
0.00264903870899197));
#46904=CARTESIAN_POINT('Ctrl Pts',(-46.8461635220347,-3.92797149977701,
0.00239191756703917));
#46905=CARTESIAN_POINT('Ctrl Pts',(-46.8050970092247,-3.9234708535981,-0.811847634111943));
#46906=CARTESIAN_POINT('Ctrl Pts',(-46.7640304964146,-3.67701518999008,
-1.6285840611087));
#46907=CARTESIAN_POINT('Ctrl Pts',(-46.7229639836046,-3.20794814162277,
-2.28664194722862));
#46908=CARTESIAN_POINT('Ctrl Pts',(-46.6566728063721,-2.4507616967675,-3.34890482208725));
#46909=CARTESIAN_POINT('Ctrl Pts',(-46.5903816291397,-1.11350154287413,
-3.99768817140092));
#46910=CARTESIAN_POINT('Ctrl Pts',(-46.5240904519072,0.189493632478917,
-3.93494025843041));
#46911=CARTESIAN_POINT('Ctrl Pts',(-46.4577992746747,1.49248880783197,-3.8721923454599));
#46912=CARTESIAN_POINT('Ctrl Pts',(-46.3915080974422,2.7612190046447,-3.0979131702052));
#46913=CARTESIAN_POINT('Ctrl Pts',(-46.3252169202097,3.41282826797689,-1.96780738068143));
#46914=CARTESIAN_POINT('Ctrl Pts',(-46.2589257429772,4.06443753130908,-0.837701591157649));
#46915=CARTESIAN_POINT('Ctrl Pts',(-46.1926345657448,4.09892586116073,0.648230812635207));
#46916=CARTESIAN_POINT('Ctrl Pts',(-46.1263433885123,3.50044928339101,1.80735095888258));
#46917=CARTESIAN_POINT('Ctrl Pts',(-46.0600522112798,2.90197270562126,2.96647110513002));
#46918=CARTESIAN_POINT('Ctrl Pts',(-45.9937610340473,1.67053122023008,3.79877899383193));
#46919=CARTESIAN_POINT('Ctrl Pts',(-45.9274698568148,0.371850309848739,
3.92191152644114));
#46920=CARTESIAN_POINT('Ctrl Pts',(-45.8611786795823,-0.926830600532456,
4.04504405905032));
#46921=CARTESIAN_POINT('Ctrl Pts',(-45.7948875023499,-2.29275093590379,
3.45900123556699));
#46922=CARTESIAN_POINT('Ctrl Pts',(-45.7285963251174,-3.09840549189236,
2.43301173075218));
#46923=CARTESIAN_POINT('Ctrl Pts',(-45.6844520574232,-3.63490268312317,
1.74979026384193));
#46924=CARTESIAN_POINT('Ctrl Pts',(-45.640307789729,-3.92295429860531,0.87147780518392));
#46925=CARTESIAN_POINT('Ctrl Pts',(-45.5961635220348,-3.92927121084188,
-0.0030586176504822));
#46926=CARTESIAN_POINT('Origin',(-54.75,0.,0.));
#46927=CARTESIAN_POINT('',(-44.1628364779651,-3.93877450621935,-0.00153765925571148));
#46928=CARTESIAN_POINT('',(-44.3461635220348,-3.93907979130839,-0.00117182323445835));
#46929=CARTESIAN_POINT('',(-54.75,-3.933,-4.81653586104654E-16));
#46930=CARTESIAN_POINT('Ctrl Pts',(-44.1628364779651,-3.93877450621935,
-0.00153765925571148));
#46931=CARTESIAN_POINT('Ctrl Pts',(-44.2248235081541,-3.93270920820415,
1.21886943562029));
#46932=CARTESIAN_POINT('Ctrl Pts',(-44.2868105383432,-3.32143279835113,
2.44451926788589));
#46933=CARTESIAN_POINT('Ctrl Pts',(-44.3487975685322,-2.3401643356023,3.16911557954921));
#46934=CARTESIAN_POINT('Ctrl Pts',(-44.4150887457647,-1.29076026868109,
3.94402514324342));
#46935=CARTESIAN_POINT('Ctrl Pts',(-44.4813799229971,0.181801451039536,
4.14588285340311));
#46936=CARTESIAN_POINT('Ctrl Pts',(-44.5476711002296,1.40102445773471,3.68195507074647));
#46937=CARTESIAN_POINT('Ctrl Pts',(-44.6139622774621,2.62024746442988,3.21802728808982));
#46938=CARTESIAN_POINT('Ctrl Pts',(-44.6802534546946,3.58613175809952,2.08831401261689));
#46939=CARTESIAN_POINT('Ctrl Pts',(-44.7465446319271,3.85494910261997,0.811806682884503));
#46940=CARTESIAN_POINT('Ctrl Pts',(-44.8128358091596,4.12376644714041,-0.464700646847811));
#46941=CARTESIAN_POINT('Ctrl Pts',(-44.8791269863921,3.69551684251162,-1.88800203083967));
#46942=CARTESIAN_POINT('Ctrl Pts',(-44.9454181636245,2.76693859675673,-2.80423135207214));
#46943=CARTESIAN_POINT('Ctrl Pts',(-45.011709340857,1.83836035100179,-3.72046067330466));
#46944=CARTESIAN_POINT('Ctrl Pts',(-45.0780005180896,0.409453464120721,
-4.12961793177789));
#46945=CARTESIAN_POINT('Ctrl Pts',(-45.144291695322,-0.863340773085724,
-3.84373586289357));
#46946=CARTESIAN_POINT('Ctrl Pts',(-45.2105828725545,-2.13613501029217,
-3.55785379400925));
#46947=CARTESIAN_POINT('Ctrl Pts',(-45.276874049787,-3.25281659782392,-2.57693239776739));
#46948=CARTESIAN_POINT('Ctrl Pts',(-45.3431652270194,-3.70038086794309,
-1.35160797065096));
#46949=CARTESIAN_POINT('Ctrl Pts',(-45.3663889773347,-3.85717580345627,
-0.922340762879227));
#46950=CARTESIAN_POINT('Ctrl Pts',(-45.3896127276499,-3.93184949598054,
-0.463077797766648));
#46951=CARTESIAN_POINT('Ctrl Pts',(-45.4128364779651,-3.92877816963689,
-0.00284985070313576));
#46952=CARTESIAN_POINT('Ctrl Pts',(-45.5961635220348,-3.92927121084188,
-0.0030586176504822));
#46953=CARTESIAN_POINT('Ctrl Pts',(-45.5740166124965,-3.93244036713718,
-0.441808200690738));
#46954=CARTESIAN_POINT('Ctrl Pts',(-45.5518697029582,-3.86469781064446,
-0.879607367737818));
#46955=CARTESIAN_POINT('Ctrl Pts',(-45.5297227934199,-3.72183996581203,
-1.29134423878791));
#46956=CARTESIAN_POINT('Ctrl Pts',(-45.4634316161874,-3.2942311071373,-2.523774517367));
#46957=CARTESIAN_POINT('Ctrl Pts',(-45.3971404389549,-2.19362461318191,
-3.52269888837872));
#46958=CARTESIAN_POINT('Ctrl Pts',(-45.3308492617225,-0.925640237191606,
-3.82921047024818));
#46959=CARTESIAN_POINT('Ctrl Pts',(-45.26455808449,0.34234413879855,-4.13572205211761));
#46960=CARTESIAN_POINT('Ctrl Pts',(-45.1982669072575,1.77770639682364,-3.74982084484499));
#46961=CARTESIAN_POINT('Ctrl Pts',(-45.131975730025,2.72103964195195,-2.84879025923153));
#46962=CARTESIAN_POINT('Ctrl Pts',(-45.0656845527925,3.66437288708031,-1.94775967361802));
#46963=CARTESIAN_POINT('Ctrl Pts',(-44.99939337556,4.11567711931186,-0.53159970966378));
#46964=CARTESIAN_POINT('Ctrl Pts',(-44.9331021983276,3.86762271103424,0.749104291309692));
#46965=CARTESIAN_POINT('Ctrl Pts',(-44.8668110210951,3.61956830275662,2.02980829228316));
#46966=CARTESIAN_POINT('Ctrl Pts',(-44.8005198438626,2.67215525396966,3.17505633027576));
#46967=CARTESIAN_POINT('Ctrl Pts',(-44.7342286666301,1.46062609193479,3.65872028088043));
#46968=CARTESIAN_POINT('Ctrl Pts',(-44.6679374893976,0.24909692989985,4.14238423148512));
#46969=CARTESIAN_POINT('Ctrl Pts',(-44.6016463121651,-1.22654834538313,
3.96446409470183));
#46970=CARTESIAN_POINT('Ctrl Pts',(-44.5353551349326,-2.28839677949802,
3.20669656402809));
#46971=CARTESIAN_POINT('Ctrl Pts',(-44.4722912639667,-3.29855039918072,
2.48582003457673));
#46972=CARTESIAN_POINT('Ctrl Pts',(-44.4092273930007,-3.93421683623724,
1.24018015439934));
#46973=CARTESIAN_POINT('Ctrl Pts',(-44.3461635220348,-3.93907979130839,
-0.00117182323445835));
#46974=CARTESIAN_POINT('Origin',(-54.75,0.,0.));
#46975=CARTESIAN_POINT('',(-42.9128364779651,-3.93348651618965,0.00360571708670418));
#46976=CARTESIAN_POINT('',(-43.0961635220348,-3.93283616785734,0.00363483404017096));
#46977=CARTESIAN_POINT('',(-54.75,-3.933,-4.81653586104654E-16));
#46978=CARTESIAN_POINT('Ctrl Pts',(-42.9128364779651,-3.93348651618965,
0.00360571708670418));
#46979=CARTESIAN_POINT('Ctrl Pts',(-42.9274519341934,-3.93617042421601,
0.292363665661577));
#46980=CARTESIAN_POINT('Ctrl Pts',(-42.9420673904217,-3.90708356166905,
0.580585604486907));
#46981=CARTESIAN_POINT('Ctrl Pts',(-42.95668284665,-3.84420764986457,0.861237608845054));
#46982=CARTESIAN_POINT('Ctrl Pts',(-43.0229740238825,-3.55902201159384,
2.13418807107819));
#46983=CARTESIAN_POINT('Ctrl Pts',(-43.089265201115,-2.57871173560324,3.25140618600691));
#46984=CARTESIAN_POINT('Ctrl Pts',(-43.1555563783475,-1.35363236910501,
3.69964080465626));
#46985=CARTESIAN_POINT('Ctrl Pts',(-43.2218475555799,-0.128553002606771,
4.14787542330561));
#46986=CARTESIAN_POINT('Ctrl Pts',(-43.2881387328124,1.34129545439917,3.9271265456756));
#46987=CARTESIAN_POINT('Ctrl Pts',(-43.3544299100449,2.38066311176446,3.13880643277829));
#46988=CARTESIAN_POINT('Ctrl Pts',(-43.4207210872774,3.42003076912981,2.35048631988094));
#46989=CARTESIAN_POINT('Ctrl Pts',(-43.4870122645099,4.02891762685445,0.994594971716387));
#46990=CARTESIAN_POINT('Ctrl Pts',(-43.5533034417424,3.92760043739446,-0.305969734361532));
#46991=CARTESIAN_POINT('Ctrl Pts',(-43.6195946189749,3.82628324793448,-1.6065344404393));
#46992=CARTESIAN_POINT('Ctrl Pts',(-43.6858857962073,3.01476201128989,-2.85177250443036));
#46993=CARTESIAN_POINT('Ctrl Pts',(-43.7521769734398,1.86585041671237,-3.46962028133061));
#46994=CARTESIAN_POINT('Ctrl Pts',(-43.8184681506723,0.716938822134715,
-4.08746805823093));
#46995=CARTESIAN_POINT('Ctrl Pts',(-43.8847593279048,-0.769363130376017,
-4.07792554804035));
#46996=CARTESIAN_POINT('Ctrl Pts',(-43.9510505051373,-1.91024679794475,
-3.44537658973707));
#46997=CARTESIAN_POINT('Ctrl Pts',(-44.0173416823698,-3.05113046551329,
-2.81282763143391));
#46998=CARTESIAN_POINT('Ctrl Pts',(-44.0836328596022,-3.84659584814002,
-1.55727222501828));
#46999=CARTESIAN_POINT('Ctrl Pts',(-44.1499240368347,-3.93120533239265,
-0.255513813196189));
#47000=CARTESIAN_POINT('Ctrl Pts',(-44.1542281838782,-3.93669884867488,
-0.170993370907197));
#47001=CARTESIAN_POINT('Ctrl Pts',(-44.1585323309216,-3.93919565778025,
-0.0862781537303368));
#47002=CARTESIAN_POINT('Ctrl Pts',(-44.1628364779651,-3.93877450621935,
-0.00153765925571148));
#47003=CARTESIAN_POINT('Ctrl Pts',(-44.3461635220348,-3.93907979130839,
-0.00117182323445835));
#47004=CARTESIAN_POINT('Ctrl Pts',(-44.3429362157683,-3.93932865401114,
-0.0646982600836412));
#47005=CARTESIAN_POINT('Ctrl Pts',(-44.3397089095017,-3.93792550472575,
-0.128213467339758));
#47006=CARTESIAN_POINT('Ctrl Pts',(-44.3364816032352,-3.9348359912255,-0.191646540075454));
#47007=CARTESIAN_POINT('Ctrl Pts',(-44.2701904260027,-3.87137517589129,
-1.49460718894119));
#47008=CARTESIAN_POINT('Ctrl Pts',(-44.2038992487702,-3.09640195227602,
-2.76291356210852));
#47009=CARTESIAN_POINT('Ctrl Pts',(-44.1376080715377,-1.96593981492416,
-3.41390440965508));
#47010=CARTESIAN_POINT('Ctrl Pts',(-44.0713168943052,-0.835477677572302,
-4.06489525720164));
#47011=CARTESIAN_POINT('Ctrl Pts',(-44.0050257170728,0.650473373516086,
-4.09857057912738));
#47012=CARTESIAN_POINT('Ctrl Pts',(-43.9387345398403,1.8092658999398,-3.49945989796732));
#47013=CARTESIAN_POINT('Ctrl Pts',(-43.8724433626078,2.96805842636345,-2.9003492168073));
#47014=CARTESIAN_POINT('Ctrl Pts',(-43.8061521853753,3.79969242812238,-1.66845253256158));
#47015=CARTESIAN_POINT('Ctrl Pts',(-43.7398610081428,3.922114391023,-0.369704446682378));
#47016=CARTESIAN_POINT('Ctrl Pts',(-43.6735698309103,4.04453635392363,0.929043639196903));
#47017=CARTESIAN_POINT('Ctrl Pts',(-43.6072786536779,3.45774627796568,2.29464312670978));
#47018=CARTESIAN_POINT('Ctrl Pts',(-43.5409874764454,2.43131612646438,3.09973620931858));
#47019=CARTESIAN_POINT('Ctrl Pts',(-43.4746962992129,1.40488597496313,3.90482929192733));
#47020=CARTESIAN_POINT('Ctrl Pts',(-43.4084051219804,-0.0611842520814183,
4.14941596963223));
#47021=CARTESIAN_POINT('Ctrl Pts',(-43.3421139447479,-1.29338038724425,
3.72113287159413));
#47022=CARTESIAN_POINT('Ctrl Pts',(-43.2758227675154,-2.52557652240714,
3.292849773556));
#47023=CARTESIAN_POINT('Ctrl Pts',(-43.209531590283,-3.52389856568822,2.1916968997748));
#47024=CARTESIAN_POINT('Ctrl Pts',(-43.1432404130505,-3.82971634549056,
0.923545010949064));
#47025=CARTESIAN_POINT('Ctrl Pts',(-43.1275481160453,-3.90210883617312,
0.623350974306624));
#47026=CARTESIAN_POINT('Ctrl Pts',(-43.11185581904,-3.9356966539327,0.313799100465172));
#47027=CARTESIAN_POINT('Ctrl Pts',(-43.0961635220348,-3.93283616785734,
0.00363483404017096));
#47028=CARTESIAN_POINT('Origin',(-54.75,0.,0.));
#47029=CARTESIAN_POINT('',(-41.6628364779652,-3.92648186165433,-0.000127976707175181));
#47030=CARTESIAN_POINT('',(-41.8461635220348,-3.92653091726897,-0.000480548798261107));
#47031=CARTESIAN_POINT('',(-54.75,-3.933,-4.81653586104654E-16));
#47032=CARTESIAN_POINT('Ctrl Pts',(-41.6628364779652,-3.92648186165433,
-0.000127976707175181));
#47033=CARTESIAN_POINT('Ctrl Pts',(-41.6963715374652,-3.92628947513322,
0.665413412504115));
#47034=CARTESIAN_POINT('Ctrl Pts',(-41.7299065969653,-3.76609621217257,
1.33104174019653));
#47035=CARTESIAN_POINT('Ctrl Pts',(-41.7634416564653,-3.44642123324494,
1.90836143253966));
#47036=CARTESIAN_POINT('Ctrl Pts',(-41.8297328336978,-2.81449658480804,
3.04959101779987));
#47037=CARTESIAN_POINT('Ctrl Pts',(-41.8960240109302,-1.55937659174049,
3.84574323725253));
#47038=CARTESIAN_POINT('Ctrl Pts',(-41.9623151881627,-0.257664667409214,
3.93106494392236));
#47039=CARTESIAN_POINT('Ctrl Pts',(-42.0286063653952,1.04404725692214,4.0163866505922));
#47040=CARTESIAN_POINT('Ctrl Pts',(-42.0948975426277,2.39235111251722,3.39087784447915));
#47041=CARTESIAN_POINT('Ctrl Pts',(-42.1611887198602,3.167834723898,2.34189791328156));
#47042=CARTESIAN_POINT('Ctrl Pts',(-42.2274798970927,3.94331833527879,1.29291798208397));
#47043=CARTESIAN_POINT('Ctrl Pts',(-42.2937710743251,4.14598170244526,-0.179533074198152));
#47044=CARTESIAN_POINT('Ctrl Pts',(-42.3600622515576,3.68272106645958,-1.39900972863711));
#47045=CARTESIAN_POINT('Ctrl Pts',(-42.4263534287901,3.2194604304739,-2.61848638307606));
#47046=CARTESIAN_POINT('Ctrl Pts',(-42.4926446060227,2.09027579133607,-3.58498863567185));
#47047=CARTESIAN_POINT('Ctrl Pts',(-42.5589357832551,0.813915731527926,
-3.85450435933569));
#47048=CARTESIAN_POINT('Ctrl Pts',(-42.6252269604876,-0.462444328280213,
-4.12402008299952));
#47049=CARTESIAN_POINT('Ctrl Pts',(-42.6915181377201,-1.88597980875866,
-3.6965492777314));
#47050=CARTESIAN_POINT('Ctrl Pts',(-42.7578093149525,-2.80271704872243,
-2.76847247032855));
#47051=CARTESIAN_POINT('Ctrl Pts',(-42.8094850359567,-3.51733790513564,
-2.04501212202889));
#47052=CARTESIAN_POINT('Ctrl Pts',(-42.8611607569609,-3.92399704968205,
-1.01735284590414));
#47053=CARTESIAN_POINT('Ctrl Pts',(-42.9128364779651,-3.93348651618965,
0.00360571708670418));
#47054=CARTESIAN_POINT('Ctrl Pts',(-43.0961635220348,-3.93283616785734,
0.00363483404017096));
#47055=CARTESIAN_POINT('Ctrl Pts',(-43.0455646418076,-3.92361270030057,
-0.996471432262334));
#47056=CARTESIAN_POINT('Ctrl Pts',(-42.9949657615803,-3.53543558165237,
-2.00294475494378));
#47057=CARTESIAN_POINT('Ctrl Pts',(-42.944366881353,-2.8473010620486,-2.72259790204565));
#47058=CARTESIAN_POINT('Ctrl Pts',(-42.8780757041205,-1.94575448248074,
-3.6654380223444));
#47059=CARTESIAN_POINT('Ctrl Pts',(-42.811784526888,-0.529347807021448,
-4.11596735907168));
#47060=CARTESIAN_POINT('Ctrl Pts',(-42.7454933496556,0.751220283488789,
-3.86721227240521));
#47061=CARTESIAN_POINT('Ctrl Pts',(-42.6792021724231,2.03178837399903,-3.61845718573874));
#47062=CARTESIAN_POINT('Ctrl Pts',(-42.6129109951906,3.17651787956021,-2.67041767567851));
#47063=CARTESIAN_POINT('Ctrl Pts',(-42.5466198179581,3.65951889009668,-1.45862406643797));
#47064=CARTESIAN_POINT('Ctrl Pts',(-42.4803286407256,4.14251990063314,-0.246830457197423));
#47065=CARTESIAN_POINT('Ctrl Pts',(-42.4140374634931,3.9637924161449,1.22871725122344));
#47066=CARTESIAN_POINT('Ctrl Pts',(-42.3477462862606,3.20544402649396,2.29015092672527));
#47067=CARTESIAN_POINT('Ctrl Pts',(-42.2814551090281,2.44709563684303,3.35158460222709));
#47068=CARTESIAN_POINT('Ctrl Pts',(-42.2151639317957,1.1091263420294,3.99890424480987));
#47069=CARTESIAN_POINT('Ctrl Pts',(-42.1488727545632,-0.193799390301712,
3.93473054610924));
#47070=CARTESIAN_POINT('Ctrl Pts',(-42.0825815773307,-1.49672512263282,
3.87055684740861));
#47071=CARTESIAN_POINT('Ctrl Pts',(-42.0162904000982,-2.76460729248141,
3.09488980742457));
#47072=CARTESIAN_POINT('Ctrl Pts',(-41.9499992228657,-3.4149795293652,1.96407166065373));
#47073=CARTESIAN_POINT('Ctrl Pts',(-41.9153873225887,-3.75455139919333,
1.37364972878524));
#47074=CARTESIAN_POINT('Ctrl Pts',(-41.8807754223118,-3.92578480029153,
0.68641057942328));
#47075=CARTESIAN_POINT('Ctrl Pts',(-41.8461635220348,-3.92653091726897,
-0.000480548798261107));
#47076=CARTESIAN_POINT('Origin',(-54.75,0.,0.));
#47077=CARTESIAN_POINT('',(-40.4128364779651,-3.93395781977791,-0.00356119310522762));
#47078=CARTESIAN_POINT('',(-40.5961635220348,-3.93460565980472,-0.0034672176766425));
#47079=CARTESIAN_POINT('',(-54.75,-3.933,-4.81653586104654E-16));
#47080=CARTESIAN_POINT('Ctrl Pts',(-40.4128364779651,-3.93395781977791,
-0.00356119310522762));
#47081=CARTESIAN_POINT('Ctrl Pts',(-40.465291140737,-3.92433020604628,1.03246856934012));
#47082=CARTESIAN_POINT('Ctrl Pts',(-40.5177458035087,-3.50397405571284,
2.07540741768839));
#47083=CARTESIAN_POINT('Ctrl Pts',(-40.5702004662806,-2.77000551514533,
2.80120190636642));
#47084=CARTESIAN_POINT('Ctrl Pts',(-40.6364916435131,-1.84243042391868,
3.71844679063188));
#47085=CARTESIAN_POINT('Ctrl Pts',(-40.7027828207456,-0.413972119407498,
4.12916740833972));
#47086=CARTESIAN_POINT('Ctrl Pts',(-40.769073997978,0.859134186788709,3.84467828605429));
#47087=CARTESIAN_POINT('Ctrl Pts',(-40.8353651752105,2.13224049298506,3.56018916376883));
#47088=CARTESIAN_POINT('Ctrl Pts',(-40.901656352443,3.24999480086639,2.58049030148992));
#47089=CARTESIAN_POINT('Ctrl Pts',(-40.9679475296755,3.69889963386485,1.35565636234294));
#47090=CARTESIAN_POINT('Ctrl Pts',(-41.0342387069079,4.14780446686328,0.130822423196035));
#47091=CARTESIAN_POINT('Ctrl Pts',(-41.1005298841405,3.92785982497892,-1.33914659281891));
#47092=CARTESIAN_POINT('Ctrl Pts',(-41.1668210613729,3.14010850249658,-2.37894541062108));
#47093=CARTESIAN_POINT('Ctrl Pts',(-41.2331122386054,2.35235718001424,-3.41874422842326));
#47094=CARTESIAN_POINT('Ctrl Pts',(-41.2994034158379,0.996799176933934,
-4.02837284801268));
#47095=CARTESIAN_POINT('Ctrl Pts',(-41.3656945930704,-0.303820768464218,
-3.92776725568309));
#47096=CARTESIAN_POINT('Ctrl Pts',(-41.4319857703029,-1.60444071386237,
-3.8271616633535));
#47097=CARTESIAN_POINT('Ctrl Pts',(-41.4982769475354,-2.85012260157836,
-3.01632185910491));
#47098=CARTESIAN_POINT('Ctrl Pts',(-41.5645681247679,-3.46859889353324,
-1.86774848144669));
#47099=CARTESIAN_POINT('Ctrl Pts',(-41.5973242425003,-3.77420339596868,
-1.30020983824283));
#47100=CARTESIAN_POINT('Ctrl Pts',(-41.6300803602327,-3.92666977948211,
-0.650210380788743));
#47101=CARTESIAN_POINT('Ctrl Pts',(-41.6628364779652,-3.92648186165433,
-0.000127976707175181));
#47102=CARTESIAN_POINT('Ctrl Pts',(-41.8461635220348,-3.92653091726897,
-0.000480548798261107));
#47103=CARTESIAN_POINT('Ctrl Pts',(-41.8144842450793,-3.92721381668161,
-0.629172244864202));
#47104=CARTESIAN_POINT('Ctrl Pts',(-41.7828049681238,-3.7850758618333,-1.257572396157));
#47105=CARTESIAN_POINT('Ctrl Pts',(-41.7511256911683,-3.49846946496413,
-1.81118029938491));
#47106=CARTESIAN_POINT('Ctrl Pts',(-41.6848345139358,-2.89872485976027,
-2.96964485909509));
#47107=CARTESIAN_POINT('Ctrl Pts',(-41.6185433367033,-1.66637334543348,
-3.80060472495772));
#47108=CARTESIAN_POINT('Ctrl Pts',(-41.5522521594708,-0.367558472842394,
-3.92231608150187));
#47109=CARTESIAN_POINT('Ctrl Pts',(-41.4859609822384,0.931256399748549,
-4.04402743804601));
#47110=CARTESIAN_POINT('Ctrl Pts',(-41.4196698050059,2.29653463060386,-3.45649028527188));
#47111=CARTESIAN_POINT('Ctrl Pts',(-41.3533786277734,3.10106599882443,-2.42961979435086));
#47112=CARTESIAN_POINT('Ctrl Pts',(-41.2870874505409,3.90559736704504,-1.40274930342978));
#47113=CARTESIAN_POINT('Ctrl Pts',(-41.2207962733084,4.1493818726309,0.0634545256380817));
#47114=CARTESIAN_POINT('Ctrl Pts',(-41.1545050960759,3.7204246634379,1.29541614852119));
#47115=CARTESIAN_POINT('Ctrl Pts',(-41.0882139188435,3.29146745424492,2.52737777140422));
#47116=CARTESIAN_POINT('Ctrl Pts',(-41.021922741611,2.18976853027304,3.52509718810241));
#47117=CARTESIAN_POINT('Ctrl Pts',(-40.9556315643785,0.921449508239053,
3.83022107428964));
#47118=CARTESIAN_POINT('Ctrl Pts',(-40.889340387146,-0.346869513795076,
4.1353449604769));
#47119=CARTESIAN_POINT('Ctrl Pts',(-40.8230492099135,-1.78180863389144,
3.74787331615304));
#47120=CARTESIAN_POINT('Ctrl Pts',(-40.756758032681,-2.72415534711707,2.84581101251294));
#47121=CARTESIAN_POINT('Ctrl Pts',(-40.7032265291323,-3.48511990573802,
2.11737695198714));
#47122=CARTESIAN_POINT('Ctrl Pts',(-40.6496950255835,-3.92486997045577,
1.05338356108175));
#47123=CARTESIAN_POINT('Ctrl Pts',(-40.5961635220348,-3.93460565980472,
-0.0034672176766425));
#47124=CARTESIAN_POINT('Origin',(-54.75,0.,0.));
#47125=CARTESIAN_POINT('',(-39.1628364779651,-3.93851028872272,0.00178997264115022));
#47126=CARTESIAN_POINT('',(-39.3461635220348,-3.93809135854538,0.00211875562057622));
#47127=CARTESIAN_POINT('',(-54.75,-3.933,-4.81653586104654E-16));
#47128=CARTESIAN_POINT('Ctrl Pts',(-39.1628364779651,-3.93851028872272,
0.00178997264115022));
#47129=CARTESIAN_POINT('Ctrl Pts',(-39.1679195667762,-3.93907624687778,
0.101884155187649));
#47130=CARTESIAN_POINT('Ctrl Pts',(-39.1730026555873,-3.93559258861192,
0.201938296474208));
#47131=CARTESIAN_POINT('Ctrl Pts',(-39.1780857443984,-3.92793289817642,
0.301671711616751));
#47132=CARTESIAN_POINT('Ctrl Pts',(-39.2443769216309,-3.82803893309399,
1.60234650698859));
#47133=CARTESIAN_POINT('Ctrl Pts',(-39.3106680988634,-3.01788080397012,
2.84847184552886));
#47134=CARTESIAN_POINT('Ctrl Pts',(-39.3769592760959,-1.86964598706206,
3.46757646739465));
#47135=CARTESIAN_POINT('Ctrl Pts',(-39.4432504533283,-0.721411170153998,
4.08668108926045));
#47136=CARTESIAN_POINT('Ctrl Pts',(-39.5095416305608,0.764900334538259,
4.07876499445177));
#47137=CARTESIAN_POINT('Ctrl Pts',(-39.5758328077933,1.90647549585776,3.44746484505069));
#47138=CARTESIAN_POINT('Ctrl Pts',(-39.6421239850258,3.04805065717726,2.8161646956496));
#47139=CARTESIAN_POINT('Ctrl Pts',(-39.7084151622583,3.84488947512401,1.5614804916561));
#47140=CARTESIAN_POINT('Ctrl Pts',(-39.7747063394908,3.93092337866962,0.259815444489133));
#47141=CARTESIAN_POINT('Ctrl Pts',(-39.8409975167232,4.01695728221523,-1.04184960267776));
#47142=CARTESIAN_POINT('Ctrl Pts',(-39.9072886939557,3.39218627135978,-2.39049549301812));
#47143=CARTESIAN_POINT('Ctrl Pts',(-39.9735798711882,2.34363078990284,-3.16655291994083));
#47144=CARTESIAN_POINT('Ctrl Pts',(-40.0398710484207,1.29507530844585,-3.94261034686359));
#47145=CARTESIAN_POINT('Ctrl Pts',(-40.1061622256532,-0.177264643612693,
-4.14607931036863));
#47146=CARTESIAN_POINT('Ctrl Pts',(-40.1724534028857,-1.39699458073947,
-3.68348595973311));
#47147=CARTESIAN_POINT('Ctrl Pts',(-40.2387445801181,-2.61672451786624,
-3.2208926090976));
#47148=CARTESIAN_POINT('Ctrl Pts',(-40.3050357573506,-3.58384444006126,
-2.09223694432154));
#47149=CARTESIAN_POINT('Ctrl Pts',(-40.3713269345831,-3.8540584621877,-0.816024536521914));
#47150=CARTESIAN_POINT('Ctrl Pts',(-40.3851634490438,-3.91045842943398,
-0.549649248397481));
#47151=CARTESIAN_POINT('Ctrl Pts',(-40.3989999635045,-3.93649739604398,
-0.276845588281384));
#47152=CARTESIAN_POINT('Ctrl Pts',(-40.4128364779651,-3.93395781977791,
-0.00356119310522762));
#47153=CARTESIAN_POINT('Ctrl Pts',(-40.5961635220348,-3.93460565980472,
-0.0034672176766425));
#47154=CARTESIAN_POINT('Ctrl Pts',(-40.5834038483511,-3.93692624134911,
-0.255376283841459));
#47155=CARTESIAN_POINT('Ctrl Pts',(-40.5706441746673,-3.91481571134161,
-0.506879545074775));
#47156=CARTESIAN_POINT('Ctrl Pts',(-40.5578845009836,-3.86680067610839,
-0.753336050786185));
#47157=CARTESIAN_POINT('Ctrl Pts',(-40.4915933237511,-3.6173449855192,-2.03376784748931));
#47158=CARTESIAN_POINT('Ctrl Pts',(-40.4253021465186,-2.66867929798575,
-3.17797847793916));
#47159=CARTESIAN_POINT('Ctrl Pts',(-40.3590109692861,-1.4566216042955,-3.66031640381895));
#47160=CARTESIAN_POINT('Ctrl Pts',(-40.2927197920536,-0.244563910605384,
-4.14265432969868));
#47161=CARTESIAN_POINT('Ctrl Pts',(-40.2264286148211,1.23088578924157,-3.96311955100839));
#47162=CARTESIAN_POINT('Ctrl Pts',(-40.1601374375887,2.29190438838525,-3.20419052939536));
#47163=CARTESIAN_POINT('Ctrl Pts',(-40.0938462603562,3.35292298752899,-2.44526150778228));
#47164=CARTESIAN_POINT('Ctrl Pts',(-40.0275550831237,3.99951048596956,-1.10693824324645));
#47165=CARTESIAN_POINT('Ctrl Pts',(-39.9612639058912,3.9346239231132,0.195952182513227));
#47166=CARTESIAN_POINT('Ctrl Pts',(-39.8949727286587,3.86973736025686,1.49884260827283));
#47167=CARTESIAN_POINT('Ctrl Pts',(-39.8286815514262,3.09337673610367,2.76630019525617));
#47168=CARTESIAN_POINT('Ctrl Pts',(-39.7623903741937,1.96220291842955,3.4160536267853));
#47169=CARTESIAN_POINT('Ctrl Pts',(-39.6960991969613,0.831029100755363,
4.06580705831447));
#47170=CARTESIAN_POINT('Ctrl Pts',(-39.6298080197288,-0.654957910439967,
4.09785633438925));
#47171=CARTESIAN_POINT('Ctrl Pts',(-39.5635168424963,-1.81309415664482,
3.49747798467794));
#47172=CARTESIAN_POINT('Ctrl Pts',(-39.4972256652638,-2.97123040284968,
2.89709963496662));
#47173=CARTESIAN_POINT('Ctrl Pts',(-39.4309344880313,-3.80151588406417,
1.66429365946932));
#47174=CARTESIAN_POINT('Ctrl Pts',(-39.3646433107988,-3.92251659781723,
0.365412388972747));
#47175=CARTESIAN_POINT('Ctrl Pts',(-39.3584833812108,-3.9337602641381,0.244717335671718));
#47176=CARTESIAN_POINT('Ctrl Pts',(-39.3523234516228,-3.93887957109934,
0.123451751506461));
#47177=CARTESIAN_POINT('Ctrl Pts',(-39.3461635220348,-3.93809135854538,
0.00211875562057622));
#47178=CARTESIAN_POINT('Origin',(-54.75,0.,0.));
#47179=CARTESIAN_POINT('',(-37.9128364779651,-3.92844641092988,0.00268183597320199));
#47180=CARTESIAN_POINT('',(-38.0961635220348,-3.9280248704326,0.00242793667101629));
#47181=CARTESIAN_POINT('',(-54.75,-3.933,-4.81653586104654E-16));
#47182=CARTESIAN_POINT('Ctrl Pts',(-37.9128364779651,-3.92844641092988,
0.00268183597320199));
#47183=CARTESIAN_POINT('Ctrl Pts',(-37.936839170048,-3.93141775465169,0.478447039929781));
#47184=CARTESIAN_POINT('Ctrl Pts',(-37.9608418621308,-3.85150376888296,
0.953247942279258));
#47185=CARTESIAN_POINT('Ctrl Pts',(-37.9848445542137,-3.6842497503381,1.39497901464505));
#47186=CARTESIAN_POINT('Ctrl Pts',(-38.0511357314461,-3.22232382353224,
2.61496186932779));
#47187=CARTESIAN_POINT('Ctrl Pts',(-38.1174269086786,-2.09419747098634,
3.58269917161015));
#47188=CARTESIAN_POINT('Ctrl Pts',(-38.1837180859111,-0.818133097235401,
3.85361141130945));
#47189=CARTESIAN_POINT('Ctrl Pts',(-38.2500092631436,0.457931276515689,
4.12452365100879));
#47190=CARTESIAN_POINT('Ctrl Pts',(-38.3163004403761,1.88193367147187,3.69861082812487));
#47191=CARTESIAN_POINT('Ctrl Pts',(-38.3825916176086,2.79968592545767,2.77153773074816));
#47192=CARTESIAN_POINT('Ctrl Pts',(-38.4488827948411,3.71743817944343,1.8444646333715));
#47193=CARTESIAN_POINT('Ctrl Pts',(-38.5151739720736,4.12894029245886,0.416231261502113));
#47194=CARTESIAN_POINT('Ctrl Pts',(-38.581465149306,3.84514777132169,-0.857030507547004));
#47195=CARTESIAN_POINT('Ctrl Pts',(-38.6477563265385,3.56135525018452,-2.13029227659612));
#47196=CARTESIAN_POINT('Ctrl Pts',(-38.714047503771,2.58226809489474,-3.24858244282497));
#47197=CARTESIAN_POINT('Ctrl Pts',(-38.7803386810035,1.35767994975888,-3.69815735579074));
#47198=CARTESIAN_POINT('Ctrl Pts',(-38.846629858236,0.133091804623014,-4.14773226875652));
#47199=CARTESIAN_POINT('Ctrl Pts',(-38.9129210354685,-1.33699733035893,
-3.92859192845923));
#47200=CARTESIAN_POINT('Ctrl Pts',(-38.979212212701,-2.3772269973294,-3.14140963220887));
#47201=CARTESIAN_POINT('Ctrl Pts',(-39.0404203011223,-3.33769371541464,
-2.41458706540369));
#47202=CARTESIAN_POINT('Ctrl Pts',(-39.1016283895437,-3.93169529530333,
-1.20349559357064));
#47203=CARTESIAN_POINT('Ctrl Pts',(-39.1628364779651,-3.93851028872272,
0.00178997264115022));
#47204=CARTESIAN_POINT('Ctrl Pts',(-39.3461635220348,-3.93809135854538,
0.00211875562057622));
#47205=CARTESIAN_POINT('Ctrl Pts',(-39.2860322743903,-3.93039708158953,
-1.18229485151587));
#47206=CARTESIAN_POINT('Ctrl Pts',(-39.2259010267458,-3.35977318684557,
-2.37313214528199));
#47207=CARTESIAN_POINT('Ctrl Pts',(-39.1657697791014,-2.42792273491924,
-3.10239486001197));
#47208=CARTESIAN_POINT('Ctrl Pts',(-39.0994786018689,-1.4006122119768,-3.90636427300412));
#47209=CARTESIAN_POINT('Ctrl Pts',(-39.0331874246364,0.0657247801994387,
-4.14934653349288));
#47210=CARTESIAN_POINT('Ctrl Pts',(-38.9668962474039,1.29745152200931,-3.71971534155534));
#47211=CARTESIAN_POINT('Ctrl Pts',(-38.9006050701714,2.52917826381926,-3.29008414961777));
#47212=CARTESIAN_POINT('Ctrl Pts',(-38.834313892939,3.52629475526267,-2.18783950525372));
#47213=CARTESIAN_POINT('Ctrl Pts',(-38.7680227157065,3.83072465649444,-0.91935372968844));
#47214=CARTESIAN_POINT('Ctrl Pts',(-38.701731538474,4.1351545577262,0.349132045876837));
#47215=CARTESIAN_POINT('Ctrl Pts',(-38.6354403612415,3.74689786874632,1.78385895264344));
#47216=CARTESIAN_POINT('Ctrl Pts',(-38.569149184009,2.84432011107059,2.7257119767));
#47217=CARTESIAN_POINT('Ctrl Pts',(-38.5028580067765,1.94174235339486,3.66756500075656));
#47218=CARTESIAN_POINT('Ctrl Pts',(-38.4365668295441,0.524843527023436,
4.1165441421031));
#47219=CARTESIAN_POINT('Ctrl Pts',(-38.3702756523116,-0.755451592569169,
3.86638792226687));
#47220=CARTESIAN_POINT('Ctrl Pts',(-38.3039844750791,-2.03574671216185,
3.61623170243063));
#47221=CARTESIAN_POINT('Ctrl Pts',(-38.2376932978466,-3.17943812497561,
2.66694012141135));
#47222=CARTESIAN_POINT('Ctrl Pts',(-38.1714021206141,-3.66111282180858,
1.45461870610661));
#47223=CARTESIAN_POINT('Ctrl Pts',(-38.1463225877544,-3.84334184369755,
0.99596861055748));
#47224=CARTESIAN_POINT('Ctrl Pts',(-38.1212430548946,-3.93081712177783,
0.499671336424599));
#47225=CARTESIAN_POINT('Ctrl Pts',(-38.0961635220348,-3.9280248704326,0.00242793667101629));
#47226=CARTESIAN_POINT('Origin',(-54.75,0.,0.));
#47227=CARTESIAN_POINT('',(-36.6628364779652,-3.92871471926708,-0.00281959343416821));
#47228=CARTESIAN_POINT('',(-36.8461635220348,-3.92920254662071,-0.00303214147515514));
#47229=CARTESIAN_POINT('',(-54.75,-3.933,-4.81653586104654E-16));
#47230=CARTESIAN_POINT('Ctrl Pts',(-36.6628364779652,-3.92871471926708,
-0.00281959343416821));
#47231=CARTESIAN_POINT('Ctrl Pts',(-36.7057587733198,-3.92310430500018,
0.847811380770198));
#47232=CARTESIAN_POINT('Ctrl Pts',(-36.7486810686744,-3.65202702481909,
1.70169988563318));
#47233=CARTESIAN_POINT('Ctrl Pts',(-36.791603364029,-3.14270982152566,2.37550787240382));
#47234=CARTESIAN_POINT('Ctrl Pts',(-36.8578945412614,-2.35609678715395,
3.41616807714502));
#47235=CARTESIAN_POINT('Ctrl Pts',(-36.9241857184939,-1.00120669152006,
4.02727967275646));
#47236=CARTESIAN_POINT('Ctrl Pts',(-36.9904768957264,0.299522564462462,
3.92809736482489));
#47237=CARTESIAN_POINT('Ctrl Pts',(-37.0567680729589,1.60025182044498,3.82891505689333));
#47238=CARTESIAN_POINT('Ctrl Pts',(-37.1230592501914,2.84682023677614,3.01943884541876));
#47239=CARTESIAN_POINT('Ctrl Pts',(-37.1893504274239,3.46655300322102,1.87154293299026));
#47240=CARTESIAN_POINT('Ctrl Pts',(-37.2556416046563,4.0862857696659,0.72364702056176));
#47241=CARTESIAN_POINT('Ctrl Pts',(-37.3219327818888,4.0791828862245,-0.762668592820669));
#47242=CARTESIAN_POINT('Ctrl Pts',(-37.3882239591213,3.44850742484189,-1.9045889884636));
#47243=CARTESIAN_POINT('Ctrl Pts',(-37.4545151363538,2.81783196345931,-3.04650938410646));
#47244=CARTESIAN_POINT('Ctrl Pts',(-37.5208063135863,1.56358392413559,-3.84403456200987));
#47245=CARTESIAN_POINT('Ctrl Pts',(-37.5870974908188,0.261966143792537,
-3.93078063667676));
#47246=CARTESIAN_POINT('Ctrl Pts',(-37.6533886680512,-1.03965163655066,
-4.01752671134365));
#47247=CARTESIAN_POINT('Ctrl Pts',(-37.7196798452837,-2.3886391579132,-3.39349368277382));
#47248=CARTESIAN_POINT('Ctrl Pts',(-37.7859710225162,-3.16527016806154,
-2.34536296494725));
#47249=CARTESIAN_POINT('Ctrl Pts',(-37.8282595076659,-3.66069882554678,
-1.67673914280205));
#47250=CARTESIAN_POINT('Ctrl Pts',(-37.8705479928155,-3.92321143043598,
-0.835532048235915));
#47251=CARTESIAN_POINT('Ctrl Pts',(-37.9128364779651,-3.92844641092988,
0.00268183597320199));
#47252=CARTESIAN_POINT('Ctrl Pts',(-38.0961635220348,-3.9280248704326,0.00242793667101629));
#47253=CARTESIAN_POINT('Ctrl Pts',(-38.0549518776621,-3.92343653658755,
-0.814661371646528));
#47254=CARTESIAN_POINT('Ctrl Pts',(-38.0137402332894,-3.67510497528553,
-1.63430543817939));
#47255=CARTESIAN_POINT('Ctrl Pts',(-37.9725285889167,-3.2029360731075,-2.29365716395305));
#47256=CARTESIAN_POINT('Ctrl Pts',(-37.9062374116842,-2.44342664672121,
-3.35426036911786));
#47257=CARTESIAN_POINT('Ctrl Pts',(-37.8399462344517,-1.10474981309637,
-4.00011552985729));
#47258=CARTESIAN_POINT('Ctrl Pts',(-37.7736550572192,0.198104916065548,
-3.93451612226931));
#47259=CARTESIAN_POINT('Ctrl Pts',(-37.7073638799867,1.50095964522754,-3.86891671468132));
#47260=CARTESIAN_POINT('Ctrl Pts',(-37.6410727027542,2.76799226992662,-3.09186273876585));
#47261=CARTESIAN_POINT('Ctrl Pts',(-37.5747815255217,3.41712670159429,-1.96033358881028));
#47262=CARTESIAN_POINT('Ctrl Pts',(-37.5084903482892,4.06626113326188,-0.828804438854842));
#47263=CARTESIAN_POINT('Ctrl Pts',(-37.4421991710568,4.09749737189823,0.65719988514059));
#47264=CARTESIAN_POINT('Ctrl Pts',(-37.3759079938243,3.49648545740553,1.81500747114662));
#47265=CARTESIAN_POINT('Ctrl Pts',(-37.3096168165918,2.8954735429128,2.97281505715271));
#47266=CARTESIAN_POINT('Ctrl Pts',(-37.2433256393593,1.66221347529096,3.80242590516937));
#47267=CARTESIAN_POINT('Ctrl Pts',(-37.1770344621268,0.363266195714995,
3.92271593990913));
#47268=CARTESIAN_POINT('Ctrl Pts',(-37.1107432848943,-0.935681083860891,
4.04300597464889));
#47269=CARTESIAN_POINT('Ctrl Pts',(-37.0444521076619,-2.30031557539088,
3.45397519611184));
#47270=CARTESIAN_POINT('Ctrl Pts',(-36.9781609304294,-3.10372279248287,
2.42622494867826));
#47271=CARTESIAN_POINT('Ctrl Pts',(-36.9341617942979,-3.63696454484935,
1.74408103550773));
#47272=CARTESIAN_POINT('Ctrl Pts',(-36.8901626581663,-3.92296807898683,
0.868667435112945));
#47273=CARTESIAN_POINT('Ctrl Pts',(-36.8461635220348,-3.92920254662071,
-0.00303214147515514));
#47274=CARTESIAN_POINT('Origin',(-54.75,0.,0.));
#47275=CARTESIAN_POINT('',(-35.4128364779651,-3.93872791654916,-0.00158551424731923));
#47276=CARTESIAN_POINT('',(-35.5961635220348,-3.93904295656044,-0.00122215278806678));
#47277=CARTESIAN_POINT('',(-54.75,-3.933,-4.81653586104654E-16));
#47278=CARTESIAN_POINT('Ctrl Pts',(-35.4128364779651,-3.93872791654916,
-0.00158551424731923));
#47279=CARTESIAN_POINT('Ctrl Pts',(-35.4746783765915,-3.93251546723464,
1.21600245087171));
#47280=CARTESIAN_POINT('Ctrl Pts',(-35.5365202752179,-3.32448100290972,
2.43894589304352));
#47281=CARTESIAN_POINT('Ctrl Pts',(-35.5983621738442,-2.34709443789658,
3.16398646864385));
#47282=CARTESIAN_POINT('Ctrl Pts',(-35.6646533510767,-1.29938879746337,
3.94119082952965));
#47283=CARTESIAN_POINT('Ctrl Pts',(-35.7309445283092,0.172727623926127,
4.14627080274248));
#47284=CARTESIAN_POINT('Ctrl Pts',(-35.7972357055417,1.39296303095743,3.68501243804582));
#47285=CARTESIAN_POINT('Ctrl Pts',(-35.8635268827742,2.61319843798872,3.22375407334915));
#47286=CARTESIAN_POINT('Ctrl Pts',(-35.9298180600067,3.58155283066183,2.09615737074299));
#47287=CARTESIAN_POINT('Ctrl Pts',(-35.9961092372392,3.85316320683496,0.820241413036307));
#47288=CARTESIAN_POINT('Ctrl Pts',(-36.0624004144716,4.12477358300807,-0.455674544670307));
#47289=CARTESIAN_POINT('Ctrl Pts',(-36.1286915917041,3.69963994268129,-1.87990975747744));
#47290=CARTESIAN_POINT('Ctrl Pts',(-36.1949827689366,2.77306911667835,-2.79816910645));
#47291=CARTESIAN_POINT('Ctrl Pts',(-36.2612739461691,1.84649829067536,-3.71642845542261));
#47292=CARTESIAN_POINT('Ctrl Pts',(-36.3275651234016,0.418490278996138,
-4.1287119405606));
#47293=CARTESIAN_POINT('Ctrl Pts',(-36.393856300634,-0.854926571749036,
-3.84561610552638));
#47294=CARTESIAN_POINT('Ctrl Pts',(-36.4601474778665,-2.12834342249421,
-3.56252027049216));
#47295=CARTESIAN_POINT('Ctrl Pts',(-36.526438655099,-3.24716911230534,-2.58404511528574));
#47296=CARTESIAN_POINT('Ctrl Pts',(-36.5927298323315,-3.69741397065613,
-1.35970313074704));
#47297=CARTESIAN_POINT('Ctrl Pts',(-36.6160987142094,-3.85613371814269,
-0.928099644290867));
#47298=CARTESIAN_POINT('Ctrl Pts',(-36.6394675960873,-3.93176928816201,
-0.465942420245586));
#47299=CARTESIAN_POINT('Ctrl Pts',(-36.6628364779652,-3.92871471926708,
-0.00281959343416821));
#47300=CARTESIAN_POINT('Ctrl Pts',(-36.8461635220348,-3.92920254662071,
-0.00303214147515514));
#47301=CARTESIAN_POINT('Ctrl Pts',(-36.8238714809338,-3.93236122247111,
-0.444676330372303));
#47302=CARTESIAN_POINT('Ctrl Pts',(-36.8015794398329,-3.86370557634453,
-0.885367161184453));
#47303=CARTESIAN_POINT('Ctrl Pts',(-36.7792873987319,-3.7190049061588,-1.29948650709933));
#47304=CARTESIAN_POINT('Ctrl Pts',(-36.7129962214994,-3.28869986008875,
-2.53097799911303));
#47305=CARTESIAN_POINT('Ctrl Pts',(-36.646705044267,-2.18590982529467,-3.52749126681019));
#47306=CARTESIAN_POINT('Ctrl Pts',(-36.5804138670345,-0.917257675925253,
-3.83122709195405));
#47307=CARTESIAN_POINT('Ctrl Pts',(-36.514122689802,0.35139447344417,-4.13496291709791));
#47308=CARTESIAN_POINT('Ctrl Pts',(-36.4478315125695,1.78590873738895,-3.74592129968847));
#47309=CARTESIAN_POINT('Ctrl Pts',(-36.381540335337,2.72726779032845,-2.84282835816787));
#47310=CARTESIAN_POINT('Ctrl Pts',(-36.3152491581045,3.668626843268,-1.93973541664722));
#47311=CARTESIAN_POINT('Ctrl Pts',(-36.2489579808721,4.11683068520223,-0.522591151015356));
#47312=CARTESIAN_POINT('Ctrl Pts',(-36.1826668036396,3.86597401100417,0.757566908204662));
#47313=CARTESIAN_POINT('Ctrl Pts',(-36.1163756264071,3.61511733680615,2.03772496742454));
#47314=CARTESIAN_POINT('Ctrl Pts',(-36.0500844491746,2.66520014647603,3.1808968202326));
#47315=CARTESIAN_POINT('Ctrl Pts',(-35.9837932719421,1.4526153724709,3.66190814382716));
#47316=CARTESIAN_POINT('Ctrl Pts',(-35.9175020947096,0.240030598465757,
4.14291946742173));
#47317=CARTESIAN_POINT('Ctrl Pts',(-35.8512109174772,-1.23522175921441,
3.96177026180279));
#47318=CARTESIAN_POINT('Ctrl Pts',(-35.7849197402447,-2.2954092529038,3.20168065800605));
#47319=CARTESIAN_POINT('Ctrl Pts',(-35.7220010008414,-3.3016617199574,2.48025917024576));
#47320=CARTESIAN_POINT('Ctrl Pts',(-35.6590822614381,-3.93400637947865,
1.23730393257168));
#47321=CARTESIAN_POINT('Ctrl Pts',(-35.5961635220348,-3.93904295656044,
-0.00122215278806678));
#47322=CARTESIAN_POINT('Origin',(-54.75,0.,0.));
#47323=CARTESIAN_POINT('',(-34.1628364779651,-3.93357436621185,0.00359891632991313));
#47324=CARTESIAN_POINT('',(-34.3461635220348,-3.93292354923884,0.0036330978440403));
#47325=CARTESIAN_POINT('',(-54.75,-3.933,-4.81653586104654E-16));
#47326=CARTESIAN_POINT('Ctrl Pts',(-34.1628364779651,-3.93357436621185,
0.00359891632991313));
#47327=CARTESIAN_POINT('Ctrl Pts',(-34.1773068026308,-3.9362323744975,0.289473138192191));
#47328=CARTESIAN_POINT('Ctrl Pts',(-34.1917771272964,-3.90772657673974,
0.574821677658488));
#47329=CARTESIAN_POINT('Ctrl Pts',(-34.206247451962,-3.84608328852811,0.852822380024853));
#47330=CARTESIAN_POINT('Ctrl Pts',(-34.2725386291945,-3.5636842243429,2.1263939312628));
#47331=CARTESIAN_POINT('Ctrl Pts',(-34.338829806427,-2.58582136213101,3.24575480973049));
#47332=CARTESIAN_POINT('Ctrl Pts',(-34.4051209836595,-1.361725904702,3.69666947868347));
#47333=CARTESIAN_POINT('Ctrl Pts',(-34.471412160892,-0.137630447272919,
4.14758414763648));
#47334=CARTESIAN_POINT('Ctrl Pts',(-34.5377033381245,1.33269760537326,3.93005260707466));
#47335=CARTESIAN_POINT('Ctrl Pts',(-34.6039945153569,2.37378803635881,3.14400907005788));
#47336=CARTESIAN_POINT('Ctrl Pts',(-34.6702856925894,3.41487846734437,2.35796553304111));
#47337=CARTESIAN_POINT('Ctrl Pts',(-34.7365768698219,4.02673127666927,1.0034099995692));
#47338=CARTESIAN_POINT('Ctrl Pts',(-34.8028680470544,3.92826065557925,-0.297373327644713));
#47339=CARTESIAN_POINT('Ctrl Pts',(-34.8691592242869,3.82979003448924,-1.59815665485862));
#47340=CARTESIAN_POINT('Ctrl Pts',(-34.9354504015194,3.02099598298444,-2.84516777581461));
#47341=CARTESIAN_POINT('Ctrl Pts',(-35.0017415787519,1.87343931866343,-3.46552850131871));
#47342=CARTESIAN_POINT('Ctrl Pts',(-35.0680327559843,0.725882654342432,
-4.08588922682282));
#47343=CARTESIAN_POINT('Ctrl Pts',(-35.1343239332168,-0.760436622794699,
-4.07959955687498));
#47344=CARTESIAN_POINT('Ctrl Pts',(-35.2006151104493,-1.90270191092192,
-3.44954897230645));
#47345=CARTESIAN_POINT('Ctrl Pts',(-35.2669062876818,-3.04496719904915,
-2.81949838773792));
#47346=CARTESIAN_POINT('Ctrl Pts',(-35.3331974649143,-3.8431784981664,-1.56568688854873));
#47347=CARTESIAN_POINT('Ctrl Pts',(-35.3994886421468,-3.93063671798657,
-0.264116764674724));
#47348=CARTESIAN_POINT('Ctrl Pts',(-35.4039379207529,-3.93650666935296,
-0.176759014393482));
#47349=CARTESIAN_POINT('Ctrl Pts',(-35.408387199359,-3.93917487756493,-0.0891861249111568));
#47350=CARTESIAN_POINT('Ctrl Pts',(-35.4128364779651,-3.93872791654916,
-0.00158551424731923));
#47351=CARTESIAN_POINT('Ctrl Pts',(-35.5961635220348,-3.93904295656044,
-0.00122215278806678));
#47352=CARTESIAN_POINT('Ctrl Pts',(-35.5927910842056,-3.93931291656347,
-0.0676070209899404));
#47353=CARTESIAN_POINT('Ctrl Pts',(-35.5894186463764,-3.93778065259506,
-0.133979164464208));
#47354=CARTESIAN_POINT('Ctrl Pts',(-35.5860462085472,-3.93440714360982,
-0.200257590314247));
#47355=CARTESIAN_POINT('Ctrl Pts',(-35.5197550313147,-3.8680949109277,-1.50307623286285));
#47356=CARTESIAN_POINT('Ctrl Pts',(-35.4534638540823,-3.0903478158649,-2.76968351598535));
#47357=CARTESIAN_POINT('Ctrl Pts',(-35.3871726768498,-1.95846367235667,
-3.41819875347027));
#47358=CARTESIAN_POINT('Ctrl Pts',(-35.3208814996173,-0.826579528848437,
-4.06671399095518));
#47359=CARTESIAN_POINT('Ctrl Pts',(-35.2545903223848,0.659441663105231,
-4.09713718280251));
#47360=CARTESIAN_POINT('Ctrl Pts',(-35.1882991451523,1.81692024231754,-3.49549188344405));
#47361=CARTESIAN_POINT('Ctrl Pts',(-35.1220079679198,2.97439882152978,-2.89384658408562));
#47362=CARTESIAN_POINT('Ctrl Pts',(-35.0557167906874,3.80333478800069,-1.66013279352146));
#47363=CARTESIAN_POINT('Ctrl Pts',(-34.9894256134549,3.92291410771786,-0.361119893712047));
#47364=CARTESIAN_POINT('Ctrl Pts',(-34.9231344362224,4.04249342743504,0.937893006097444));
#47365=CARTESIAN_POINT('Ctrl Pts',(-34.8568432589899,3.45271610039835,2.30220501515221));
#47366=CARTESIAN_POINT('Ctrl Pts',(-34.7905520817574,2.42452643613527,3.10504979584027));
#47367=CARTESIAN_POINT('Ctrl Pts',(-34.7242609045249,1.39633677187219,3.90789457652833));
#47368=CARTESIAN_POINT('Ctrl Pts',(-34.6579697272925,-0.0702652296172822,
4.14927212884968));
#47369=CARTESIAN_POINT('Ctrl Pts',(-34.59167855006,-1.30152110318205,3.71829335746095));
#47370=CARTESIAN_POINT('Ctrl Pts',(-34.5253873728275,-2.53277697674682,
3.28731458607222));
#47371=CARTESIAN_POINT('Ctrl Pts',(-34.459096195595,-3.52868672238688,2.1839794909734));
#47372=CARTESIAN_POINT('Ctrl Pts',(-34.3928050183625,-3.83172838051812,
0.915161347576742));
#47373=CARTESIAN_POINT('Ctrl Pts',(-34.3772578529199,-3.90280026355969,
0.617587425744959));
#47374=CARTESIAN_POINT('Ctrl Pts',(-34.3617106874774,-3.93576191957382,
0.310911343410304));
#47375=CARTESIAN_POINT('Ctrl Pts',(-34.3461635220348,-3.93292354923884,
0.0036330978440403));
#47376=CARTESIAN_POINT('Origin',(-54.75,0.,0.));
#47377=CARTESIAN_POINT('',(-32.9128364779652,-3.9264796012353,-8.02974850103166E-5));
#47378=CARTESIAN_POINT('',(-33.0961635220348,-3.92652099442121,-0.000433216618794752));
#47379=CARTESIAN_POINT('',(-54.75,-3.933,-4.81653586104654E-16));
#47380=CARTESIAN_POINT('Ctrl Pts',(-32.9128364779652,-3.9264796012353,-8.02974850103167E-5));
#47381=CARTESIAN_POINT('Ctrl Pts',(-32.9462264059025,-3.92635941678331,
0.662581741630279));
#47382=CARTESIAN_POINT('Ctrl Pts',(-32.9796163338399,-3.76762221461801,
1.32529785623839));
#47383=CARTESIAN_POINT('Ctrl Pts',(-33.0130062617773,-3.45058948713258,
1.90081426379763));
#47384=CARTESIAN_POINT('Ctrl Pts',(-33.0792974390098,-2.82116396798668,
3.04342410246678));
#47385=CARTESIAN_POINT('Ctrl Pts',(-33.1455886162423,-1.56778938426622,
3.84232128384968));
#47386=CARTESIAN_POINT('Ctrl Pts',(-33.2118797934748,-0.266267306492336,
3.9304916226421));
#47387=CARTESIAN_POINT('Ctrl Pts',(-33.2781709707073,1.0352547712814,4.01866196143452));
#47388=CARTESIAN_POINT('Ctrl Pts',(-33.3444621479397,2.38492434310865,3.39610545763665));
#47389=CARTESIAN_POINT('Ctrl Pts',(-33.4107533251722,3.16270182207219,2.34882520823234));
#47390=CARTESIAN_POINT('Ctrl Pts',(-33.4770445024047,3.94047930103577,1.30154495882797));
#47391=CARTESIAN_POINT('Ctrl Pts',(-33.5433356796372,4.14636468713564,-0.170459036182738));
#47392=CARTESIAN_POINT('Ctrl Pts',(-33.6096268568697,3.68577402262817,-1.39094663027945));
#47393=CARTESIAN_POINT('Ctrl Pts',(-33.6759180341022,3.22518335812068,-2.61143422437624));
#47394=CARTESIAN_POINT('Ctrl Pts',(-33.7422092113346,2.09811664300563,-3.58040541755886));
#47395=CARTESIAN_POINT('Ctrl Pts',(-33.8085003885671,0.822349483294592,
-3.85271384889815));
#47396=CARTESIAN_POINT('Ctrl Pts',(-33.8747915657996,-0.453417676416301,
-4.1250222802374));
#47397=CARTESIAN_POINT('Ctrl Pts',(-33.9410827430321,-1.87788528072323,
-3.70066794973349));
#47398=CARTESIAN_POINT('Ctrl Pts',(-34.0073739202646,-2.79665144979747,
-2.77459967247749));
#47399=CARTESIAN_POINT('Ctrl Pts',(-34.0591947728315,-3.5148653687333,-2.05067758109228));
#47400=CARTESIAN_POINT('Ctrl Pts',(-34.1110156253983,-3.92405555729255,
-1.02016843140461));
#47401=CARTESIAN_POINT('Ctrl Pts',(-34.1628364779651,-3.93357436621185,
0.00359891632991313));
#47402=CARTESIAN_POINT('Ctrl Pts',(-34.3461635220348,-3.93292354923884,
0.0036330978440403));
#47403=CARTESIAN_POINT('Ctrl Pts',(-34.2954195102449,-3.92365946195074,
-0.999284827832049));
#47404=CARTESIAN_POINT('Ctrl Pts',(-34.244675498455,-3.53302188146874,-2.00861752797984));
#47405=CARTESIAN_POINT('Ctrl Pts',(-34.1939314866651,-2.84133575425134,
-2.72882278753667));
#47406=CARTESIAN_POINT('Ctrl Pts',(-34.1276403094326,-1.93772789923092,
-3.66968758755893));
#47407=CARTESIAN_POINT('Ctrl Pts',(-34.0613491322001,-0.520338618567738,
-4.11711599590891));
#47408=CARTESIAN_POINT('Ctrl Pts',(-33.9950579549676,0.759681997058345,
-3.8655589424444));
#47409=CARTESIAN_POINT('Ctrl Pts',(-33.9287667777351,2.03970261268443,-3.6140018889799));
#47410=CARTESIAN_POINT('Ctrl Pts',(-33.8624756005026,3.18235456327333,-2.66345937370094));
#47411=CARTESIAN_POINT('Ctrl Pts',(-33.7961844232701,3.66270236963661,-1.45061160398805));
#47412=CARTESIAN_POINT('Ctrl Pts',(-33.7298932460376,4.14305017599989,-0.237763834275166));
#47413=CARTESIAN_POINT('Ctrl Pts',(-33.6636020688052,3.96109383813746,1.23738918987177));
#47414=CARTESIAN_POINT('Ctrl Pts',(-33.5973108915727,3.20042428446631,2.29716065471372));
#47415=CARTESIAN_POINT('Ctrl Pts',(-33.5310197143402,2.4397547307952,3.35693211955562));
#47416=CARTESIAN_POINT('Ctrl Pts',(-33.4647285371077,1.10037196131553,4.00132202509275));
#47417=CARTESIAN_POINT('Ctrl Pts',(-33.3984373598752,-0.202410204614914,
3.93429698716736));
#47418=CARTESIAN_POINT('Ctrl Pts',(-33.3321461826427,-1.50519237054536,
3.86727194924197));
#47419=CARTESIAN_POINT('Ctrl Pts',(-33.2658550054103,-2.77137393292651,
3.08883196785406));
#47420=CARTESIAN_POINT('Ctrl Pts',(-33.1995638281778,-3.41926978209264,
1.9565931696279));
#47421=CARTESIAN_POINT('Ctrl Pts',(-33.1650970594635,-3.75613024100211,
1.36790830360129));
#47422=CARTESIAN_POINT('Ctrl Pts',(-33.1306302907491,-3.92585128094651,
0.683582009327261));
#47423=CARTESIAN_POINT('Ctrl Pts',(-33.0961635220348,-3.92652099442121,
-0.000433216618794752));
#47424=CARTESIAN_POINT('Origin',(-54.75,0.,0.));
#47425=CARTESIAN_POINT('',(-31.6628364779652,-3.93387008195027,-0.00357098358684305));
#47426=CARTESIAN_POINT('',(-31.8461635220348,-3.9345187971462,-0.00348206949214982));
#47427=CARTESIAN_POINT('',(-54.75,-3.933,-4.81653586104654E-16));
#47428=CARTESIAN_POINT('Ctrl Pts',(-31.6628364779652,-3.93387008195027,
-0.00357098358684305));
#47429=CARTESIAN_POINT('Ctrl Pts',(-31.7151460091743,-3.9242645441804,1.02965144060316));
#47430=CARTESIAN_POINT('Ctrl Pts',(-31.7674555403835,-3.50648141256207,
2.06974646053407));
#47431=CARTESIAN_POINT('Ctrl Pts',(-31.8197650715926,-2.77612939768722,
2.79513295595455));
#47432=CARTESIAN_POINT('Ctrl Pts',(-31.8860562488251,-1.85056394640085,
3.71440567009357));
#47433=CARTESIAN_POINT('Ctrl Pts',(-31.9523474260576,-0.42300793747674,
4.1282515289858));
#47434=CARTESIAN_POINT('Ctrl Pts',(-32.0186386032901,0.850717933004561,
3.84654932018698));
#47435=CARTESIAN_POINT('Ctrl Pts',(-32.0849297805226,2.12444380348579,3.56484711138817));
#47436=CARTESIAN_POINT('Ctrl Pts',(-32.151220957755,3.24433953552423,2.58759683489839));
#47437=CARTESIAN_POINT('Ctrl Pts',(-32.2175121349875,3.69592388009588,1.36374827101759));
#47438=CARTESIAN_POINT('Ctrl Pts',(-32.28380331222,4.14750822466752,0.139899707136798));
#47439=CARTESIAN_POINT('Ctrl Pts',(-32.3500944894525,3.93078118177237,-1.33054714413501));
#47440=CARTESIAN_POINT('Ctrl Pts',(-32.416385666685,3.14530737741631,-2.37206748970955));
#47441=CARTESIAN_POINT('Ctrl Pts',(-32.4826768439175,2.35983357306016,-3.4135878352842));
#47442=CARTESIAN_POINT('Ctrl Pts',(-32.5489680211499,1.00561300724294,-4.02618167516146));
#47443=CARTESIAN_POINT('Ctrl Pts',(-32.6152591983824,-0.29522400180688,
-3.92842277039063));
#47444=CARTESIAN_POINT('Ctrl Pts',(-32.6815503756149,-1.59606101085663,
-3.8306638656198));
#47445=CARTESIAN_POINT('Ctrl Pts',(-32.7478415528474,-2.84351446313897,
-3.02255221620097));
#47446=CARTESIAN_POINT('Ctrl Pts',(-32.8141327300799,-3.46450296199443,
-1.87533514351389));
#47447=CARTESIAN_POINT('Ctrl Pts',(-32.847033979375,-3.77270834109907,-1.30595507696754));
#47448=CARTESIAN_POINT('Ctrl Pts',(-32.8799352286701,-3.92659802672648,
-0.653043939341669));
#47449=CARTESIAN_POINT('Ctrl Pts',(-32.9128364779652,-3.9264796012353,-8.02974850103167E-5));
#47450=CARTESIAN_POINT('Ctrl Pts',(-33.0961635220348,-3.92652099442121,
-0.000433216618794752));
#47451=CARTESIAN_POINT('Ctrl Pts',(-33.0643391135166,-3.9271393649852,-0.632009102469086));
#47452=CARTESIAN_POINT('Ctrl Pts',(-33.0325147049985,-3.78363313240224,
-1.26331978720999));
#47453=CARTESIAN_POINT('Ctrl Pts',(-33.0006902964803,-3.49449726309091,
-1.81883246958498));
#47454=CARTESIAN_POINT('Ctrl Pts',(-32.9343991192478,-2.89221875897201,
-2.97598169550694));
#47455=CARTESIAN_POINT('Ctrl Pts',(-32.8681079420153,-1.65805161478326,
-3.80424253228636));
#47456=CARTESIAN_POINT('Ctrl Pts',(-32.8018167647829,-0.358973483605743,
-3.92311110118416));
#47457=CARTESIAN_POINT('Ctrl Pts',(-32.7355255875504,0.940104647571701,
-4.04197967008195));
#47458=CARTESIAN_POINT('Ctrl Pts',(-32.6692344103179,2.30409376573791,-3.4514559710982));
#47459=CARTESIAN_POINT('Ctrl Pts',(-32.6029432330854,3.10637586968665,-2.42282719779908));
#47460=CARTESIAN_POINT('Ctrl Pts',(-32.5366520558529,3.90865797363544,-1.3941984244999));
#47461=CARTESIAN_POINT('Ctrl Pts',(-32.4703608786204,4.14923306336671,0.0725354231147142));
#47462=CARTESIAN_POINT('Ctrl Pts',(-32.4040697013879,3.71758069567479,1.30355530964841));
#47463=CARTESIAN_POINT('Ctrl Pts',(-32.3377785241555,3.28592832798287,2.53457519618211));
#47464=CARTESIAN_POINT('Ctrl Pts',(-32.271487346923,2.18204850286777,3.5298811216349));
#47465=CARTESIAN_POINT('Ctrl Pts',(-32.2051961696905,0.913064745270451,
3.83222852203658));
#47466=CARTESIAN_POINT('Ctrl Pts',(-32.138904992458,-0.355919012326873,
4.13457592243826));
#47467=CARTESIAN_POINT('Ctrl Pts',(-32.0726138152255,-1.79000670240642,
3.74396479778884));
#47468=CARTESIAN_POINT('Ctrl Pts',(-32.006322637993,-2.73037696785918,2.83984229976781));
#47469=CARTESIAN_POINT('Ctrl Pts',(-31.952936266007,-3.48768674710849,2.11172398877361));
#47470=CARTESIAN_POINT('Ctrl Pts',(-31.8995498940209,-3.92479174814375,
1.05056336001));
#47471=CARTESIAN_POINT('Ctrl Pts',(-31.8461635220348,-3.9345187971462,-0.00348206949214982));
#47472=CARTESIAN_POINT('Origin',(-54.75,0.,0.));
#47473=CARTESIAN_POINT('',(-30.4128364779652,-3.93856210802547,0.00174382912284086));
#47474=CARTESIAN_POINT('',(-30.5961635220348,-3.93815120456093,0.00207590725787368));
#47475=CARTESIAN_POINT('',(-54.75,-3.933,-4.81653586104654E-16));
#47476=CARTESIAN_POINT('Ctrl Pts',(-30.4128364779652,-3.93856210802547,
0.00174382912284086));
#47477=CARTESIAN_POINT('Ctrl Pts',(-30.4177744352136,-3.93909995995488,
0.0989767503555888));
#47478=CARTESIAN_POINT('Ctrl Pts',(-30.422712392462,-3.93581264589787,0.196172692623262));
#47479=CARTESIAN_POINT('Ctrl Pts',(-30.4276503497104,-3.92858370921048,
0.29307458759238));
#47480=CARTESIAN_POINT('Ctrl Pts',(-30.4939415269429,-3.83153655002342,
1.59396488906649));
#47481=CARTESIAN_POINT('Ctrl Pts',(-30.5602327041754,-3.02410754460245,
2.84186029924427));
#47482=CARTESIAN_POINT('Ctrl Pts',(-30.6265238814079,-1.8772304069739,3.46347638555528));
#47483=CARTESIAN_POINT('Ctrl Pts',(-30.6928150586404,-0.73035326934548,
4.08509247186621));
#47484=CARTESIAN_POINT('Ctrl Pts',(-30.7591062358729,0.755972000490423,
4.08042923431056));
#47485=CARTESIAN_POINT('Ctrl Pts',(-30.8253974131053,1.8989260476558,3.4516289690088));
#47486=CARTESIAN_POINT('Ctrl Pts',(-30.8916885903378,3.04188009482125,2.82282870370701));
#47487=CARTESIAN_POINT('Ctrl Pts',(-30.9579797675703,3.84146291931614,1.56989141065905));
#47488=CARTESIAN_POINT('Ctrl Pts',(-31.0242709448028,3.93034535068678,0.268417768602042));
#47489=CARTESIAN_POINT('Ctrl Pts',(-31.0905621220353,4.01922778205741,-1.03305587345496));
#47490=CARTESIAN_POINT('Ctrl Pts',(-31.1568532992678,3.39740982030379,-2.38306586452101));
#47491=CARTESIAN_POINT('Ctrl Pts',(-31.2231444765002,2.35055527543642,-3.16141622873111));
#47492=CARTESIAN_POINT('Ctrl Pts',(-31.2894356537327,1.30370073056905,-3.93976659294122));
#47493=CARTESIAN_POINT('Ctrl Pts',(-31.3557268309652,-0.168190397412086,
-4.14645733029538));
#47494=CARTESIAN_POINT('Ctrl Pts',(-31.4220180081977,-1.3889298132156,-3.68653450385688));
#47495=CARTESIAN_POINT('Ctrl Pts',(-31.4883091854302,-2.60966922901911,
-3.22661167741839));
#47496=CARTESIAN_POINT('Ctrl Pts',(-31.5546003626627,-3.57925693264501,
-2.10007528718724));
#47497=CARTESIAN_POINT('Ctrl Pts',(-31.6208915398952,-3.85226333763363,
-0.82445730737876));
#47498=CARTESIAN_POINT('Ctrl Pts',(-31.6348731859185,-3.90984383440576,
-0.555413374245061));
#47499=CARTESIAN_POINT('Ctrl Pts',(-31.6488548319418,-3.93643751518581,
-0.279737675669086));
#47500=CARTESIAN_POINT('Ctrl Pts',(-31.6628364779652,-3.93387008195027,
-0.00357098358684305));
#47501=CARTESIAN_POINT('Ctrl Pts',(-31.8461635220348,-3.9345187971462,-0.00348206949214982));
#47502=CARTESIAN_POINT('Ctrl Pts',(-31.8332587167884,-3.9368700652382,-0.258270894477957));
#47503=CARTESIAN_POINT('Ctrl Pts',(-31.820353911542,-3.91424928270523,-0.512643972429283));
#47504=CARTESIAN_POINT('Ctrl Pts',(-31.8074491062956,-3.86514271671165,
-0.761796858497929));
#47505=CARTESIAN_POINT('Ctrl Pts',(-31.7411579290631,-3.61288535928538,
-2.04167964735));
#47506=CARTESIAN_POINT('Ctrl Pts',(-31.6748667518306,-2.66171780360684,
-3.18381135366156));
#47507=CARTESIAN_POINT('Ctrl Pts',(-31.6085755745981,-1.44860740125792,
-3.66349549899918));
#47508=CARTESIAN_POINT('Ctrl Pts',(-31.5422843973656,-0.235496998908926,
-4.14317964433682));
#47509=CARTESIAN_POINT('Ctrl Pts',(-31.4759932201332,1.23955625011055,-3.96041622870047));
#47510=CARTESIAN_POINT('Ctrl Pts',(-31.4097020429007,2.29891136885762,-3.19916695286502));
#47511=CARTESIAN_POINT('Ctrl Pts',(-31.3434108656682,3.35826648760463,-2.43791767702961));
#47512=CARTESIAN_POINT('Ctrl Pts',(-31.2771196884357,4.00192347607932,-1.09818254099537));
#47513=CARTESIAN_POINT('Ctrl Pts',(-31.2108285112032,3.93418565297491,0.204562758323147));
#47514=CARTESIAN_POINT('Ctrl Pts',(-31.1445373339707,3.86644782987051,1.50730805764167));
#47515=CARTESIAN_POINT('Ctrl Pts',(-31.0782461567383,3.08731519518687,2.77306352024438));
#47516=CARTESIAN_POINT('Ctrl Pts',(-31.0119549795058,1.95472208118354,3.42033978714103));
#47517=CARTESIAN_POINT('Ctrl Pts',(-30.9456638022733,0.822128967180207,
4.06761605403768));
#47518=CARTESIAN_POINT('Ctrl Pts',(-30.8793726250408,-0.663924626142901,
4.09641312522832));
#47519=CARTESIAN_POINT('Ctrl Pts',(-30.8130814478083,-1.82074415237652,
3.49350159664385));
#47520=CARTESIAN_POINT('Ctrl Pts',(-30.7467902705758,-2.97756367861014,
2.89059006805938));
#47521=CARTESIAN_POINT('Ctrl Pts',(-30.6804990933433,-3.80514913775434,
1.65596993969977));
#47522=CARTESIAN_POINT('Ctrl Pts',(-30.6142079161109,-3.92330692024899,
0.35682696603929));
#47523=CARTESIAN_POINT('Ctrl Pts',(-30.6081931180855,-3.93402773147151,
0.238951814038115));
#47524=CARTESIAN_POINT('Ctrl Pts',(-30.6021783200602,-3.93890819421201,
0.120545479065067));
#47525=CARTESIAN_POINT('Ctrl Pts',(-30.5961635220348,-3.93815120456093,
0.00207590725787368));
#47526=CARTESIAN_POINT('Origin',(-54.75,0.,0.));
#47527=CARTESIAN_POINT('',(-29.1628364779652,-3.92850656573534,0.00271417295257592));
#47528=CARTESIAN_POINT('',(-29.3461635220348,-3.92807907470128,0.00246354187033206));
#47529=CARTESIAN_POINT('',(-54.75,-3.933,-4.81653586104654E-16));
#47530=CARTESIAN_POINT('Ctrl Pts',(-29.1628364779652,-3.92850656573534,
0.00271417295257592));
#47531=CARTESIAN_POINT('Ctrl Pts',(-29.1866940384854,-3.93149841301045,
0.475584504066331));
#47532=CARTESIAN_POINT('Ctrl Pts',(-29.2105515990055,-3.85257530886676,
0.94748964595665));
#47533=CARTESIAN_POINT('Ctrl Pts',(-29.2344091595257,-3.68729388150453,
1.38691258036898));
#47534=CARTESIAN_POINT('Ctrl Pts',(-29.3007003367582,-3.22803903081511,
2.60790345244531));
#47535=CARTESIAN_POINT('Ctrl Pts',(-29.3669915139907,-2.10203330270165,
3.57810737626403));
#47536=CARTESIAN_POINT('Ctrl Pts',(-29.4332826912232,-0.826564884657816,
3.85181167317628));
#47537=CARTESIAN_POINT('Ctrl Pts',(-29.4995738684556,0.448903533386023,
4.12551597008853));
#47538=CARTESIAN_POINT('Ctrl Pts',(-29.5658650456881,1.87383464136024,3.70272064009429));
#47539=CARTESIAN_POINT('Ctrl Pts',(-29.6321562229206,2.7936136253755,2.77765829184995));
#47540=CARTESIAN_POINT('Ctrl Pts',(-29.6984474001531,3.71339260939076,1.85259594360561));
#47541=CARTESIAN_POINT('Ctrl Pts',(-29.7647385773856,4.12801946944707,0.425266577111169));
#47542=CARTESIAN_POINT('Ctrl Pts',(-29.8310297546181,3.84701420036357,-0.848613231317707));
#47543=CARTESIAN_POINT('Ctrl Pts',(-29.8973209318506,3.56600893128009,-2.12249303974651));
#47544=CARTESIAN_POINT('Ctrl Pts',(-29.963612109083,2.58937153305671,-3.24292329010991));
#47545=CARTESIAN_POINT('Ctrl Pts',(-30.0299032863155,1.36577022908884,-3.69517717511638));
#47546=CARTESIAN_POINT('Ctrl Pts',(-30.096194463548,0.142168925120821,-4.1474310601229));
#47547=CARTESIAN_POINT('Ctrl Pts',(-30.1624856407805,-1.32839628459159,
-3.93150857977258));
#47548=CARTESIAN_POINT('Ctrl Pts',(-30.228776818013,-2.37034623297127,-3.14660474321217));
#47549=CARTESIAN_POINT('Ctrl Pts',(-30.2901300379971,-3.33468246992064,
-2.42016753450283));
#47550=CARTESIAN_POINT('Ctrl Pts',(-30.3514832579811,-3.93187939570464,
-1.20635751845283));
#47551=CARTESIAN_POINT('Ctrl Pts',(-30.4128364779652,-3.93856210802547,
0.00174382912284086));
#47552=CARTESIAN_POINT('Ctrl Pts',(-30.5961635220348,-3.93815120456093,
0.00207590725787368));
#47553=CARTESIAN_POINT('Ctrl Pts',(-30.5358871428277,-3.93056514845859,
-1.18514880164594));
#47554=CARTESIAN_POINT('Ctrl Pts',(-30.4756107636206,-3.35682441040137,
-2.37872422133875));
#47555=CARTESIAN_POINT('Ctrl Pts',(-30.4153343844134,-2.42112723417837,
-3.10770101362506));
#47556=CARTESIAN_POINT('Ctrl Pts',(-30.3490432071809,-1.39205965976785,
-3.90942020066774));
#47557=CARTESIAN_POINT('Ctrl Pts',(-30.2827520299484,0.0748055948983133,
-4.14919275579165));
#47558=CARTESIAN_POINT('Ctrl Pts',(-30.216460852716,1.30558912588946,-3.71686692101367));
#47559=CARTESIAN_POINT('Ctrl Pts',(-30.1501696754835,2.53637265688055,-3.28454108623571));
#47560=CARTESIAN_POINT('Ctrl Pts',(-30.083878498251,3.53107446419656,-2.18011686155598));
#47561=CARTESIAN_POINT('Ctrl Pts',(-30.0175873210185,3.83272751635967,-0.91096786963422));
#47562=CARTESIAN_POINT('Ctrl Pts',(-29.951296143786,4.13438056852279,0.358181122287614));
#47563=CARTESIAN_POINT('Ctrl Pts',(-29.8850049665535,3.74298486553277,1.79205488145162));
#47564=CARTESIAN_POINT('Ctrl Pts',(-29.818713789321,2.83834799516436,2.73193033083072));
#47565=CARTESIAN_POINT('Ctrl Pts',(-29.7524226120885,1.9337111247959,3.67180578020988));
#47566=CARTESIAN_POINT('Ctrl Pts',(-29.6861314348561,0.515833087049026,
4.11768291980425));
#47567=CARTESIAN_POINT('Ctrl Pts',(-29.6198402576236,-0.763911491890319,
3.86472533393052));
#47568=CARTESIAN_POINT('Ctrl Pts',(-29.5535490803911,-2.04365607082952,
3.61176774805681));
#47569=CARTESIAN_POINT('Ctrl Pts',(-29.4872579031586,-3.18526719096115,
2.6599754367152));
#47570=CARTESIAN_POINT('Ctrl Pts',(-29.4209667259261,-3.66428753167743,
1.44660276488046));
#47571=CARTESIAN_POINT('Ctrl Pts',(-29.396032324629,-3.84446362604685,0.990211395990211));
#47572=CARTESIAN_POINT('Ctrl Pts',(-29.3710979233319,-3.93089823856218,
0.496812372634598));
#47573=CARTESIAN_POINT('Ctrl Pts',(-29.3461635220348,-3.92807907470128,
0.00246354187033206));
#47574=CARTESIAN_POINT('Origin',(-54.75,0.,0.));
#47575=CARTESIAN_POINT('',(-27.9128364779652,-3.92865200925827,-0.00278885010489755));
#47576=CARTESIAN_POINT('',(-28.0961635220348,-3.92913455543446,-0.00300513829252201));
#47577=CARTESIAN_POINT('',(-54.75,-3.933,-4.81653586104654E-16));
#47578=CARTESIAN_POINT('Ctrl Pts',(-27.9128364779652,-3.92865200925827,
-0.00278885010489754));
#47579=CARTESIAN_POINT('Ctrl Pts',(-27.9556136417571,-3.92312711758811,
0.844999904541822));
#47580=CARTESIAN_POINT('Ctrl Pts',(-27.9983908055491,-3.65402535614722,
1.69598532263604));
#47581=CARTESIAN_POINT('Ctrl Pts',(-28.041167969341,-3.14790116705762,2.36862426665854));
#47582=CARTESIAN_POINT('Ctrl Pts',(-28.1074591465735,-2.36356753325771,
3.41100350593077));
#47583=CARTESIAN_POINT('Ctrl Pts',(-28.173750323806,-1.01001811882594,4.02507885654247));
#47584=CARTESIAN_POINT('Ctrl Pts',(-28.2400415010384,0.290925085644865,
3.92874347199063));
#47585=CARTESIAN_POINT('Ctrl Pts',(-28.3063326782709,1.59186829011552,3.83240808743879));
#47586=CARTESIAN_POINT('Ctrl Pts',(-28.3726238555034,2.84020528462515,3.02566196772358));
#47587=CARTESIAN_POINT('Ctrl Pts',(-28.4389150327359,3.46244877230814,1.87912510847689));
#47588=CARTESIAN_POINT('Ctrl Pts',(-28.5052062099684,4.08469225999124,0.732588249230013));
#47589=CARTESIAN_POINT('Ctrl Pts',(-28.5714973872008,4.08084224084741,-0.753739349548403));
#47590=CARTESIAN_POINT('Ctrl Pts',(-28.6377885644333,3.45266741762393,-1.89703726306168));
#47591=CARTESIAN_POINT('Ctrl Pts',(-28.7040797416658,2.82449259440052,-3.04033517657484));
#47592=CARTESIAN_POINT('Ctrl Pts',(-28.7703709188983,1.5719929670974,-3.84060340482301));
#47593=CARTESIAN_POINT('Ctrl Pts',(-28.8366620961308,0.270568150359426,
-3.93019790216441));
#47594=CARTESIAN_POINT('Ctrl Pts',(-28.9029532733633,-1.03085666637862,
-4.01979239950582));
#47595=CARTESIAN_POINT('Ctrl Pts',(-28.9692444505958,-2.38120667255164,
-3.39871316594053));
#47596=CARTESIAN_POINT('Ctrl Pts',(-29.0355356278283,-3.16012968900548,
-2.35228463899091));
#47597=CARTESIAN_POINT('Ctrl Pts',(-29.0779692445406,-3.65872576330176,
-1.68245572837013));
#47598=CARTESIAN_POINT('Ctrl Pts',(-29.1204028612529,-3.92318519599903,
-0.838344088982128));
#47599=CARTESIAN_POINT('Ctrl Pts',(-29.1628364779652,-3.92850656573534,
0.00271417295257592));
#47600=CARTESIAN_POINT('Ctrl Pts',(-29.3461635220348,-3.92807907470128,
0.00246354187033206));
#47601=CARTESIAN_POINT('Ctrl Pts',(-29.3048067460994,-3.92340314417738,
-0.81747488713848));
#47602=CARTESIAN_POINT('Ctrl Pts',(-29.2634499701641,-3.67318732149573,
-1.64002626562861));
#47603=CARTESIAN_POINT('Ctrl Pts',(-29.2220931942287,-3.19790866357844,
-2.30066139481159));
#47604=CARTESIAN_POINT('Ctrl Pts',(-29.1558020169962,-2.43607989346235,
-3.35959985034084));
#47605=CARTESIAN_POINT('Ctrl Pts',(-29.0895108397637,-1.09599279192933,
-4.00252372907152));
#47606=CARTESIAN_POINT('Ctrl Pts',(-29.0232196625312,0.206715250794351,
-3.93407314106582));
#47607=CARTESIAN_POINT('Ctrl Pts',(-28.9569284852988,1.50942329351825,-3.8656225530601));
#47608=CARTESIAN_POINT('Ctrl Pts',(-28.8906373080663,2.7747522774328,-3.08579749831771));
#47609=CARTESIAN_POINT('Ctrl Pts',(-28.8243461308338,3.42140876829489,-1.95285040758408));
#47610=CARTESIAN_POINT('Ctrl Pts',(-28.7580549536013,4.06806525915686,-0.819903316850643));
#47611=CARTESIAN_POINT('Ctrl Pts',(-28.6917637763688,4.09604925696662,0.666165809873902));
#47612=CARTESIAN_POINT('Ctrl Pts',(-28.6254725991363,3.49250488440095,1.82265529011987));
#47613=CARTESIAN_POINT('Ctrl Pts',(-28.5591814219038,2.88896051183525,2.97914477036591));
#47614=CARTESIAN_POINT('Ctrl Pts',(-28.4928902446714,1.65388776889405,3.80605460413334));
#47615=CARTESIAN_POINT('Ctrl Pts',(-28.4265990674389,0.354680341655036,
3.92350156485376));
#47616=CARTESIAN_POINT('Ctrl Pts',(-28.3603078902064,-0.944527085583904,
4.04094852557418));
#47617=CARTESIAN_POINT('Ctrl Pts',(-28.2940167129739,-2.30786919712065,
3.44893261324767));
#47618=CARTESIAN_POINT('Ctrl Pts',(-28.2277255357414,-3.10902522725881,
2.41942654578203));
#47619=CARTESIAN_POINT('Ctrl Pts',(-28.1838715311726,-3.63901883535004,
1.7383711524227));
#47620=CARTESIAN_POINT('Ctrl Pts',(-28.1400175266037,-3.92298296771959,
0.865856957318394));
#47621=CARTESIAN_POINT('Ctrl Pts',(-28.0961635220348,-3.92913455543446,
-0.00300513829252201));
#47622=CARTESIAN_POINT('Origin',(-54.75,0.,0.));
#47623=CARTESIAN_POINT('',(-26.6628364779652,-3.93868009607648,-0.00163299323942157));
#47624=CARTESIAN_POINT('',(-26.8461635220348,-3.93900474281862,-0.00127218255392029));
#47625=CARTESIAN_POINT('',(-54.75,-3.933,-4.81653586104654E-16));
#47626=CARTESIAN_POINT('Ctrl Pts',(-26.6628364779652,-3.93868009607648,
-0.00163299323942157));
#47627=CARTESIAN_POINT('Ctrl Pts',(-26.7245332450289,-3.93232394690408,
1.21313664908943));
#47628=CARTESIAN_POINT('Ctrl Pts',(-26.7862300120925,-3.32752073202559,
2.43337087631873));
#47629=CARTESIAN_POINT('Ctrl Pts',(-26.8479267791562,-2.3540132983783,3.15884220328027));
#47630=CARTESIAN_POINT('Ctrl Pts',(-26.9142179563887,-1.3080111025996,3.93833763880378));
#47631=CARTESIAN_POINT('Ctrl Pts',(-26.9805091336212,0.16365296950363,4.14663889280402));
#47632=CARTESIAN_POINT('Ctrl Pts',(-27.0468003108537,1.38489493234366,3.6880521553437));
#47633=CARTESIAN_POINT('Ctrl Pts',(-27.1130914880862,2.60613689518355,3.22946541788343));
#47634=CARTESIAN_POINT('Ctrl Pts',(-27.1793826653187,3.57695674876007,2.10399068896269));
#47635=CARTESIAN_POINT('Ctrl Pts',(-27.2456738425512,3.8513588556613,0.828672214500858));
#47636=CARTESIAN_POINT('Ctrl Pts',(-27.3119650197836,4.1257609625625,-0.4466462599609));
#47637=CARTESIAN_POINT('Ctrl Pts',(-27.3782561970162,3.70374532278838,-1.87180847996394));
#47638=CARTESIAN_POINT('Ctrl Pts',(-27.4445473742486,2.77918635450782,-2.79209345851531));
#47639=CARTESIAN_POINT('Ctrl Pts',(-27.5108385514811,1.85462738622716,-3.71237843706677));
#47640=CARTESIAN_POINT('Ctrl Pts',(-27.5771297287136,0.427525089440144,
-4.12778617416664));
#47641=CARTESIAN_POINT('Ctrl Pts',(-27.6434209059461,-0.846508275594557,
-3.84747792891868));
#47642=CARTESIAN_POINT('Ctrl Pts',(-27.7097120831786,-2.12054164062919,
-3.56716968367073));
#47643=CARTESIAN_POINT('Ctrl Pts',(-27.776003260411,-3.24150607391136,-2.59114545607491));
#47644=CARTESIAN_POINT('Ctrl Pts',(-27.8422944376435,-3.69442936396844,
-1.36779177831066));
#47645=CARTESIAN_POINT('Ctrl Pts',(-27.8658084510841,-3.85508489573833,
-0.933858394979657));
#47646=CARTESIAN_POINT('Ctrl Pts',(-27.8893224645246,-3.9316889655563,-0.468806566203696));
#47647=CARTESIAN_POINT('Ctrl Pts',(-27.9128364779652,-3.92865200925827,
-0.00278885010489754));
#47648=CARTESIAN_POINT('Ctrl Pts',(-28.0961635220348,-3.92913455543446,
-0.00300513829252201));
#47649=CARTESIAN_POINT('Ctrl Pts',(-28.0737263493712,-3.93228191306054,
-0.44754399059901));
#47650=CARTESIAN_POINT('Ctrl Pts',(-28.0512891767076,-3.86270663719881,
-0.891126837505349));
#47651=CARTESIAN_POINT('Ctrl Pts',(-28.028852004044,-3.71615203369125,-1.30762255129638));
#47652=CARTESIAN_POINT('Ctrl Pts',(-27.9625608268115,-3.28315286124596,
-2.53816935830421));
#47653=CARTESIAN_POINT('Ctrl Pts',(-27.896269649579,-2.17818456761584,-3.53226674971499));
#47654=CARTESIAN_POINT('Ctrl Pts',(-27.8299784723465,-0.908870721295116,
-3.83322536333816));
#47655=CARTESIAN_POINT('Ctrl Pts',(-27.763687295114,0.360443125025604,-4.13418397696132));
#47656=CARTESIAN_POINT('Ctrl Pts',(-27.6973961178816,1.79410252403693,-3.74200381279686));
#47657=CARTESIAN_POINT('Ctrl Pts',(-27.6311049406491,2.73348287598629,-2.83685284088832));
#47658=CARTESIAN_POINT('Ctrl Pts',(-27.5648137634166,3.67286322793571,-1.93170186897973));
#47659=CARTESIAN_POINT('Ctrl Pts',(-27.4985225861841,4.11796453282311,-0.513580089327008));
#47660=CARTESIAN_POINT('Ctrl Pts',(-27.4322314089516,3.86430679422603,0.766025896602054));
#47661=CARTESIAN_POINT('Ctrl Pts',(-27.3659402317191,3.61064905562898,2.04563188253097));
#47662=CARTESIAN_POINT('Ctrl Pts',(-27.2996490544866,2.65823227354765,3.18672207473626));
#47663=CARTESIAN_POINT('Ctrl Pts',(-27.2333578772542,1.44459769545578,3.66507846743426));
#47664=CARTESIAN_POINT('Ctrl Pts',(-27.1670667000217,0.230963117363835,
4.14343486013229));
#47665=CARTESIAN_POINT('Ctrl Pts',(-27.1007755227892,-1.24388925673868,
3.95905745332295));
#47666=CARTESIAN_POINT('Ctrl Pts',(-27.0344843455567,-2.30241073205211,
3.19664941698299));
#47667=CARTESIAN_POINT('Ctrl Pts',(-26.9717107377161,-3.30476451058249,
2.47469658576527));
#47668=CARTESIAN_POINT('Ctrl Pts',(-26.9089371298754,-3.93379819990021,
1.23442900344055));
#47669=CARTESIAN_POINT('Ctrl Pts',(-26.8461635220348,-3.93900474281862,
-0.00127218255392029));
#47670=CARTESIAN_POINT('Origin',(-54.75,0.,0.));
#47671=CARTESIAN_POINT('',(-25.4128364779652,-3.93366221636038,0.00359143100450002));
#47672=CARTESIAN_POINT('',(-25.5961635220348,-3.93301104109986,0.00363068149465887));
#47673=CARTESIAN_POINT('',(-54.75,-3.933,-4.81653586104654E-16));
#47674=CARTESIAN_POINT('Ctrl Pts',(-25.4128364779652,-3.93366221636038,
0.00359143100450002));
#47675=CARTESIAN_POINT('Ctrl Pts',(-25.4271616710682,-3.93629385844204,
0.286582248783829));
#47676=CARTESIAN_POINT('Ctrl Pts',(-25.4414868641711,-3.90836307935993,
0.569057703773814));
#47677=CARTESIAN_POINT('Ctrl Pts',(-25.4558120572741,-3.84794050571348,
0.844403066465243));
#47678=CARTESIAN_POINT('Ctrl Pts',(-25.5221032345066,-3.56832936821265,
2.11858960671787));
#47679=CARTESIAN_POINT('Ctrl Pts',(-25.5883944117391,-2.59291860342171,
3.24008788735299));
#47680=CARTESIAN_POINT('Ctrl Pts',(-25.6546855889715,-1.36981291807769,
3.69368044687598));
#47681=CARTESIAN_POINT('Ctrl Pts',(-25.720976766204,-0.146707232733672,
4.14727300639897));
#47682=CARTESIAN_POINT('Ctrl Pts',(-25.7872679434365,1.32409337316342,3.93295984480984));
#47683=CARTESIAN_POINT('Ctrl Pts',(-25.853559120669,2.36690159128718,3.14919664856431));
#47684=CARTESIAN_POINT('Ctrl Pts',(-25.9198502979015,3.40970980941095,2.36543345231877));
#47685=CARTESIAN_POINT('Ctrl Pts',(-25.986141475134,4.02452563976139,1.01222022141682));
#47686=CARTESIAN_POINT('Ctrl Pts',(-26.0524326523664,3.92890205868327,-0.288775496607364));
#47687=CARTESIAN_POINT('Ctrl Pts',(-26.1187238295989,3.83327847760514,-1.58977121463163));
#47688=CARTESIAN_POINT('Ctrl Pts',(-26.1850150068314,3.02721548509852,-2.83854941977796));
#47689=CARTESIAN_POINT('Ctrl Pts',(-26.2513061840639,1.88101924745432,-3.46142012256138));
#47690=CARTESIAN_POINT('Ctrl Pts',(-26.3175973612964,0.734823009810316,
-4.08429082534469));
#47691=CARTESIAN_POINT('Ctrl Pts',(-26.3838885385289,-0.75150647297135,
-4.08125402576508));
#47692=CARTESIAN_POINT('Ctrl Pts',(-26.4501797157614,-1.89514791058069,
-3.4537048326671));
#47693=CARTESIAN_POINT('Ctrl Pts',(-26.5164708929938,-3.03878934819016,
-2.82615563956904));
#47694=CARTESIAN_POINT('Ctrl Pts',(-26.5827620702263,-3.83974274062748,
-1.57409405295251));
#47695=CARTESIAN_POINT('Ctrl Pts',(-26.6490532474588,-3.93004927711913,
-0.272718451120987));
#47696=CARTESIAN_POINT('Ctrl Pts',(-26.6536476576276,-3.93630810803581,
-0.182524649349915));
#47697=CARTESIAN_POINT('Ctrl Pts',(-26.6582420677964,-3.93915342325037,
-0.0920939730132787));
#47698=CARTESIAN_POINT('Ctrl Pts',(-26.6628364779652,-3.93868009607648,
-0.00163299323942157));
#47699=CARTESIAN_POINT('Ctrl Pts',(-26.8461635220348,-3.93900474281862,
-0.00127218255392029));
#47700=CARTESIAN_POINT('Ctrl Pts',(-26.842645952643,-3.93929649562107,-0.0705156882063396));
#47701=CARTESIAN_POINT('Ctrl Pts',(-26.8391283832511,-3.93762942433138,
-0.139744855324124));
#47702=CARTESIAN_POINT('Ctrl Pts',(-26.8356108138592,-3.93395945147371,
-0.208867681384836));
#47703=CARTESIAN_POINT('Ctrl Pts',(-26.7693196366268,-3.86479611905754,
-1.51153807754211));
#47704=CARTESIAN_POINT('Ctrl Pts',(-26.7030284593943,-3.08427887770083,
-2.7764402039861));
#47705=CARTESIAN_POINT('Ctrl Pts',(-26.6367372821618,-1.95097814939022,
-3.42247672523399));
#47706=CARTESIAN_POINT('Ctrl Pts',(-26.5704461049293,-0.8176774210796,-4.06851324648187));
#47707=CARTESIAN_POINT('Ctrl Pts',(-26.5041549276968,0.66840679418499,-4.09568416253368));
#47708=CARTESIAN_POINT('Ctrl Pts',(-26.4378637504643,1.82456588224294,-3.49150712666056));
#47709=CARTESIAN_POINT('Ctrl Pts',(-26.3715725732318,2.98072497030096,-2.8873300907874));
#47710=CARTESIAN_POINT('Ctrl Pts',(-26.3052813959994,3.80695893115228,-1.65180510298944));
#47711=CARTESIAN_POINT('Ctrl Pts',(-26.2389902187669,3.92369503494019,-0.352533611095581));
#47712=CARTESIAN_POINT('Ctrl Pts',(-26.1726990415344,4.04043113872808,0.946737880798055));
#47713=CARTESIAN_POINT('Ctrl Pts',(-26.1064078643019,3.44766938545265,2.30975587678741));
#47714=CARTESIAN_POINT('Ctrl Pts',(-26.0401166870694,2.41772513311934,3.11034851019134));
#47715=CARTESIAN_POINT('Ctrl Pts',(-25.973825509837,1.38778088078586,3.9109411435954));
#47716=CARTESIAN_POINT('Ctrl Pts',(-25.9075343326045,-0.0793458706057278,
4.14910841441386));
#47717=CARTESIAN_POINT('Ctrl Pts',(-25.841243155372,-1.30965558526044,3.71543603392153));
#47718=CARTESIAN_POINT('Ctrl Pts',(-25.7749519781395,-2.53996529991508,
3.28176365342923));
#47719=CARTESIAN_POINT('Ctrl Pts',(-25.708660800907,-3.53345797783293,2.17625162162621));
#47720=CARTESIAN_POINT('Ctrl Pts',(-25.6423696236745,-3.83372206282286,
0.906773300881576));
#47721=CARTESIAN_POINT('Ctrl Pts',(-25.6269675897946,-3.90348515654062,
0.611823823105227));
#47722=CARTESIAN_POINT('Ctrl Pts',(-25.6115655559147,-3.93582675359008,
0.308023204452773));
#47723=CARTESIAN_POINT('Ctrl Pts',(-25.5961635220348,-3.93301104109986,
0.00363068149465887));
#47724=CARTESIAN_POINT('Origin',(-54.75,0.,0.));
#47725=CARTESIAN_POINT('',(-24.1628364779652,-3.92647812505579,-3.26061429916406E-5));
#47726=CARTESIAN_POINT('',(-24.3461635220348,-3.92651210140376,-0.000385812242292873));
#47727=CARTESIAN_POINT('',(-54.75,-3.933,-4.81653586104654E-16));
#47728=CARTESIAN_POINT('Ctrl Pts',(-24.1628364779652,-3.92647837592232,
-3.26048887833164E-5));
#47729=CARTESIAN_POINT('Ctrl Pts',(-24.1960812743399,-3.9264297878317,0.659749642360009));
#47730=CARTESIAN_POINT('Ctrl Pts',(-24.2293260707147,-3.76914112069753,
1.31955365614632));
#47731=CARTESIAN_POINT('Ctrl Pts',(-24.2625708670894,-3.45474121382766,
1.89325799077861));
#47732=CARTESIAN_POINT('Ctrl Pts',(-24.3288620443219,-2.82781783871468,
3.03724261012995));
#47733=CARTESIAN_POINT('Ctrl Pts',(-24.3951532215543,-1.57619466759501,
3.83888092698731));
#47734=CARTESIAN_POINT('Ctrl Pts',(-24.4614443987868,-0.274868670242791,
3.92989947559545));
#47735=CARTESIAN_POINT('Ctrl Pts',(-24.5277355760193,1.02645732710936,4.02091802420358));
#47736=CARTESIAN_POINT('Ctrl Pts',(-24.5940267532518,2.37748615069405,3.40131680456257));
#47737=CARTESIAN_POINT('Ctrl Pts',(-24.6603179304843,3.15755377194132,2.35574125308056));
#47738=CARTESIAN_POINT('Ctrl Pts',(-24.7266091077168,3.93762139318864,1.31016570159849));
#47739=CARTESIAN_POINT('Ctrl Pts',(-24.7929002849492,4.14672781209847,-0.161384181724622));
#47740=CARTESIAN_POINT('Ctrl Pts',(-24.8591914621817,3.68880932514741,-1.38287686974364));
#47741=CARTESIAN_POINT('Ctrl Pts',(-24.9254826394142,3.23089083819637,-2.60436955776259));
#47742=CARTESIAN_POINT('Ctrl Pts',(-24.9917738166467,2.10594744538451,-3.57580505047746));
#47743=CARTESIAN_POINT('Ctrl Pts',(-25.0580649938792,0.830779296277255,
-3.85090488522419));
#47744=CARTESIAN_POINT('Ctrl Pts',(-25.1243561711117,-0.444388852830141,
-4.12600471997094));
#47745=CARTESIAN_POINT('Ctrl Pts',(-25.1906473483441,-1.86978175823297,
-3.70476889674934));
#47746=CARTESIAN_POINT('Ctrl Pts',(-25.2569385255766,-2.79057245582902,
-2.78071358520342));
#47747=CARTESIAN_POINT('Ctrl Pts',(-25.3089045097062,-3.5123848715306,-2.05634202236053));
#47748=CARTESIAN_POINT('Ctrl Pts',(-25.3608704938357,-3.92411568741188,
-1.02298435333687));
#47749=CARTESIAN_POINT('Ctrl Pts',(-25.4128364779652,-3.93366221636038,
0.00359143100450002));
#47750=CARTESIAN_POINT('Ctrl Pts',(-25.5961635220348,-3.93301104109986,
0.00363068149465887));
#47751=CARTESIAN_POINT('Ctrl Pts',(-25.5452743786822,-3.92370777650038,
-1.00209848759207));
#47752=CARTESIAN_POINT('Ctrl Pts',(-25.4943852353297,-3.53060027531191,
-2.01428933941688));
#47753=CARTESIAN_POINT('Ctrl Pts',(-25.4434960919771,-2.83535683738727,
-2.73503460286112));
#47754=CARTESIAN_POINT('Ctrl Pts',(-25.3772049147446,-1.92969203489976,
-3.67391957617286));
#47755=CARTESIAN_POINT('Ctrl Pts',(-25.3109137375121,-0.511326937862769,
-4.11824491311015));
#47756=CARTESIAN_POINT('Ctrl Pts',(-25.2446225602796,0.76814007199996,-3.86388709772353));
#47757=CARTESIAN_POINT('Ctrl Pts',(-25.1783313830471,2.04760708186283,-3.60952928233688));
#47758=CARTESIAN_POINT('Ctrl Pts',(-25.1120402058146,3.18817600455133,-2.65648831462615));
#47759=CARTESIAN_POINT('Ctrl Pts',(-25.0457490285822,3.66586830603292,-1.4425921935841));
#47760=CARTESIAN_POINT('Ctrl Pts',(-24.9794578513497,4.14356060751448,-0.22869607254211));
#47761=CARTESIAN_POINT('Ctrl Pts',(-24.9131666741172,3.95837628778912,1.2460552018313));
#47762=CARTESIAN_POINT('Ctrl Pts',(-24.8468754968847,3.19538921345563,2.30415938005552));
#47763=CARTESIAN_POINT('Ctrl Pts',(-24.7805843196522,2.43240213912218,3.36226355827968));
#47764=CARTESIAN_POINT('Ctrl Pts',(-24.7142931424197,1.09161231018076,4.00372064035487));
#47765=CARTESIAN_POINT('Ctrl Pts',(-24.6480019651873,-0.211020049449589,
3.93384458423267));
#47766=CARTESIAN_POINT('Ctrl Pts',(-24.5817107879548,-1.51365240908001,
3.86396852811048));
#47767=CARTESIAN_POINT('Ctrl Pts',(-24.5154196107223,-2.77812729939929,
3.08275933379082));
#47768=CARTESIAN_POINT('Ctrl Pts',(-24.4491284334898,-3.42354365763898,
1.94910530716183));
#47769=CARTESIAN_POINT('Ctrl Pts',(-24.4148067963381,-3.7577019421051,1.36216653518887));
#47770=CARTESIAN_POINT('Ctrl Pts',(-24.3804851591865,-3.92591825646931,
0.680753029737708));
#47771=CARTESIAN_POINT('Ctrl Pts',(-24.3461635220348,-3.92651210140376,
-0.000385812242292873));
#47772=CARTESIAN_POINT('Origin',(-54.75,0.,0.));
#47773=CARTESIAN_POINT('',(-22.9128364779652,-3.93378229249503,-0.00358008960437806));
#47774=CARTESIAN_POINT('',(-23.0961635220348,-3.93443176527693,-0.00349624190913098));
#47775=CARTESIAN_POINT('',(-54.75,-3.933,-4.81653586104654E-16));
#47776=CARTESIAN_POINT('Ctrl Pts',(-22.9128364779652,-3.93378229249503,
-0.00358008960437806));
#47777=CARTESIAN_POINT('Ctrl Pts',(-22.9650008776117,-3.92420053618949,
1.02683468227007));
#47778=CARTESIAN_POINT('Ctrl Pts',(-23.0171652772582,-3.50898078364747,
2.06408445940646));
#47779=CARTESIAN_POINT('Ctrl Pts',(-23.0693296769046,-2.78223998347954,
2.78905061777197));
#47780=CARTESIAN_POINT('Ctrl Pts',(-23.1356208541371,-1.85868860528863,
3.71034675876961));
#47781=CARTESIAN_POINT('Ctrl Pts',(-23.2019120313696,-0.432041729477022,
4.12731587666033));
#47782=CARTESIAN_POINT('Ctrl Pts',(-23.2682032086021,0.842297604559967,
3.84840193060951));
#47783=CARTESIAN_POINT('Ctrl Pts',(-23.3344943858346,2.11663693859703,3.56948798455867));
#47784=CARTESIAN_POINT('Ctrl Pts',(-23.4007855630671,3.23866873085946,2.59469097456621));
#47785=CARTESIAN_POINT('Ctrl Pts',(-23.4670767402996,3.69293042406328,1.37183364778468));
#47786=CARTESIAN_POINT('Ctrl Pts',(-23.533367917532,4.14719211726705,0.14897632100329));
#47787=CARTESIAN_POINT('Ctrl Pts',(-23.5996590947645,3.93368371141241,-1.3219413225671));
#47788=CARTESIAN_POINT('Ctrl Pts',(-23.665950271997,3.15049118734441,-2.36517820737289));
#47789=CARTESIAN_POINT('Ctrl Pts',(-23.7322414492295,2.36729866327638,-3.40841509217874));
#47790=CARTESIAN_POINT('Ctrl Pts',(-23.798532626462,1.01442202099493,-4.02397121821994));
#47791=CARTESIAN_POINT('Ctrl Pts',(-23.8648238036945,-0.286625821123579,
-3.92905946924091));
#47792=CARTESIAN_POINT('Ctrl Pts',(-23.931114980927,-1.58767366324201,-3.83414772026189));
#47793=CARTESIAN_POINT('Ctrl Pts',(-23.9974061581594,-2.83689270519751,
-3.02876809626271));
#47794=CARTESIAN_POINT('Ctrl Pts',(-24.0636973353919,-3.46039043662218,
-1.88291282334053));
#47795=CARTESIAN_POINT('Ctrl Pts',(-24.0967437162497,-3.77120620965261,
-1.31170001135402));
#47796=CARTESIAN_POINT('Ctrl Pts',(-24.1297900971074,-3.92652667402376,
-0.655877061868211));
#47797=CARTESIAN_POINT('Ctrl Pts',(-24.1628364779652,-3.92647837592232,
-3.26048887833164E-5));
#47798=CARTESIAN_POINT('Ctrl Pts',(-24.3461635220348,-3.92651210140376,
-0.000385812242292873));
#47799=CARTESIAN_POINT('Ctrl Pts',(-24.314193981954,-3.92706524953448,-0.634845509286078));
#47800=CARTESIAN_POINT('Ctrl Pts',(-24.2822244418732,-3.78218336924519,
-1.26906689884118));
#47801=CARTESIAN_POINT('Ctrl Pts',(-24.2502549017923,-3.49050832372137,
-1.82647592817378));
#47802=CARTESIAN_POINT('Ctrl Pts',(-24.1839637245598,-2.885698805404,-2.98230427794211));
#47803=CARTESIAN_POINT('Ctrl Pts',(-24.1176725473274,-1.64972194260919,
-3.80786211854049));
#47804=CARTESIAN_POINT('Ctrl Pts',(-24.0513813700949,-0.350386775003562,
-3.92388733045038));
#47805=CARTESIAN_POINT('Ctrl Pts',(-23.9850901928624,0.948948392601992,
-4.03991254236027));
#47806=CARTESIAN_POINT('Ctrl Pts',(-23.9187990156299,2.31164186501836,-3.44640512558175));
#47807=CARTESIAN_POINT('Ctrl Pts',(-23.8525078383975,3.11167086202694,-2.41602299669911));
#47808=CARTESIAN_POINT('Ctrl Pts',(-23.786216661165,3.91169985903557,-1.38564086781641));
#47809=CARTESIAN_POINT('Ctrl Pts',(-23.7199254839325,4.14906438063636,0.0816159731704677));
#47810=CARTESIAN_POINT('Ctrl Pts',(-23.6536343067,3.71471892191887,1.31168822717304));
#47811=CARTESIAN_POINT('Ctrl Pts',(-23.5873431294675,3.28037346320138,2.54176048117561));
#47812=CARTESIAN_POINT('Ctrl Pts',(-23.521051952235,2.17431802416562,3.53464814819388));
#47813=CARTESIAN_POINT('Ctrl Pts',(-23.4547607750026,0.904675609021257,
3.83421761466514));
#47814=CARTESIAN_POINT('Ctrl Pts',(-23.3884695977701,-0.364966806123031,
4.13378708113639));
#47815=CARTESIAN_POINT('Ctrl Pts',(-23.3221784205376,-1.7981961973759,3.7400383470607));
#47816=CARTESIAN_POINT('Ctrl Pts',(-23.2558872433051,-2.73658551099054,
2.83385998510919));
#47817=CARTESIAN_POINT('Ctrl Pts',(-23.2026460028817,-3.4902455475549,2.10606992239897));
#47818=CARTESIAN_POINT('Ctrl Pts',(-23.1494047624583,-3.92471524826081,
1.04774360683275));
#47819=CARTESIAN_POINT('Ctrl Pts',(-23.0961635220348,-3.93443176527693,
-0.00349624190913098));
#47820=CARTESIAN_POINT('Origin',(-54.75,0.,0.));
#47821=CARTESIAN_POINT('',(-21.6628364779652,-3.93861276308604,0.00169727802626606));
#47822=CARTESIAN_POINT('',(-21.8461635220348,-3.93821003127031,0.00203258821323272));
#47823=CARTESIAN_POINT('',(-54.75,-3.933,-4.81653586104654E-16));
#47824=CARTESIAN_POINT('Ctrl Pts',(-21.6628364779652,-3.93861276308604,
0.00169727802626606));
#47825=CARTESIAN_POINT('Ctrl Pts',(-21.667629303651,-3.93912300404395,0.0960692092454155));
#47826=CARTESIAN_POINT('Ctrl Pts',(-21.6724221293367,-3.93602631799819,
0.190407079145342));
#47827=CARTESIAN_POINT('Ctrl Pts',(-21.6772149550225,-3.92921570361644,
0.284476059837029));
#47828=CARTESIAN_POINT('Ctrl Pts',(-21.743506132255,-3.83501581514877,1.58557563657516));
#47829=CARTESIAN_POINT('Ctrl Pts',(-21.8097973094874,-3.03031980075104,
2.83523514138036));
#47830=CARTESIAN_POINT('Ctrl Pts',(-21.8760884867199,-1.88480583556769,
3.45935971479932));
#47831=CARTESIAN_POINT('Ctrl Pts',(-21.9423796639524,-0.739291870384334,
4.08348428821828));
#47832=CARTESIAN_POINT('Ctrl Pts',(-22.0086708411849,0.747040045584634,
4.082073930251));
#47833=CARTESIAN_POINT('Ctrl Pts',(-22.0749620184174,1.89136750422079,3.45577656079557));
#47834=CARTESIAN_POINT('Ctrl Pts',(-22.1412531956499,3.03569496285695,2.82947919134014));
#47835=CARTESIAN_POINT('Ctrl Pts',(-22.2075443728823,3.8380179641603,1.57829481039657));
#47836=CARTESIAN_POINT('Ctrl Pts',(-22.2738355501148,3.92974849763818,0.277018807081612));
#47837=CARTESIAN_POINT('Ctrl Pts',(-22.3401267273473,4.02147903111605,-1.02425719623327));
#47838=CARTESIAN_POINT('Ctrl Pts',(-22.4064179045798,3.40261709676853,-2.37562482191952));
#47839=CARTESIAN_POINT('Ctrl Pts',(-22.4727090818123,2.35746850258097,-3.15626439537392));
#47840=CARTESIAN_POINT('Ctrl Pts',(-22.5390002590448,1.31231990839341,-3.93690396882831));
#47841=CARTESIAN_POINT('Ctrl Pts',(-22.6052914362772,-0.159115345634208,
-4.14681549005081));
#47842=CARTESIAN_POINT('Ctrl Pts',(-22.6715826135097,-1.38085839317283,
-3.68956539068907));
#47843=CARTESIAN_POINT('Ctrl Pts',(-22.7378737907422,-2.60260144071159,
-3.23231529132727));
#47844=CARTESIAN_POINT('Ctrl Pts',(-22.8041649679747,-3.57465228176129,
-2.10790357138104));
#47845=CARTESIAN_POINT('Ctrl Pts',(-22.8704561452072,-3.85044976200099,
-0.832886129355597));
#47846=CARTESIAN_POINT('Ctrl Pts',(-22.8845829227932,-3.9092227363964,-0.561177455988717));
#47847=CARTESIAN_POINT('Ctrl Pts',(-22.8987097003792,-3.93637715299624,
-0.282629410640403));
#47848=CARTESIAN_POINT('Ctrl Pts',(-22.9128364779652,-3.93378229249503,
-0.00358008960437806));
#47849=CARTESIAN_POINT('Ctrl Pts',(-23.0961635220348,-3.93443176527693,
-0.00349624190913098));
#47850=CARTESIAN_POINT('Ctrl Pts',(-23.0831135852258,-3.93681337645008,
-0.261165174641599));
#47851=CARTESIAN_POINT('Ctrl Pts',(-23.0700636484167,-3.91367637085558,
-0.51840836169853));
#47852=CARTESIAN_POINT('Ctrl Pts',(-23.0570137116076,-3.86346624454843,
-0.770254017452239));
#47853=CARTESIAN_POINT('Ctrl Pts',(-22.9907225343752,-3.60840842851518,
-2.04958166823441));
#47854=CARTESIAN_POINT('Ctrl Pts',(-22.9244313571426,-2.65474356047235,
-3.18962897997126));
#47855=CARTESIAN_POINT('Ctrl Pts',(-22.8581401799102,-1.44058625986577,
-3.66665704723695));
#47856=CARTESIAN_POINT('Ctrl Pts',(-22.7918490026777,-0.226428959259131,
-4.14368511450266));
#47857=CARTESIAN_POINT('Ctrl Pts',(-22.7255578254452,1.24822077391129,-3.95769393729713));
#47858=CARTESIAN_POINT('Ctrl Pts',(-22.6592666482127,2.30590733829799,-3.19412805337387));
#47859=CARTESIAN_POINT('Ctrl Pts',(-22.5929754709802,3.36359390268457,-2.43056216945069));
#47860=CARTESIAN_POINT('Ctrl Pts',(-22.5266842937477,4.00431729828756,-1.08942157880993));
#47861=CARTESIAN_POINT('Ctrl Pts',(-22.4603931165152,3.93372853937707,0.213172354344517));
#47862=CARTESIAN_POINT('Ctrl Pts',(-22.3941019392827,3.86313978046657,1.51576628749911));
#47863=CARTESIAN_POINT('Ctrl Pts',(-22.3278107620503,3.08123886704243,2.77981356316738));
#47864=CARTESIAN_POINT('Ctrl Pts',(-22.2615195848178,1.94723188145956,3.42460956519045));
#47865=CARTESIAN_POINT('Ctrl Pts',(-22.1952284075853,0.813224895876891,
4.06940556721341));
#47866=CARTESIAN_POINT('Ctrl Pts',(-22.1289372303528,-0.672888161864364,
4.09495029559142));
#47867=CARTESIAN_POINT('Ctrl Pts',(-22.0626460531203,-1.82838542734041,
3.48950847588248));
#47868=CARTESIAN_POINT('Ctrl Pts',(-21.9963548758879,-2.98388269281665,
2.88406665617344));
#47869=CARTESIAN_POINT('Ctrl Pts',(-21.9300636986554,-3.80876416602755,
1.6476382883772));
#47870=CARTESIAN_POINT('Ctrl Pts',(-21.8637725214229,-3.92407845132676,
0.348239834021639));
#47871=CARTESIAN_POINT('Ctrl Pts',(-21.8579028549602,-3.93428880542434,
0.233186280176151));
#47872=CARTESIAN_POINT('Ctrl Pts',(-21.8520331884975,-3.93893616145868,
0.117639041623225));
#47873=CARTESIAN_POINT('Ctrl Pts',(-21.8461635220348,-3.93821003127031,
0.00203258821323272));
#47874=CARTESIAN_POINT('Origin',(-54.75,0.,0.));
#47875=CARTESIAN_POINT('',(-20.4128364779652,-3.92856748927321,0.00274604364064041));
#47876=CARTESIAN_POINT('',(-20.5961635220349,-3.92813410533466,0.00249872673611579));
#47877=CARTESIAN_POINT('',(-54.75,-3.933,-4.81653586104654E-16));
#47878=CARTESIAN_POINT('Ctrl Pts',(-20.4128364779652,-3.92856748927321,
0.00274604364064041));
#47879=CARTESIAN_POINT('Ctrl Pts',(-20.4365489069227,-3.9315789798689,0.472721489178729));
#47880=CARTESIAN_POINT('Ctrl Pts',(-20.4602613358802,-3.85364009669069,
0.941731212379603));
#47881=CARTESIAN_POINT('Ctrl Pts',(-20.4839737648377,-3.69032035174204,
1.3788395032363));
#47882=CARTESIAN_POINT('Ctrl Pts',(-20.5502649420702,-3.2337387768493,2.60083254456009));
#47883=CARTESIAN_POINT('Ctrl Pts',(-20.6165561193027,-2.1098590663668,3.57349844295636));
#47884=CARTESIAN_POINT('Ctrl Pts',(-20.6828472965352,-0.834992713105839,
3.84999348612781));
#47885=CARTESIAN_POINT('Ctrl Pts',(-20.7491384737677,0.439873640155124,
4.12648852929926));
#47886=CARTESIAN_POINT('Ctrl Pts',(-20.8154296510002,1.86572663619477,3.70681271724578));
#47887=CARTESIAN_POINT('Ctrl Pts',(-20.8817208282327,2.78752794479972,2.78376554887926));
#47888=CARTESIAN_POINT('Ctrl Pts',(-20.9480120054651,3.70932925340478,1.86071838051265));
#47889=CARTESIAN_POINT('Ctrl Pts',(-21.0143031826976,4.12707887457528,0.434299855833041));
#47890=CARTESIAN_POINT('Ctrl Pts',(-21.0805943599301,3.84886220346862,-0.840191890509009));
#47891=CARTESIAN_POINT('Ctrl Pts',(-21.1468855371626,3.570645532362,-2.11468363685091));
#47892=CARTESIAN_POINT('Ctrl Pts',(-21.2131767143951,2.59646256897831,-3.23724860485509));
#47893=CARTESIAN_POINT('Ctrl Pts',(-21.2794678916276,1.37385396682755,-3.69217929575456));
#47894=CARTESIAN_POINT('Ctrl Pts',(-21.34575906886,0.15124536467666,-4.14710998665408));
#47895=CARTESIAN_POINT('Ctrl Pts',(-21.4120502460925,-1.31978887624136,
-3.9344064004487));
#47896=CARTESIAN_POINT('Ctrl Pts',(-21.478341423325,-2.36345411543157,-3.15178478301042));
#47897=CARTESIAN_POINT('Ctrl Pts',(-21.5398397748717,-3.33166277390398,
-2.42574639650694));
#47898=CARTESIAN_POINT('Ctrl Pts',(-21.6013381264185,-3.93206569046954,
-1.20922057769968));
#47899=CARTESIAN_POINT('Ctrl Pts',(-21.6628364779652,-3.93861276308604,
0.00169727802626606));
#47900=CARTESIAN_POINT('Ctrl Pts',(-21.8461635220348,-3.93821003127031,
0.00203258821323272));
#47901=CARTESIAN_POINT('Ctrl Pts',(-21.785742011265,-3.9307353505068,-1.18800378168487));
#47902=CARTESIAN_POINT('Ctrl Pts',(-21.7253205004952,-3.35386723851819,
-2.38431476535265));
#47903=CARTESIAN_POINT('Ctrl Pts',(-21.6648989897255,-2.4143201370314,-3.11299228236934));
#47904=CARTESIAN_POINT('Ctrl Pts',(-21.598607812493,-1.38350044004909,-3.9124574034903));
#47905=CARTESIAN_POINT('Ctrl Pts',(-21.5323166352605,0.0838860513029625,
-4.14901910481729));
#47906=CARTESIAN_POINT('Ctrl Pts',(-21.466025458028,1.31372047642571,-3.71400069789792));
#47907=CARTESIAN_POINT('Ctrl Pts',(-21.3997342807955,2.54355490154839,-3.27898229097857));
#47908=CARTESIAN_POINT('Ctrl Pts',(-21.333443103563,3.53583726044157,-2.17238377581286));
#47909=CARTESIAN_POINT('Ctrl Pts',(-21.2671519263305,3.83471201871666,-0.902577646342112));
#47910=CARTESIAN_POINT('Ctrl Pts',(-21.2008607490981,4.13358677699174,0.367228483128639));
#47911=CARTESIAN_POINT('Ctrl Pts',(-21.1345695718656,3.73905393464871,1.80024222690445));
#47912=CARTESIAN_POINT('Ctrl Pts',(-21.0682783946331,2.83236228450172,2.73813559991076));
#47913=CARTESIAN_POINT('Ctrl Pts',(-21.0019872174006,1.92567063435478,3.67602897291702));
#47914=CARTESIAN_POINT('Ctrl Pts',(-20.9356960401681,0.506820176403872,
4.11880197515389));
#47915=CARTESIAN_POINT('Ctrl Pts',(-20.8694048629356,-0.772367732324979,
3.86304423482693));
#47916=CARTESIAN_POINT('Ctrl Pts',(-20.8031136857032,-2.05155564105398,
3.60728649449995));
#47917=CARTESIAN_POINT('Ctrl Pts',(-20.7368225084707,-3.19108100056096,
2.65299801160893));
#47918=CARTESIAN_POINT('Ctrl Pts',(-20.6705313312382,-3.66744469081024,
1.43857989490129));
#47919=CARTESIAN_POINT('Ctrl Pts',(-20.6457420615037,-3.84557862208538,
0.984454028952772));
#47920=CARTESIAN_POINT('Ctrl Pts',(-20.6209527917693,-3.93097931647737,
0.493952925906998));
#47921=CARTESIAN_POINT('Ctrl Pts',(-20.5961635220349,-3.92813410533466,
0.00249872673611579));
#47922=CARTESIAN_POINT('Origin',(-54.75,0.,0.));
#47923=CARTESIAN_POINT('',(-19.1628364779652,-3.92859004817972,-0.00275762651098022));
#47924=CARTESIAN_POINT('',(-19.3461635220348,-3.92906724673901,-0.00297761340060153));
#47925=CARTESIAN_POINT('',(-54.75,-3.933,-4.81653586104654E-16));
#47926=CARTESIAN_POINT('Ctrl Pts',(-19.1628364779652,-3.92859004817972,
-0.00275762651098022));
#47927=CARTESIAN_POINT('Ctrl Pts',(-19.2054685101945,-3.92315095775244,
0.842188267718036));
#47928=CARTESIAN_POINT('Ctrl Pts',(-19.2481005424238,-3.65601617471943,
1.69027015247434));
#47929=CARTESIAN_POINT('Ctrl Pts',(-19.290732574653,-3.15307743517508,2.36172931597933));
#47930=CARTESIAN_POINT('Ctrl Pts',(-19.3570237518855,-2.37102695864804,
3.40582259712777));
#47931=CARTESIAN_POINT('Ctrl Pts',(-19.423314929118,-1.01882470847633,4.02285876152022));
#47932=CARTESIAN_POINT('Ctrl Pts',(-19.4896061063505,0.282326213391258,
3.92937076176308));
#47933=CARTESIAN_POINT('Ctrl Pts',(-19.555897283583,1.58347713525885,3.83588276200594));
#47934=CARTESIAN_POINT('Ctrl Pts',(-19.6221884608154,2.83357672882233,3.03187059809921));
#47935=CARTESIAN_POINT('Ctrl Pts',(-19.6884796380479,3.45832795740103,1.8866982835697));
#47936=CARTESIAN_POINT('Ctrl Pts',(-19.7547708152804,4.08307918597977,0.741525969040118));
#47937=CARTESIAN_POINT('Ctrl Pts',(-19.8210619925129,4.08248204957366,-0.744806496112277));
#47938=CARTESIAN_POINT('Ctrl Pts',(-19.8873531697454,3.45681087326069,-1.88947645147357));
#47939=CARTESIAN_POINT('Ctrl Pts',(-19.9536443469779,2.83113969694779,-3.03414640683473));
#47940=CARTESIAN_POINT('Ctrl Pts',(-20.0199355242103,1.5803944807282,-3.83715385240487));
#47941=CARTESIAN_POINT('Ctrl Pts',(-20.0862267014428,0.279168860993574,
-3.92959634329253));
#47942=CARTESIAN_POINT('Ctrl Pts',(-20.1525178786753,-1.02205675874106,
-4.02203883418018));
#47943=CARTESIAN_POINT('Ctrl Pts',(-20.2188090559078,-2.37376278199073,
-3.40391637038534));
#47944=CARTESIAN_POINT('Ctrl Pts',(-20.2851002331403,-3.15497407396417,
-2.35919504636229));
#47945=CARTESIAN_POINT('Ctrl Pts',(-20.3276789814153,-3.65674520459068,
-1.68817171972752));
#47946=CARTESIAN_POINT('Ctrl Pts',(-20.3702577296902,-3.92315996648268,
-0.841155955046957));
#47947=CARTESIAN_POINT('Ctrl Pts',(-20.4128364779652,-3.92856748927321,
0.00274604364064041));
#47948=CARTESIAN_POINT('Ctrl Pts',(-20.5961635220349,-3.92813410533466,
0.00249872673611579));
#47949=CARTESIAN_POINT('Ctrl Pts',(-20.5546616145368,-3.92337068588254,
-0.820288185989406));
#47950=CARTESIAN_POINT('Ctrl Pts',(-20.5131597070388,-3.67126222185311,
-1.64574653828059));
#47951=CARTESIAN_POINT('Ctrl Pts',(-20.4716577995407,-3.19286593711536,
-2.30765460625607));
#47952=CARTESIAN_POINT('Ctrl Pts',(-20.4053666223083,-2.42872147217945,
-3.36492324018196));
#47953=CARTESIAN_POINT('Ctrl Pts',(-20.3390754450758,-1.08723052131588,
-4.00491275750937));
#47954=CARTESIAN_POINT('Ctrl Pts',(-20.2727842678433,0.215324595425315,
-3.93361131694164));
#47955=CARTESIAN_POINT('Ctrl Pts',(-20.2064930906108,1.51787971216637,-3.86230987637392));
#47956=CARTESIAN_POINT('Ctrl Pts',(-20.1402019133783,2.78149899478498,-3.07971747791123));
#47957=CARTESIAN_POINT('Ctrl Pts',(-20.0739107361458,3.42567444756889,-1.94535787284501));
#47958=CARTESIAN_POINT('Ctrl Pts',(-20.0076195589133,4.06984990035283,-0.810998267778726));
#47959=CARTESIAN_POINT('Ctrl Pts',(-19.9413283816809,4.09458152330189,0.675128543891286));
#47960=CARTESIAN_POINT('Ctrl Pts',(-19.8750372044484,3.48850758344289,1.8302943791718));
#47961=CARTESIAN_POINT('Ctrl Pts',(-19.8087460272159,2.8824336435839,2.98546021445231));
#47962=CARTESIAN_POINT('Ctrl Pts',(-19.7424548499834,1.64555414091693,3.80966507334347));
#47963=CARTESIAN_POINT('Ctrl Pts',(-19.6761636727509,0.346092788792513,
3.92426839751211));
#47964=CARTESIAN_POINT('Ctrl Pts',(-19.6098724955184,-0.953368563331904,
4.03887172168075));
#47965=CARTESIAN_POINT('Ctrl Pts',(-19.5435813182859,-2.31541176491369,
3.44387351112686));
#47966=CARTESIAN_POINT('Ctrl Pts',(-19.4772901410534,-3.11431277082326,
2.41261655462562));
#47967=CARTESIAN_POINT('Ctrl Pts',(-19.4335812680472,-3.64106556161118,
1.73266062036312));
#47968=CARTESIAN_POINT('Ctrl Pts',(-19.389872395041,-3.92299895519764,0.863046365293776));
#47969=CARTESIAN_POINT('Ctrl Pts',(-19.3461635220348,-3.92906724673901,
-0.00297761340060153));
#47970=CARTESIAN_POINT('Origin',(-54.75,0.,0.));
#47971=CARTESIAN_POINT('',(-17.9128364779652,-3.93863106461684,-0.00168008665984931));
#47972=CARTESIAN_POINT('',(-18.0961635220349,-3.93896517016805,-0.00132190172209247));
#47973=CARTESIAN_POINT('',(-54.75,-3.933,-4.81653586104654E-16));
#47974=CARTESIAN_POINT('Ctrl Pts',(-17.9128364779652,-3.93863106461684,
-0.00168008665984931));
#47975=CARTESIAN_POINT('Ctrl Pts',(-17.9743881134662,-3.93213463944834,
1.21027201576146));
#47976=CARTESIAN_POINT('Ctrl Pts',(-18.0359397489673,-3.33055199309392,
2.427794228091));
#47977=CARTESIAN_POINT('Ctrl Pts',(-18.0974913844683,-2.36092088390748,
3.15368280809849));
#47978=CARTESIAN_POINT('Ctrl Pts',(-18.1637825617008,-1.31662714279099,
3.93546558473174));
#47979=CARTESIAN_POINT('Ctrl Pts',(-18.2300737389333,0.154577531237571,
4.14698712182452));
#47980=CARTESIAN_POINT('Ctrl Pts',(-18.2963649161657,1.37682020053737,3.69107420808071));
#47981=CARTESIAN_POINT('Ctrl Pts',(-18.3626560933982,2.59906286983725,3.23516129433688));
#47982=CARTESIAN_POINT('Ctrl Pts',(-18.4289472706308,3.57234353440834,2.11181392975638));
#47983=CARTESIAN_POINT('Ctrl Pts',(-18.4952384478632,3.84953605774138,0.837099046896719));
#47984=CARTESIAN_POINT('Ctrl Pts',(-18.5615296250957,4.12672858107439,-0.437615835962802));
#47985=CARTESIAN_POINT('Ctrl Pts',(-18.6278208023282,3.70783296316955,-1.86369823710145));
#47986=CARTESIAN_POINT('Ctrl Pts',(-18.6941119795607,2.78529028094574,-2.78600443736826));
#47987=CARTESIAN_POINT('Ctrl Pts',(-18.7604031567931,1.86274759872194,-3.70831063763507));
#47988=CARTESIAN_POINT('Ctrl Pts',(-18.8266943340256,0.436557852179171,
-4.12684063703003));
#47989=CARTESIAN_POINT('Ctrl Pts',(-18.8929855112581,-0.838085924942725,
-3.84932132415304));
#47990=CARTESIAN_POINT('Ctrl Pts',(-18.9592766884906,-2.11272970206469,
-3.57180201127604));
#47991=CARTESIAN_POINT('Ctrl Pts',(-19.0255678657231,-3.23582750976577,
-2.598233386127));
#47992=CARTESIAN_POINT('Ctrl Pts',(-19.0918590429556,-3.69142706217513,
-1.37587387460027));
#47993=CARTESIAN_POINT('Ctrl Pts',(-19.1155181879588,-3.85402933179616,
-0.939617013029593));
#47994=CARTESIAN_POINT('Ctrl Pts',(-19.139177332962,-3.93160853503985,-0.471670234850337));
#47995=CARTESIAN_POINT('Ctrl Pts',(-19.1628364779652,-3.92859004817972,
-0.00275762651098022));
#47996=CARTESIAN_POINT('Ctrl Pts',(-19.3461635220348,-3.92906724673901,
-0.00297761340060153));
#47997=CARTESIAN_POINT('Ctrl Pts',(-19.3235812178085,-3.93220244552808,
-0.450411180295741));
#47998=CARTESIAN_POINT('Ctrl Pts',(-19.3009989135823,-3.86170098893934,
-0.8968863949304));
#47999=CARTESIAN_POINT('Ctrl Pts',(-19.278416609356,-3.71328136207362,-1.31575233241029));
#48000=CARTESIAN_POINT('Ctrl Pts',(-19.2121254321235,-3.27759013717716,
-2.54534856049627));
#48001=CARTESIAN_POINT('Ctrl Pts',(-19.145834254891,-2.17044887714702,-3.53702531421994));
#48002=CARTESIAN_POINT('Ctrl Pts',(-19.0795430776586,-0.90047941347239,
-3.83520527482935));
#48003=CARTESIAN_POINT('Ctrl Pts',(-19.0132519004261,0.369490050202456,
-4.13338523543881));
#48004=CARTESIAN_POINT('Ctrl Pts',(-18.9469607231936,1.80228771752193,-3.73806840293375));
#48005=CARTESIAN_POINT('Ctrl Pts',(-18.8806695459611,2.73968486915726,-2.83086373601366));
#48006=CARTESIAN_POINT('Ctrl Pts',(-18.8143783687286,3.67708202079254,-1.92365906909362));
#48007=CARTESIAN_POINT('Ctrl Pts',(-18.7480871914961,4.11907865674376,-0.504566567758773));
#48008=CARTESIAN_POINT('Ctrl Pts',(-18.6817960142637,3.86262106868525,0.774481215986085));
#48009=CARTESIAN_POINT('Ctrl Pts',(-18.6155048370312,3.60616348062672,2.05352899973102));
#48010=CARTESIAN_POINT('Ctrl Pts',(-18.5492136597987,2.65125166855823,3.19253206588583));
#48011=CARTESIAN_POINT('Ctrl Pts',(-18.4829224825662,1.43657309929127,3.66823123651701));
#48012=CARTESIAN_POINT('Ctrl Pts',(-18.4166313053337,0.221894530024308,
4.14393040714819));
#48013=CARTESIAN_POINT('Ctrl Pts',(-18.3503401281012,-1.25255079644121,
3.95632568225578));
#48014=CARTESIAN_POINT('Ctrl Pts',(-18.2840489508687,-2.3094011834078,3.19160286505716));
#48015=CARTESIAN_POINT('Ctrl Pts',(-18.2214204745908,-3.30785877841104,
2.46913229181379));
#48016=CARTESIAN_POINT('Ctrl Pts',(-18.1587919983128,-3.9335922899934,1.23155535200719));
#48017=CARTESIAN_POINT('Ctrl Pts',(-18.0961635220349,-3.93896517016805,
-0.00132190172209248));
#48018=CARTESIAN_POINT('Origin',(-54.75,0.,0.));
#48019=CARTESIAN_POINT('',(-16.6628364779652,-3.93375005137208,0.00358326100158749));
#48020=CARTESIAN_POINT('',(-16.8461635220349,-3.93309862886983,0.00362758403216595));
#48021=CARTESIAN_POINT('',(-54.75,-3.933,-4.81653586104654E-16));
#48022=CARTESIAN_POINT('Ctrl Pts',(-16.6628364779652,-3.93375005137208,
0.00358326100158748));
#48023=CARTESIAN_POINT('Ctrl Pts',(-16.6770165395055,-3.93635487154669,
0.283691000235229));
#48024=CARTESIAN_POINT('Ctrl Pts',(-16.6911966010458,-3.90899307237427,
0.563293683724424));
#48025=CARTESIAN_POINT('Ctrl Pts',(-16.7053766625861,-3.84977929252528,
0.83597970849176));
#48026=CARTESIAN_POINT('Ctrl Pts',(-16.7716678398186,-3.57295742095455,
2.11077513482312));
#48027=CARTESIAN_POINT('Ctrl Pts',(-16.8379590170511,-2.60000342548255,
3.23440544601643));
#48028=CARTESIAN_POINT('Ctrl Pts',(-16.9042501942836,-1.37789337049898,
3.69067372354986));
#48029=CARTESIAN_POINT('Ctrl Pts',(-16.9705413715161,-0.155783315515329,
4.14694200108332));
#48030=CARTESIAN_POINT('Ctrl Pts',(-17.0368325487485,1.31548279897993,3.93584824495684));
#48031=CARTESIAN_POINT('Ctrl Pts',(-17.103123725981,2.3600038095325,3.15436914345143));
#48032=CARTESIAN_POINT('Ctrl Pts',(-17.1694149032135,3.40452482008502,2.37289004194606));
#48033=CARTESIAN_POINT('Ctrl Pts',(-17.235706080446,4.0223007266949,1.02102559506183));
#48034=CARTESIAN_POINT('Ctrl Pts',(-17.3019972576785,3.92952464363444,-0.280176282429607));
#48035=CARTESIAN_POINT('Ctrl Pts',(-17.368288434911,3.83674856057397,-1.58137815992119));
#48036=CARTESIAN_POINT('Ctrl Pts',(-17.4345796121435,3.03342048784297,-2.83191746801997));
#48037=CARTESIAN_POINT('Ctrl Pts',(-17.500870789376,1.88859016677985,-3.45729516473628));
#48038=CARTESIAN_POINT('Ctrl Pts',(-17.5671619666084,0.743759845716805,
-4.08267286145256));
#48039=CARTESIAN_POINT('Ctrl Pts',(-17.6334531438409,-0.742572723678316,
-4.08288894678644));
#48040=CARTESIAN_POINT('Ctrl Pts',(-17.6997443210734,-1.88758483310244,
-3.4578441509137));
#48041=CARTESIAN_POINT('Ctrl Pts',(-17.7660354983059,-3.03259694252663,
-2.83279935504092));
#48042=CARTESIAN_POINT('Ctrl Pts',(-17.8323266755384,-3.83628859197978,
-1.58249367796145));
#48043=CARTESIAN_POINT('Ctrl Pts',(-17.8986178527708,-3.92944301260406,
-0.281318831334825));
#48044=CARTESIAN_POINT('Ctrl Pts',(-17.9033573945023,-3.93610316381045,
-0.188290275455156));
#48045=CARTESIAN_POINT('Ctrl Pts',(-17.9080969362338,-3.93913129629941,
-0.0950016941068158));
#48046=CARTESIAN_POINT('Ctrl Pts',(-17.9128364779652,-3.93863106461684,
-0.00168008665984931));
#48047=CARTESIAN_POINT('Ctrl Pts',(-18.0961635220349,-3.93896517016805,
-0.00132190172209248));
#48048=CARTESIAN_POINT('Ctrl Pts',(-18.0925008210803,-3.93927939230012,
-0.0734242577495321));
#48049=CARTESIAN_POINT('Ctrl Pts',(-18.0888381201258,-3.93747181923847,
-0.145510539624574));
#48050=CARTESIAN_POINT('Ctrl Pts',(-18.0851754191713,-3.93349291696148,
-0.217476772047698));
#48051=CARTESIAN_POINT('Ctrl Pts',(-18.0188842419388,-3.86147881608094,
-1.5199926824495));
#48052=CARTESIAN_POINT('Ctrl Pts',(-17.9525930647063,-3.07819516685206,
-2.78318359374845));
#48053=CARTESIAN_POINT('Ctrl Pts',(-17.8863018874738,-1.943483281878,-3.42673830445617));
#48054=CARTESIAN_POINT('Ctrl Pts',(-17.8200107102413,-0.808771396903944,
-4.07029301516389));
#48055=CARTESIAN_POINT('Ctrl Pts',(-17.7537195330088,0.677368723815286,
-4.09421152528039));
#48056=CARTESIAN_POINT('Ctrl Pts',(-17.6874283557764,1.83220278309591,-3.48750564670253));
#48057=CARTESIAN_POINT('Ctrl Pts',(-17.6211371785439,2.98703684237646,-2.88079976812471));
#48058=CARTESIAN_POINT('Ctrl Pts',(-17.5548460013114,3.81056484021844,-1.64346950085261));
#48059=CARTESIAN_POINT('Ctrl Pts',(-17.4885548240789,3.92445716894955,-0.343945639959133));
#48060=CARTESIAN_POINT('Ctrl Pts',(-17.4222636468464,4.03834949768068,0.955578220934493));
#48061=CARTESIAN_POINT('Ctrl Pts',(-17.3559724696139,3.44260615730077,2.31729567544951));
#48062=CARTESIAN_POINT('Ctrl Pts',(-17.2896812923815,2.4109122499921,3.11563232699311));
#48063=CARTESIAN_POINT('Ctrl Pts',(-17.223390115149,1.37921834268355,3.91396897853661));
#48064=CARTESIAN_POINT('Ctrl Pts',(-17.1570989379165,-0.0884261315536491,
4.14892482710885));
#48065=CARTESIAN_POINT('Ctrl Pts',(-17.090807760684,-1.31778379451791,3.71256091466152));
#48066=CARTESIAN_POINT('Ctrl Pts',(-17.0245165834515,-2.54714145748224,
3.27619700221418));
#48067=CARTESIAN_POINT('Ctrl Pts',(-16.9582254062191,-3.53821230917362,
2.1685133287472));
#48068=CARTESIAN_POINT('Ctrl Pts',(-16.8919342289866,-3.83569738285571,
0.898380911039564));
#48069=CARTESIAN_POINT('Ctrl Pts',(-16.8766773266693,-3.90416351816185,
0.606060167376271));
#48070=CARTESIAN_POINT('Ctrl Pts',(-16.8614204243521,-3.93589115117029,
0.305134686198502));
#48071=CARTESIAN_POINT('Ctrl Pts',(-16.8461635220349,-3.93309862886983,
0.00362758403216595));
#48072=CARTESIAN_POINT('Origin',(-54.75,0.,0.));
#48073=CARTESIAN_POINT('',(-15.4128364779652,-3.9264779963057,1.50935765152131E-5));
#48074=CARTESIAN_POINT('',(-15.5961635220349,-3.92650423935062,-0.000338343577294592));
#48075=CARTESIAN_POINT('',(-54.75,-3.933,-4.81653586104654E-16));
#48076=CARTESIAN_POINT('Ctrl Pts',(-15.4128364779652,-3.92647818587147,
1.50931378117836E-5));
#48077=CARTESIAN_POINT('Ctrl Pts',(-15.4459361427773,-3.92650057953867,
0.6569171123658));
#48078=CARTESIAN_POINT('Ctrl Pts',(-15.4790358075893,-3.77065293631031,
1.31380914345544));
#48079=CARTESIAN_POINT('Ctrl Pts',(-15.5121354724014,-3.45887639344497,
1.88569264967426));
#48080=CARTESIAN_POINT('Ctrl Pts',(-15.5784266496339,-2.8344581651224,3.03104657039658));
#48081=CARTESIAN_POINT('Ctrl Pts',(-15.6447178268664,-1.58459240146811,
3.83542218314378));
#48082=CARTESIAN_POINT('Ctrl Pts',(-15.7110090040989,-0.283468717462426,
3.92928850561862));
#48083=CARTESIAN_POINT('Ctrl Pts',(-15.7773001813313,1.01765496654326,4.02315482809346));
#48084=CARTESIAN_POINT('Ctrl Pts',(-15.8435913585638,2.37003657090034,3.40651186029594));
#48085=CARTESIAN_POINT('Ctrl Pts',(-15.9098825357963,3.15239059816314,2.36264601470027));
#48086=CARTESIAN_POINT('Ctrl Pts',(-15.9761737130288,3.93474462542595,1.31878016910461));
#48087=CARTESIAN_POINT('Ctrl Pts',(-16.0424648902613,4.14707107559447,-0.152308554289197));
#48088=CARTESIAN_POINT('Ctrl Pts',(-16.1087560674938,3.69182695947925,-1.37480048568096));
#48089=CARTESIAN_POINT('Ctrl Pts',(-16.1750472447262,3.23658284336407,-2.59729241707265));
#48090=CARTESIAN_POINT('Ctrl Pts',(-16.2413384219587,2.11376816096522,-3.57118755646233));
#48091=CARTESIAN_POINT('Ctrl Pts',(-16.3076295991912,0.839205130099,-3.84907747697835));
#48092=CARTESIAN_POINT('Ctrl Pts',(-16.3739207764237,-0.435357900767366,
-4.12696739749439));
#48093=CARTESIAN_POINT('Ctrl Pts',(-16.4402119536562,-1.86166928010115,
-3.70885209913657));
#48094=CARTESIAN_POINT('Ctrl Pts',(-16.5065031308887,-2.78448009593333,
-2.78681417922285));
#48095=CARTESIAN_POINT('Ctrl Pts',(-16.5586142465808,-3.5098964061186,-2.06200543810343));
#48096=CARTESIAN_POINT('Ctrl Pts',(-16.610725362273,-3.92417744937094,-1.02580062171259));
#48097=CARTESIAN_POINT('Ctrl Pts',(-16.6628364779652,-3.93375005137208,
0.00358326100158748));
#48098=CARTESIAN_POINT('Ctrl Pts',(-16.8461635220349,-3.93309862886983,
0.00362758403216595));
#48099=CARTESIAN_POINT('Ctrl Pts',(-16.7951292471196,-3.92375765336736,
-1.0049124210695));
#48100=CARTESIAN_POINT('Ctrl Pts',(-16.7440949722044,-3.52817075580835,
-2.01996018179993));
#48101=CARTESIAN_POINT('Ctrl Pts',(-16.6930606972891,-2.8293643400936,-2.74123331826628));
#48102=CARTESIAN_POINT('Ctrl Pts',(-16.6267695200566,-1.92164692797642,
-3.67813396791647));
#48103=CARTESIAN_POINT('Ctrl Pts',(-16.5604783428241,-0.502312808069129,
-4.11935410526842));
#48104=CARTESIAN_POINT('Ctrl Pts',(-16.4941871655917,0.77659446780288,-3.86219674625004));
#48105=CARTESIAN_POINT('Ctrl Pts',(-16.4278959883592,2.05550174367482,-3.60503938723167));
#48106=CARTESIAN_POINT('Ctrl Pts',(-16.3616048111267,3.19398217551149,-2.64950453184305));
#48107=CARTESIAN_POINT('Ctrl Pts',(-16.2953136338942,3.6690166841218,-1.43456587363645));
#48108=CARTESIAN_POINT('Ctrl Pts',(-16.2290224566617,4.14405119273209,-0.219627215429928));
#48109=CARTESIAN_POINT('Ctrl Pts',(-16.1627312794292,3.95563977811609,1.25471524559453));
#48110=CARTESIAN_POINT('Ctrl Pts',(-16.0964401021967,3.19033883757841,2.31114706922889));
#48111=CARTESIAN_POINT('Ctrl Pts',(-16.0301489249643,2.42503789704064,3.36757889286337));
#48112=CARTESIAN_POINT('Ctrl Pts',(-15.9638577477318,1.08284743058101,4.00610007910764));
#48113=CARTESIAN_POINT('Ctrl Pts',(-15.8975665704993,-0.219628883567405,
3.93337333947203));
#48114=CARTESIAN_POINT('Ctrl Pts',(-15.8312753932668,-1.52210519771575,
3.86064659983643));
#48115=CARTESIAN_POINT('Ctrl Pts',(-15.7649842160343,-2.78486735955289,
3.07667193432105));
#48116=CARTESIAN_POINT('Ctrl Pts',(-15.6986930388018,-3.42780113553339,
1.94160810912049));
#48117=CARTESIAN_POINT('Ctrl Pts',(-15.6645165332128,-3.75926650853602,
1.3564244272893));
#48118=CARTESIAN_POINT('Ctrl Pts',(-15.6303400276238,-3.92598571797408,
0.677923637937626));
#48119=CARTESIAN_POINT('Ctrl Pts',(-15.5961635220349,-3.92650423935062,
-0.000338343577294592));
#48120=CARTESIAN_POINT('Origin',(-54.75,0.,0.));
#48121=CARTESIAN_POINT('',(-14.1628364779652,-3.93369446688928,-0.00358851098580137));
#48122=CARTESIAN_POINT('',(-14.3461635220349,-3.93434458032143,-0.00350973384803158));
#48123=CARTESIAN_POINT('',(-54.75,-3.933,-4.81653586104654E-16));
#48124=CARTESIAN_POINT('Ctrl Pts',(-14.1628364779652,-3.93369446688928,
-0.00358851098580137));
#48125=CARTESIAN_POINT('Ctrl Pts',(-14.214855746049,-3.92413817277373,1.02401828417443));
#48126=CARTESIAN_POINT('Ctrl Pts',(-14.2668750141329,-3.5114721763875,2.05842142212482));
#48127=CARTESIAN_POINT('Ctrl Pts',(-14.3188942822167,-2.78833724325426,
2.78295492095141));
#48128=CARTESIAN_POINT('Ctrl Pts',(-14.3851854594492,-1.86680436166715,
3.70627007610107));
#48129=CARTESIAN_POINT('Ctrl Pts',(-14.4514766366817,-0.441073452138983,
4.12636045584482));
#48130=CARTESIAN_POINT('Ctrl Pts',(-14.5177678139141,0.833873241785975,
3.85023610844839));
#48131=CARTESIAN_POINT('Ctrl Pts',(-14.5840589911466,2.10881993571108,3.57411176105193));
#48132=CARTESIAN_POINT('Ctrl Pts',(-14.6503501683791,3.23298241403293,2.60177268651509));
#48133=CARTESIAN_POINT('Ctrl Pts',(-14.7166413456116,3.68991928010443,1.37991245391873));
#48134=CARTESIAN_POINT('Ctrl Pts',(-14.7829325228441,4.14685614617589,0.158052221322513));
#48135=CARTESIAN_POINT('Ctrl Pts',(-14.8492237000766,3.93656739999716,-1.31332916933317));
#48136=CARTESIAN_POINT('Ctrl Pts',(-14.915514877309,3.1556599074528,-2.35827759660763));
#48137=CARTESIAN_POINT('Ctrl Pts',(-14.9818060545415,2.37475241490839,-3.40322602388214));
#48138=CARTESIAN_POINT('Ctrl Pts',(-15.048097231774,1.02322617599829,-4.02174148777539));
#48139=CARTESIAN_POINT('Ctrl Pts',(-15.1143884090065,-0.278026267596332,
-3.9296773491844));
#48140=CARTESIAN_POINT('Ctrl Pts',(-15.180679586239,-1.57927871119088,-3.8376132105934));
#48141=CARTESIAN_POINT('Ctrl Pts',(-15.2469707634715,-2.83025735946995,
-3.03496946951824));
#48142=CARTESIAN_POINT('Ctrl Pts',(-15.3132619407039,-3.45626133711414,
-1.89048148463201));
#48143=CARTESIAN_POINT('Ctrl Pts',(-15.3464534531244,-3.76969699577422,
-1.31744463793124));
#48144=CARTESIAN_POINT('Ctrl Pts',(-15.3796449655448,-3.92645573006452,
-0.658709750573194));
#48145=CARTESIAN_POINT('Ctrl Pts',(-15.4128364779652,-3.92647818587147,
1.50931378117836E-5));
#48146=CARTESIAN_POINT('Ctrl Pts',(-15.5961635220349,-3.92650423935062,
-0.000338343577294592));
#48147=CARTESIAN_POINT('Ctrl Pts',(-15.5640488503914,-3.92699147885803,
-0.637681467142005));
#48148=CARTESIAN_POINT('Ctrl Pts',(-15.5319341787479,-3.78072656664845,
-1.27481372777769));
#48149=CARTESIAN_POINT('Ctrl Pts',(-15.4998195071044,-3.48650266596134,
-1.83411063854145));
#48150=CARTESIAN_POINT('Ctrl Pts',(-15.4335283298719,-2.87916503028493,
-2.98861257611725));
#48151=CARTESIAN_POINT('Ctrl Pts',(-15.3672371526394,-1.64138436880819,
-3.8114634663832));
#48152=CARTESIAN_POINT('Ctrl Pts',(-15.3009459754069,-0.341798388164035,
-3.9246447655826));
#48153=CARTESIAN_POINT('Ctrl Pts',(-15.2346547981745,0.957787592480191,
-4.03782606478201));
#48154=CARTESIAN_POINT('Ctrl Pts',(-15.168363620942,2.31917889229184,-3.44133777291475));
#48155=CARTESIAN_POINT('Ctrl Pts',(-15.1020724437095,3.11695095048374,-2.4092072236412));
#48156=CARTESIAN_POINT('Ctrl Pts',(-15.035781266477,3.91472300867565,-1.37707667436765));
#48157=CARTESIAN_POINT('Ctrl Pts',(-14.9694900892445,4.14887582524779,0.0906961323124485));
#48158=CARTESIAN_POINT('Ctrl Pts',(-14.903198912012,3.71183935587708,1.31981486214107));
#48159=CARTESIAN_POINT('Ctrl Pts',(-14.8369077347795,3.27480288650638,2.54893359196969));
#48160=CARTESIAN_POINT('Ctrl Pts',(-14.7706165575471,2.16657713119312,3.53939824494685));
#48161=CARTESIAN_POINT('Ctrl Pts',(-14.7043253803146,0.896282139672688,
3.83618834264823));
#48162=CARTESIAN_POINT('Ctrl Pts',(-14.6380342030821,-0.374012851847812,
4.13297844034962));
#48163=CARTESIAN_POINT('Ctrl Pts',(-14.5717430258496,-1.80637707957535,
3.73609398277492));
#48164=CARTESIAN_POINT('Ctrl Pts',(-14.5054518486171,-2.74278094677474,
2.82786409718994));
#48165=CARTESIAN_POINT('Ctrl Pts',(-14.4523557397564,-3.49279631452224,
2.10041476096114));
#48166=CARTESIAN_POINT('Ctrl Pts',(-14.3992596308956,-3.9246404616156,1.04492429089517));
#48167=CARTESIAN_POINT('Ctrl Pts',(-14.3461635220349,-3.93434458032143,
-0.00350973384803158));
#48168=CARTESIAN_POINT('Origin',(-54.75,0.,0.));
#48169=CARTESIAN_POINT('',(-12.9128364779652,-3.93866223418523,0.00165032853560287));
#48170=CARTESIAN_POINT('',(-13.0961635220349,-3.93826781928793,0.00198880647917068));
#48171=CARTESIAN_POINT('',(-54.75,-3.933,-4.81653586104654E-16));
#48172=CARTESIAN_POINT('Ctrl Pts',(-12.9128364779652,-3.93866223418523,
0.00165032853560287));
#48173=CARTESIAN_POINT('Ctrl Pts',(-12.9174841720883,-3.93914537757192,
0.0931615357668376));
#48174=CARTESIAN_POINT('Ctrl Pts',(-12.9221318662114,-3.93623360589491,
0.18464145637103));
#48175=CARTESIAN_POINT('Ctrl Pts',(-12.9267795603345,-3.92982887836725,
0.275876169534834));
#48176=CARTESIAN_POINT('Ctrl Pts',(-12.993070737567,-3.83847671180549,1.57717878969641));
#48177=CARTESIAN_POINT('Ctrl Pts',(-13.0593619147995,-3.03651754266122,
2.82859640366949));
#48178=CARTESIAN_POINT('Ctrl Pts',(-13.1256530920319,-1.8923722365596,3.45522647484428));
#48179=CARTESIAN_POINT('Ctrl Pts',(-13.1919442692644,-0.748226930457651,
4.08185654601926));
#48180=CARTESIAN_POINT('Ctrl Pts',(-13.2582354464969,0.738104512601858,
4.08369907439556));
#48181=CARTESIAN_POINT('Ctrl Pts',(-13.3245266237294,1.88379990175547,3.4599076005455));
#48182=CARTESIAN_POINT('Ctrl Pts',(-13.3908178009619,3.02949529090888,2.83611612669555));
#48183=CARTESIAN_POINT('Ctrl Pts',(-13.4571089781944,3.83455462615653,1.58669065061949));
#48184=CARTESIAN_POINT('Ctrl Pts',(-13.5234001554269,3.92913282238253,0.285618518732132));
#48185=CARTESIAN_POINT('Ctrl Pts',(-13.5896913326594,4.02371101860855,-1.01545361315538));
#48186=CARTESIAN_POINT('Ctrl Pts',(-13.6559825098918,3.40780807581275,-2.3681724008542));
#48187=CARTESIAN_POINT('Ctrl Pts',(-13.7222736871243,2.36437043822387,-3.15109744454523));
#48188=CARTESIAN_POINT('Ctrl Pts',(-13.7885648643568,1.32093280063517,-3.93402248823613));
#48189=CARTESIAN_POINT('Ctrl Pts',(-13.8548560415893,-0.150039531746455,
-4.14715378791947));
#48190=CARTESIAN_POINT('Ctrl Pts',(-13.9211472188218,-1.37278035927145,
-3.69257860571241));
#48191=CARTESIAN_POINT('Ctrl Pts',(-13.9874383960543,-2.59552118679665,
-3.23800342350527));
#48192=CARTESIAN_POINT('Ctrl Pts',(-14.0537295732867,-3.57003050946513,
-2.11572175940747));
#48193=CARTESIAN_POINT('Ctrl Pts',(-14.1200207505192,-3.84861774397631,
-0.841310962080693));
#48194=CARTESIAN_POINT('Ctrl Pts',(-14.1342926596679,-3.90859513262605,
-0.566941492765959));
#48195=CARTESIAN_POINT('Ctrl Pts',(-14.1485645688166,-3.93631631387865,
-0.28552079033751));
#48196=CARTESIAN_POINT('Ctrl Pts',(-14.1628364779652,-3.93369446688928,
-0.00358851098580137));
#48197=CARTESIAN_POINT('Ctrl Pts',(-14.3461635220349,-3.93434458032143,
-0.00350973384803158));
#48198=CARTESIAN_POINT('Ctrl Pts',(-14.3329684536631,-3.93675617907242,
-0.264059121299957));
#48199=CARTESIAN_POINT('Ctrl Pts',(-14.3197733852914,-3.91309697321702,
-0.524172712108927));
#48200=CARTESIAN_POINT('Ctrl Pts',(-14.3065783169196,-3.86177126764843,
-0.778707487142311));
#48201=CARTESIAN_POINT('Ctrl Pts',(-14.2402871396872,-3.60391421465153,
-2.05747387229453));
#48202=CARTESIAN_POINT('Ctrl Pts',(-14.1739959624547,-2.64775660198649,
-3.19543132900379));
#48203=CARTESIAN_POINT('Ctrl Pts',(-14.1077047852222,-1.4325582185377,-3.66980103338948));
#48204=CARTESIAN_POINT('Ctrl Pts',(-14.0414136079897,-0.217359835088917,
-4.14417073777518));
#48205=CARTESIAN_POINT('Ctrl Pts',(-13.9751224307572,1.25687931914355,-3.95495268983729));
#48206=CARTESIAN_POINT('Ctrl Pts',(-13.9088312535247,2.31289226319796,-3.18907385505658));
#48207=CARTESIAN_POINT('Ctrl Pts',(-13.8425400762923,3.36890520725237,-2.42319502027587));
#48208=CARTESIAN_POINT('Ctrl Pts',(-13.7762488990598,4.00669194112866,-1.08065539865238));
#48209=CARTESIAN_POINT('Ctrl Pts',(-13.7099577218273,3.93325258450909,0.221780929340192));
#48210=CARTESIAN_POINT('Ctrl Pts',(-13.6436665445948,3.85981322788952,1.52421725733269));
#48211=CARTESIAN_POINT('Ctrl Pts',(-13.5773753673623,3.07514778077402,2.78655029169444));
#48212=CARTESIAN_POINT('Ctrl Pts',(-13.5110841901298,1.9397323551336,3.4288629404825));
#48213=CARTESIAN_POINT('Ctrl Pts',(-13.4447930128974,0.804316929493125,
4.07117558927059));
#48214=CARTESIAN_POINT('Ctrl Pts',(-13.3785018356649,-0.681848474672325,
4.0934678524851));
#48215=CARTESIAN_POINT('Ctrl Pts',(-13.3122106584324,-1.83601794493788,
3.48549864151925));
#48216=CARTESIAN_POINT('Ctrl Pts',(-13.2459194811999,-2.99018741520344,
2.87752943055339));
#48217=CARTESIAN_POINT('Ctrl Pts',(-13.1796283039674,-3.81236095156904,
1.63929874540721));
#48218=CARTESIAN_POINT('Ctrl Pts',(-13.1133371267349,-3.92483118735515,
0.339651034049346));
#48219=CARTESIAN_POINT('Ctrl Pts',(-13.1076125918349,-3.93454348719428,
0.227420734453008));
#48220=CARTESIAN_POINT('Ctrl Pts',(-13.1018880569349,-3.93896347092205,
0.114732443021119));
#48221=CARTESIAN_POINT('Ctrl Pts',(-13.0961635220349,-3.93826781928793,
0.00198880647917068));
#48222=CARTESIAN_POINT('Origin',(-54.75,0.,0.));
#48223=CARTESIAN_POINT('',(-11.6628364779652,-3.92862917326101,0.00277744209242731));
#48224=CARTESIAN_POINT('',(-11.8461635220349,-3.92818995496044,0.00253348489050703));
#48225=CARTESIAN_POINT('',(-54.75,-3.933,-4.81653586104654E-16));
#48226=CARTESIAN_POINT('Ctrl Pts',(-11.6628364779652,-3.92862917326101,
0.00277744209242731));
#48227=CARTESIAN_POINT('Ctrl Pts',(-11.6864037753601,-3.93165944827161,
0.469857995963653));
#48228=CARTESIAN_POINT('Ctrl Pts',(-11.7099710727549,-3.8546981368583,0.93597264351165));
#48229=CARTESIAN_POINT('Ctrl Pts',(-11.7335383701498,-3.69332914655501,
1.37075982191401));
#48230=CARTESIAN_POINT('Ctrl Pts',(-11.7998295473823,-3.23942303433508,
2.59374917953944));
#48231=CARTESIAN_POINT('Ctrl Pts',(-11.8661207246148,-2.11767472449869,
3.5688723937627));
#48232=CARTESIAN_POINT('Ctrl Pts',(-11.9324119018472,-0.843416542212277,
3.84815685887272));
#48233=CARTESIAN_POINT('Ctrl Pts',(-11.9987030790797,0.430841640074067,
4.12744132398272));
#48234=CARTESIAN_POINT('Ctrl Pts',(-12.0649942563122,1.85760969481043,3.71088703997956));
#48235=CARTESIAN_POINT('Ctrl Pts',(-12.1312854335447,2.78142891287907,2.78985947258402));
#48236=CARTESIAN_POINT('Ctrl Pts',(-12.1975766107772,3.70524813094765,1.86883190518855));
#48237=CARTESIAN_POINT('Ctrl Pts',(-12.2638677880097,4.12611851234857,0.443331054400757));
#48238=CARTESIAN_POINT('Ctrl Pts',(-12.3301589652421,3.85069177178547,-0.831766525456592));
#48239=CARTESIAN_POINT('Ctrl Pts',(-12.3964501424746,3.57526503122234,-2.10686410531409));
#48240=CARTESIAN_POINT('Ctrl Pts',(-12.4627413197071,2.60354116869499,-3.2315584142411));
#48241=CARTESIAN_POINT('Ctrl Pts',(-12.5290324969396,1.38193112425552,-3.68916373206453));
#48242=CARTESIAN_POINT('Ctrl Pts',(-12.5953236741721,0.160321079816128,
-4.14676904988794));
#48243=CARTESIAN_POINT('Ctrl Pts',(-12.6616148514046,-1.31117514653535,
-3.93728537660784));
#48244=CARTESIAN_POINT('Ctrl Pts',(-12.7279060286371,-2.35655067772163,
-3.15694972679265));
#48245=CARTESIAN_POINT('Ctrl Pts',(-12.7895495117465,-3.32863461995813,
-2.43132364113208));
#48246=CARTESIAN_POINT('Ctrl Pts',(-12.8511929948558,-3.93225418744031,
-1.2120847856676));
#48247=CARTESIAN_POINT('Ctrl Pts',(-12.9128364779652,-3.93866223418523,
0.00165032853560287));
#48248=CARTESIAN_POINT('Ctrl Pts',(-13.0961635220349,-3.93826781928793,
0.00198880647917068));
#48249=CARTESIAN_POINT('Ctrl Pts',(-13.0355968797024,-3.93090769581103,
-1.19085980549745));
#48250=CARTESIAN_POINT('Ctrl Pts',(-12.9750302373699,-3.35090166376052,
-2.38990376733619));
#48251=CARTESIAN_POINT('Ctrl Pts',(-12.9144635950375,-2.40750147608245,
-3.11826864090111));
#48252=CARTESIAN_POINT('Ctrl Pts',(-12.848172417805,-1.37493459381688,-3.91547586692441));
#48253=CARTESIAN_POINT('Ctrl Pts',(-12.7818812405725,0.0929661059210794,
-4.14882558140152));
#48254=CARTESIAN_POINT('Ctrl Pts',(-12.71559006334,1.32184553467154,-3.71111668593637));
#48255=CARTESIAN_POINT('Ctrl Pts',(-12.6492988861076,2.55072496342201,-3.27340779047122));
#48256=CARTESIAN_POINT('Ctrl Pts',(-12.5830077088751,3.540583121185,-2.16464028506394));
#48257=CARTESIAN_POINT('Ctrl Pts',(-12.5167165316426,3.83667815406009,-0.894183099999397));
#48258=CARTESIAN_POINT('Ctrl Pts',(-12.4504253544101,4.13277318693521,0.376274085065291));
#48259=CARTESIAN_POINT('Ctrl Pts',(-12.3841341771776,3.73510509492216,1.80842094978705));
#48260=CARTESIAN_POINT('Ctrl Pts',(-12.3178429999451,2.82636300775224,2.74432775421889));
#48261=CARTESIAN_POINT('Ctrl Pts',(-12.2515518227126,1.91762092058248,3.68023455865058));
#48262=CARTESIAN_POINT('Ctrl Pts',(-12.1852606454802,0.497804838255918,
4.11990130279241));
#48263=CARTESIAN_POINT('Ctrl Pts',(-12.1189694682477,-0.780820273371836,
3.86134463300778));
#48264=CARTESIAN_POINT('Ctrl Pts',(-12.0526782910152,-2.05944538499966,
3.60278796322313));
#48265=CARTESIAN_POINT('Ctrl Pts',(-11.9863871137827,-3.19687952592881,
2.64600787951188));
#48266=CARTESIAN_POINT('Ctrl Pts',(-11.9200959365502,-3.67058428408519,
1.43055013459624));
#48267=CARTESIAN_POINT('Ctrl Pts',(-11.8954517983784,-3.8466868364911,0.978696511562696));
#48268=CARTESIAN_POINT('Ctrl Pts',(-11.8708076602067,-3.93106034832633,
0.491092996637599));
#48269=CARTESIAN_POINT('Ctrl Pts',(-11.8461635220349,-3.92818995496044,
0.00253348489050703));
#48270=CARTESIAN_POINT('Origin',(-54.75,0.,0.));
#48271=CARTESIAN_POINT('',(-10.4128364779653,-3.92852884447977,-0.00272592851332826));
#48272=CARTESIAN_POINT('',(-10.5961635220349,-3.92900062987189,-0.00294957216901129));
#48273=CARTESIAN_POINT('',(-54.75,-3.933,-4.81653586104654E-16));
#48274=CARTESIAN_POINT('Ctrl Pts',(-10.4128364779653,-3.92852884447977,
-0.00272592851332826));
#48275=CARTESIAN_POINT('Ctrl Pts',(-10.4553233786319,-3.92317581591888,
0.839376464306679));
#48276=CARTESIAN_POINT('Ctrl Pts',(-10.4978102792985,-3.6579994874255,1.68455438064328));
#48277=CARTESIAN_POINT('Ctrl Pts',(-10.5402971799651,-3.15823860108501,
2.35482305339129));
#48278=CARTESIAN_POINT('Ctrl Pts',(-10.6065883571976,-2.37847502759617,
3.40062537555125));
#48279=CARTESIAN_POINT('Ctrl Pts',(-10.67287953443,-1.02762641829007,4.02061939832335));
#48280=CARTESIAN_POINT('Ctrl Pts',(-10.7391707116625,0.273725988887863,
3.92997923113772));
#48281=CARTESIAN_POINT('Ctrl Pts',(-10.805461888895,1.57507839606587,3.83933906395208));
#48282=CARTESIAN_POINT('Ctrl Pts',(-10.8717530661275,2.82693460111579,3.03806470680862));
#48283=CARTESIAN_POINT('Ctrl Pts',(-10.93804424336,3.45419057823663,1.89426242199642));
#48284=CARTESIAN_POINT('Ctrl Pts',(-11.0043354205925,4.0814465553575,0.750460137184154));
#48285=CARTESIAN_POINT('Ctrl Pts',(-11.0706265978249,4.0841023045493,-0.735870075296754));
#48286=CARTESIAN_POINT('Ctrl Pts',(-11.1369177750574,3.4609377719068,-1.88190658991227));
#48287=CARTESIAN_POINT('Ctrl Pts',(-11.2032089522899,2.83777323926437,-3.02794310452766));
#48288=CARTESIAN_POINT('Ctrl Pts',(-11.2695001295224,1.58878842478775,-3.83368592127761));
#48289=CARTESIAN_POINT('Ctrl Pts',(-11.3357913067549,0.287768234500619,
-3.92897596294236));
#48290=CARTESIAN_POINT('Ctrl Pts',(-11.4020824839874,-1.01325195578666,
-4.02426600460712));
#48291=CARTESIAN_POINT('Ctrl Pts',(-11.4683736612199,-2.36630752188455,
-3.40910327118653));
#48292=CARTESIAN_POINT('Ctrl Pts',(-11.5346648384523,-3.1498033476316,-2.36609415396244));
#48293=CARTESIAN_POINT('Ctrl Pts',(-11.57738871829,-3.65475714254024,-1.69388711142402));
#48294=CARTESIAN_POINT('Ctrl Pts',(-11.6201125981276,-3.92313575145455,
-0.843967652339101));
#48295=CARTESIAN_POINT('Ctrl Pts',(-11.6628364779652,-3.92862917326101,
0.00277744209242731));
#48296=CARTESIAN_POINT('Ctrl Pts',(-11.8461635220349,-3.92818995496044,
0.00253348489050703));
#48297=CARTESIAN_POINT('Ctrl Pts',(-11.8045164829742,-3.92333917122454,
-0.823101273662933));
#48298=CARTESIAN_POINT('Ctrl Pts',(-11.7628694439135,-3.66932966957637,
-1.65146625092852));
#48299=CARTESIAN_POINT('Ctrl Pts',(-11.7212224048528,-3.18780791787102,
-2.31463676479168));
#48300=CARTESIAN_POINT('Ctrl Pts',(-11.6549312276203,-2.4213514181168,-3.37023051314387));
#48301=CARTESIAN_POINT('Ctrl Pts',(-11.5886400503878,-1.07846304322473,
-4.00728260372794));
#48302=CARTESIAN_POINT('Ctrl Pts',(-11.5223488731553,0.22393290872183,-3.9331306521088));
#48303=CARTESIAN_POINT('Ctrl Pts',(-11.4560576959228,1.52632886066824,-3.85897870048967));
#48304=CARTESIAN_POINT('Ctrl Pts',(-11.3897665186903,2.78823238966908,-3.07362270666749));
#48305=CARTESIAN_POINT('Ctrl Pts',(-11.3234753414579,3.42992371898552,-1.93785602047907));
#48306=CARTESIAN_POINT('Ctrl Pts',(-11.2571841642254,4.071615048302,-0.802089334290585));
#48307=CARTESIAN_POINT('Ctrl Pts',(-11.1908929869929,4.09309417793392,0.684088044264345));
#48308=CARTESIAN_POINT('Ctrl Pts',(-11.1246018097604,3.48449357367713,1.83792470171366));
#48309=CARTESIAN_POINT('Ctrl Pts',(-11.0583106325279,2.87589296942037,2.99176135916291));
#48310=CARTESIAN_POINT('Ctrl Pts',(-10.9920194552954,1.63721263127506,3.81325729550672));
#48311=CARTESIAN_POINT('Ctrl Pts',(-10.925728278063,0.337503578259211,3.92501643421129));
#48312=CARTESIAN_POINT('Ctrl Pts',(-10.8594371008305,-0.962205474756632,
4.03677557291586));
#48313=CARTESIAN_POINT('Ctrl Pts',(-10.793145923598,-2.32294324264293,3.43879791398117));
#48314=CARTESIAN_POINT('Ctrl Pts',(-10.7268547463655,-3.11958539785007,
2.40579500782736));
#48315=CARTESIAN_POINT('Ctrl Pts',(-10.683291004922,-3.64310473060778,1.72694944507178));
#48316=CARTESIAN_POINT('Ctrl Pts',(-10.6397272634784,-3.92301603181814,
0.860235652593407));
#48317=CARTESIAN_POINT('Ctrl Pts',(-10.5961635220349,-3.92900062987189,
-0.00294957216901129));
#48318=CARTESIAN_POINT('Origin',(-54.75,0.,0.));
#48319=CARTESIAN_POINT('',(-9.16283647796523,-3.93858084194566,-0.00172678509975766));
#48320=CARTESIAN_POINT('',(-9.34616352203489,-3.93892425866043,-0.00137129965302642));
#48321=CARTESIAN_POINT('',(-54.75,-3.933,-4.81653586104654E-16));
#48322=CARTESIAN_POINT('Ctrl Pts',(-9.16283647796523,-3.93858084194566,
-0.00172678509975766));
#48323=CARTESIAN_POINT('Ctrl Pts',(-9.22424298190359,-3.93194753706968,
1.20740853644141));
#48324=CARTESIAN_POINT('Ctrl Pts',(-9.28564948584196,-3.33357479351524,
2.42221595869824));
#48325=CARTESIAN_POINT('Ctrl Pts',(-9.34705598978033,-2.36781716140013,
3.1485083078095));
#48326=CARTESIAN_POINT('Ctrl Pts',(-9.41334716701282,-1.32523687677053,
3.93257468106957));
#48327=CARTESIAN_POINT('Ctrl Pts',(-9.4796383442453,0.145501352595422,4.14731548813625));
#48328=CARTESIAN_POINT('Ctrl Pts',(-9.54592952147779,1.36873887421348,3.69407858178237));
#48329=CARTESIAN_POINT('Ctrl Pts',(-9.61222069871027,2.59197639583146,3.24084167542852));
#48330=CARTESIAN_POINT('Ctrl Pts',(-9.67851187594275,3.56771320970172,2.11962705565427));
#48331=CARTESIAN_POINT('Ctrl Pts',(-9.74480305317524,3.84769482180553,0.845521869863438));
#48332=CARTESIAN_POINT('Ctrl Pts',(-9.81109423040773,4.12767643390936,-0.428583315927544));
#48333=CARTESIAN_POINT('Ctrl Pts',(-9.87738540764022,3.71190284424656,-1.85557906773504));
#48334=CARTESIAN_POINT('Ctrl Pts',(-9.94367658487271,2.79138086675646,-2.77990207217312));
#48335=CARTESIAN_POINT('Ctrl Pts',(-10.0099677621052,1.87085888926651,-3.70422507661104));
#48336=CARTESIAN_POINT('Ctrl Pts',(-10.0762589393377,0.445588523949287,
-4.12587533367967));
#48337=CARTESIAN_POINT('Ctrl Pts',(-10.1425501165701,-0.829659560134056,
-3.85114628240017));
#48338=CARTESIAN_POINT('Ctrl Pts',(-10.2088412938026,-2.10490764421762,
-3.57641723112061));
#48339=CARTESIAN_POINT('Ctrl Pts',(-10.2751324710351,-3.23013344706731,
-2.60530887149283));
#48340=CARTESIAN_POINT('Ctrl Pts',(-10.3414236482676,-3.68840707965641,
-1.38394938090485));
#48341=CARTESIAN_POINT('Ctrl Pts',(-10.3652279248335,-3.85296702184515,
-0.945375496504573));
#48342=CARTESIAN_POINT('Ctrl Pts',(-10.3890322013994,-3.93152800352243,
-0.474533425435142));
#48343=CARTESIAN_POINT('Ctrl Pts',(-10.4128364779653,-3.92852884447977,
-0.00272592851332826));
#48344=CARTESIAN_POINT('Ctrl Pts',(-10.5961635220349,-3.92900062987189,
-0.00294957216901129));
#48345=CARTESIAN_POINT('Ctrl Pts',(-10.5734360862459,-3.93212282653091,
-0.453277898425794));
#48346=CARTESIAN_POINT('Ctrl Pts',(-10.550708650457,-3.86068862727375,-0.902645831670076));
#48347=CARTESIAN_POINT('Ctrl Pts',(-10.527981214668,-3.71039290505572,-1.32387581150145));
#48348=CARTESIAN_POINT('Ctrl Pts',(-10.4616900374356,-3.27201171452627,
-2.5525155713031));
#48349=CARTESIAN_POINT('Ctrl Pts',(-10.3953988602031,-2.16270279093953,
-3.54176693753334));
#48350=CARTESIAN_POINT('Ctrl Pts',(-10.3291076829706,-0.892083792648041,
-3.83716681694465));
#48351=CARTESIAN_POINT('Ctrl Pts',(-10.2628165057381,0.378535205643446,
-4.13256669635596));
#48352=CARTESIAN_POINT('Ctrl Pts',(-10.1965253285056,1.81046427863968,-3.73411508894833));
#48353=CARTESIAN_POINT('Ctrl Pts',(-10.1302341512731,2.74587374013584,-2.82486107222972));
#48354=CARTESIAN_POINT('Ctrl Pts',(-10.0639429740407,3.68128320163195,-1.91560705551115));
#48355=CARTESIAN_POINT('Ctrl Pts',(-9.99765179680817,4.12017305162805,-0.49555062948166));
#48356=CARTESIAN_POINT('Ctrl Pts',(-9.93136061957568,3.86091684245572,0.782932825859423));
#48357=CARTESIAN_POINT('Ctrl Pts',(-9.86506944234319,3.60166063328335,2.06141628120065));
#48358=CARTESIAN_POINT('Ctrl Pts',(-9.79877826511069,2.64425836494236,3.19832676585343));
#48359=CARTESIAN_POINT('Ctrl Pts',(-9.73248708787821,1.42854162241256,3.67136643597467));
#48360=CARTESIAN_POINT('Ctrl Pts',(-9.66619591064573,0.212824879882835,
4.14440610609588));
#48361=CARTESIAN_POINT('Ctrl Pts',(-9.59990473341325,-1.26120633683568,
3.95357496168562));
#48362=CARTESIAN_POINT('Ctrl Pts',(-9.53361355618077,-2.31638057348854,
3.18654102640015));
#48363=CARTESIAN_POINT('Ctrl Pts',(-9.47113021146548,-3.31094453080447,
2.46356629902905));
#48364=CARTESIAN_POINT('Ctrl Pts',(-9.40864686675018,-3.93338864221481,
1.22868296333715));
#48365=CARTESIAN_POINT('Ctrl Pts',(-9.34616352203489,-3.93892425866043,
-0.00137129965302642));
#48366=CARTESIAN_POINT('Origin',(-54.75,0.,0.));
#48367=CARTESIAN_POINT('',(-7.91283647796524,-3.933837855893,0.00357440632912626));
#48368=CARTESIAN_POINT('',(-8.09616352203487,-3.93318629788295,0.00362380460979597));
#48369=CARTESIAN_POINT('',(-54.75,-3.933,-4.81653586104654E-16));
#48370=CARTESIAN_POINT('Ctrl Pts',(-7.91283647796524,-3.933837855893,0.00357440632912626));
#48371=CARTESIAN_POINT('Ctrl Pts',(-7.92687140794288,-3.93641540935061,
0.28079939536921));
#48372=CARTESIAN_POINT('Ctrl Pts',(-7.94090633792052,-3.90961655860019,
0.557529618388759));
#48373=CARTESIAN_POINT('Ctrl Pts',(-7.95494126789816,-3.85159964015645,
0.827552346449105));
#48374=CARTESIAN_POINT('Ctrl Pts',(-8.02123244513065,-3.57756836040193,
2.10295055300727));
#48375=CARTESIAN_POINT('Ctrl Pts',(-8.08752362236314,-2.60707579437936,
3.22870751293816));
#48376=CARTESIAN_POINT('Ctrl Pts',(-8.15381479959562,-1.38596722326251,
3.68764932310658));
#48377=CARTESIAN_POINT('Ctrl Pts',(-8.2201059768281,-0.164858652145793,
4.14659113327494));
#48378=CARTESIAN_POINT('Ctrl Pts',(-8.28639715406057,1.30686592406514,3.93871779368097));
#48379=CARTESIAN_POINT('Ctrl Pts',(-8.35268833129305,2.35309472413324,3.15952652994444));
#48380=CARTESIAN_POINT('Ctrl Pts',(-8.41897950852553,3.39932352420134,2.3803352662079));
#48381=CARTESIAN_POINT('Ctrl Pts',(-8.48527068575802,4.0200565481266,1.0298260783288));
#48382=CARTESIAN_POINT('Ctrl Pts',(-8.5515618629905,3.93012840745075,-0.271575726299527));
#48383=CARTESIAN_POINT('Ctrl Pts',(-8.617853040223,3.84020026677489,-1.572977530928));
#48384=CARTESIAN_POINT('Ctrl Pts',(-8.68414421745548,3.03961096149769,-2.82527195230569));
#48385=CARTESIAN_POINT('Ctrl Pts',(-8.75043539468797,1.89615204037761,-3.45315364760073));
#48386=CARTESIAN_POINT('Ctrl Pts',(-8.81672657192046,0.752693119257527,
-4.08103534289578));
#48387=CARTESIAN_POINT('Ctrl Pts',(-8.88301774915295,-0.733635417705434,
-4.08450431210817));
#48388=CARTESIAN_POINT('Ctrl Pts',(-8.94930892638544,-1.88001271471163,
-3.46196690722038));
#48389=CARTESIAN_POINT('Ctrl Pts',(-9.01560010361792,-3.0263900117177,-2.83942950233266));
#48390=CARTESIAN_POINT('Ctrl Pts',(-9.08189128085039,-3.83281606876708,
-1.59088572334489));
#48391=CARTESIAN_POINT('Ctrl Pts',(-9.14818245808288,-3.92881792734507,
-0.289917864124349));
#48392=CARTESIAN_POINT('Ctrl Pts',(-9.15306713137699,-3.93589183573467,
-0.19405589238482));
#48393=CARTESIAN_POINT('Ctrl Pts',(-9.15795180467111,-3.93910849822148,
-0.0979092842701217));
#48394=CARTESIAN_POINT('Ctrl Pts',(-9.16283647796523,-3.93858084194566,
-0.00172678509975766));
#48395=CARTESIAN_POINT('Ctrl Pts',(-9.34616352203489,-3.93892425866043,
-0.00137129965302642));
#48396=CARTESIAN_POINT('Ctrl Pts',(-9.34235568951769,-3.93926160776363,
-0.0763327256438075));
#48397=CARTESIAN_POINT('Ctrl Pts',(-9.33854785700049,-3.9373078365908,-0.151276217068159));
#48398=CARTESIAN_POINT('Ctrl Pts',(-9.3347400244833,-3.93300754230767,-0.226084821068116));
#48399=CARTESIAN_POINT('Ctrl Pts',(-9.26844884725081,-3.85814301788671,
-1.52844000709018));
#48400=CARTESIAN_POINT('Ctrl Pts',(-9.20215767001835,-3.07209671245766,
-2.78991365297364));
#48401=CARTESIAN_POINT('Ctrl Pts',(-9.13586649278587,-1.93597910571819,
-3.43098347072513));
#48402=CARTESIAN_POINT('Ctrl Pts',(-9.06957531555338,-0.799861498978523,
-4.07205328847674));
#48403=CARTESIAN_POINT('Ctrl Pts',(-9.00328413832087,0.686327409071799,
-4.09271927809607));
#48404=CARTESIAN_POINT('Ctrl Pts',(-8.93699296108838,1.83983090829858,-3.48348746273554));
#48405=CARTESIAN_POINT('Ctrl Pts',(-8.8707017838559,2.99333440752502,-2.87425564737518));
#48406=CARTESIAN_POINT('Ctrl Pts',(-8.80441060662344,3.8141524979283,-1.63512602703546));
#48407=CARTESIAN_POINT('Ctrl Pts',(-8.73811942939096,3.92520050609562,-0.335356021435604));
#48408=CARTESIAN_POINT('Ctrl Pts',(-8.67182825215848,4.03624851426296,0.964413984164396));
#48409=CARTESIAN_POINT('Ctrl Pts',(-8.60553707492599,3.43752644019418,2.32482437502443));
#48410=CARTESIAN_POINT('Ctrl Pts',(-8.53924589769351,2.40408781938623,3.12090122093686));
#48411=CARTESIAN_POINT('Ctrl Pts',(-8.47295472046101,1.3706491985781,3.91697806684944));
#48412=CARTESIAN_POINT('Ctrl Pts',(-8.40666354322852,-0.0975059689694893,
4.14872136781416));
#48413=CARTESIAN_POINT('Ctrl Pts',(-8.34037236599602,-1.32590569202342,
3.70966801345165));
#48414=CARTESIAN_POINT('Ctrl Pts',(-8.27408118876355,-2.554305415077,3.27061465908927));
#48415=CARTESIAN_POINT('Ctrl Pts',(-8.20779001153107,-3.54294969363718,
2.16076464940022));
#48416=CARTESIAN_POINT('Ctrl Pts',(-8.14149883429859,-3.83765433115549,
0.889984218247712));
#48417=CARTESIAN_POINT('Ctrl Pts',(-8.12638706354402,-3.90483535144222,
0.600296459533917));
#48418=CARTESIAN_POINT('Ctrl Pts',(-8.11127529278945,-3.9359551075444,0.3022457912809));
#48419=CARTESIAN_POINT('Ctrl Pts',(-8.09616352203487,-3.93318629788295,
0.00362380460979597));
#48420=CARTESIAN_POINT('Origin',(-54.75,0.,0.));
#48421=CARTESIAN_POINT('',(-6.66283647796524,-3.92647855971048,6.27931888395146E-5));
#48422=CARTESIAN_POINT('',(-6.84616352203489,-3.92649740926382,-0.000290818540083879));
#48423=CARTESIAN_POINT('',(-54.75,-3.933,-4.81653586104654E-16));
#48424=CARTESIAN_POINT('Ctrl Pts',(-6.66283647796524,-3.92647903110527,
6.27886499063313E-5));
#48425=CARTESIAN_POINT('Ctrl Pts',(-6.69579101121463,-3.92657178318442,
0.65408414937199));
#48426=CARTESIAN_POINT('Ctrl Pts',(-6.72874554446403,-3.77215766733763,
1.30806432167412));
#48427=CARTESIAN_POINT('Ctrl Pts',(-6.76170007771342,-3.46299500617961,
1.87811827672048));
#48428=CARTESIAN_POINT('Ctrl Pts',(-6.82799125494591,-2.84108491540716,
3.02483601294439));
#48429=CARTESIAN_POINT('Ctrl Pts',(-6.89428243217839,-1.59298254566306,
3.83194506888531));
#48430=CARTESIAN_POINT('Ctrl Pts',(-6.96057360941088,-0.292067406959177,
3.92865871563777));
#48431=CARTESIAN_POINT('Ctrl Pts',(-7.02686478664336,1.00884773174456,4.02537236239023));
#48432=CARTESIAN_POINT('Ctrl Pts',(-7.09315596387586,2.36257563940807,3.41169059995439));
#48433=CARTESIAN_POINT('Ctrl Pts',(-7.15944714110833,3.14721232546681,2.36953946002056));
#48434=CARTESIAN_POINT('Ctrl Pts',(-7.22573831834082,3.93184901152565,1.32738832008662));
#48435=CARTESIAN_POINT('Ctrl Pts',(-7.2920294955733,4.14739447597958,-0.143232197345431));
#48436=CARTESIAN_POINT('Ctrl Pts',(-7.35832067280579,3.6948269111705,-1.36671751677449));
#48437=CARTESIAN_POINT('Ctrl Pts',(-7.42461185003827,3.24225934636147,-2.59020283620341));
#48438=CARTESIAN_POINT('Ctrl Pts',(-7.49090302727077,2.12157875228958,-3.5665529576294));
#48439=CARTESIAN_POINT('Ctrl Pts',(-7.55719420450325,0.847626944403404,
-3.84723163291313));
#48440=CARTESIAN_POINT('Ctrl Pts',(-7.62348538173574,-0.426324863482916,
-4.12791030819688));
#48441=CARTESIAN_POINT('Ctrl Pts',(-7.68977655896822,-1.85354788518356,
-3.71291753733821));
#48442=CARTESIAN_POINT('Ctrl Pts',(-7.7560677362007,-2.77837439929059,-2.79290142531614));
#48443=CARTESIAN_POINT('Ctrl Pts',(-7.80832398345555,-3.50739996508378,
-2.06766782055368));
#48444=CARTESIAN_POINT('Ctrl Pts',(-7.8605802307104,-3.92424085248734,-1.0286172466098));
#48445=CARTESIAN_POINT('Ctrl Pts',(-7.91283647796524,-3.933837855893,0.00357440632912626));
#48446=CARTESIAN_POINT('Ctrl Pts',(-8.09616352203487,-3.93318629788295,
0.00362380460979597));
#48447=CARTESIAN_POINT('Ctrl Pts',(-8.04498411555696,-3.92380910195901,
-1.00772663785624));
#48448=CARTESIAN_POINT('Ctrl Pts',(-7.99380470907904,-3.52573331557938,
-2.02563004763744));
#48449=CARTESIAN_POINT('Ctrl Pts',(-7.94262530260113,-2.82335829107196,
-2.74741890406279));
#48450=CARTESIAN_POINT('Ctrl Pts',(-7.87633412536865,-1.91359261699404,
-3.68233074260415));
#48451=CARTESIAN_POINT('Ctrl Pts',(-7.81004294813616,-0.493296272362007,
-4.12044356707083));
#48452=CARTESIAN_POINT('Ctrl Pts',(-7.74375177090368,0.785045143972438,
-3.86048789612034));
#48453=CARTESIAN_POINT('Ctrl Pts',(-7.67746059367119,2.0633865603071,-3.60053222516981));
#48454=CARTESIAN_POINT('Ctrl Pts',(-7.61116941643871,3.19977304834405,-2.64250805880205));
#48455=CARTESIAN_POINT('Ctrl Pts',(-7.54487823920622,3.67214748882358,-1.42653268258857));
#48456=CARTESIAN_POINT('Ctrl Pts',(-7.47858706197375,4.14452192930298,-0.210557306375435));
#48457=CARTESIAN_POINT('Ctrl Pts',(-7.41229588474128,3.95288432222515,1.26336927968317));
#48458=CARTESIAN_POINT('Ctrl Pts',(-7.34600470750881,3.18527318102397,2.31812368876547));
#48459=CARTESIAN_POINT('Ctrl Pts',(-7.27971353027631,2.41766203982253,3.37287809784814));
#48460=CARTESIAN_POINT('Ctrl Pts',(-7.21342235304382,1.07407736449723,4.00846032995424));
#48461=CARTESIAN_POINT('Ctrl Pts',(-7.14713117581133,-0.228236665734775,
3.93288325514251));
#48462=CARTESIAN_POINT('Ctrl Pts',(-7.08083999857884,-1.53055069596648,
3.85730618033079));
#48463=CARTESIAN_POINT('Ctrl Pts',(-7.01454882134635,-2.79159408110498,
3.07056979860157));
#48464=CARTESIAN_POINT('Ctrl Pts',(-6.94825764411387,-3.43204219538415,
1.93410161141309));
#48465=CARTESIAN_POINT('Ctrl Pts',(-6.91422627008754,-3.76082394631091,
1.35068198361555));
#48466=CARTESIAN_POINT('Ctrl Pts',(-6.88019489606122,-3.9260536565938,0.675093831262958));
#48467=CARTESIAN_POINT('Ctrl Pts',(-6.84616352203489,-3.92649740926382,
-0.000290818540083879));
#48468=CARTESIAN_POINT('Origin',(-54.75,0.,0.));
#48469=CARTESIAN_POINT('',(-5.41283647796527,-3.93360662039214,-0.00359624771770317));
#48470=CARTESIAN_POINT('',(-5.59616352203489,-3.93425725830108,-0.00352254436509695));
#48471=CARTESIAN_POINT('',(-54.75,-3.933,-4.81653586104654E-16));
#48472=CARTESIAN_POINT('Ctrl Pts',(-5.41283647796527,-3.93360662039214,
-0.00359624771770317));
#48473=CARTESIAN_POINT('Ctrl Pts',(-5.46471061448641,-3.92407744450487,
1.02120223617962));
#48474=CARTESIAN_POINT('Ctrl Pts',(-5.51658475100756,-3.51395559821539,
2.05275735647589));
#48475=CARTESIAN_POINT('Ctrl Pts',(-5.56845888752871,-2.79442114786394,
2.776845894706));
#48476=CARTESIAN_POINT('Ctrl Pts',(-5.63475006476119,-1.87491117676923,
3.70217564164551));
#48477=CARTESIAN_POINT('Ctrl Pts',(-5.70104124199368,-0.450103062199543,
4.1253852711142));
#48478=CARTESIAN_POINT('Ctrl Pts',(-5.76733241922616,0.825444885062228,
3.85205184490948));
#48479=CARTESIAN_POINT('Ctrl Pts',(-5.83362359645865,2.10099283232414,3.57871841870473));
#48480=CARTESIAN_POINT('Ctrl Pts',(-5.89991477369114,3.22728061227828,2.60884193682636));
#48481=CARTESIAN_POINT('Ctrl Pts',(-5.96620595092363,3.68689046262614,1.38798465072928));
#48482=CARTESIAN_POINT('Ctrl Pts',(-6.03249712815611,4.14650031297395,0.167127364632348));
#48483=CARTESIAN_POINT('Ctrl Pts',(-6.09878830538858,3.93943223371586,-1.30471072568299));
#48484=CARTESIAN_POINT('Ctrl Pts',(-6.16507948262105,3.16081351299333,-2.35136569046795));
#48485=CARTESIAN_POINT('Ctrl Pts',(-6.23137065985354,2.38219479227071,-3.39802065525303));
#48486=CARTESIAN_POINT('Ctrl Pts',(-6.29766183708603,1.03202543008335,-4.0194924945073));
#48487=CARTESIAN_POINT('Ctrl Pts',(-6.36395301431851,-0.269425382418601,
-3.93027640726029));
#48488=CARTESIAN_POINT('Ctrl Pts',(-6.43024419155099,-1.57087619492055,
-3.84106032001328));
#48489=CARTESIAN_POINT('Ctrl Pts',(-6.49653536878348,-2.82360845773726,
-3.041156306265));
#48490=CARTESIAN_POINT('Ctrl Pts',(-6.56282654601597,-3.4521156832451,-1.89804109113744));
#48491=CARTESIAN_POINT('Ctrl Pts',(-6.59616318999905,-3.76818069358685,
-1.32318895320192));
#48492=CARTESIAN_POINT('Ctrl Pts',(-6.62949983398215,-3.92638520355753,
-0.661542007713824));
#48493=CARTESIAN_POINT('Ctrl Pts',(-6.66283647796524,-3.92647903110527,
6.27886499063313E-5));
#48494=CARTESIAN_POINT('Ctrl Pts',(-6.84616352203489,-3.92649740926382,
-0.000290818540083879));
#48495=CARTESIAN_POINT('Ctrl Pts',(-6.81390371882873,-3.92691806150654,
-0.640516977914417));
#48496=CARTESIAN_POINT('Ctrl Pts',(-6.78164391562257,-3.77926271887843,
-1.28056027072101));
#48497=CARTESIAN_POINT('Ctrl Pts',(-6.74938411241641,-3.48248030899597,
-1.84173656412097));
#48498=CARTESIAN_POINT('Ctrl Pts',(-6.68309293518393,-2.87261746490879,
-2.99490655981828));
#48499=CARTESIAN_POINT('Ctrl Pts',(-6.61680175795143,-1.63303893331471,
-3.81504655856512));
#48500=CARTESIAN_POINT('Ctrl Pts',(-6.55051058071895,-0.333208364222228,
-3.92538340295274));
#48501=CARTESIAN_POINT('Ctrl Pts',(-6.48421940348646,0.966622204870406,
-4.03572024734038));
#48502=CARTESIAN_POINT('Ctrl Pts',(-6.41792822625399,2.32670481146146,-3.43625393736864));
#48503=CARTESIAN_POINT('Ctrl Pts',(-6.3516370490215,3.12221610976888,-2.40237991127052));
#48504=CARTESIAN_POINT('Ctrl Pts',(-6.28534587178902,3.9177274080762,-1.36850588517251));
#48505=CARTESIAN_POINT('Ctrl Pts',(-6.21905469455653,4.14866739810001,0.0997758570517888));
#48506=CARTESIAN_POINT('Ctrl Pts',(-6.15276351732404,3.70894201133942,1.32793517562964));
#48507=CARTESIAN_POINT('Ctrl Pts',(-6.08647234009155,3.26921662457878,2.55609449420764));
#48508=CARTESIAN_POINT('Ctrl Pts',(-6.02018116285907,2.15882586103359,3.54413138913913));
#48509=CARTESIAN_POINT('Ctrl Pts',(-5.95388998562658,0.887884377429989,
3.83814069654488));
#48510=CARTESIAN_POINT('Ctrl Pts',(-5.8875988083941,-0.38305710617347,4.1321500039506));
#48511=CARTESIAN_POINT('Ctrl Pts',(-5.82130763116161,-1.81454930983531,
3.73213172383073));
#48512=CARTESIAN_POINT('Ctrl Pts',(-5.75501645392913,-2.74896324554502,
2.82185466473268));
#48513=CARTESIAN_POINT('Ctrl Pts',(-5.70206547663104,-3.49533905545499,
2.09475851252179));
#48514=CARTESIAN_POINT('Ctrl Pts',(-5.64911449933297,-3.92456737898498,
1.04210540159905));
#48515=CARTESIAN_POINT('Ctrl Pts',(-5.59616352203489,-3.93425725830108,
-0.00352254436509695));
#48516=CARTESIAN_POINT('Origin',(-54.75,0.,0.));
#48517=CARTESIAN_POINT('',(-4.16283647796528,-3.938710497775,0.00160298884803723));
#48518=CARTESIAN_POINT('',(-4.34616352203491,-3.93832454869238,0.00194456996648914));
#48519=CARTESIAN_POINT('',(-54.75,-3.933,-4.81653586104654E-16));
#48520=CARTESIAN_POINT('Ctrl Pts',(-4.16283647796528,-3.938710497775,0.00160298884803723));
#48521=CARTESIAN_POINT('Ctrl Pts',(-4.1673390405257,-3.93916707483314,0.0902537325677592));
#48522=CARTESIAN_POINT('Ctrl Pts',(-4.17184160308612,-3.93643450601992,
0.178875823251529));
#48523=CARTESIAN_POINT('Ctrl Pts',(-4.17634416564655,-3.93042322572512,
0.267274956415375));
#48524=CARTESIAN_POINT('Ctrl Pts',(-4.24263534287903,-3.84191921449391,
1.56877438593398));
#48525=CARTESIAN_POINT('Ctrl Pts',(-4.30892652011151,-3.04270074100715,
2.82194411801858));
#48526=CARTESIAN_POINT('Ctrl Pts',(-4.37521769734399,-1.89992957625108,
3.45107668626067));
#48527=CARTESIAN_POINT('Ctrl Pts',(-4.44150887457647,-0.757158411495012,
4.08020925450276));
#48528=CARTESIAN_POINT('Ctrl Pts',(-4.50780005180894,0.729165444530365,
4.08530465890234));
#48529=CARTESIAN_POINT('Ctrl Pts',(-4.57409122904142,1.87622327785216,3.46402206806303));
#48530=CARTESIAN_POINT('Ctrl Pts',(-4.64038240627392,3.02328111117421,2.84273947722358));
#48531=CARTESIAN_POINT('Ctrl Pts',(-4.70667358350641,3.83107292179253,1.59507889114495));
#48532=CARTESIAN_POINT('Ctrl Pts',(-4.77296476073891,3.92849832715561,0.294216862580042));
#48533=CARTESIAN_POINT('Ctrl Pts',(-4.83925593797138,4.02592373251865,-1.00664516598442));
#48534=CARTESIAN_POINT('Ctrl Pts',(-4.90554711520386,3.412982732627,-2.36070863703513));
#48535=CARTESIAN_POINT('Ctrl Pts',(-4.97183829243634,2.37126104968588,-3.14591540110713));
#48536=CARTESIAN_POINT('Ctrl Pts',(-5.03812946966882,1.32953936674452,-3.93112216517931));
#48537=CARTESIAN_POINT('Ctrl Pts',(-5.10442064690131,-0.140962999246524,
-4.14747222227252));
#48538=CARTESIAN_POINT('Ctrl Pts',(-5.1707118241338,-1.36469575040221,-3.6955741344339));
#48539=CARTESIAN_POINT('Ctrl Pts',(-5.23700300136628,-2.58842850155775,
-3.24367604659533));
#48540=CARTESIAN_POINT('Ctrl Pts',(-5.30329417859877,-3.56539163787799,
-2.12352981382508));
#48541=CARTESIAN_POINT('Ctrl Pts',(-5.36958535583125,-3.84676729222827,
-0.84973176523474));
#48542=CARTESIAN_POINT('Ctrl Pts',(-5.38400239654259,-3.90796102016165,
-0.572705483741063));
#48543=CARTESIAN_POINT('Ctrl Pts',(-5.39841943725393,-3.93625500214701,
-0.288411811967996));
#48544=CARTESIAN_POINT('Ctrl Pts',(-5.41283647796527,-3.93360662039214,
-0.00359624771770317));
#48545=CARTESIAN_POINT('Ctrl Pts',(-5.59616352203489,-3.93425725830108,
-0.00352254436509695));
#48546=CARTESIAN_POINT('Ctrl Pts',(-5.5828233221005,-3.93669847721738,-0.266952731453627));
#48547=CARTESIAN_POINT('Ctrl Pts',(-5.5694831221661,-3.91251108716881,-0.529937022884259));
#48548=CARTESIAN_POINT('Ctrl Pts',(-5.5561429222317,-3.8600577941153,-0.787157227085798));
#48549=CARTESIAN_POINT('Ctrl Pts',(-5.48985174499922,-3.59940273921825,
-2.06535622173015));
#48550=CARTESIAN_POINT('Ctrl Pts',(-5.42356056776673,-2.64075696166643,
-3.20121837294244));
#48551=CARTESIAN_POINT('Ctrl Pts',(-5.35726939053424,-1.42452331575331,
-3.67292744238449));
#48552=CARTESIAN_POINT('Ctrl Pts',(-5.29097821330175,-0.208289669840187,
-4.14463651182654));
#48553=CARTESIAN_POINT('Ctrl Pts',(-5.22468703606926,1.26553184443423,-3.95219249949835));
#48554=CARTESIAN_POINT('Ctrl Pts',(-5.15839585883677,2.31986611015527,-3.18400438214645));
#48555=CARTESIAN_POINT('Ctrl Pts',(-5.09210468160428,3.3742003758762,-2.41581626479464));
#48556=CARTESIAN_POINT('Ctrl Pts',(-5.02581350437181,4.0090473930439,-1.07188404241932));
#48557=CARTESIAN_POINT('Ctrl Pts',(-4.95952232713933,3.93275779055114,0.230388442126491));
#48558=CARTESIAN_POINT('Ctrl Pts',(-4.89323114990684,3.85646818805839,1.5326609266723));
#48559=CARTESIAN_POINT('Ctrl Pts',(-4.82693997267436,3.06904196590517,2.79327367338859));
#48560=CARTESIAN_POINT('Ctrl Pts',(-4.76064879544188,1.93222353831344,3.43309989255341));
#48561=CARTESIAN_POINT('Ctrl Pts',(-4.69435761820939,0.795405110721587,
4.0729261117183));
#48562=CARTESIAN_POINT('Ctrl Pts',(-4.6280664409769,-0.690805522308857,
4.09196580333158));
#48563=CARTESIAN_POINT('Ctrl Pts',(-4.56177526374441,-1.84364166896585,
3.48147211293344));
#48564=CARTESIAN_POINT('Ctrl Pts',(-4.49548408651194,-2.99647781562258,
2.87097842253544));
#48565=CARTESIAN_POINT('Ctrl Pts',(-4.42919290927946,-3.81593947590601,
1.6309513501263));
#48566=CARTESIAN_POINT('Ctrl Pts',(-4.36290173204699,-3.9255651240589,0.331060606933602));
#48567=CARTESIAN_POINT('Ctrl Pts',(-4.35732232870963,-3.9347917773286,0.221655176926881));
#48568=CARTESIAN_POINT('Ctrl Pts',(-4.35174292537227,-3.9389901201714,0.111825686834663));
#48569=CARTESIAN_POINT('Ctrl Pts',(-4.34616352203491,-3.93832454869238,
0.00194456996648914));
#48570=CARTESIAN_POINT('Origin',(-54.75,0.,0.));
#48571=CARTESIAN_POINT('',(-2.91283647796527,-3.92869173988258,0.0028084021417174));
#48572=CARTESIAN_POINT('',(-3.09616352203495,-3.9282466370004,0.0025678202255927));
#48573=CARTESIAN_POINT('',(-54.75,-3.933,-4.81653586104654E-16));
#48574=CARTESIAN_POINT('Ctrl Pts',(-2.91283647796527,-3.92869173988258,
0.0028084021417174));
#48575=CARTESIAN_POINT('Ctrl Pts',(-2.93625864379745,-3.93173980158221,
0.466994022202747));
#48576=CARTESIAN_POINT('Ctrl Pts',(-2.95968080962962,-3.85574928228062,
0.930213895198008));
#48577=CARTESIAN_POINT('Ctrl Pts',(-2.9831029754618,-3.69632003395113,1.36267350892606));
#48578=CARTESIAN_POINT('Ctrl Pts',(-3.04939415269429,-3.24509137163283,
2.5866532683107));
#48579=CARTESIAN_POINT('Ctrl Pts',(-3.11568532992677,-2.12548025594738,
3.56422925579285));
#48580=CARTESIAN_POINT('Ctrl Pts',(-3.18197650715925,-0.851836446862079,
3.8463018352547));
#48581=CARTESIAN_POINT('Ctrl Pts',(-3.24826768439174,0.421807362223362,
4.12837441471658));
#48582=CARTESIAN_POINT('Ctrl Pts',(-3.31455886162423,1.84948386470868,3.714943586158));
#48583=CARTESIAN_POINT('Ctrl Pts',(-3.38085003885672,2.77531661985273,2.79594001521562));
#48584=CARTESIAN_POINT('Ctrl Pts',(-3.4471412160892,3.70114937499666,1.87693644427334));
#48585=CARTESIAN_POINT('Ctrl Pts',(-3.51343239332168,4.12513838279943,0.452360130947363));
#48586=CARTESIAN_POINT('Ctrl Pts',(-3.57972357055417,3.85250286423086,-0.823337166685192));
#48587=CARTESIAN_POINT('Ctrl Pts',(-3.64601474778666,3.57986734566225,-2.09903446431789));
#48588=CARTESIAN_POINT('Ctrl Pts',(-3.71230592501914,2.61060730072214,-3.22585274625714));
#48589=CARTESIAN_POINT('Ctrl Pts',(-3.77859710225163,1.39000167980377,-3.68613050369547));
#48590=CARTESIAN_POINT('Ctrl Pts',(-3.84488827948411,0.169396058885551,
-4.14640826113375));
#48591=CARTESIAN_POINT('Ctrl Pts',(-3.9111794567166,-1.30255513801086,-3.94014549407127));
#48592=CARTESIAN_POINT('Ctrl Pts',(-3.97747063394908,-2.3496359619713,-3.16209954706376));
#48593=CARTESIAN_POINT('Ctrl Pts',(-4.03925924862115,-3.32559801700176,
-2.43689925309078));
#48594=CARTESIAN_POINT('Ctrl Pts',(-4.10104786329321,-3.93244489601268,
-1.21495015629594));
#48595=CARTESIAN_POINT('Ctrl Pts',(-4.16283647796528,-3.938710497775,0.00160298884803723));
#48596=CARTESIAN_POINT('Ctrl Pts',(-4.34616352203491,-3.93832454869238,
0.00194456996648914));
#48597=CARTESIAN_POINT('Ctrl Pts',(-4.28545174813977,-3.93108219270887,
-1.19371688687386));
#48598=CARTESIAN_POINT('Ctrl Pts',(-4.22473997424464,-3.34792768095492,
-2.39549121615994));
#48599=CARTESIAN_POINT('Ctrl Pts',(-4.1640282003495,-2.4006712852553,-3.12353006333101));
#48600=CARTESIAN_POINT('Ctrl Pts',(-4.09773702311702,-1.36636216227721,
-3.91847557642554));
#48601=CARTESIAN_POINT('Ctrl Pts',(-4.03144584588453,0.102045719700945,
-4.1486121886383));
#48602=CARTESIAN_POINT('Ctrl Pts',(-3.96515466865205,1.32996426409882,-3.70821490010836));
#48603=CARTESIAN_POINT('Ctrl Pts',(-3.89886349141955,2.55788280849698,-3.26781761157831));
#48604=CARTESIAN_POINT('Ctrl Pts',(-3.83257231418708,3.54531201531465,-2.15688642230563));
#48605=CARTESIAN_POINT('Ctrl Pts',(-3.76628113695459,3.83862590846361,-0.885784268610713));
#48606=CARTESIAN_POINT('Ctrl Pts',(-3.69998995972212,4.13193980161248,0.385317885083766));
#48607=CARTESIAN_POINT('Ctrl Pts',(-3.63369878248965,3.73113838109276,1.8165910032001));
#48608=CARTESIAN_POINT('Ctrl Pts',(-3.56740760525718,2.82035020216559,2.75050675993973));
#48609=CARTESIAN_POINT('Ctrl Pts',(-3.5011164280247,1.90956202323822,3.68442251667957));
#48610=CARTESIAN_POINT('Ctrl Pts',(-3.4348252507922,0.488787085902983,4.12098091204254));
#48611=CARTESIAN_POINT('Ctrl Pts',(-3.36853407355971,-0.789269090623166,
3.85962654446236));
#48612=CARTESIAN_POINT('Ctrl Pts',(-3.30224289632722,-2.06732526714932,
3.59827217688217));
#48613=CARTESIAN_POINT('Ctrl Pts',(-3.23595171909473,-3.20266268286653,
2.63900504635881));
#48614=CARTESIAN_POINT('Ctrl Pts',(-3.16966054186224,-3.67370626610708,
1.42251350760468));
#48615=CARTESIAN_POINT('Ctrl Pts',(-3.14516153525315,-3.84778825319431,
0.972938835799878));
#48616=CARTESIAN_POINT('Ctrl Pts',(-3.12066252864405,-3.93114132743054,
0.488232585502865));
#48617=CARTESIAN_POINT('Ctrl Pts',(-3.09616352203495,-3.9282466370004,0.0025678202255927));
#48618=CARTESIAN_POINT('Origin',(-54.75,0.,0.));
#48619=CARTESIAN_POINT('',(-1.66283647796526,-3.92848774701504,-0.00268787972552448));
#48620=CARTESIAN_POINT('',(-1.84616352203493,-3.92893748603655,-0.00291966682171161));
#48621=CARTESIAN_POINT('',(-54.75,-3.933,-4.81653586104654E-16));
#48622=CARTESIAN_POINT('Ctrl Pts',(-1.66283647796526,-3.92848774701504,
-0.00268787972552448));
#48623=CARTESIAN_POINT('Ctrl Pts',(-1.7051782470692,-3.923213871108,0.836568195474228));
#48624=CARTESIAN_POINT('Ctrl Pts',(-1.74752001617314,-3.65997084863724,
1.67883665840762));
#48625=CARTESIAN_POINT('Ctrl Pts',(-1.78986178527708,-3.16337477926387,
2.34790251287165));
#48626=CARTESIAN_POINT('Ctrl Pts',(-1.85615296250957,-2.38589337627915,
3.39540629169586));
#48627=CARTESIAN_POINT('Ctrl Pts',(-1.92244413974206,-1.03642394411599,
4.01836100213633));
#48628=CARTESIAN_POINT('Ctrl Pts',(-1.98873531697455,0.265119230997025,
3.9305704655395));
#48629=CARTESIAN_POINT('Ctrl Pts',(-2.05502649420703,1.56666240610989,3.84277992894269));
#48630=CARTESIAN_POINT('Ctrl Pts',(-2.12131767143951,2.82027932417245,3.04424414530877));
#48631=CARTESIAN_POINT('Ctrl Pts',(-2.187608848672,3.45003942039896,1.90181664633624));
#48632=CARTESIAN_POINT('Ctrl Pts',(-2.25390002590448,4.07979951662547,0.759389147363717));
#48633=CARTESIAN_POINT('Ctrl Pts',(-2.32019120313698,4.08570279101577,-0.726930066947709));
#48634=CARTESIAN_POINT('Ctrl Pts',(-2.38648238036946,3.46504662903402,-1.87432726913705));
#48635=CARTESIAN_POINT('Ctrl Pts',(-2.45277355760195,2.84439046705227,-3.02172447132639));
#48636=CARTESIAN_POINT('Ctrl Pts',(-2.51906473483443,1.59717486869864,-3.83019966139392));
#48637=CARTESIAN_POINT('Ctrl Pts',(-2.58535591206691,0.296367005435699,
-3.92833700002301));
#48638=CARTESIAN_POINT('Ctrl Pts',(-2.65164708929939,-1.00444085782724,
-4.0264743386521));
#48639=CARTESIAN_POINT('Ctrl Pts',(-2.71793826653186,-2.35884098599932,
-3.41427382584272));
#48640=CARTESIAN_POINT('Ctrl Pts',(-2.78422944376434,-3.14461794560989,
-2.37298180379444));
#48641=CARTESIAN_POINT('Ctrl Pts',(-2.82709845516465,-3.6527622092351,-1.69960170363885));
#48642=CARTESIAN_POINT('Ctrl Pts',(-2.86996746656496,-3.92311294786624,
-0.84677906901001));
#48643=CARTESIAN_POINT('Ctrl Pts',(-2.91283647796527,-3.92869173988258,
0.0028084021417174));
#48644=CARTESIAN_POINT('Ctrl Pts',(-3.09616352203495,-3.9282466370004,0.0025678202255927));
#48645=CARTESIAN_POINT('Ctrl Pts',(-3.05437135141156,-3.92330866550267,
-0.825914128454525));
#48646=CARTESIAN_POINT('Ctrl Pts',(-3.01257918078818,-3.66738974622449,
-1.65718535520051));
#48647=CARTESIAN_POINT('Ctrl Pts',(-2.97078701016479,-3.18273468739347,
-2.32160780899296));
#48648=CARTESIAN_POINT('Ctrl Pts',(-2.9044958329323,-2.41396977467525,-3.37552163985192));
#48649=CARTESIAN_POINT('Ctrl Pts',(-2.83820465569982,-1.06969019847474,
-4.00963335458485));
#48650=CARTESIAN_POINT('Ctrl Pts',(-2.77191347846733,0.232540257688125,
-3.93263120170715));
#48651=CARTESIAN_POINT('Ctrl Pts',(-2.70562230123485,1.53477071385084,-3.85562904882945));
#48652=CARTESIAN_POINT('Ctrl Pts',(-2.63933112400237,2.79495204997593,-3.0675130283413));
#48653=CARTESIAN_POINT('Ctrl Pts',(-2.57303994676988,3.43415635782225,-1.93034478664988));
#48654=CARTESIAN_POINT('Ctrl Pts',(-2.50674876953739,4.07336066566865,-0.793176544958324));
#48655=CARTESIAN_POINT('Ctrl Pts',(-2.4404575923049,4.09158794523613,0.693043917936572));
#48656=CARTESIAN_POINT('Ctrl Pts',(-2.37416641507241,3.480463260221,1.84554603281607));
#48657=CARTESIAN_POINT('Ctrl Pts',(-2.30787523783993,2.86933857520593,2.99804814769544));
#48658=CARTESIAN_POINT('Ctrl Pts',(-2.24158406060745,1.6288619256084,3.81683191455948));
#48659=CARTESIAN_POINT('Ctrl Pts',(-2.17529288337497,0.328912022552463,
3.92574602707322));
#48660=CARTESIAN_POINT('Ctrl Pts',(-2.10900170614248,-0.971037880503623,
4.03466013958697));
#48661=CARTESIAN_POINT('Ctrl Pts',(-2.04271052890999,-2.33046103701813,
3.43370459775025));
#48662=CARTESIAN_POINT('Ctrl Pts',(-1.9764193516775,-3.12484170726232,2.39896126641609));
#48663=CARTESIAN_POINT('Ctrl Pts',(-1.93300074179664,-3.64513574725602,
1.72123733835161));
#48664=CARTESIAN_POINT('Ctrl Pts',(-1.88958213191578,-3.92303600768351,
0.85742570116635));
#48665=CARTESIAN_POINT('Ctrl Pts',(-1.84616352203493,-3.92893748603655,
-0.00291966682171161));
#48666=CARTESIAN_POINT('Origin',(-54.75,0.,0.));
#48667=CARTESIAN_POINT('',(-0.412836477965312,-3.93946807025562,-0.00149173430430305));
#48668=CARTESIAN_POINT('',(-0.596163522034903,-3.93901438905508,-0.00135576060872734));
#48669=CARTESIAN_POINT('',(-54.75,-3.933,-4.81653586104654E-16));
#48670=CARTESIAN_POINT('Ctrl Pts',(-0.412836477965312,-3.93946807025562,
-0.00149173430430305));
#48671=CARTESIAN_POINT('Ctrl Pts',(-0.474097850340994,-3.9331312283141,
1.20496832338296));
#48672=CARTESIAN_POINT('Ctrl Pts',(-0.535359222716679,-3.33651390232707,
2.41661565923732));
#48673=CARTESIAN_POINT('Ctrl Pts',(-0.596620595092361,-2.37426143690827,
3.14318560345314));
#48674=CARTESIAN_POINT('Ctrl Pts',(-0.662911772324848,-1.33300417717378,
3.92940985988084));
#48675=CARTESIAN_POINT('Ctrl Pts',(-0.72920294955734,0.136393222589551,
4.1476331777127));
#48676=CARTESIAN_POINT('Ctrl Pts',(-0.795494126789824,1.36041507745367,
3.69713690330391));
#48677=CARTESIAN_POINT('Ctrl Pts',(-0.861785304022308,2.58443693231779,
3.24664062889511));
#48678=CARTESIAN_POINT('Ctrl Pts',(-0.928076481254795,3.56308324228286,
2.12742476224559));
#48679=CARTESIAN_POINT('Ctrl Pts',(-0.994367658487279,3.84596040873201,
0.853902561958117));
#48680=CARTESIAN_POINT('Ctrl Pts',(-1.06065883571976,4.12883757518116,-0.419619638329351));
#48681=CARTESIAN_POINT('Ctrl Pts',(-1.12695001295223,3.71594559811471,-1.84744817225453));
#48682=CARTESIAN_POINT('Ctrl Pts',(-1.19324119018472,2.79739171077215,-2.77376620717791));
#48683=CARTESIAN_POINT('Ctrl Pts',(-1.2595323674172,1.8788378234297,-3.7000842421012));
#48684=CARTESIAN_POINT('Ctrl Pts',(-1.32582354464969,0.454622025811202,
-4.12489177802249));
#48685=CARTESIAN_POINT('Ctrl Pts',(-1.39211472188217,-0.821194066006917,
-3.85296348705388));
#48686=CARTESIAN_POINT('Ctrl Pts',(-1.45840589911466,-2.09701015782518,
-3.58103519608524));
#48687=CARTESIAN_POINT('Ctrl Pts',(-1.52469707634715,-3.22442654384318,
-2.61237107822653));
#48688=CARTESIAN_POINT('Ctrl Pts',(-1.59098825357964,-3.68538804994898,
-1.39201259569326));
#48689=CARTESIAN_POINT('Ctrl Pts',(-1.61493766170818,-3.85192235665705,
-0.951126423785145));
#48690=CARTESIAN_POINT('Ctrl Pts',(-1.63888706983672,-3.93147076376634,
-0.477389024592041));
#48691=CARTESIAN_POINT('Ctrl Pts',(-1.66283647796526,-3.92848774701504,
-0.00268787972552448));
#48692=CARTESIAN_POINT('Ctrl Pts',(-1.84616352203493,-3.92893748603655,
-0.00291966682171161));
#48693=CARTESIAN_POINT('Ctrl Pts',(-1.82329095468331,-3.9320463363999,-0.456142545881115));
#48694=CARTESIAN_POINT('Ctrl Pts',(-1.80041838733169,-3.85967291538721,
-0.908403501985509));
#48695=CARTESIAN_POINT('Ctrl Pts',(-1.77754581998007,-3.70748927430689,
-1.33199168146346));
#48696=CARTESIAN_POINT('Ctrl Pts',(-1.71125464274758,-3.26641798713338,
-2.55967017717775));
#48697=CARTESIAN_POINT('Ctrl Pts',(-1.64496346551509,-2.15493722881242,
-3.54649604777468));
#48698=CARTESIAN_POINT('Ctrl Pts',(-1.5786722882826,-0.883678993796144,
-3.83911237490377));
#48699=CARTESIAN_POINT('Ctrl Pts',(-1.51238111105012,0.387579241219839,
-4.13172870203281));
#48700=CARTESIAN_POINT('Ctrl Pts',(-1.44608993381766,1.8186149529309,-3.7301354856943));
#48701=CARTESIAN_POINT('Ctrl Pts',(-1.37979875658518,2.75204019720566,-2.81884035677723));
#48702=CARTESIAN_POINT('Ctrl Pts',(-1.31350757935269,3.68546544148063,-1.90754522785995));
#48703=CARTESIAN_POINT('Ctrl Pts',(-1.24721640212018,4.12128021831895,-0.486548186363495));
#48704=CARTESIAN_POINT('Ctrl Pts',(-1.18092522488769,3.85921161225801,0.791372148289516));
#48705=CARTESIAN_POINT('Ctrl Pts',(-1.1146340476552,3.59714300619707,2.06929248294253));
#48706=CARTESIAN_POINT('Ctrl Pts',(-1.04834287042271,2.63719101723718,3.20413611075232));
#48707=CARTESIAN_POINT('Ctrl Pts',(-0.982051693190223,1.42047028231716,
3.67450017059044));
#48708=CARTESIAN_POINT('Ctrl Pts',(-0.915760515957748,0.20374954739741,
4.14486423042845));
#48709=CARTESIAN_POINT('Ctrl Pts',(-0.849469338725274,-1.26973993348217,
3.95074872229507));
#48710=CARTESIAN_POINT('Ctrl Pts',(-0.783178161492798,-2.32328652660156,
3.1814334930799));
#48711=CARTESIAN_POINT('Ctrl Pts',(-0.720839948340164,-3.31400979974224,
2.45799277679574));
#48712=CARTESIAN_POINT('Ctrl Pts',(-0.658501735187536,-3.93337961985426,
1.22590574495181));
#48713=CARTESIAN_POINT('Ctrl Pts',(-0.596163522034903,-3.93901438905508,
-0.00135576060872734));
#48714=CARTESIAN_POINT('Origin',(-111.877773449273,0.,0.));
#48715=CARTESIAN_POINT('',(-0.00277344927343423,-3.22805001866674,-0.00122234597570187));
#48716=CARTESIAN_POINT('',(0.,-3.22275,5.46201577318104E-12));
#48717=CARTESIAN_POINT('',(-111.877773449273,-3.22275,5.46201577318104E-12));
#48718=CARTESIAN_POINT('',(0.,-3.22243683749934,-0.0449265047300178));
#48719=CARTESIAN_POINT('Ctrl Pts',(-0.00277344927343414,-3.22805001866674,
-0.00122234597570214));
#48720=CARTESIAN_POINT('Ctrl Pts',(-0.00184896618229052,-3.22812837747028,
-0.0161409391011512));
#48721=CARTESIAN_POINT('Ctrl Pts',(-0.000924483091146902,-3.22809658599603,
-0.0310585642458751));
#48722=CARTESIAN_POINT('Ctrl Pts',(-3.28431943100171E-15,-3.22795401163284,
-0.0459738408030352));
#48723=CARTESIAN_POINT('Origin',(0.,0.,0.));
#48724=CARTESIAN_POINT('Origin',(-111.877773449273,0.,0.));
#48725=CARTESIAN_POINT('',(-1.25277344927345,-3.21905260276956,-0.00220248267844716));
#48726=CARTESIAN_POINT('',(-1.00622655072714,-3.22767826654644,-0.0011109274034582));
#48727=CARTESIAN_POINT('',(-111.877773449273,-3.22275,5.46201577318104E-12));
#48728=CARTESIAN_POINT('Ctrl Pts',(-1.25277344927345,-3.21905260276956,
-0.00220248267844716));
#48729=CARTESIAN_POINT('Ctrl Pts',(-1.22882404114487,-3.22149692446714,
-0.391178611491322));
#48730=CARTESIAN_POINT('Ctrl Pts',(-1.20487463301629,-3.15631395243283,
-0.779365034896385));
#48731=CARTESIAN_POINT('Ctrl Pts',(-1.18092522488771,-3.01985363284375,
-1.14063274669891));
#48732=CARTESIAN_POINT('Ctrl Pts',(-1.11463404765522,-2.64213593800486,
-2.14060993957577));
#48733=CARTESIAN_POINT('Ctrl Pts',(-1.04834287042274,-1.71831667585426,
-2.93434558306168));
#48734=CARTESIAN_POINT('Ctrl Pts',(-0.982051693190246,-0.672896815720211,
-3.15716706786221));
#48735=CARTESIAN_POINT('Ctrl Pts',(-0.91576051595777,0.372523044413605,
-3.37998855266269));
#48736=CARTESIAN_POINT('Ctrl Pts',(-0.849469338725299,1.53954350253069,
-3.03189587877802));
#48737=CARTESIAN_POINT('Ctrl Pts',(-0.783178161492821,2.29221818863138,
-2.27285915183992));
#48738=CARTESIAN_POINT('Ctrl Pts',(-0.716886984260322,3.04489287473232,
-1.51382242490155));
#48739=CARTESIAN_POINT('Ctrl Pts',(-0.650595807027827,3.38322178881643,
-0.343841644909505));
#48740=CARTESIAN_POINT('Ctrl Pts',(-0.584304629795333,3.15142865681201,
0.69969857145897));
#48741=CARTESIAN_POINT('Ctrl Pts',(-0.518013452562862,2.91963552480766,
1.74323878782709));
#48742=CARTESIAN_POINT('Ctrl Pts',(-0.451722275330373,2.11772034671489,
2.66033844057194));
#48743=CARTESIAN_POINT('Ctrl Pts',(-0.385431098097901,1.11474134016462,
3.02948079204712));
#48744=CARTESIAN_POINT('Ctrl Pts',(-0.319139920865414,0.111762333614127,
3.39862314352239));
#48745=CARTESIAN_POINT('Ctrl Pts',(-0.252848743632928,-1.09228050139405,
3.21980819372804));
#48746=CARTESIAN_POINT('Ctrl Pts',(-0.186557566400438,-1.94549988451387,
2.57556608276912));
#48747=CARTESIAN_POINT('Ctrl Pts',(-0.125296194024769,-2.73398173880538,
1.98020547058501));
#48748=CARTESIAN_POINT('Ctrl Pts',(-0.0640348216491032,-3.22285753014165,
0.987366301598871));
#48749=CARTESIAN_POINT('Ctrl Pts',(-0.00277344927343423,-3.22805001866674,
-0.00122234597570187));
#48750=CARTESIAN_POINT('',(0.,-1.09131022003071,3.03235215074973));
#48751=CARTESIAN_POINT('Origin',(0.,0.,0.));
#48752=CARTESIAN_POINT('Ctrl Pts',(-1.00622655072714,-3.22767826654644,
-0.00111092740345839));
#48753=CARTESIAN_POINT('Ctrl Pts',(-1.00227358664718,-3.22797105053401,
-0.0648797357467673));
#48754=CARTESIAN_POINT('Ctrl Pts',(-0.932029445334739,-3.19723962854479,
-1.19776843518848));
#48755=CARTESIAN_POINT('Ctrl Pts',(-0.795494126789802,-1.86525717936383,
-3.32418745080932));
#48756=CARTESIAN_POINT('Ctrl Pts',(-0.596620595092344,1.78624879507146,
-3.36601485692819));
#48757=CARTESIAN_POINT('Ctrl Pts',(-0.397747063394925,3.80117096935424,
-0.317409156202402));
#48758=CARTESIAN_POINT('Ctrl Pts',(-0.198873531697423,2.31445171887122,
3.02736545452069));
#48759=CARTESIAN_POINT('Ctrl Pts',(-0.0662911772324812,-0.0808825703380203,
3.39599395944883));
#48760=CARTESIAN_POINT('Ctrl Pts',(0.,-1.09131022003071,3.03235215074973));
#48761=CARTESIAN_POINT('Origin',(-111.877773449273,0.,0.));
#48762=CARTESIAN_POINT('',(-2.50277344927344,-3.21921975710822,0.0023012402776184));
#48763=CARTESIAN_POINT('',(-2.25622655072717,-3.2194211246184,-0.00239241195666928));
#48764=CARTESIAN_POINT('',(-111.877773449273,-3.22275,5.46201577318104E-12));
#48765=CARTESIAN_POINT('Ctrl Pts',(-2.50277344927344,-3.21921975710822,
0.0023012402776184));
#48766=CARTESIAN_POINT('Ctrl Pts',(-2.45990443787309,-3.21464842429137,
-0.693861491137611));
#48767=CARTESIAN_POINT('Ctrl Pts',(-2.41703542647275,-2.99311960585182,
-1.39267515647013));
#48768=CARTESIAN_POINT('Ctrl Pts',(-2.37416641507242,-2.57673976206881,
-1.94445133693756));
#48769=CARTESIAN_POINT('Ctrl Pts',(-2.30787523783994,-1.93286417178559,
-2.79769920473741));
#48770=CARTESIAN_POINT('Ctrl Pts',(-2.24158406060747,-0.823051557225173,
-3.29934405667177));
#48771=CARTESIAN_POINT('Ctrl Pts',(-2.17529288337499,0.242846876878725,
-3.21892907877561));
#48772=CARTESIAN_POINT('Ctrl Pts',(-2.10900170614251,1.30874531098262,-3.13851410087944));
#48773=CARTESIAN_POINT('Ctrl Pts',(-2.04271052891002,2.33072956463,-2.47603929315276));
#48774=CARTESIAN_POINT('Ctrl Pts',(-1.97641935167754,2.8393030825623,-1.53584749723235));
#48775=CARTESIAN_POINT('Ctrl Pts',(-1.91012817444505,3.34787660049467,-0.595655701311836));
#48776=CARTESIAN_POINT('Ctrl Pts',(-1.84383699721256,3.34303938271184,0.622253082802464));
#48777=CARTESIAN_POINT('Ctrl Pts',(-1.77754581998007,2.82700598578506,1.55837264098061));
#48778=CARTESIAN_POINT('Ctrl Pts',(-1.71125464274759,2.31097258885834,2.49449219915864));
#48779=CARTESIAN_POINT('Ctrl Pts',(-1.64496346551511,1.28374301278778,3.14882253140059));
#48780=CARTESIAN_POINT('Ctrl Pts',(-1.57867228828262,0.217242054843513,
3.22075920870002));
#48781=CARTESIAN_POINT('Ctrl Pts',(-1.51238111105013,-0.849258903100873,
3.29269588599945));
#48782=CARTESIAN_POINT('Ctrl Pts',(-1.44608993381765,-1.95503124291897,
2.78223890835625));
#48783=CARTESIAN_POINT('Ctrl Pts',(-1.37979875658516,-2.59210934906441,
1.92390104840077));
#48784=CARTESIAN_POINT('Ctrl Pts',(-1.33745698748126,-2.99902645625288,
1.3756600154815));
#48785=CARTESIAN_POINT('Ctrl Pts',(-1.29511521837735,-3.21473112207246,
0.685494572075572));
#48786=CARTESIAN_POINT('Ctrl Pts',(-1.25277344927345,-3.21905260276956,
-0.00220248267844716));
#48787=CARTESIAN_POINT('Ctrl Pts',(-2.25622655072717,-3.2194211246184,-0.00239241195666928));
#48788=CARTESIAN_POINT('Ctrl Pts',(-2.23335398337544,-3.22196855597136,
-0.373768977808676));
#48789=CARTESIAN_POINT('Ctrl Pts',(-2.2104814160237,-3.1626648583949,-0.744357331811508));
#48790=CARTESIAN_POINT('Ctrl Pts',(-2.18760884867197,-3.03796365593016,
-1.09145084958913));
#48791=CARTESIAN_POINT('Ctrl Pts',(-2.12131767143949,-2.67654425833608,
-2.09742615395299));
#48792=CARTESIAN_POINT('Ctrl Pts',(-2.055026494207,-1.76578285129882,-2.90604376759822));
#48793=CARTESIAN_POINT('Ctrl Pts',(-1.98873531697452,-0.724097756740481,
-3.14581729118237));
#48794=CARTESIAN_POINT('Ctrl Pts',(-1.92244413974204,0.317587337817736,
-3.38559081476649));
#48795=CARTESIAN_POINT('Ctrl Pts',(-1.85615296250958,1.49019611989687,-3.05652024828963));
#48796=CARTESIAN_POINT('Ctrl Pts',(-1.78986178527711,2.25505658417029,-2.30979348075427));
#48797=CARTESIAN_POINT('Ctrl Pts',(-1.72357060804462,3.0199170484438,-1.56306671321882));
#48798=CARTESIAN_POINT('Ctrl Pts',(-1.65727943081212,3.37702919491142,-0.398683744624477));
#48799=CARTESIAN_POINT('Ctrl Pts',(-1.59098825357964,3.16228686076928,0.648460358732475));
#48800=CARTESIAN_POINT('Ctrl Pts',(-1.52469707634714,2.94754452662709,1.69560446208966));
#48801=CARTESIAN_POINT('Ctrl Pts',(-1.45840589911467,2.16094771187536,2.62550970020934));
#48802=CARTESIAN_POINT('Ctrl Pts',(-1.39211472188217,1.16395133545451,3.01093196663321));
#48803=CARTESIAN_POINT('Ctrl Pts',(-1.32582354464969,0.166954959034,3.39635423305696));
#48804=CARTESIAN_POINT('Ctrl Pts',(-1.2595323674172,-1.04044097905563,3.23729352778482));
#48805=CARTESIAN_POINT('Ctrl Pts',(-1.19324119018472,-1.90373039755963,
2.6069068878275));
#48806=CARTESIAN_POINT('Ctrl Pts',(-1.13090297703219,-2.71554159219717,
2.01411040463404));
#48807=CARTESIAN_POINT('Ctrl Pts',(-1.06856476387967,-3.22306106531334,
1.0045226899468));
#48808=CARTESIAN_POINT('Ctrl Pts',(-1.00622655072714,-3.22767826654644,
-0.0011109274034582));
#48809=CARTESIAN_POINT('Origin',(-111.877773449273,0.,0.));
#48810=CARTESIAN_POINT('',(-3.75277344927344,-3.22742925418368,0.00131350936171883));
#48811=CARTESIAN_POINT('',(-3.50622655072716,-3.21885503417064,0.00210410441258302));
#48812=CARTESIAN_POINT('',(-111.877773449273,-3.22275,5.46201577318104E-12));
#48813=CARTESIAN_POINT('Ctrl Pts',(-3.75277344927344,-3.22742925418368,
0.00131350936171883));
#48814=CARTESIAN_POINT('Ctrl Pts',(-3.69098483460135,-3.2222951407648,-0.995545541875145));
#48815=CARTESIAN_POINT('Ctrl Pts',(-3.62919621992925,-2.72503712415365,
-1.99682610421916));
#48816=CARTESIAN_POINT('Ctrl Pts',(-3.56740760525716,-1.92532145854212,
-2.59106440765253));
#48817=CARTESIAN_POINT('Ctrl Pts',(-3.50111642802467,-1.06733017315741,
-3.22860510831862));
#48818=CARTESIAN_POINT('Ctrl Pts',(-3.43482525079217,0.138805275558225,
-3.39761943136768));
#48819=CARTESIAN_POINT('Ctrl Pts',(-3.36853407355969,1.13898497675701,-3.02046200884451));
#48820=CARTESIAN_POINT('Ctrl Pts',(-3.3022428963272,2.1391646779558,-2.64330458632134));
#48821=CARTESIAN_POINT('Ctrl Pts',(-3.23595171909473,2.93338863163767,-1.7199754182263));
#48822=CARTESIAN_POINT('Ctrl Pts',(-3.16966054186224,3.15678962768858,-0.674652899552124));
#48823=CARTESIAN_POINT('Ctrl Pts',(-3.10336936462976,3.38019062373947,0.370669619121929));
#48824=CARTESIAN_POINT('Ctrl Pts',(-3.03707818739727,3.03276866215923,1.53798548837486));
#48825=CARTESIAN_POINT('Ctrl Pts',(-2.97078701016479,2.27412957961686,2.29102865091111));
#48826=CARTESIAN_POINT('Ctrl Pts',(-2.90449583293231,1.51549049707441,3.04407181344744));
#48827=CARTESIAN_POINT('Ctrl Pts',(-2.83820465569982,0.34563429356962,3.38284226926708));
#48828=CARTESIAN_POINT('Ctrl Pts',(-2.77191347846733,-0.698005570587585,
3.15170842602795));
#48829=CARTESIAN_POINT('Ctrl Pts',(-2.70562230123485,-1.74164543474467,
2.92057458278884));
#48830=CARTESIAN_POINT('Ctrl Pts',(-2.63933112400237,-2.65906895955433,
2.11953644049109));
#48831=CARTESIAN_POINT('Ctrl Pts',(-2.57303994676988,-3.02881143895618,
1.11659192750956));
#48832=CARTESIAN_POINT('Ctrl Pts',(-2.54961778093773,-3.15944978374479,
0.762229044178745));
#48833=CARTESIAN_POINT('Ctrl Pts',(-2.52619561510558,-3.22171737745944,
0.38266081491523));
#48834=CARTESIAN_POINT('Ctrl Pts',(-2.50277344927344,-3.21921975710822,
0.0023012402776184));
#48835=CARTESIAN_POINT('Ctrl Pts',(-3.50622655072716,-3.21885503417064,
0.00210410441258302));
#48836=CARTESIAN_POINT('Ctrl Pts',(-3.46443438010368,-3.21480879780153,
-0.67676449465048));
#48837=CARTESIAN_POINT('Ctrl Pts',(-3.4226422094802,-3.00510559487675,-1.35791866347924));
#48838=CARTESIAN_POINT('Ctrl Pts',(-3.38085003885672,-2.60797310292387,
-1.90235483509507));
#48839=CARTESIAN_POINT('Ctrl Pts',(-3.31455886162423,-1.97803739927232,
-2.76594517285287));
#48840=CARTESIAN_POINT('Ctrl Pts',(-3.24826768439174,-0.876517693144756,
-3.28554434108499));
#48841=CARTESIAN_POINT('Ctrl Pts',(-3.18197650715925,0.190546431594337,
-3.22244780200914));
#48842=CARTESIAN_POINT('Ctrl Pts',(-3.11568532992677,1.25761055633331,-3.1593512629333));
#48843=CARTESIAN_POINT('Ctrl Pts',(-3.04939415269428,2.29021909968395,-2.5135590165496));
#48844=CARTESIAN_POINT('Ctrl Pts',(-2.9831029754618,2.81399120319597,-1.5817489603812));
#48845=CARTESIAN_POINT('Ctrl Pts',(-2.91681179822931,3.33776330670811,-0.6499389042126));
#48846=CARTESIAN_POINT('Ctrl Pts',(-2.85052062099683,3.35269897038154,0.567888961740592));
#48847=CARTESIAN_POINT('Ctrl Pts',(-2.78422944376434,2.85193566536462,1.5122637877586));
#48848=CARTESIAN_POINT('Ctrl Pts',(-2.71793826653186,2.35117236034781,2.45663861377639));
#48849=CARTESIAN_POINT('Ctrl Pts',(-2.65164708929937,1.33471008664077,3.12756039985888));
#48850=CARTESIAN_POINT('Ctrl Pts',(-2.58535591206689,0.269514675994107,
3.21680600273325));
#48851=CARTESIAN_POINT('Ctrl Pts',(-2.5190647348344,-0.795680734652675,
3.30605160560764));
#48852=CARTESIAN_POINT('Ctrl Pts',(-2.45277355760191,-1.90960928223922,
2.8136210252738));
#48853=CARTESIAN_POINT('Ctrl Pts',(-2.38648238036942,-2.5605348619571,1.96573923756561));
#48854=CARTESIAN_POINT('Ctrl Pts',(-2.34306377048867,-2.98687038633703,
1.41040366950969));
#48855=CARTESIAN_POINT('Ctrl Pts',(-2.29964516060792,-3.21458537852958,
0.702585476341522));
#48856=CARTESIAN_POINT('Ctrl Pts',(-2.25622655072717,-3.2194211246184,-0.00239241195666928));
#48857=CARTESIAN_POINT('Origin',(-111.877773449273,0.,0.));
#48858=CARTESIAN_POINT('',(-5.00277344927341,-3.22324707243039,-0.00294681091381338));
#48859=CARTESIAN_POINT('',(-4.75622655072715,-3.22711300261848,0.00159340525895835));
#48860=CARTESIAN_POINT('',(-111.877773449273,-3.22275,5.46201577318104E-12));
#48861=CARTESIAN_POINT('Ctrl Pts',(-5.00277344927341,-3.22324707243039,
-0.00294681091381289));
#48862=CARTESIAN_POINT('Ctrl Pts',(-4.98835640856205,-3.22541718997454,
-0.23632829062118));
#48863=CARTESIAN_POINT('Ctrl Pts',(-4.90764819061821,-3.09562804344372,
-1.54043009724623));
#48864=CARTESIAN_POINT('Ctrl Pts',(-4.76064879544187,-1.32045512479611,
-3.57577123082234));
#48865=CARTESIAN_POINT('Ctrl Pts',(-4.56177526374442,2.29438965018289,-3.04393130214526));
#48866=CARTESIAN_POINT('Ctrl Pts',(-4.36290173204696,3.80114449946005,0.284678958212554));
#48867=CARTESIAN_POINT('Ctrl Pts',(-4.1640282003495,1.81539998560147,3.35172560488281));
#48868=CARTESIAN_POINT('Ctrl Pts',(-3.96515466865207,-1.83833777717959,
3.33919988823347));
#48869=CARTESIAN_POINT('Ctrl Pts',(-3.82806975162671,-3.19259801208126,
1.21572803160912));
#48870=CARTESIAN_POINT('Ctrl Pts',(-3.75727601183384,-3.22780337920628,
0.0739550512688685));
#48871=CARTESIAN_POINT('Ctrl Pts',(-3.75277344927344,-3.22742925418368,
0.00131350936171882));
#48872=CARTESIAN_POINT('Ctrl Pts',(-4.75622655072715,-3.22711300261848,
0.00159340525895835));
#48873=CARTESIAN_POINT('Ctrl Pts',(-4.69551477683191,-3.22117852442416,
-0.978146732050712));
#48874=CARTESIAN_POINT('Ctrl Pts',(-4.56851182570419,-2.22157632985661,
-3.03814323849845));
#48875=CARTESIAN_POINT('Ctrl Pts',(-4.37521769734396,1.28684956643968,-3.58800221152922));
#48876=CARTESIAN_POINT('Ctrl Pts',(-4.17634416564651,3.71418555139234,-0.857068961927461));
#48877=CARTESIAN_POINT('Ctrl Pts',(-3.97747063394909,2.72892027452058,2.66134098575405));
#48878=CARTESIAN_POINT('Ctrl Pts',(-3.77859710225162,-0.76368264637654,
3.73450541646114));
#48879=CARTESIAN_POINT('Ctrl Pts',(-3.62151574117766,-2.96811382736398,
1.87194161459359));
#48880=CARTESIAN_POINT('Ctrl Pts',(-3.53072555733616,-3.22122698016124,
0.400063962610161));
#48881=CARTESIAN_POINT('Ctrl Pts',(-3.50622655072716,-3.21885503417064,
0.00210410441258326));
#48882=CARTESIAN_POINT('Origin',(-111.877773449273,0.,0.));
#48883=CARTESIAN_POINT('',(-6.25277344927341,-3.21740618512558,5.14541539371783E-5));
#48884=CARTESIAN_POINT('',(-6.00622655072713,-3.22378021337137,-0.00288641744942336));
#48885=CARTESIAN_POINT('',(-111.877773449273,-3.22275,5.46201577318104E-12));
#48886=CARTESIAN_POINT('Ctrl Pts',(-6.25277344927341,-3.21740663551856,
5.14498172248315E-5));
#48887=CARTESIAN_POINT('Ctrl Pts',(-6.21943680529028,-3.2173297520383,-0.542075897623197));
#48888=CARTESIAN_POINT('Ctrl Pts',(-6.11980898407466,-2.82991131366294,
-2.16234719346006));
#48889=CARTESIAN_POINT('Ctrl Pts',(-5.9538899856266,-0.260691166334333,
-3.80286493939216));
#48890=CARTESIAN_POINT('Ctrl Pts',(-5.75501645392915,3.05834644769266,-2.27513925674164));
#48891=CARTESIAN_POINT('Ctrl Pts',(-5.5561429222317,3.56736906587033,1.34298904651157));
#48892=CARTESIAN_POINT('Ctrl Pts',(-5.35726939053425,0.798685661716399,
3.72717625625544));
#48893=CARTESIAN_POINT('Ctrl Pts',(-5.17281289954814,-2.44992198009203,
2.76224489299424));
#48894=CARTESIAN_POINT('Ctrl Pts',(-5.05464758579454,-3.21543874504854,
0.83678604288195));
#48895=CARTESIAN_POINT('Ctrl Pts',(-5.00277344927341,-3.22324707243039,
-0.00294681091381289));
#48896=CARTESIAN_POINT('Ctrl Pts',(-6.00622655072713,-3.22378021337137,
-0.0028864174494234));
#48897=CARTESIAN_POINT('Ctrl Pts',(-5.99288635079263,-3.22578057906275,
-0.218744448328217));
#48898=CARTESIAN_POINT('Ctrl Pts',(-5.91325497362564,-3.10747272775033,
-1.50508027811392));
#48899=CARTESIAN_POINT('Ctrl Pts',(-5.76733241922618,-1.3783432033079,-3.55385869799583));
#48900=CARTESIAN_POINT('Ctrl Pts',(-5.5684588875287,2.24466082806341,-3.08078551666176));
#48901=CARTESIAN_POINT('Ctrl Pts',(-5.36958535583126,3.80526588113653,0.222919723353213));
#48902=CARTESIAN_POINT('Ctrl Pts',(-5.17071182413379,1.86958483045521,3.32180586330821));
#48903=CARTESIAN_POINT('Ctrl Pts',(-4.97183829243635,-1.78387460325836,
3.36860995647996));
#48904=CARTESIAN_POINT('Ctrl Pts',(-4.83367653463412,-3.18334407284146,
1.25090254757947));
#48905=CARTESIAN_POINT('Ctrl Pts',(-4.76180595406439,-3.22765838031572,
0.0916313837435054));
#48906=CARTESIAN_POINT('Ctrl Pts',(-4.75622655072715,-3.22711300261848,
0.00159340525895835));
#48907=CARTESIAN_POINT('Origin',(-111.877773449273,0.,0.));
#48908=CARTESIAN_POINT('',(-7.50277344927341,-3.22343654972774,0.00292891380799201));
#48909=CARTESIAN_POINT('',(-7.25622655072713,-3.21742169481438,-0.000238300387980783));
#48910=CARTESIAN_POINT('',(-111.877773449273,-3.22275,5.46201577318104E-12));
#48911=CARTESIAN_POINT('Ctrl Pts',(-7.50277344927341,-3.22343654972774,
0.00292891380799198));
#48912=CARTESIAN_POINT('Ctrl Pts',(-7.45051720201854,-3.21557264361966,
-0.842861996314261));
#48913=CARTESIAN_POINT('Ctrl Pts',(-7.33196977753116,-2.4407061395756,-2.77435554718224));
#48914=CARTESIAN_POINT('Ctrl Pts',(-7.14713117581134,0.820148624304898,
-3.72251230562602));
#48915=CARTESIAN_POINT('Ctrl Pts',(-6.94825764411385,3.57504823112902,-1.32241134923795));
#48916=CARTESIAN_POINT('Ctrl Pts',(-6.74938411241644,3.04518618264129,2.29272387010146));
#48917=CARTESIAN_POINT('Ctrl Pts',(-6.55051058071893,-0.282599183050784,
3.80129969000349));
#48918=CARTESIAN_POINT('Ctrl Pts',(-6.38497369300464,-2.83642887895705,
2.14981730773864));
#48919=CARTESIAN_POINT('Ctrl Pts',(-6.28572798252277,-3.21748263774626,
0.535964834069746));
#48920=CARTESIAN_POINT('Ctrl Pts',(-6.25277344927341,-3.21740663551856,
5.14498172248315E-5));
#48921=CARTESIAN_POINT('Ctrl Pts',(-7.25622655072713,-3.21742169481438,
-0.000238300387980818));
#48922=CARTESIAN_POINT('Ctrl Pts',(-7.22396674752086,-3.21776638258936,
-0.524847721982282));
#48923=CARTESIAN_POINT('Ctrl Pts',(-7.12541576708212,-2.84815011952815,
-2.12702754070791));
#48924=CARTESIAN_POINT('Ctrl Pts',(-6.96057360941086,-0.322406435201958,
-3.79813055621078));
#48925=CARTESIAN_POINT('Ctrl Pts',(-6.76170007771344,3.02100029278552,-2.32449970155028));
#48926=CARTESIAN_POINT('Ctrl Pts',(-6.56282654601595,3.58870574881201,1.28488625173232));
#48927=CARTESIAN_POINT('Ctrl Pts',(-6.36395301431852,0.85910099426281,3.71371607868986));
#48928=CARTESIAN_POINT('Ctrl Pts',(-6.17841968255555,-2.42380063763367,
2.79633723357069));
#48929=CARTESIAN_POINT('Ctrl Pts',(-6.0591775280251,-3.21584020356402,0.853914361307076));
#48930=CARTESIAN_POINT('Ctrl Pts',(-6.00622655072713,-3.22378021337137,
-0.0028864174494234));
#48931=CARTESIAN_POINT('Origin',(-111.877773449273,0.,0.));
#48932=CARTESIAN_POINT('',(-8.75277344927343,-3.22732301255539,-0.00141494957263923));
#48933=CARTESIAN_POINT('',(-8.50622655072714,-3.22290265484426,0.00296939138868677));
#48934=CARTESIAN_POINT('',(-111.877773449273,-3.22275,5.46201577318104E-12));
#48935=CARTESIAN_POINT('Ctrl Pts',(-8.75277344927343,-3.22732301255539,
-0.00141494957263976));
#48936=CARTESIAN_POINT('Ctrl Pts',(-8.74788877597928,-3.2277553807891,-0.0802281072649062));
#48937=CARTESIAN_POINT('Ctrl Pts',(-8.67671292545264,-3.18934882974505,
-1.22820668054782));
#48938=CARTESIAN_POINT('Ctrl Pts',(-8.53924589769349,-1.81906657383958,
-3.34973706899915));
#48939=CARTESIAN_POINT('Ctrl Pts',(-8.34037236599607,1.83468269579965,-3.34120951710917));
#48940=CARTESIAN_POINT('Ctrl Pts',(-8.14149883429859,3.80272173743456,-0.262771800485379));
#48941=CARTESIAN_POINT('Ctrl Pts',(-7.94262530260113,2.27681223869029,3.05710118596646));
#48942=CARTESIAN_POINT('Ctrl Pts',(-7.74375177090369,-1.34103701987869,
3.5681033256903));
#48943=CARTESIAN_POINT('Ctrl Pts',(-7.59713448646112,-3.09986887883355,
1.52788449672985));
#48944=CARTESIAN_POINT('Ctrl Pts',(-7.51680837925102,-3.22554862966795,
0.23009058007471));
#48945=CARTESIAN_POINT('Ctrl Pts',(-7.50277344927341,-3.22343654972774,
0.00292891380799198));
#48946=CARTESIAN_POINT('Ctrl Pts',(-8.50622655072714,-3.22290265484426,
0.00296939138868704));
#48947=CARTESIAN_POINT('Ctrl Pts',(-8.45504714424911,-3.21521886177093,
-0.825743966980133));
#48948=CARTESIAN_POINT('Ctrl Pts',(-8.33757656053859,-2.46652837635199,
-2.74018996961731));
#48949=CARTESIAN_POINT('Ctrl Pts',(-8.1538147995956,0.759595596975361,-3.73533882807744));
#48950=CARTESIAN_POINT('Ctrl Pts',(-7.95494126789815,3.55310402895249,-1.38028743054838));
#48951=CARTESIAN_POINT('Ctrl Pts',(-7.7560677362007,3.08201318363674,2.24297489227504));
#48952=CARTESIAN_POINT('Ctrl Pts',(-7.55719420450326,-0.220837703017022,
3.80538727863702));
#48953=CARTESIAN_POINT('Ctrl Pts',(-7.39058047601204,-2.81793219209313,
2.18511889975105));
#48954=CARTESIAN_POINT('Ctrl Pts',(-7.29025792475335,-3.21705807825673,
0.553180433440147));
#48955=CARTESIAN_POINT('Ctrl Pts',(-7.25622655072713,-3.21742169481438,
-0.000238300387980818));
#48956=CARTESIAN_POINT('Origin',(-111.877773449273,0.,0.));
#48957=CARTESIAN_POINT('',(-10.0027734492734,-3.21908627855254,-0.00223366033731866));
#48958=CARTESIAN_POINT('',(-9.75622655072715,-3.22760441255983,-0.00112366029274946));
#48959=CARTESIAN_POINT('',(-111.877773449273,-3.22275,5.46201577318104E-12));
#48960=CARTESIAN_POINT('Ctrl Pts',(-10.0027734492734,-3.21908627855254,
-0.00223366033731895));
#48961=CARTESIAN_POINT('Ctrl Pts',(-9.97896917270751,-3.22154382744801,
-0.388838697384529));
#48962=CARTESIAN_POINT('Ctrl Pts',(-9.88887371890911,-2.97789885064663,
-1.84908401298488));
#48963=CARTESIAN_POINT('Ctrl Pts',(-9.73248708787821,-0.80276370563772,
-3.72630005023728));
#48964=CARTESIAN_POINT('Ctrl Pts',(-9.53361355618079,2.70089004709043,-2.68978337139171));
#48965=CARTESIAN_POINT('Ctrl Pts',(-9.33474002448332,3.72296047888839,0.818111791946939));
#48966=CARTESIAN_POINT('Ctrl Pts',(-9.13586649278587,1.32436717843105,3.5743241610383));
#48967=CARTESIAN_POINT('Ctrl Pts',(-8.94187763438256,-2.20225640776817,
3.05940588394578));
#48968=CARTESIAN_POINT('Ctrl Pts',(-8.81417995321176,-3.22188759854761,
0.989365843077845));
#48969=CARTESIAN_POINT('Ctrl Pts',(-8.75277344927343,-3.22732301255539,
-0.00141494957263976));
#48970=CARTESIAN_POINT('Ctrl Pts',(-9.75622655072715,-3.22760441255983,
-0.00112366029274946));
#48971=CARTESIAN_POINT('Ctrl Pts',(-9.75241871820984,-3.22788084068667,
-0.0625480019197435));
#48972=CARTESIAN_POINT('Ctrl Pts',(-9.74861088569253,-3.22627989584886,
-0.123957647735919));
#48973=CARTESIAN_POINT('Ctrl Pts',(-9.74480305317522,-3.22275618026246,
-0.185256765088582));
#48974=CARTESIAN_POINT('Ctrl Pts',(-9.67851187594274,-3.1614112410109,-1.25242309505367));
#48975=CARTESIAN_POINT('Ctrl Pts',(-9.61222069871026,-2.51731494535359,
-2.28609057338361));
#48976=CARTESIAN_POINT('Ctrl Pts',(-9.54592952147779,-1.58636579276803,
-2.81139129933321));
#48977=CARTESIAN_POINT('Ctrl Pts',(-9.4796383442453,-0.65541664018237,-3.33669202528286));
#48978=CARTESIAN_POINT('Ctrl Pts',(-9.41334716701282,0.562385369331491,
-3.353625998852));
#48979=CARTESIAN_POINT('Ctrl Pts',(-9.34705598978033,1.50758074236322,-2.85441373519793));
#48980=CARTESIAN_POINT('Ctrl Pts',(-9.28076481254784,2.45277611539483,-2.35520147154391));
#48981=CARTESIAN_POINT('Ctrl Pts',(-9.21447363531536,3.12536485194425,-1.33984297066688));
#48982=CARTESIAN_POINT('Ctrl Pts',(-9.14818245808287,3.21635899593677,-0.274794970273445));
#48983=CARTESIAN_POINT('Ctrl Pts',(-9.0818912808504,3.30735313992928,0.790253030119865));
#48984=CARTESIAN_POINT('Ctrl Pts',(-9.01560010361792,2.8167526913648,1.90499053002971));
#48985=CARTESIAN_POINT('Ctrl Pts',(-8.94930892638544,1.96993999998221,2.55730597756723));
#48986=CARTESIAN_POINT('Ctrl Pts',(-8.88301774915295,1.12312730859944,3.20962142510489));
#48987=CARTESIAN_POINT('Ctrl Pts',(-8.81672657192045,-0.0798976256015836,
3.3995148202703));
#48988=CARTESIAN_POINT('Ctrl Pts',(-8.75043539468796,-1.08646391277993,
3.03974894237302));
#48989=CARTESIAN_POINT('Ctrl Pts',(-8.68414421745548,-2.09303019995817,
2.67998306447579));
#48990=CARTESIAN_POINT('Ctrl Pts',(-8.617853040223,-2.90313784011365,1.77055791351603));
#48991=CARTESIAN_POINT('Ctrl Pts',(-8.55156186299052,-3.14462255167314,
0.729264337493415));
#48992=CARTESIAN_POINT('Ctrl Pts',(-8.53645009223606,-3.19967153034788,
0.491890519952649));
#48993=CARTESIAN_POINT('Ctrl Pts',(-8.5213383214816,-3.22517145253926,0.247664028443626));
#48994=CARTESIAN_POINT('Ctrl Pts',(-8.50622655072714,-3.22290265484426,
0.00296939138868677));
#48995=CARTESIAN_POINT('Origin',(-111.877773449273,0.,0.));
#48996=CARTESIAN_POINT('',(-11.2527734492734,-3.21916848922627,0.00227587122066043));
#48997=CARTESIAN_POINT('',(-11.0062265507271,-3.21947286547661,-0.00241691677691058));
#48998=CARTESIAN_POINT('',(-111.877773449273,-3.22275,5.46201577318104E-12));
#48999=CARTESIAN_POINT('Ctrl Pts',(-11.2527734492734,-3.21916848922627,
0.00227587122066008));
#49000=CARTESIAN_POINT('Ctrl Pts',(-11.2100495694357,-3.21466710984026,
-0.691557780719506));
#49001=CARTESIAN_POINT('Ctrl Pts',(-11.1010345123656,-2.65353338684402,
-2.4685938576754));
#49002=CARTESIAN_POINT('Ctrl Pts',(-10.925728278063,0.278439380911714,-3.80160665280418));
#49003=CARTESIAN_POINT('Ctrl Pts',(-10.7268547463655,3.34874129613322,-1.82089905350606));
#49004=CARTESIAN_POINT('Ctrl Pts',(-10.5279812146681,3.34221283258897,1.83285433495541));
#49005=CARTESIAN_POINT('Ctrl Pts',(-10.3291076829706,0.264852355988142,
3.80257739711041));
#49006=CARTESIAN_POINT('Ctrl Pts',(-10.154038427839,-2.65838111784463,2.46091167050225));
#49007=CARTESIAN_POINT('Ctrl Pts',(-10.04526034994,-3.21469993916871,0.687795703115145));
#49008=CARTESIAN_POINT('Ctrl Pts',(-10.0027734492734,-3.21908627855254,
-0.00223366033731895));
#49009=CARTESIAN_POINT('Ctrl Pts',(-11.0062265507271,-3.21947286547661,
-0.00241691677691058));
#49010=CARTESIAN_POINT('Ctrl Pts',(-10.9834991149381,-3.22203123295323,
-0.371421649411236));
#49011=CARTESIAN_POINT('Ctrl Pts',(-10.960771679149,-3.1634971455758,-0.73963942385066));
#49012=CARTESIAN_POINT('Ctrl Pts',(-10.93804424336,-3.04034292773192,-1.08480060297804));
#49013=CARTESIAN_POINT('Ctrl Pts',(-10.8717530661275,-2.68112782939031,
-2.09156357930684));
#49014=CARTESIAN_POINT('Ctrl Pts',(-10.805461888895,-1.77214605123412,-2.90216867478603));
#49015=CARTESIAN_POINT('Ctrl Pts',(-10.7391707116625,-0.730984755342044,
-3.14422307635583));
#49016=CARTESIAN_POINT('Ctrl Pts',(-10.67287953443,0.310176540550037,-3.38627747792563));
#49017=CARTESIAN_POINT('Ctrl Pts',(-10.6065883571975,1.48351735417808,-3.05978118558606));
#49018=CARTESIAN_POINT('Ctrl Pts',(-10.540297179965,2.25000371116705,-2.31472693123087));
#49019=CARTESIAN_POINT('Ctrl Pts',(-10.4740060027326,3.01649006815602,-1.56967267687569));
#49020=CARTESIAN_POINT('Ctrl Pts',(-10.4077148255001,3.37612196850593,-0.40606046050502));
#49021=CARTESIAN_POINT('Ctrl Pts',(-10.3414236482676,3.16368414798498,0.641545071074154));
#49022=CARTESIAN_POINT('Ctrl Pts',(-10.2751324710351,2.95124632746403,1.68915060265333));
#49023=CARTESIAN_POINT('Ctrl Pts',(-10.2088412938026,2.16673878607194,2.62074944944104));
#49024=CARTESIAN_POINT('Ctrl Pts',(-10.1425501165701,1.17056509372838,3.00836414480955));
#49025=CARTESIAN_POINT('Ctrl Pts',(-10.0762589393376,0.174391401384763,
3.39597884017807));
#49026=CARTESIAN_POINT('Ctrl Pts',(-10.0099677621052,-1.03344844191028,
3.23960938412756));
#49027=CARTESIAN_POINT('Ctrl Pts',(-9.94367658487268,-1.89807157213503,
2.61109206530215));
#49028=CARTESIAN_POINT('Ctrl Pts',(-9.88119324015751,-2.71302987201674,
2.01867741932453));
#49029=CARTESIAN_POINT('Ctrl Pts',(-9.81870989544233,-3.22306845834968,
1.00679837785737));
#49030=CARTESIAN_POINT('Ctrl Pts',(-9.75622655072715,-3.22760441255983,
-0.00112366029274946));
#49031=CARTESIAN_POINT('Origin',(-111.877773449273,0.,0.));
#49032=CARTESIAN_POINT('',(-12.5027734492734,-3.2273897063871,0.00135230010112807));
#49033=CARTESIAN_POINT('',(-12.2562265507271,-3.21880858818939,0.00207596960425688));
#49034=CARTESIAN_POINT('',(-111.877773449273,-3.22275,5.46201577318104E-12));
#49035=CARTESIAN_POINT('Ctrl Pts',(-12.5027734492734,-3.2273897063871,0.00135230010112817));
#49036=CARTESIAN_POINT('Ctrl Pts',(-12.441129966164,-3.22213887174583,-0.993197620900722));
#49037=CARTESIAN_POINT('Ctrl Pts',(-12.3131953058221,-2.19561978059315,
-3.06664260054507));
#49038=CARTESIAN_POINT('Ctrl Pts',(-12.1189694682477,1.33713176289026,-3.56956864062838));
#49039=CARTESIAN_POINT('Ctrl Pts',(-11.9200959365502,3.72586027392076,-0.804802367483259));
#49040=CARTESIAN_POINT('Ctrl Pts',(-11.7212224048527,2.69126071506615,2.6994179733841));
#49041=CARTESIAN_POINT('Ctrl Pts',(-11.5223488731553,-0.816074714683047,
3.72340753766527));
#49042=CARTESIAN_POINT('Ctrl Pts',(-11.3661992212955,-2.98120175167232,
1.84128690775568));
#49043=CARTESIAN_POINT('Ctrl Pts',(-11.2763407466682,-3.22165153493936,
0.385007591278511));
#49044=CARTESIAN_POINT('Ctrl Pts',(-11.2527734492734,-3.21916848922627,
0.00227587122066008));
#49045=CARTESIAN_POINT('Ctrl Pts',(-12.2562265507271,-3.21880858818939,
0.00207596960425688));
#49046=CARTESIAN_POINT('Ctrl Pts',(-12.2145795116663,-3.21483379457629,
-0.674459605817695));
#49047=CARTESIAN_POINT('Ctrl Pts',(-12.106641295373,-2.67539305780387,-2.43366078039877));
#49048=CARTESIAN_POINT('Ctrl Pts',(-11.9324119018472,0.216673464944433,
-3.80562665550321));
#49049=CARTESIAN_POINT('Ctrl Pts',(-11.7335383701498,3.31873265494329,-1.87503471874537));
#49050=CARTESIAN_POINT('Ctrl Pts',(-11.5346648384523,3.37153346731751,1.77834296755299));
#49051=CARTESIAN_POINT('Ctrl Pts',(-11.3357913067549,0.326562407243348,
3.79777548384086));
#49052=CARTESIAN_POINT('Ctrl Pts',(-11.1596452108464,-2.63618345387206,
2.49579366496414));
#49053=CARTESIAN_POINT('Ctrl Pts',(-11.0497902921705,-3.21456901005255,
0.704887986120656));
#49054=CARTESIAN_POINT('Ctrl Pts',(-11.0062265507271,-3.21947286547661,
-0.00241691677691072));
#49055=CARTESIAN_POINT('Origin',(-111.877773449273,0.,0.));
#49056=CARTESIAN_POINT('',(-13.7527734492734,-3.22331905496246,-0.00294047133718037));
#49057=CARTESIAN_POINT('',(-13.5062265507271,-3.22706651782617,0.00162965321757597));
#49058=CARTESIAN_POINT('',(-111.877773449273,-3.22275,5.46201577318104E-12));
#49059=CARTESIAN_POINT('Ctrl Pts',(-13.7527734492734,-3.22331905496246,
-0.0029404713371806));
#49060=CARTESIAN_POINT('Ctrl Pts',(-13.7385015401247,-3.22546742958381,
-0.233959350890419));
#49061=CARTESIAN_POINT('Ctrl Pts',(-13.6579384537435,-3.09724369363227,
-1.53566484139185));
#49062=CARTESIAN_POINT('Ctrl Pts',(-13.5110841901299,-1.32827764686602,
-3.57287281110364));
#49063=CARTESIAN_POINT('Ctrl Pts',(-13.3122106584324,2.28772241734737,-3.04894535415999));
#49064=CARTESIAN_POINT('Ctrl Pts',(-13.113337126735,3.80175842718431,0.276359354501727));
#49065=CARTESIAN_POINT('Ctrl Pts',(-12.9144635950375,1.82273098807798,3.34774452080618));
#49066=CARTESIAN_POINT('Ctrl Pts',(-12.7155900633401,-1.83102542543786,
3.3432151475619));
#49067=CARTESIAN_POINT('Ctrl Pts',(-12.578360014752,-3.19136838569029,1.22046724841446));
#49068=CARTESIAN_POINT('Ctrl Pts',(-12.5074211433965,-3.2277856001957,0.076337742028997));
#49069=CARTESIAN_POINT('Ctrl Pts',(-12.5027734492734,-3.2273897063871,0.00135230010112817));
#49070=CARTESIAN_POINT('Ctrl Pts',(-13.5062265507271,-3.22706651782617,
0.00162965321757594));
#49071=CARTESIAN_POINT('Ctrl Pts',(-13.4456599083945,-3.22103553945658,
-0.975805603394261));
#49072=CARTESIAN_POINT('Ctrl Pts',(-13.3188020888295,-2.22558674433784,
-3.03369259275898));
#49073=CARTESIAN_POINT('Ctrl Pts',(-13.125653092032,1.27899402439183,-3.59080992494138));
#49074=CARTESIAN_POINT('Ctrl Pts',(-12.9267795603345,3.71230094882514,-0.865195525207697));
#49075=CARTESIAN_POINT('Ctrl Pts',(-12.727906028637,2.7347381391122,2.65536229956906));
#49076=CARTESIAN_POINT('Ctrl Pts',(-12.5290324969396,-0.755507687979863,
3.73616779131918));
#49077=CARTESIAN_POINT('Ctrl Pts',(-12.3718060043029,-2.96605047436436,
1.87671656148758));
#49078=CARTESIAN_POINT('Ctrl Pts',(-12.2808706888988,-3.22116062485788,
0.402407819712684));
#49079=CARTESIAN_POINT('Ctrl Pts',(-12.2562265507271,-3.21880858818939,
0.00207596960425688));
#49080=CARTESIAN_POINT('Origin',(-111.877773449273,0.,0.));
#49081=CARTESIAN_POINT('',(-15.0027734492734,-3.21740572002881,1.23680267080692E-5));
#49082=CARTESIAN_POINT('',(-14.7562265507271,-3.22385176614053,-0.00287592034953293));
#49083=CARTESIAN_POINT('',(-111.877773449273,-3.22275,5.46201577318104E-12));
#49084=CARTESIAN_POINT('Ctrl Pts',(-15.0027734492734,-3.21740594292328,
1.23675108736412E-5));
#49085=CARTESIAN_POINT('Ctrl Pts',(-14.9695819368529,-3.21738754235116,
-0.539755110259676));
#49086=CARTESIAN_POINT('Ctrl Pts',(-14.8700992472,-2.83239271434753,-2.15758856500936));
#49087=CARTESIAN_POINT('Ctrl Pts',(-14.7043253803146,-0.269013228516049,
-3.80228530154838));
#49088=CARTESIAN_POINT('Ctrl Pts',(-14.5054518486171,3.05335991141382,-2.28182709311162));
#49089=CARTESIAN_POINT('Ctrl Pts',(-14.3065783169197,3.5702996953566,1.33517853368896));
#49090=CARTESIAN_POINT('Ctrl Pts',(-14.1077047852222,0.806840788407417,
3.72541938225076));
#49091=CARTESIAN_POINT('Ctrl Pts',(-13.9231031626735,-2.44642853613299,
2.76684638869372));
#49092=CARTESIAN_POINT('Ctrl Pts',(-13.8047927173572,-3.21548850656084,
0.839093548266301));
#49093=CARTESIAN_POINT('Ctrl Pts',(-13.7527734492734,-3.22331905496246,
-0.0029404713371806));
#49094=CARTESIAN_POINT('Ctrl Pts',(-14.7562265507271,-3.22385176614053,
-0.00287592034953311));
#49095=CARTESIAN_POINT('Ctrl Pts',(-14.7430314823553,-3.22582786069339,
-0.216373387529147));
#49096=CARTESIAN_POINT('Ctrl Pts',(-14.6635452367509,-3.10904390727391,
-1.50031730597109));
#49097=CARTESIAN_POINT('Ctrl Pts',(-14.5177678139141,-1.38611763102972,
-3.55083364077171));
#49098=CARTESIAN_POINT('Ctrl Pts',(-14.3188942822166,2.23791305875133,-3.08569064764402));
#49099=CARTESIAN_POINT('Ctrl Pts',(-14.1200207505192,3.80574463510616,0.214591248302973));
#49100=CARTESIAN_POINT('Ctrl Pts',(-13.9211472188217,1.87685022649435,3.31770626469487));
#49101=CARTESIAN_POINT('Ctrl Pts',(-13.7222736871243,-1.77649802390547,
3.37250595292984));
#49102=CARTESIAN_POINT('Ctrl Pts',(-13.5839667977594,-3.18207374482736,
1.25564508237175));
#49103=CARTESIAN_POINT('Ctrl Pts',(-13.511951085627,-3.22763654358338,0.0940132165684776));
#49104=CARTESIAN_POINT('Ctrl Pts',(-13.5062265507271,-3.22706651782617,
0.00162965321757594));
#49105=CARTESIAN_POINT('Origin',(-111.877773449273,0.,0.));
#49106=CARTESIAN_POINT('',(-16.2527734492734,-3.22336460159151,0.00293616943835841));
#49107=CARTESIAN_POINT('',(-16.0062265507271,-3.21742729147399,-0.000277243005420702));
#49108=CARTESIAN_POINT('',(-111.877773449273,-3.22275,5.46201577318104E-12));
#49109=CARTESIAN_POINT('Ctrl Pts',(-16.2527734492734,-3.22336460159151,
0.00293616943835843));
#49110=CARTESIAN_POINT('Ctrl Pts',(-16.2006623335812,-3.21552069030317,
-0.840554018209381));
#49111=CARTESIAN_POINT('Ctrl Pts',(-16.0822600406565,-2.44421333433486,
-2.76975741814941));
#49112=CARTESIAN_POINT('Ctrl Pts',(-15.8975665704993,0.811999827878098,
-3.7242983112277));
#49113=CARTESIAN_POINT('Ctrl Pts',(-15.6986930388018,3.57214553169364,-1.33023228493699));
#49114=CARTESIAN_POINT('Ctrl Pts',(-15.4998195071044,3.05019658640061,2.28605389608329));
#49115=CARTESIAN_POINT('Ctrl Pts',(-15.3009459754069,-0.274279245362296,
3.80190906349047));
#49116=CARTESIAN_POINT('Ctrl Pts',(-15.1352639561299,-2.83395933390405,
2.1545767662713));
#49117=CARTESIAN_POINT('Ctrl Pts',(-15.0358731140854,-3.21742429257731,
0.538286199818229));
#49118=CARTESIAN_POINT('Ctrl Pts',(-15.0027734492734,-3.21740594292328,
1.23675108736412E-5));
#49119=CARTESIAN_POINT('Ctrl Pts',(-16.0062265507271,-3.21742729147399,
-0.000277243005420841));
#49120=CARTESIAN_POINT('Ctrl Pts',(-15.9741118790835,-3.21782654169675,
-0.522524268552057));
#49121=CARTESIAN_POINT('Ctrl Pts',(-15.8757060302074,-2.85057785483279,
-2.12226533114537));
#49122=CARTESIAN_POINT('Ctrl Pts',(-15.7110090040988,-0.330717988254753,
-3.79741586394379));
#49123=CARTESIAN_POINT('Ctrl Pts',(-15.5121354724014,3.01590581912008,-2.33110568651127));
#49124=CARTESIAN_POINT('Ctrl Pts',(-15.3132619407039,3.59150916741074,1.27702918208321));
#49125=CARTESIAN_POINT('Ctrl Pts',(-15.1143884090065,0.867226518337144,
3.71182701609064));
#49126=CARTESIAN_POINT('Ctrl Pts',(-14.9287099456809,-2.42024454403094,
2.80092311042059));
#49127=CARTESIAN_POINT('Ctrl Pts',(-14.8093226595878,-3.21590008839693,
0.856224194889351));
#49128=CARTESIAN_POINT('Ctrl Pts',(-14.7562265507271,-3.22385176614053,
-0.00287592034953311));
#49129=CARTESIAN_POINT('Origin',(-111.877773449273,0.,0.));
#49130=CARTESIAN_POINT('',(-17.5027734492734,-3.22736416564808,-0.00137668428022306));
#49131=CARTESIAN_POINT('',(-17.2562265507271,-3.22283081774483,0.00297248829486646));
#49132=CARTESIAN_POINT('',(-111.877773449273,-3.22275,5.46201577318104E-12));
#49133=CARTESIAN_POINT('Ctrl Pts',(-17.5027734492734,-3.22736416564808,
-0.00137668428022343));
#49134=CARTESIAN_POINT('Ctrl Pts',(-17.4980339075419,-3.22777406182281,
-0.0778455910693476));
#49135=CARTESIAN_POINT('Ctrl Pts',(-17.4270031885779,-3.19058738217639,
-1.22346672950067));
#49136=CARTESIAN_POINT('Ctrl Pts',(-17.2896812923814,-1.82639321974484,
-3.34574796396226));
#49137=CARTESIAN_POINT('Ctrl Pts',(-17.0908077606841,1.82736596257257,-3.34521677478736));
#49138=CARTESIAN_POINT('Ctrl Pts',(-16.8919342289865,3.8021375463979,-0.271093544295971));
#49139=CARTESIAN_POINT('Ctrl Pts',(-16.6930606972891,2.28349734576807,3.05211099132349));
#49140=CARTESIAN_POINT('Ctrl Pts',(-16.4941871655916,-1.33322490479584,
3.57102968129913));
#49141=CARTESIAN_POINT('Ctrl Pts',(-16.3474247495864,-3.09826305778849,
1.53264926624996));
#49142=CARTESIAN_POINT('Ctrl Pts',(-16.2669535108137,-3.2254990242249,0.232459997715443));
#49143=CARTESIAN_POINT('Ctrl Pts',(-16.2527734492734,-3.22336460159151,
0.00293616943835843));
#49144=CARTESIAN_POINT('Ctrl Pts',(-17.2562265507271,-3.22283081774483,
0.00297248829486629));
#49145=CARTESIAN_POINT('Ctrl Pts',(-17.2051922758117,-3.21517670414338,
-0.823437962111514));
#49146=CARTESIAN_POINT('Ctrl Pts',(-17.0878668236639,-2.46997325366766,
-2.73557685842927));
#49147=CARTESIAN_POINT('Ctrl Pts',(-16.9042501942836,0.75141887432542,-3.73699228080485));
#49148=CARTESIAN_POINT('Ctrl Pts',(-16.7053766625861,3.55007471849215,-1.38806020208435));
#49149=CARTESIAN_POINT('Ctrl Pts',(-16.5065031308886,3.08691462203722,2.23622444037719));
#49150=CARTESIAN_POINT('Ctrl Pts',(-16.3076295991912,-0.212508967422626,
3.80586147544186));
#49151=CARTESIAN_POINT('Ctrl Pts',(-16.1408707391373,-2.81540856813534,
2.18987439132723));
#49152=CARTESIAN_POINT('Ctrl Pts',(-16.040403056316,-3.2170024084915,0.555499212860509));
#49153=CARTESIAN_POINT('Ctrl Pts',(-16.0062265507271,-3.21742729147399,
-0.000277243005420841));
#49154=CARTESIAN_POINT('Origin',(-111.877773449273,0.,0.));
#49155=CARTESIAN_POINT('',(-18.7527734492734,-3.21913642963925,-0.00225963407795738));
#49156=CARTESIAN_POINT('',(-18.5062265507271,-3.2276379359672,-0.0010831830032082));
#49157=CARTESIAN_POINT('',(-111.877773449273,-3.22275,5.46201577318104E-12));
#49158=CARTESIAN_POINT('Ctrl Pts',(-18.7527734492734,-3.21913642963925,
-0.00225963407795737));
#49159=CARTESIAN_POINT('Ctrl Pts',(-18.7291143042701,-3.22160981599308,
-0.38649256276537));
#49160=CARTESIAN_POINT('Ctrl Pts',(-18.6391639820344,-2.97992372187582,
-1.84430888910775));
#49161=CARTESIAN_POINT('Ctrl Pts',(-18.4829224825662,-0.810916905050859,
-3.72453425337853));
#49162=CARTESIAN_POINT('Ctrl Pts',(-18.2840489508687,2.69499690552984,-2.69568791047329));
#49163=CARTESIAN_POINT('Ctrl Pts',(-18.0851754191713,3.72474202574661,0.809962019556789));
#49164=CARTESIAN_POINT('Ctrl Pts',(-17.8863018874738,1.33218652479678,3.57141718294536));
#49165=CARTESIAN_POINT('Ctrl Pts',(-17.6921678975079,-2.19819478851725,
3.06383880510527));
#49166=CARTESIAN_POINT('Ctrl Pts',(-17.5643250847744,-3.22204091260597,
0.991712214289981));
#49167=CARTESIAN_POINT('Ctrl Pts',(-17.5027734492734,-3.22736416564808,
-0.00137668428022343));
#49168=CARTESIAN_POINT('Ctrl Pts',(-18.5062265507271,-3.2276379359672,-0.00108318300320796));
#49169=CARTESIAN_POINT('Ctrl Pts',(-18.5025638497725,-3.22789541356105,
-0.0601647665002562));
#49170=CARTESIAN_POINT('Ctrl Pts',(-18.4326099715853,-3.19960698219719,
-1.18831160629045));
#49171=CARTESIAN_POINT('Ctrl Pts',(-18.2963649161657,-1.88047955591764,
-3.31565050499345));
#49172=CARTESIAN_POINT('Ctrl Pts',(-18.0974913844683,1.7728065417542,-3.37444789513792));
#49173=CARTESIAN_POINT('Ctrl Pts',(-17.8986178527708,3.79723434880727,-0.332795630568509));
#49174=CARTESIAN_POINT('Ctrl Pts',(-17.6997443210734,2.33275543941922,3.01462994268742));
#49175=CARTESIAN_POINT('Ctrl Pts',(-17.5008707893759,-1.27506395749001,
3.59220733474523));
#49176=CARTESIAN_POINT('Ctrl Pts',(-17.3530315325938,-3.08615971431661,
1.56801179161404));
#49177=CARTESIAN_POINT('Ctrl Pts',(-17.2714834530442,-3.22511904587652,
0.250031225518313));
#49178=CARTESIAN_POINT('Ctrl Pts',(-17.2562265507271,-3.22283081774483,
0.00297248829486629));
#49179=CARTESIAN_POINT('Origin',(-111.877773449273,0.,0.));
#49180=CARTESIAN_POINT('',(-20.0027734492734,-3.21911794458563,0.00225014293279763));
#49181=CARTESIAN_POINT('',(-19.7562265507271,-3.21952745218103,-0.00243989411713524));
#49182=CARTESIAN_POINT('',(-111.877773449273,-3.22275,5.46201577318104E-12));
#49183=CARTESIAN_POINT('Ctrl Pts',(-20.0027734492734,-3.21911794458563,
0.00225014293279763));
#49184=CARTESIAN_POINT('Ctrl Pts',(-19.9601947009984,-3.21468695194116,
-0.689253840355445));
#49185=CARTESIAN_POINT('Ctrl Pts',(-19.9176159527234,-2.99638332267943,
-1.38330928292528));
#49186=CARTESIAN_POINT('Ctrl Pts',(-19.8750372044484,-2.58522570477275,
-1.9331542933282));
#49187=CARTESIAN_POINT('Ctrl Pts',(-19.8087460272159,-1.9450912803623,-2.78921217458851));
#49188=CARTESIAN_POINT('Ctrl Pts',(-19.7424548499834,-0.837486249488049,
-3.29570954814478));
#49189=CARTESIAN_POINT('Ctrl Pts',(-19.6761636727509,0.228754499558577,
-3.21996100059655));
#49190=CARTESIAN_POINT('Ctrl Pts',(-19.6098724955184,1.29499524860508,-3.14421245304832));
#49191=CARTESIAN_POINT('Ctrl Pts',(-19.5435813182859,2.31987171582406,-2.48621798439587));
#49192=CARTESIAN_POINT('Ctrl Pts',(-19.4772901410535,2.83255459999984,-1.54826092905904));
#49193=CARTESIAN_POINT('Ctrl Pts',(-19.410998963821,3.34523748417564,-0.610303873722163));
#49194=CARTESIAN_POINT('Ctrl Pts',(-19.3447077865885,3.34572678530815,0.607615768299051));
#49195=CARTESIAN_POINT('Ctrl Pts',(-19.278416609356,2.83379771795475,1.54598446309963));
#49196=CARTESIAN_POINT('Ctrl Pts',(-19.2121254321235,2.32186865060138,2.48435315790015));
#49197=CARTESIAN_POINT('Ctrl Pts',(-19.145834254891,1.29752121476204,3.14317090548006));
#49198=CARTESIAN_POINT('Ctrl Pts',(-19.0795430776586,0.231341674093708,
3.21977615623486));
#49199=CARTESIAN_POINT('Ctrl Pts',(-19.0132519004261,-0.834837866574687,
3.29638140698965));
#49200=CARTESIAN_POINT('Ctrl Pts',(-18.9469607231936,-1.9428495120721,2.79077416091938));
#49201=CARTESIAN_POINT('Ctrl Pts',(-18.8806695459611,-2.58367157493215,
1.93523090594343));
#49202=CARTESIAN_POINT('Ctrl Pts',(-18.8380375137319,-2.99578594637027,
1.38502876529158));
#49203=CARTESIAN_POINT('Ctrl Pts',(-18.7954054815026,-3.21467957007237,
0.690099730433788));
#49204=CARTESIAN_POINT('Ctrl Pts',(-18.7527734492734,-3.21913642963925,
-0.00225963407795738));
#49205=CARTESIAN_POINT('Ctrl Pts',(-19.7562265507271,-3.21952745218103,
-0.00243989411713538));
#49206=CARTESIAN_POINT('Ctrl Pts',(-19.7336442465007,-3.22209647376765,
-0.369072624276772));
#49207=CARTESIAN_POINT('Ctrl Pts',(-19.6447707650418,-2.99474137424233,
-1.80887857682269));
#49208=CARTESIAN_POINT('Ctrl Pts',(-19.4896061063505,-0.871287725163321,
-3.71087581730611));
#49209=CARTESIAN_POINT('Ctrl Pts',(-19.290732574653,2.65086992728046,-2.7390929630313));
#49210=CARTESIAN_POINT('Ctrl Pts',(-19.0918590429556,3.73740284758043,0.749374129781112));
#49211=CARTESIAN_POINT('Ctrl Pts',(-18.8929855112581,1.39000235761673,3.5493147334813));
#49212=CARTESIAN_POINT('Ctrl Pts',(-18.6977746805153,-2.16778118645096,
3.09663127955505));
#49213=CARTESIAN_POINT('Ctrl Pts',(-18.5688550270049,-3.22323532991824,
1.00915204950376));
#49214=CARTESIAN_POINT('Ctrl Pts',(-18.5062265507271,-3.2276379359672,-0.00108318300320796));
#49215=CARTESIAN_POINT('Origin',(-111.877773449273,0.,0.));
#49216=CARTESIAN_POINT('',(-21.2527734492734,-3.22734916914202,0.00139077110789292));
#49217=CARTESIAN_POINT('',(-21.0062265507271,-3.21876282429886,0.00204748833280491));
#49218=CARTESIAN_POINT('',(-111.877773449273,-3.22275,5.46201577318104E-12));
#49219=CARTESIAN_POINT('Ctrl Pts',(-21.2527734492734,-3.22734916914202,
0.00139077110789292));
#49220=CARTESIAN_POINT('Ctrl Pts',(-21.1912750977266,-3.2219844149411,-0.990850652625185));
#49221=CARTESIAN_POINT('Ctrl Pts',(-21.1297767461798,-2.73000666275173,
-1.98768731231595));
#49222=CARTESIAN_POINT('Ctrl Pts',(-21.0682783946331,-1.93664422845416,
-2.58261235938075));
#49223=CARTESIAN_POINT('Ctrl Pts',(-21.0019872174006,-1.0814517164788,-3.22390242233522));
#49224=CARTESIAN_POINT('Ctrl Pts',(-20.9356960401681,0.123932366897174,
-3.39819443414427));
#49225=CARTESIAN_POINT('Ctrl Pts',(-20.8694048629357,1.12575333627981,-3.02541846564833));
#49226=CARTESIAN_POINT('Ctrl Pts',(-20.8031136857032,2.12757430566257,-2.65264249715234));
#49227=CARTESIAN_POINT('Ctrl Pts',(-20.7368225084707,2.92583216105199,-1.73279854835118));
#49228=CARTESIAN_POINT('Ctrl Pts',(-20.6705313312382,3.15380642416163,-0.688463873669388));
#49229=CARTESIAN_POINT('Ctrl Pts',(-20.6042401540057,3.38178068727125,0.355870801012347));
#49230=CARTESIAN_POINT('Ctrl Pts',(-20.5379489767732,3.03947135810111,1.52469620157494));
#49231=CARTESIAN_POINT('Ctrl Pts',(-20.4716577995407,2.2841356938992,2.28105273904104));
#49232=CARTESIAN_POINT('Ctrl Pts',(-20.4053666223082,1.52880002969724,3.03740927650718));
#49233=CARTESIAN_POINT('Ctrl Pts',(-20.3390754450758,0.360438030463874,
3.3812969508769));
#49234=CARTESIAN_POINT('Ctrl Pts',(-20.2727842678433,-0.684203601870848,
3.15473341149739));
#49235=CARTESIAN_POINT('Ctrl Pts',(-20.2064930906108,-1.72884523420545,
2.9281698721179));
#49236=CARTESIAN_POINT('Ctrl Pts',(-20.1402019133783,-2.64976649964112,
2.13115511898911));
#49237=CARTESIAN_POINT('Ctrl Pts',(-20.0739107361458,-3.02389522338553,
1.12983854794265));
#49238=CARTESIAN_POINT('Ctrl Pts',(-20.0501983071884,-3.15772149036564,
0.771666479710817));
#49239=CARTESIAN_POINT('Ctrl Pts',(-20.0264858782309,-3.22158559811115,
0.387353973877421));
#49240=CARTESIAN_POINT('Ctrl Pts',(-20.0027734492734,-3.21911794458563,
0.00225014293279763));
#49241=CARTESIAN_POINT('Ctrl Pts',(-21.0062265507271,-3.21876282429886,
0.00204748833280501));
#49242=CARTESIAN_POINT('Ctrl Pts',(-20.964724643229,-3.21485961808616,-0.672154526158193));
#49243=CARTESIAN_POINT('Ctrl Pts',(-20.8569315584983,-2.67830623265808,
-2.42894787761703));
#49244=CARTESIAN_POINT('Ctrl Pts',(-20.6828472965351,0.20834421543868,-3.80609173817195));
#49245=CARTESIAN_POINT('Ctrl Pts',(-20.4839737648378,3.31462113615585,-1.88229337650549));
#49246=CARTESIAN_POINT('Ctrl Pts',(-20.2851002331403,3.37541735115235,1.77096000435559));
#49247=CARTESIAN_POINT('Ctrl Pts',(-20.0862267014428,0.334873173258265,
3.79705169695109));
#49248=CARTESIAN_POINT('Ctrl Pts',(-19.9099354739718,-2.63315844852102,
2.50048966296161));
#49249=CARTESIAN_POINT('Ctrl Pts',(-19.7999354237332,-3.21455501725349,
0.707191119696958));
#49250=CARTESIAN_POINT('Ctrl Pts',(-19.7562265507271,-3.21952745218103,
-0.00243989411713538));
#49251=CARTESIAN_POINT('Origin',(-111.877773449273,0.,0.));
#49252=CARTESIAN_POINT('',(-22.5027734492734,-3.22339102037588,-0.00293357075097584));
#49253=CARTESIAN_POINT('',(-22.2562265507271,-3.22701916559281,0.00166552852483643));
#49254=CARTESIAN_POINT('',(-111.877773449273,-3.22275,5.46201577318104E-12));
#49255=CARTESIAN_POINT('Ctrl Pts',(-22.5027734492734,-3.22339102037588,
-0.00293357075097572));
#49256=CARTESIAN_POINT('Ctrl Pts',(-22.4886466716873,-3.22551728192709,
-0.231590117755942));
#49257=CARTESIAN_POINT('Ctrl Pts',(-22.4082287168688,-3.0988533213393,-1.53089988227506));
#49258=CARTESIAN_POINT('Ctrl Pts',(-22.2615195848178,-1.33609380754272,
-3.56995727830645));
#49259=CARTESIAN_POINT('Ctrl Pts',(-22.0626460531204,2.28104422824517,-3.05394480308283));
#49260=CARTESIAN_POINT('Ctrl Pts',(-21.8637725214229,3.80235414351597,0.268038427794315));
#49261=CARTESIAN_POINT('Ctrl Pts',(-21.6648989897255,1.83005326445484,3.34374740085816));
#49262=CARTESIAN_POINT('Ctrl Pts',(-21.466025458028,-1.82370431158557,3.34721439638869));
#49263=CARTESIAN_POINT('Ctrl Pts',(-21.3286502778773,-3.19013329224575,
1.22520691434576));
#49264=CARTESIAN_POINT('Ctrl Pts',(-21.2575662749591,-3.22776726704359,
0.0787203264943862));
#49265=CARTESIAN_POINT('Ctrl Pts',(-21.2527734492734,-3.22734916914202,
0.00139077110789282));
#49266=CARTESIAN_POINT('Ctrl Pts',(-22.2562265507271,-3.22701916559281,
0.00166552852483633));
#49267=CARTESIAN_POINT('Ctrl Pts',(-22.1958050399572,-3.22089431753202,
-0.973465341318993));
#49268=CARTESIAN_POINT('Ctrl Pts',(-22.0690923519548,-2.22958833490889,
-3.02923894111559));
#49269=CARTESIAN_POINT('Ctrl Pts',(-21.8760884867199,1.27113236380313,-3.59360044317391));
#49270=CARTESIAN_POINT('Ctrl Pts',(-21.6772149550225,3.71039855154082,-0.873317937644316));
#49271=CARTESIAN_POINT('Ctrl Pts',(-21.478341423325,2.74054293166321,2.64937088215266));
#49272=CARTESIAN_POINT('Ctrl Pts',(-21.2794678916276,-0.747329160908197,
3.73781229554719));
#49273=CARTESIAN_POINT('Ctrl Pts',(-21.1220962674282,-2.96398036377416,
1.88149141963838));
#49274=CARTESIAN_POINT('Ctrl Pts',(-21.0310158204614,-3.22109422633476,
0.404751281969014));
#49275=CARTESIAN_POINT('Ctrl Pts',(-21.0062265507271,-3.21876282429886,
0.00204748833280501));
#49276=CARTESIAN_POINT('Origin',(-111.877773449273,0.,0.));
#49277=CARTESIAN_POINT('',(-23.7527734492733,-3.21740582208574,-2.67182391447498E-5));
#49278=CARTESIAN_POINT('',(-23.5062265507271,-3.22392320659701,-0.00286486488396187));
#49279=CARTESIAN_POINT('',(-111.877773449273,-3.22275,5.46201577318104E-12));
#49280=CARTESIAN_POINT('Ctrl Pts',(-23.7527734492733,-3.21740609865336,
-2.67168564435302E-5));
#49281=CARTESIAN_POINT('Ctrl Pts',(-23.7197270684156,-3.2174456747296,-0.537433969267299));
#49282=CARTESIAN_POINT('Ctrl Pts',(-23.6203895103253,-2.83486685131597,
-2.15282942535465));
#49283=CARTESIAN_POINT('Ctrl Pts',(-23.4547607750025,-0.277334002226216,
-3.80168745200032));
#49284=CARTESIAN_POINT('Ctrl Pts',(-23.2558872433051,3.04835875056794,-2.28850400028564));
#49285=CARTESIAN_POINT('Ctrl Pts',(-23.0570137116076,3.57321322422885,1.32736162581399));
#49286=CARTESIAN_POINT('Ctrl Pts',(-22.8581401799102,0.814992050687579,
3.7236446646805));
#49287=CARTESIAN_POINT('Ctrl Pts',(-22.6733934257988,-2.44292667337299,
2.77144582727945));
#49288=CARTESIAN_POINT('Ctrl Pts',(-22.5549378489198,-3.21553960793346,
0.841401340527108));
#49289=CARTESIAN_POINT('Ctrl Pts',(-22.5027734492734,-3.22339102037588,
-0.00293357075097572));
#49290=CARTESIAN_POINT('Ctrl Pts',(-23.5062265507271,-3.22392320659701,
-0.00286486488396215));
#49291=CARTESIAN_POINT('Ctrl Pts',(-23.4931766139179,-3.22587472894888,
-0.214002050993878));
#49292=CARTESIAN_POINT('Ctrl Pts',(-23.4138354998762,-3.11060913095701,
-1.49555465574787));
#49293=CARTESIAN_POINT('Ctrl Pts',(-23.2682032086021,-1.39388541978934,
-3.54779157617611));
#49294=CARTESIAN_POINT('Ctrl Pts',(-23.0693296769047,2.23115457073302,-3.09058099925963));
#49295=CARTESIAN_POINT('Ctrl Pts',(-22.8704561452071,3.8062051604974,0.206261745581809));
#49296=CARTESIAN_POINT('Ctrl Pts',(-22.6715826135097,1.8841066336201,3.31359077507109));
#49297=CARTESIAN_POINT('Ctrl Pts',(-22.4727090818123,-1.76911293681183,
3.37638579672));
#49298=CARTESIAN_POINT('Ctrl Pts',(-22.3342570608847,-3.18079789745064,
1.26038805836638));
#49299=CARTESIAN_POINT('Ctrl Pts',(-22.2620962171897,-3.22761416586329,
0.0963949202665974));
#49300=CARTESIAN_POINT('Ctrl Pts',(-22.2562265507271,-3.22701916559281,
0.00166552852483633));
#49301=CARTESIAN_POINT('Origin',(-111.877773449273,0.,0.));
#49302=CARTESIAN_POINT('',(-25.0027734492734,-3.22329262847075,0.00294286404255992));
#49303=CARTESIAN_POINT('',(-24.7562265507271,-3.21743373373988,-0.000316139430206752));
#49304=CARTESIAN_POINT('',(-111.877773449273,-3.22275,5.46201577318104E-12));
#49305=CARTESIAN_POINT('Ctrl Pts',(-25.0027734492734,-3.22329262847075,
0.00294286404255977));
#49306=CARTESIAN_POINT('Ctrl Pts',(-24.9508074651438,-3.21547008177197,
-0.838246332242223));
#49307=CARTESIAN_POINT('Ctrl Pts',(-24.8325503037818,-2.44771210523894,
-2.76515722257126));
#49308=CARTESIAN_POINT('Ctrl Pts',(-24.6480019651872,0.803847142238303,
-3.72606647866122));
#49309=CARTESIAN_POINT('Ctrl Pts',(-24.4491284334898,3.56922572285289,-1.33804684925931));
#49310=CARTESIAN_POINT('Ctrl Pts',(-24.2502549017923,3.05519238071696,2.27937297261687));
#49311=CARTESIAN_POINT('Ctrl Pts',(-24.0513813700949,-0.265957993964293,
3.80250022707872));
#49312=CARTESIAN_POINT('Ctrl Pts',(-23.8855542192552,-2.8314825312375,2.15933571928619));
#49313=CARTESIAN_POINT('Ctrl Pts',(-23.786018245648,-3.21736628495631,0.540607210760987));
#49314=CARTESIAN_POINT('Ctrl Pts',(-23.7527734492733,-3.21740609865336,
-2.67168564435302E-5));
#49315=CARTESIAN_POINT('Ctrl Pts',(-24.7562265507271,-3.21743373373988,
-0.000316139430206856));
#49316=CARTESIAN_POINT('Ctrl Pts',(-24.7242570106461,-3.21788699032318,
-0.520200448775454));
#49317=CARTESIAN_POINT('Ctrl Pts',(-24.6259962933327,-2.85299839799472,
-2.11750267593112));
#49318=CARTESIAN_POINT('Ctrl Pts',(-24.4614443987868,-0.339027957278562,
-3.79668298329881));
#49319=CARTESIAN_POINT('Ctrl Pts',(-24.2625708670894,3.01079690025812,-2.33770050624184));
#49320=CARTESIAN_POINT('Ctrl Pts',(-24.0636973353919,3.59429538385108,1.26916599588641));
#49321=CARTESIAN_POINT('Ctrl Pts',(-23.8648238036945,0.87534788869354,3.70992017505057));
#49322=CARTESIAN_POINT('Ctrl Pts',(-23.6790002088062,-2.41667997468913,
2.80550681899019));
#49323=CARTESIAN_POINT('Ctrl Pts',(-23.5594677911504,-3.21596136952096,
0.858534378066973));
#49324=CARTESIAN_POINT('Ctrl Pts',(-23.5062265507271,-3.22392320659701,
-0.00286486488396215));
#49325=CARTESIAN_POINT('Origin',(-111.877773449273,0.,0.));
#49326=CARTESIAN_POINT('',(-26.2527734492733,-3.22740434264695,-0.00133809533540642));
#49327=CARTESIAN_POINT('',(-26.0062265507271,-3.22275904721707,0.0029750263946704));
#49328=CARTESIAN_POINT('',(-111.877773449273,-3.22275,5.46201577318104E-12));
#49329=CARTESIAN_POINT('Ctrl Pts',(-26.2527734492733,-3.22740434264695,
-0.00133809533540624));
#49330=CARTESIAN_POINT('Ctrl Pts',(-26.2481790391045,-3.2277921929266,-0.075462967587538));
#49331=CARTESIAN_POINT('Ctrl Pts',(-26.1772934517032,-3.19182047039241,
-1.21872722919777));
#49332=CARTESIAN_POINT('Ctrl Pts',(-26.0401166870694,-1.83371111782523,
-3.34174283388943));
#49333=CARTESIAN_POINT('Ctrl Pts',(-25.841243155372,1.82004047686151,-3.34920800997384));
#49334=CARTESIAN_POINT('Ctrl Pts',(-25.6423696236745,3.80153514436882,-0.279413989657449));
#49335=CARTESIAN_POINT('Ctrl Pts',(-25.4434960919771,2.29017151564223,3.04710617806936));
#49336=CARTESIAN_POINT('Ctrl Pts',(-25.2446225602796,-1.32540640400279,
3.57393893284649));
#49337=CARTESIAN_POINT('Ctrl Pts',(-25.0977150127117,-3.09665122005086,
1.53741433471344));
#49338=CARTESIAN_POINT('Ctrl Pts',(-25.0170986423763,-3.22544902931438,
0.234829123385659));
#49339=CARTESIAN_POINT('Ctrl Pts',(-25.0027734492734,-3.22329262847075,
0.00294286404255977));
#49340=CARTESIAN_POINT('Ctrl Pts',(-26.0062265507271,-3.22275904721707,
0.00297502639467036));
#49341=CARTESIAN_POINT('Ctrl Pts',(-25.9553374073744,-3.21513583440698,
-0.82113218938988));
#49342=CARTESIAN_POINT('Ctrl Pts',(-25.8381570867892,-2.47340976517071,
-2.73096178962243));
#49343=CARTESIAN_POINT('Ctrl Pts',(-25.6546855889715,0.74323855262528,-3.73862783456431));
#49344=CARTESIAN_POINT('Ctrl Pts',(-25.4558120572741,3.54702840433774,-1.39582632526716));
#49345=CARTESIAN_POINT('Ctrl Pts',(-25.2569385255766,3.09180127512853,2.22946327769737));
#49346=CARTESIAN_POINT('Ctrl Pts',(-25.0580649938792,-0.204179213979529,
3.80631744341775));
#49347=CARTESIAN_POINT('Ctrl Pts',(-24.8911610022627,-2.81287761522076,
2.19462930958641));
#49348=CARTESIAN_POINT('Ctrl Pts',(-24.7905481878786,-3.21694712968023,
0.55781765232775));
#49349=CARTESIAN_POINT('Ctrl Pts',(-24.7562265507271,-3.21743373373988,
-0.000316139430206856));
#49350=CARTESIAN_POINT('Origin',(-111.877773449273,0.,0.));
#49351=CARTESIAN_POINT('',(-27.5027734492733,-3.21918720133157,-0.00228521908616954));
#49352=CARTESIAN_POINT('',(-27.2562265507271,-3.22767036229815,-0.00104244248707641));
#49353=CARTESIAN_POINT('',(-111.877773449273,-3.22275,5.46201577318104E-12));
#49354=CARTESIAN_POINT('Ctrl Pts',(-27.5027734492733,-3.21918720133157,
-0.00228521908616927));
#49355=CARTESIAN_POINT('Ctrl Pts',(-27.4792594358328,-3.22167572177667,
-0.384146036416285));
#49356=CARTESIAN_POINT('Ctrl Pts',(-27.3894542451597,-2.98194196490443,
-1.83953375038598));
#49357=CARTESIAN_POINT('Ctrl Pts',(-27.2333578772542,-0.819066220437877,
-3.72275061722178));
#49358=CARTESIAN_POINT('Ctrl Pts',(-27.0344843455567,2.68909085581776,-2.70157953809338));
#49359=CARTESIAN_POINT('Ctrl Pts',(-26.8356108138592,3.72650573231153,0.801808367714392));
#49360=CARTESIAN_POINT('Ctrl Pts',(-26.6367372821618,1.33999949042545,3.56849309893504));
#49361=CARTESIAN_POINT('Ctrl Pts',(-26.4424581606331,-2.19412430154369,
3.06826860367683));
#49362=CARTESIAN_POINT('Ctrl Pts',(-26.314470216337,-3.22219603353229,0.994059531111112));
#49363=CARTESIAN_POINT('Ctrl Pts',(-26.2527734492733,-3.22740434264695,
-0.00133809533540624));
#49364=CARTESIAN_POINT('Ctrl Pts',(-27.2562265507271,-3.22767036229815,
-0.00104244248707691));
#49365=CARTESIAN_POINT('Ctrl Pts',(-27.2527089813351,-3.22790942823879,
-0.0577814477878739));
#49366=CARTESIAN_POINT('Ctrl Pts',(-27.1829002347107,-3.20079977205244,
-1.18357548571261));
#49367=CARTESIAN_POINT('Ctrl Pts',(-27.0468003108537,-1.88773145525861,
-3.31152707739417));
#49368=CARTESIAN_POINT('Ctrl Pts',(-26.8479267791563,1.765417213501,-3.37831965535559));
#49369=CARTESIAN_POINT('Ctrl Pts',(-26.6490532474588,3.79649692161308,-0.341105197365262));
#49370=CARTESIAN_POINT('Ctrl Pts',(-26.4501797157614,2.33934746290421,3.00951741634616));
#49371=CARTESIAN_POINT('Ctrl Pts',(-26.2513061840639,-1.26719924803898,
3.5949892485593));
#49372=CARTESIAN_POINT('Ctrl Pts',(-26.1033217957191,-3.08450295152784,
1.57277896528229));
#49373=CARTESIAN_POINT('Ctrl Pts',(-26.0216285846069,-3.22506627768389,
0.252398113950421));
#49374=CARTESIAN_POINT('Ctrl Pts',(-26.0062265507271,-3.22275904721707,
0.00297502639467036));
#49375=CARTESIAN_POINT('Origin',(-111.877773449273,0.,0.));
#49376=CARTESIAN_POINT('',(-28.7527734492734,-3.21906802306727,0.00222402768671319));
#49377=CARTESIAN_POINT('',(-28.506226550727,-3.21958260577835,-0.0024624483620983));
#49378=CARTESIAN_POINT('',(-111.877773449273,-3.22275,5.46201577318104E-12));
#49379=CARTESIAN_POINT('Ctrl Pts',(-28.7527734492734,-3.21906802306727,
0.00222402768671311));
#49380=CARTESIAN_POINT('Ctrl Pts',(-28.710339832561,-3.21470762532615,-0.686949761698418));
#49381=CARTESIAN_POINT('Ctrl Pts',(-28.6016150386162,-2.65946822477964,
-2.45918392203356));
#49382=CARTESIAN_POINT('Ctrl Pts',(-28.4265990674389,0.261796888079818,
-3.80278897927288));
#49383=CARTESIAN_POINT('Ctrl Pts',(-28.2277255357414,3.34073904970577,-1.83553922138932));
#49384=CARTESIAN_POINT('Ctrl Pts',(-28.028852004044,3.35020331301418,1.81820774196901));
#49385=CARTESIAN_POINT('Ctrl Pts',(-27.8299784723465,0.281493893444737,
3.80138169873015));
#49386=CARTESIAN_POINT('Ctrl Pts',(-27.6546189540897,-2.6524404997523,2.47032073267811));
#49387=CARTESIAN_POINT('Ctrl Pts',(-27.5455506130652,-3.21466003513985,
0.692403621248377));
#49388=CARTESIAN_POINT('Ctrl Pts',(-27.5027734492733,-3.21918720133157,
-0.00228521908616927));
#49389=CARTESIAN_POINT('Ctrl Pts',(-28.506226550727,-3.21958260577835,-0.00246244836209827));
#49390=CARTESIAN_POINT('Ctrl Pts',(-28.4837893780633,-3.22216159046997,
-0.366723212734714));
#49391=CARTESIAN_POINT('Ctrl Pts',(-28.3950610281671,-2.99671073763452,
-1.80410351630265));
#49392=CARTESIAN_POINT('Ctrl Pts',(-28.2400415010384,-0.879407004066094,
-3.70896009046836));
#49393=CARTESIAN_POINT('Ctrl Pts',(-28.041167969341,2.64486898995689,-2.74488791345875));
#49394=CARTESIAN_POINT('Ctrl Pts',(-27.8422944376435,3.73903392537052,0.741192914439823));
#49395=CARTESIAN_POINT('Ctrl Pts',(-27.6434209059461,1.3977668128979,3.54626417068001));
#49396=CARTESIAN_POINT('Ctrl Pts',(-27.4480649436406,-2.16364472461151,
3.10103735652865));
#49397=CARTESIAN_POINT('Ctrl Pts',(-27.3190001585676,-3.22340405510307,
1.01150675587474));
#49398=CARTESIAN_POINT('Ctrl Pts',(-27.2562265507271,-3.22767036229815,
-0.00104244248707691));
#49399=CARTESIAN_POINT('Origin',(-111.877773449273,0.,0.));
#49400=CARTESIAN_POINT('',(-30.0027734492733,-3.22730766174399,0.00142891566604214));
#49401=CARTESIAN_POINT('',(-29.7562265507271,-3.21871773150106,0.0020186574082677));
#49402=CARTESIAN_POINT('',(-111.877773449273,-3.22275,5.46201577318104E-12));
#49403=CARTESIAN_POINT('Ctrl Pts',(-30.0027734492733,-3.22730766174399,
0.00142891566604205));
#49404=CARTESIAN_POINT('Ctrl Pts',(-29.9414202292892,-3.22183176265191,
-0.988504625625889));
#49405=CARTESIAN_POINT('Ctrl Pts',(-29.8137758320727,-2.20374537616861,
-3.05777759031298));
#49406=CARTESIAN_POINT('Ctrl Pts',(-29.6198402576236,1.32149477066622,-3.57538714023941));
#49407=CARTESIAN_POINT('Ctrl Pts',(-29.4209667259261,3.72230192179151,-0.821102937831022));
#49408=CARTESIAN_POINT('Ctrl Pts',(-29.2220931942287,2.70305042427431,2.68761232980465));
#49409=CARTESIAN_POINT('Ctrl Pts',(-29.0232196625312,-0.799769353165428,
3.72694387041513));
#49410=CARTESIAN_POINT('Ctrl Pts',(-28.8667797475461,-2.97715376913023,
1.85083715862348));
#49411=CARTESIAN_POINT('Ctrl Pts',(-28.7766310097935,-3.22151958060727,
0.389699964527589));
#49412=CARTESIAN_POINT('Ctrl Pts',(-28.7527734492734,-3.21906802306727,
0.00222402768671311));
#49413=CARTESIAN_POINT('Ctrl Pts',(-29.7562265507271,-3.21871773150106,
0.00201865740826774));
#49414=CARTESIAN_POINT('Ctrl Pts',(-29.7148697747916,-3.21488621482395,
-0.669849273457447));
#49415=CARTESIAN_POINT('Ctrl Pts',(-29.6072218216236,-2.68121160462978,
-2.42423387462879));
#49416=CARTESIAN_POINT('Ctrl Pts',(-29.4332826912232,0.200013968032432,
-3.80653859090899));
#49417=CARTESIAN_POINT('Ctrl Pts',(-29.2344091595257,3.31049374141978,-1.88954301869738));
#49418=CARTESIAN_POINT('Ctrl Pts',(-29.0355356278283,3.37928506784462,1.76356855884025));
#49419=CARTESIAN_POINT('Ctrl Pts',(-28.8366620961308,0.343182335340544,
3.79630972342846));
#49420=CARTESIAN_POINT('Ctrl Pts',(-28.6602257370971,-2.63012550325009,
2.50518437947119));
#49421=CARTESIAN_POINT('Ctrl Pts',(-28.5500805552958,-3.21454191691153,
0.709494154389844));
#49422=CARTESIAN_POINT('Ctrl Pts',(-28.506226550727,-3.21958260577835,-0.00246244836209827));
#49423=CARTESIAN_POINT('Origin',(-111.877773449273,0.,0.));
#49424=CARTESIAN_POINT('',(-31.2527734492733,-3.22346295616709,-0.00292610916508903));
#49425=CARTESIAN_POINT('',(-31.0062265507271,-3.22697096224228,0.00170102469852499));
#49426=CARTESIAN_POINT('',(-111.877773449273,-3.22275,5.46201577318104E-12));
#49427=CARTESIAN_POINT('Ctrl Pts',(-31.2527734492733,-3.22346295616709,
-0.00292610916508954));
#49428=CARTESIAN_POINT('Ctrl Pts',(-31.23879180325,-3.22556674346952,-0.229220593505158));
#49429=CARTESIAN_POINT('Ctrl Pts',(-31.1585189799941,-3.10045693566244,
-1.52613522338862));
#49430=CARTESIAN_POINT('Ctrl Pts',(-31.0119549795058,-1.34390356876819,
-3.56702464658427));
#49431=CARTESIAN_POINT('Ctrl Pts',(-30.8130814478083,2.27435511368902,-3.05892962461122));
#49432=CARTESIAN_POINT('Ctrl Pts',(-30.6142079161109,3.80293164781777,0.259716217270925));
#49433=CARTESIAN_POINT('Ctrl Pts',(-30.4153343844134,1.83736677547631,3.33973426545636));
#49434=CARTESIAN_POINT('Ctrl Pts',(-30.216460852716,-1.81637446278761,3.35119761315571));
#49435=CARTESIAN_POINT('Ctrl Pts',(-30.0789405410026,-3.18889273168686,
1.22994703057292));
#49436=CARTESIAN_POINT('Ctrl Pts',(-30.0077114065217,-3.22774838442522,
0.0811028024957301));
#49437=CARTESIAN_POINT('Ctrl Pts',(-30.0027734492733,-3.22730766174399,
0.00142891566604205));
#49438=CARTESIAN_POINT('Ctrl Pts',(-31.0062265507271,-3.22697096224228,
0.00170102469852487));
#49439=CARTESIAN_POINT('Ctrl Pts',(-30.9459501715198,-3.22075485181861,
-0.971125934525062));
#49440=CARTESIAN_POINT('Ctrl Pts',(-30.8193826150801,-2.2335811040131,-3.02478230262524));
#49441=CARTESIAN_POINT('Ctrl Pts',(-30.6265238814079,1.26326461490713,-3.59637374923839));
#49442=CARTESIAN_POINT('Ctrl Pts',(-30.4276503497104,3.70847838266379,-0.881436167174301));
#49443=CARTESIAN_POINT('Ctrl Pts',(-30.228776818013,2.74633459791199,2.64336677511825));
#49444=CARTESIAN_POINT('Ctrl Pts',(-30.0299032863155,-0.739147054374844,
3.73943889687965));
#49445=CARTESIAN_POINT('Ctrl Pts',(-29.8723865305536,-2.96190354995556,
1.88626621384466));
#49446=CARTESIAN_POINT('Ctrl Pts',(-29.7811609520241,-3.22102779006444,
0.407094348824174));
#49447=CARTESIAN_POINT('Ctrl Pts',(-29.7562265507271,-3.21871773150106,
0.00201865740826774));
#49448=CARTESIAN_POINT('Origin',(-111.877773449273,0.,0.));
#49449=CARTESIAN_POINT('',(-32.5027734492733,-3.21740710269033,-6.57967736794519E-5));
#49450=CARTESIAN_POINT('',(-32.256226550727,-3.22399452161269,-0.00285325182603574));
#49451=CARTESIAN_POINT('',(-111.877773449273,-3.22275,5.46201577318104E-12));
#49452=CARTESIAN_POINT('Ctrl Pts',(-32.5027734492733,-3.21740710269033,
-6.57967736795301E-5));
#49453=CARTESIAN_POINT('Ctrl Pts',(-32.4698721999782,-3.21750414203768,
-0.535112472795859));
#49454=CARTESIAN_POINT('Ctrl Pts',(-32.3706797734506,-2.83733373420474,
-2.14806978347254));
#49455=CARTESIAN_POINT('Ctrl Pts',(-32.2051961696905,-0.285653447597213,
-3.80107139361567));
#49456=CARTESIAN_POINT('Ctrl Pts',(-32.0063226379931,3.04334298908304,-2.29516994627558));
#49457=CARTESIAN_POINT('Ctrl Pts',(-31.8074491062956,3.57610963858108,1.31953836031194));
#49458=CARTESIAN_POINT('Ctrl Pts',(-31.6085755745982,0.823139409423143,
3.72185211207294));
#49459=CARTESIAN_POINT('Ctrl Pts',(-31.423683688924,-2.43941638392043,2.77604319386724));
#49460=CARTESIAN_POINT('Ctrl Pts',(-31.3050829804824,-3.21559205689173,
0.843709427971166));
#49461=CARTESIAN_POINT('Ctrl Pts',(-31.2527734492733,-3.22346295616709,
-0.00292610916508954));
#49462=CARTESIAN_POINT('Ctrl Pts',(-32.256226550727,-3.22399452161269,-0.00285325182603602));
#49463=CARTESIAN_POINT('Ctrl Pts',(-32.2433217454805,-3.22592118045966,
-0.211630441180156));
#49464=CARTESIAN_POINT('Ctrl Pts',(-32.1641257630016,-3.11216840772355,
-1.49079233067677));
#49465=CARTESIAN_POINT('Ctrl Pts',(-32.0186386032901,-1.40164653229475,
-3.54473251882192));
#49466=CARTESIAN_POINT('Ctrl Pts',(-31.8197650715926,2.22438539621574,-3.09545654800542));
#49467=CARTESIAN_POINT('Ctrl Pts',(-31.6208915398952,3.8066474554137,0.1979312549345));
#49468=CARTESIAN_POINT('Ctrl Pts',(-31.4220180081977,1.89135401649272,3.30945941443378));
#49469=CARTESIAN_POINT('Ctrl Pts',(-31.2231444765003,-1.7617193762471,3.38024946872905));
#49470=CARTESIAN_POINT('Ctrl Pts',(-31.08454732401,-3.1795165237794,1.26513147465124));
#49471=CARTESIAN_POINT('Ctrl Pts',(-31.0122413487523,-3.22759124914724,
0.0987764919080167));
#49472=CARTESIAN_POINT('Ctrl Pts',(-31.0062265507271,-3.22697096224228,
0.00170102469852487));
#49473=CARTESIAN_POINT('Origin',(-111.877773449273,0.,0.));
#49474=CARTESIAN_POINT('',(-33.7527734492733,-3.22322064294668,0.00294899761280168));
#49475=CARTESIAN_POINT('',(-33.506226550727,-3.21744102079098,-0.000354983176735213));
#49476=CARTESIAN_POINT('',(-111.877773449273,-3.22275,5.46201577318104E-12));
#49477=CARTESIAN_POINT('Ctrl Pts',(-33.7527734492733,-3.22322064294668,
0.00294899761280141));
#49478=CARTESIAN_POINT('Ctrl Pts',(-33.7009525967064,-3.21542081039077,
-0.83593893015554));
#49479=CARTESIAN_POINT('Ctrl Pts',(-33.5828405669071,-2.45120246003302,
-2.76055497526885));
#49480=CARTESIAN_POINT('Ctrl Pts',(-33.3984373598752,0.795690606434006,
-3.72781679945786));
#49481=CARTESIAN_POINT('Ctrl Pts',(-33.1995638281778,3.56628881859093,-1.34585500477608));
#49482=CARTESIAN_POINT('Ctrl Pts',(-33.0006902964803,3.06017354166348,2.27268113170112));
#49483=CARTESIAN_POINT('Ctrl Pts',(-32.8018167647829,-0.257635468714778,
3.8030731779375));
#49484=CARTESIAN_POINT('Ctrl Pts',(-32.6358444823805,-2.82899846132347,
2.16409415778827));
#49485=CARTESIAN_POINT('Ctrl Pts',(-32.5361633772107,-3.21730862202821,
0.542927868763348));
#49486=CARTESIAN_POINT('Ctrl Pts',(-32.5027734492733,-3.21740710269033,
-6.57967736795301E-5));
#49487=CARTESIAN_POINT('Ctrl Pts',(-33.506226550727,-3.21744102079098,-0.000354983176735595));
#49488=CARTESIAN_POINT('Ctrl Pts',(-33.4744021422088,-3.21794772146192,
-0.517876261114896));
#49489=CARTESIAN_POINT('Ctrl Pts',(-33.376286556458,-2.85541175867603,-2.11273958371276));
#49490=CARTESIAN_POINT('Ctrl Pts',(-33.2118797934747,-0.347336302469681,
-3.79593191778697));
#49491=CARTESIAN_POINT('Ctrl Pts',(-33.0130062617774,3.005673560666,-2.34428412915341));
#49492=CARTESIAN_POINT('Ctrl Pts',(-32.8141327300798,3.59706438479482,1.26129673080056));
#49493=CARTESIAN_POINT('Ctrl Pts',(-32.6152591983825,0.883465066420513,
3.70799556470907));
#49494=CARTESIAN_POINT('Ctrl Pts',(-32.4292904719315,-2.41310692203674,
2.81008834410801));
#49495=CARTESIAN_POINT('Ctrl Pts',(-32.309612922713,-3.21602405449369,0.860844919524442));
#49496=CARTESIAN_POINT('Ctrl Pts',(-32.256226550727,-3.22399452161269,-0.00285325182603602));
#49497=CARTESIAN_POINT('Origin',(-111.877773449273,0.,0.));
#49498=CARTESIAN_POINT('',(-35.0027734492733,-3.22744352734777,-0.00129919044773077));
#49499=CARTESIAN_POINT('',(-34.756226550727,-3.22268735527833,0.00297700638213272));
#49500=CARTESIAN_POINT('',(-111.877773449273,-3.22275,5.46201577318104E-12));
#49501=CARTESIAN_POINT('Ctrl Pts',(-35.0027734492733,-3.22744352734777,
-0.0012991904477314));
#49502=CARTESIAN_POINT('Ctrl Pts',(-34.9983241706672,-3.22780977286361,
-0.0730802400329829));
#49503=CARTESIAN_POINT('Ctrl Pts',(-34.9275837148285,-3.19304810227478,
-1.2139881808383));
#49504=CARTESIAN_POINT('Ctrl Pts',(-34.7905520817575,-1.84102023303062,
-3.33772169796395));
#49505=CARTESIAN_POINT('Ctrl Pts',(-34.5916785500599,1.81270627375333,-3.35318320355194));
#49506=CARTESIAN_POINT('Ctrl Pts',(-34.3928050183625,3.80091453423265,-0.287733096717287));
#49507=CARTESIAN_POINT('Ctrl Pts',(-34.193931486665,2.29683471634544,3.04208677017568));
#49508=CARTESIAN_POINT('Ctrl Pts',(-33.9950579549676,-1.3175815549477,3.5768310663979));
#49509=CARTESIAN_POINT('Ctrl Pts',(-33.848005275837,-3.09503335659972,1.54217969858807));
#49510=CARTESIAN_POINT('Ctrl Pts',(-33.7672437739389,-3.22539864859171,
0.237197954771449));
#49511=CARTESIAN_POINT('Ctrl Pts',(-33.7527734492733,-3.22322064294668,
0.00294899761280141));
#49512=CARTESIAN_POINT('Ctrl Pts',(-34.756226550727,-3.22268735527833,0.00297700638213272));
#49513=CARTESIAN_POINT('Ctrl Pts',(-34.705482538937,-3.21509624485328,-0.818826640955584));
#49514=CARTESIAN_POINT('Ctrl Pts',(-34.5884473499145,-2.47683791878395,
-2.72634477769257));
#49515=CARTESIAN_POINT('Ctrl Pts',(-34.4051209836595,0.735054671056124,
-3.74024548152205));
#49516=CARTESIAN_POINT('Ctrl Pts',(-34.206247451962,3.54396510108007,-1.40358576289945));
#49517=CARTESIAN_POINT('Ctrl Pts',(-34.0073739202646,3.09667311950531,2.22269143661931));
#49518=CARTESIAN_POINT('Ctrl Pts',(-33.8085003885672,-0.195848482584929,
3.80675518038088));
#49519=CARTESIAN_POINT('Ctrl Pts',(-33.6414512653879,-2.8103393237568,2.19938364520229));
#49520=CARTESIAN_POINT('Ctrl Pts',(-33.5406933194413,-3.21689224908883,
0.560135754024039));
#49521=CARTESIAN_POINT('Ctrl Pts',(-33.506226550727,-3.21744102079098,-0.000354983176735595));
#49522=CARTESIAN_POINT('Origin',(-111.877773449273,0.,0.));
#49523=CARTESIAN_POINT('',(-36.2527734492733,-3.21923858670683,-0.00231041055963243));
#49524=CARTESIAN_POINT('',(-36.006226550727,-3.22770167512206,-0.00100144746363884));
#49525=CARTESIAN_POINT('',(-111.877773449273,-3.22275,5.46201577318104E-12));
#49526=CARTESIAN_POINT('Ctrl Pts',(-36.2527734492733,-3.21923858670683,
-0.00231041055963242));
#49527=CARTESIAN_POINT('Ctrl Pts',(-36.2294045673954,-3.22174153913682,
-0.381799118952256));
#49528=CARTESIAN_POINT('Ctrl Pts',(-36.139744508285,-2.98395358934763,-1.83475860293934));
#49529=CARTESIAN_POINT('Ctrl Pts',(-35.9837932719421,-0.827211612766053,
-3.72094915030997));
#49530=CARTESIAN_POINT('Ctrl Pts',(-35.7849197402446,2.68317192624198,-2.70745822603308));
#49531=CARTESIAN_POINT('Ctrl Pts',(-35.5860462085473,3.72825159013562,0.793650875472599));
#49532=CARTESIAN_POINT('Ctrl Pts',(-35.3871726768497,1.34780603789606,3.56555192301254));
#49533=CARTESIAN_POINT('Ctrl Pts',(-35.1927484237585,-2.19004494105729,
3.07269526205072));
#49534=CARTESIAN_POINT('Ctrl Pts',(-35.0646153478996,-3.22235296771607,
0.99640780537872));
#49535=CARTESIAN_POINT('Ctrl Pts',(-35.0027734492733,-3.22744352734777,
-0.0012991904477314));
#49536=CARTESIAN_POINT('Ctrl Pts',(-36.006226550727,-3.22770167512206,-0.001001447463639));
#49537=CARTESIAN_POINT('Ctrl Pts',(-36.0028541128977,-3.22792288376692,
-0.0553980490410728));
#49538=CARTESIAN_POINT('Ctrl Pts',(-35.9331904978359,-3.2019871633926,-1.17883982497487));
#49539=CARTESIAN_POINT('Ctrl Pts',(-35.7972357055417,-1.89497431298474,
-3.30738778866578));
#49540=CARTESIAN_POINT('Ctrl Pts',(-35.5983621738442,1.75801942947801,-3.3821752345296));
#49541=CARTESIAN_POINT('Ctrl Pts',(-35.3994886421468,3.79574131044322,-0.34941313038003));
#49542=CARTESIAN_POINT('Ctrl Pts',(-35.2006151104493,2.34592828168183,3.00439047540306));
#49543=CARTESIAN_POINT('Ctrl Pts',(-35.0017415787519,-1.25932846911898,
3.59775394355339));
#49544=CARTESIAN_POINT('Ctrl Pts',(-34.8536120588444,-3.08284009568445,
1.57754640695969));
#49545=CARTESIAN_POINT('Ctrl Pts',(-34.7717737161695,-3.22501315187002,
0.254764691582217));
#49546=CARTESIAN_POINT('Ctrl Pts',(-34.756226550727,-3.22268735527833,0.00297700638213272));
#49547=CARTESIAN_POINT('Origin',(-111.877773449273,0.,0.));
#49548=CARTESIAN_POINT('',(-37.5027734492733,-3.219018731458,0.00219753035672858));
#49549=CARTESIAN_POINT('',(-37.256226550727,-3.21963831861728,-0.00248457511186462));
#49550=CARTESIAN_POINT('',(-111.877773449273,-3.22275,5.46201577318104E-12));
#49551=CARTESIAN_POINT('Ctrl Pts',(-37.5027734492733,-3.219018731458,0.00219753035672829));
#49552=CARTESIAN_POINT('Ctrl Pts',(-37.4604849641236,-3.21472912215605,
-0.684645539904419));
#49553=CARTESIAN_POINT('Ctrl Pts',(-37.3519053017415,-2.66242384752364,
-2.45447718507084));
#49554=CARTESIAN_POINT('Ctrl Pts',(-37.1770344621268,0.253473740852287,
-3.80335282273231));
#49555=CARTESIAN_POINT('Ctrl Pts',(-36.9781609304294,3.33671391532343,-1.84284613540428));
#49556=CARTESIAN_POINT('Ctrl Pts',(-36.7792873987319,3.35417449321223,1.81087136499863));
#49557=CARTESIAN_POINT('Ctrl Pts',(-36.5804138670345,0.289812659703135,
3.80075653702829));
#49558=CARTESIAN_POINT('Ctrl Pts',(-36.404909217215,-2.64945837149216,2.47502346421667));
#49559=CARTESIAN_POINT('Ctrl Pts',(-36.2956957446279,-3.21464134221648,
0.694707380468959));
#49560=CARTESIAN_POINT('Ctrl Pts',(-36.2527734492733,-3.21923858670683,
-0.00231041055963242));
#49561=CARTESIAN_POINT('Ctrl Pts',(-37.256226550727,-3.21963831861728,-0.00248457511186476));
#49562=CARTESIAN_POINT('Ctrl Pts',(-37.233934509626,-3.22222657760521,-0.364373415634379));
#49563=CARTESIAN_POINT('Ctrl Pts',(-37.1453512912924,-2.99867355361791,
-1.7993284911519));
#49564=CARTESIAN_POINT('Ctrl Pts',(-36.9904768957264,-0.887522070897608,
-3.70702659892766));
#49565=CARTESIAN_POINT('Ctrl Pts',(-36.7916033640289,2.63885538457792,-2.75066971677293));
#49566=CARTESIAN_POINT('Ctrl Pts',(-36.5927298323315,3.74064709441386,0.733008149027457));
#49567=CARTESIAN_POINT('Ctrl Pts',(-36.393856300634,1.40552457333426,3.54319662243588));
#49568=CARTESIAN_POINT('Ctrl Pts',(-36.1983552067659,-2.15949934739163,
3.10544016138809));
#49569=CARTESIAN_POINT('Ctrl Pts',(-36.0691452901302,-3.22357464008568,
1.01386250920722));
#49570=CARTESIAN_POINT('Ctrl Pts',(-36.006226550727,-3.22770167512206,-0.001001447463639));
#49571=CARTESIAN_POINT('Origin',(-111.877773449273,0.,0.));
#49572=CARTESIAN_POINT('',(-38.7527734492733,-3.22726520035117,0.00146672624921877));
#49573=CARTESIAN_POINT('',(-38.506226550727,-3.21867331583696,0.00198948205692828));
#49574=CARTESIAN_POINT('',(-111.877773449273,-3.22275,5.46201577318104E-12));
#49575=CARTESIAN_POINT('Ctrl Pts',(-38.7527734492733,-3.22726520035117,
0.00146672624921861));
#49576=CARTESIAN_POINT('Ctrl Pts',(-38.6915653608519,-3.22168090845198,
-0.986159528139468));
#49577=CARTESIAN_POINT('Ctrl Pts',(-38.564066095198,-2.20779488141114,-3.05334042855296));
#49578=CARTESIAN_POINT('Ctrl Pts',(-38.3702756523116,1.31366676153256,-3.57827070959312));
#49579=CARTESIAN_POINT('Ctrl Pts',(-38.1714021206141,3.7204959985358,-0.829247343297895));
#49580=CARTESIAN_POINT('Ctrl Pts',(-37.9725285889167,2.70892587289195,2.68169018469027));
#49581=CARTESIAN_POINT('Ctrl Pts',(-37.7736550572192,-0.791610906928228,
3.7286852647441));
#49582=CARTESIAN_POINT('Ctrl Pts',(-37.6170700106714,-2.97511982063936,
1.85561225222715));
#49583=CARTESIAN_POINT('Ctrl Pts',(-37.5267761413561,-3.22145348812676,
0.392045562660032));
#49584=CARTESIAN_POINT('Ctrl Pts',(-37.5027734492733,-3.219018731458,0.00219753035672829));
#49585=CARTESIAN_POINT('Ctrl Pts',(-38.506226550727,-3.21867331583696,0.00198948205692842));
#49586=CARTESIAN_POINT('Ctrl Pts',(-38.4650149063542,-3.21491357698761,
-0.667543843238478));
#49587=CARTESIAN_POINT('Ctrl Pts',(-38.3575120847489,-2.68410918284495,
-2.419518782989));
#49588=CARTESIAN_POINT('Ctrl Pts',(-38.1837180859111,0.191682762624847,
-3.80696721157406));
#49589=CARTESIAN_POINT('Ctrl Pts',(-37.9848445542137,3.30635049050394,-1.89678361059766));
#49590=CARTESIAN_POINT('Ctrl Pts',(-37.7859710225162,3.38313659886923,1.75616866640966));
#49591=CARTESIAN_POINT('Ctrl Pts',(-37.5870974908188,0.351489853691939,
3.79554956682676));
#49592=CARTESIAN_POINT('Ctrl Pts',(-37.4105160002224,-2.62708460916839,
2.50987780220601));
#49593=CARTESIAN_POINT('Ctrl Pts',(-37.3002256868585,-3.21452971689538,
0.711797095481222));
#49594=CARTESIAN_POINT('Ctrl Pts',(-37.256226550727,-3.21963831861728,-0.00248457511186476));
#49595=CARTESIAN_POINT('Origin',(-111.877773449273,0.,0.));
#49596=CARTESIAN_POINT('',(-40.0027734492733,-3.22353484965401,-0.00291808672030292));
#49597=CARTESIAN_POINT('',(-39.756226550727,-3.22692192365936,0.00173613518965589));
#49598=CARTESIAN_POINT('',(-111.877773449273,-3.22275,5.46201577318104E-12));
#49599=CARTESIAN_POINT('Ctrl Pts',(-40.0027734492733,-3.22353484965401,
-0.00291808672030294));
#49600=CARTESIAN_POINT('Ctrl Pts',(-39.9889369348126,-3.22561581060293,
-0.226850780479683));
#49601=CARTESIAN_POINT('Ctrl Pts',(-39.9088092431194,-3.10205454560406,
-1.52137086821301));
#49602=CARTESIAN_POINT('Ctrl Pts',(-39.7623903741938,-1.35170689313597,
-3.56407492998341));
#49603=CARTESIAN_POINT('Ctrl Pts',(-39.5635168424963,2.2676551057174,-3.06389979486944));
#49604=CARTESIAN_POINT('Ctrl Pts',(-39.3646433107988,3.80349093732365,0.251392762791839));
#49605=CARTESIAN_POINT('Ctrl Pts',(-39.1657697791013,1.84467148611344,3.33570513382216));
#49606=CARTESIAN_POINT('Ctrl Pts',(-38.966896247404,-1.80903591415121,3.35516477878489));
#49607=CARTESIAN_POINT('Ctrl Pts',(-38.8292308041279,-3.18764669610349,
1.23468759585245));
#49608=CARTESIAN_POINT('Ctrl Pts',(-38.7578565380844,-3.22772895362958,
0.0834851668289423));
#49609=CARTESIAN_POINT('Ctrl Pts',(-38.7527734492733,-3.22726520035117,
0.00146672624921861));
#49610=CARTESIAN_POINT('Ctrl Pts',(-39.756226550727,-3.22692192365936,0.00173613518965601));
#49611=CARTESIAN_POINT('Ctrl Pts',(-39.6960953030824,-3.22061713569807,
-0.968787371651353));
#49612=CARTESIAN_POINT('Ctrl Pts',(-39.5696728782054,-2.23756505773814,
-3.02032269454104));
#49613=CARTESIAN_POINT('Ctrl Pts',(-39.3769592760958,1.25539081538779,-3.59912982985154));
#49614=CARTESIAN_POINT('Ctrl Pts',(-39.1780857443985,3.70654045139103,-0.889550174914005));
#49615=CARTESIAN_POINT('Ctrl Pts',(-38.9792122127009,2.75211311011837,2.63735000722356));
#49616=CARTESIAN_POINT('Ctrl Pts',(-38.7803386810035,-0.73096140756941,
3.74104758752567));
#49617=CARTESIAN_POINT('Ctrl Pts',(-38.6226767936788,-2.95982002325488,
1.89104093761493));
#49618=CARTESIAN_POINT('Ctrl Pts',(-38.5313060835867,-3.22096132194424,
0.409437019954045));
#49619=CARTESIAN_POINT('Ctrl Pts',(-38.506226550727,-3.21867331583696,0.00198948205692842));
#49620=CARTESIAN_POINT('Origin',(-111.877773449273,0.,0.));
#49621=CARTESIAN_POINT('',(-41.2527734492733,-3.2174089549063,-0.000104865731855516));
#49622=CARTESIAN_POINT('',(-41.006226550727,-3.22406569797495,-0.00284108206035388));
#49623=CARTESIAN_POINT('',(-111.877773449273,-3.22275,5.46201577318104E-12));
#49624=CARTESIAN_POINT('Ctrl Pts',(-41.2527734492733,-3.21740895490631,
-0.000104865731855551));
#49625=CARTESIAN_POINT('Ctrl Pts',(-41.2200173315409,-3.21756293715421,
-0.532790619038696));
#49626=CARTESIAN_POINT('Ctrl Pts',(-41.1209700365759,-2.83979337265085,
-2.14330964829616));
#49627=CARTESIAN_POINT('Ctrl Pts',(-40.9556315643784,-0.293971524782049,
-3.8004371293451));
#49628=CARTESIAN_POINT('Ctrl Pts',(-40.7567580326811,3.03831265098276,-2.30182489915407));
#49629=CARTESIAN_POINT('Ctrl Pts',(-40.5578845009835,3.57898892454058,1.31170877465366));
#49630=CARTESIAN_POINT('Ctrl Pts',(-40.3590109692861,0.831282825590706,
3.72004173301395));
#49631=CARTESIAN_POINT('Ctrl Pts',(-40.1739739520493,-2.43589766006429,
2.78063847357564));
#49632=CARTESIAN_POINT('Ctrl Pts',(-40.0552281120451,-3.215645861056,0.846017818929096));
#49633=CARTESIAN_POINT('Ctrl Pts',(-40.0027734492733,-3.22353484965401,
-0.00291808672030294));
#49634=CARTESIAN_POINT('Ctrl Pts',(-41.006226550727,-3.22406569797495,-0.00284108206035385));
#49635=CARTESIAN_POINT('Ctrl Pts',(-40.9934668770432,-3.22596721187625,
-0.209258560572843));
#49636=CARTESIAN_POINT('Ctrl Pts',(-40.9144160261268,-3.11372174647206,
-1.48603033395852));
#49637=CARTESIAN_POINT('Ctrl Pts',(-40.7690739979781,-1.40940093137277,
-3.54165648336101));
#49638=CARTESIAN_POINT('Ctrl Pts',(-40.5702004662805,2.21760556762163,-3.10031727052911));
#49639=CARTESIAN_POINT('Ctrl Pts',(-40.3713269345832,3.80707151773659,0.189599816261364));
#49640=CARTESIAN_POINT('Ctrl Pts',(-40.1724534028856,1.89859234039963,3.30531220257079));
#49641=CARTESIAN_POINT('Ctrl Pts',(-39.9735798711882,-1.75431737762409,
3.38409695045128));
#49642=CARTESIAN_POINT('Ctrl Pts',(-39.8348375871353,-3.17822961575262,
1.2698753297387));
#49643=CARTESIAN_POINT('Ctrl Pts',(-39.7623864803149,-3.22756779500628,
0.101157928346097));
#49644=CARTESIAN_POINT('Ctrl Pts',(-39.756226550727,-3.22692192365936,0.00173613518965601));
#49645=CARTESIAN_POINT('Origin',(-111.877773449273,0.,0.));
#49646=CARTESIAN_POINT('',(-42.5027734492733,-3.22314865752612,0.00295457023921248));
#49647=CARTESIAN_POINT('',(-42.256226550727,-3.21744915169808,-0.000393767763913477));
#49648=CARTESIAN_POINT('',(-111.877773449273,-3.22275,5.46201577318104E-12));
#49649=CARTESIAN_POINT('Ctrl Pts',(-42.5027734492733,-3.22314865752612,
0.00295457023921235));
#49650=CARTESIAN_POINT('Ctrl Pts',(-42.4510977282691,-3.21537286851395,
-0.833631803745193));
#49651=CARTESIAN_POINT('Ctrl Pts',(-42.3331308300324,-2.45468440648667,
-2.75595069101997));
#49652=CARTESIAN_POINT('Ctrl Pts',(-42.1488727545632,0.787530259532762,
-3.72954926523403));
#49653=CARTESIAN_POINT('Ctrl Pts',(-41.9499992228658,3.56333483297472,-1.35365671408838));
#49654=CARTESIAN_POINT('Ctrl Pts',(-41.7511256911682,3.06514004538181,2.2659784053879));
#49655=CARTESIAN_POINT('Ctrl Pts',(-41.5522521594708,-0.249311709475826,
3.80362791332241));
#49656=CARTESIAN_POINT('Ctrl Pts',(-41.3861347455058,-2.82650711453577,
2.16885207273882));
#49657=CARTESIAN_POINT('Ctrl Pts',(-41.2863085087734,-3.21725131095449,
0.545248175732359));
#49658=CARTESIAN_POINT('Ctrl Pts',(-41.2527734492733,-3.21740895490631,
-0.000104865731855551));
#49659=CARTESIAN_POINT('Ctrl Pts',(-42.256226550727,-3.21744915169808,-0.000393767763913581));
#49660=CARTESIAN_POINT('Ctrl Pts',(-42.2245472737714,-3.21800872812467,
-0.515551704072911));
#49661=CARTESIAN_POINT('Ctrl Pts',(-42.1265768195833,-2.85781794654228,
-2.10797606309353));
#49662=CARTESIAN_POINT('Ctrl Pts',(-41.9623151881627,-0.355642984033713,
-3.7951626710057));
#49663=CARTESIAN_POINT('Ctrl Pts',(-41.7634416564653,3.00053582488292,-2.35085652371245));
#49664=CARTESIAN_POINT('Ctrl Pts',(-41.5645681247678,3.59981615697931,1.2534214245169));
#49665=CARTESIAN_POINT('Ctrl Pts',(-41.3656945930704,0.891578012639441,
3.70605319428438));
#49666=CARTESIAN_POINT('Ctrl Pts',(-41.1795807350568,-2.40952537855057,
2.81466767056952));
#49667=CARTESIAN_POINT('Ctrl Pts',(-41.0597580542757,-3.21608815084661,
0.863155827992277));
#49668=CARTESIAN_POINT('Ctrl Pts',(-41.006226550727,-3.22406569797495,-0.00284108206035385));
#49669=CARTESIAN_POINT('Origin',(-111.877773449273,0.,0.));
#49670=CARTESIAN_POINT('',(-43.7527734492733,-3.22748170351345,-0.00125997746166298));
#49671=CARTESIAN_POINT('',(-43.506226550727,-3.22261575386789,0.00297842904322623));
#49672=CARTESIAN_POINT('',(-111.877773449273,-3.22275,5.46201577318104E-12));
#49673=CARTESIAN_POINT('Ctrl Pts',(-43.7527734492733,-3.22748170351345,
-0.00125997746166296));
#49674=CARTESIAN_POINT('Ctrl Pts',(-43.7484693022298,-3.22782680043517,
-0.0706974116263659));
#49675=CARTESIAN_POINT('Ctrl Pts',(-43.6778739779538,-3.19427028568405,
-1.20924958558968));
#49676=CARTESIAN_POINT('Ctrl Pts',(-43.5409874764454,-1.84832053035247,
-3.33368457544577));
#49677=CARTESIAN_POINT('Ctrl Pts',(-43.3421139447478,1.80536338837631,-3.35714233648167));
#49678=CARTESIAN_POINT('Ctrl Pts',(-43.1432404130505,3.80027571896185,-0.296050825630079));
#49679=CARTESIAN_POINT('Ctrl Pts',(-42.944366881353,2.30348691596348,3.03705279168351));
#49680=CARTESIAN_POINT('Ctrl Pts',(-42.7454933496556,-1.30975039510868,
3.57970606810114));
#49681=CARTESIAN_POINT('Ctrl Pts',(-42.5982955389623,-3.09340945840058,
1.54694535430405));
#49682=CARTESIAN_POINT('Ctrl Pts',(-42.5173889055015,-3.22534788574663,
0.239566489580112));
#49683=CARTESIAN_POINT('Ctrl Pts',(-42.5027734492733,-3.22314865752612,
0.00295457023921235));
#49684=CARTESIAN_POINT('Ctrl Pts',(-43.506226550727,-3.22261575386789,0.00297842904322623));
#49685=CARTESIAN_POINT('Ctrl Pts',(-43.4556276704997,-3.21505792776503,
-0.816521309002297));
#49686=CARTESIAN_POINT('Ctrl Pts',(-43.3387376130398,-2.48025772245358,
-2.72172583709136));
#49687=CARTESIAN_POINT('Ctrl Pts',(-43.1555563783475,0.726867268816058,
-3.74184521393008));
#49688=CARTESIAN_POINT('Ctrl Pts',(-42.95668284665,3.54088482339137,-1.41133847781607));
#49689=CARTESIAN_POINT('Ctrl Pts',(-42.7578093149525,3.10153013183299,2.21590894957792));
#49690=CARTESIAN_POINT('Ctrl Pts',(-42.5589357832551,-0.187516813140302,
3.80717468423465));
#49691=CARTESIAN_POINT('Ctrl Pts',(-42.3917415285133,-2.80779368415632,
2.20413738880447));
#49692=CARTESIAN_POINT('Ctrl Pts',(-42.2908384510039,-3.21683777399834,
0.562453520176393));
#49693=CARTESIAN_POINT('Ctrl Pts',(-42.256226550727,-3.21744915169808,-0.000393767763913581));
#49694=CARTESIAN_POINT('Origin',(-111.877773449273,0.,0.));
#49695=CARTESIAN_POINT('',(-45.0027734492733,-3.21929057874326,-0.00233520374894584));
#49696=CARTESIAN_POINT('',(-44.756226550727,-3.22773185798094,-0.000960206790133755));
#49697=CARTESIAN_POINT('',(-111.877773449273,-3.22275,5.46201577318104E-12));
#49698=CARTESIAN_POINT('Ctrl Pts',(-45.0027734492733,-3.21929057874326,
-0.0023352037489462));
#49699=CARTESIAN_POINT('Ctrl Pts',(-44.979549698958,-3.22180726243893,-0.379451811020904));
#49700=CARTESIAN_POINT('Ctrl Pts',(-44.8900347714103,-2.98595860481547,
-1.8299834528453));
#49701=CARTESIAN_POINT('Ctrl Pts',(-44.7342286666301,-0.835353043022,-3.7191298612715));
#49702=CARTESIAN_POINT('Ctrl Pts',(-44.5353551349326,2.67724014515226,-2.71332394613555));
#49703=CARTESIAN_POINT('Ctrl Pts',(-44.3364816032351,3.72997959085687,0.785489581903391));
#49704=CARTESIAN_POINT('Ctrl Pts',(-44.1376080715378,1.35560612981737,3.56259366926528));
#49705=CARTESIAN_POINT('Ctrl Pts',(-43.9430386868837,-2.18595670130309,
3.07711876257639));
#49706=CARTESIAN_POINT('Ctrl Pts',(-43.8147604794623,-3.22251172151965,
0.998757048983725));
#49707=CARTESIAN_POINT('Ctrl Pts',(-43.7527734492733,-3.22748170351345,
-0.00125997746166296));
#49708=CARTESIAN_POINT('Ctrl Pts',(-44.756226550727,-3.22773185798094,-0.000960206790134015));
#49709=CARTESIAN_POINT('Ctrl Pts',(-44.7529992444603,-3.2279357792308,-0.0530145735234573));
#49710=CARTESIAN_POINT('Ctrl Pts',(-44.6834807609612,-3.2031691639196,-1.17410462500792));
#49711=CARTESIAN_POINT('Ctrl Pts',(-44.5476711002297,-1.90220809440512,
-3.30323265863413));
#49712=CARTESIAN_POINT('Ctrl Pts',(-44.3487975685321,1.75061322511827,-3.386014614193));
#49713=CARTESIAN_POINT('Ctrl Pts',(-44.1499240368348,3.79496751891687,-0.357719389820383));
#49714=CARTESIAN_POINT('Ctrl Pts',(-43.9510505051372,2.35249786423195,2.99924914441454));
#49715=CARTESIAN_POINT('Ctrl Pts',(-43.7521769734399,-1.2514516584285,3.60050140648546));
#49716=CARTESIAN_POINT('Ctrl Pts',(-43.6039023219698,-3.08117113765723,
1.58231411279105));
#49717=CARTESIAN_POINT('Ctrl Pts',(-43.5219188477322,-3.22495967237728,
0.257130956278012));
#49718=CARTESIAN_POINT('Ctrl Pts',(-43.506226550727,-3.22261575386789,0.00297842904322623));
#49719=CARTESIAN_POINT('Origin',(-111.877773449273,0.,0.));
#49720=CARTESIAN_POINT('',(-46.2527734492733,-3.21897007644484,0.00217065586278493));
#49721=CARTESIAN_POINT('',(-46.006226550727,-3.21969458294954,-0.00250627002517184));
#49722=CARTESIAN_POINT('',(-111.877773449273,-3.22275,5.46201577318104E-12));
#49723=CARTESIAN_POINT('Ctrl Pts',(-46.2527734492733,-3.21897007644484,
0.0021706558627849));
#49724=CARTESIAN_POINT('Ctrl Pts',(-46.2106300956863,-3.21475143459506,
-0.682341170182447));
#49725=CARTESIAN_POINT('Ctrl Pts',(-46.1021955648668,-2.66537161816311,
-2.44976928448922));
#49726=CARTESIAN_POINT('Ctrl Pts',(-45.9274698568148,0.245149379568856,
-3.80389844937855));
#49727=CARTESIAN_POINT('Ctrl Pts',(-45.7285963251173,3.33267279917539,-1.8501442227902));
#49728=CARTESIAN_POINT('Ctrl Pts',(-45.5297227934199,3.35812960801393,1.80352631454818));
#49729=CARTESIAN_POINT('Ctrl Pts',(-45.3308492617224,0.298130037853896,
3.80011317094853));
#49730=CARTESIAN_POINT('Ctrl Pts',(-45.1551994803403,-2.64646835176648,
2.47972498007439));
#49731=CARTESIAN_POINT('Ctrl Pts',(-45.0458408761905,-3.21462349915166,
0.697011013054861));
#49732=CARTESIAN_POINT('Ctrl Pts',(-45.0027734492733,-3.21929057874326,
-0.0023352037489462));
#49733=CARTESIAN_POINT('Ctrl Pts',(-46.006226550727,-3.21969458294954,-0.0025062700251724));
#49734=CARTESIAN_POINT('Ctrl Pts',(-45.9840796411886,-3.22229142974673,
-0.362023233856792));
#49735=CARTESIAN_POINT('Ctrl Pts',(-45.8956415544178,-3.00062983176092,
-1.79455350713736));
#49736=CARTESIAN_POINT('Ctrl Pts',(-45.7409122904144,-0.895632886789359,
-3.7050753519448));
#49737=CARTESIAN_POINT('Ctrl Pts',(-45.5420387587169,2.63282913994673,-2.7564383452809));
#49738=CARTESIAN_POINT('Ctrl Pts',(-45.3431652270195,3.74224234698389,0.724819872746352));
#49739=CARTESIAN_POINT('Ctrl Pts',(-45.144291695322,1.41327560176868,3.54011210344149));
#49740=CARTESIAN_POINT('Ctrl Pts',(-44.9486454698912,-2.15534504929802,
3.10983967618609));
#49741=CARTESIAN_POINT('Ctrl Pts',(-44.8192904216928,-3.22374709101849,
1.01621932179185));
#49742=CARTESIAN_POINT('Ctrl Pts',(-44.756226550727,-3.22773185798094,-0.000960206790134015));
#49743=CARTESIAN_POINT('Origin',(-111.877773449273,0.,0.));
#49744=CARTESIAN_POINT('',(-47.5027734492733,-3.22722180108715,0.00150419546486083));
#49745=CARTESIAN_POINT('',(-47.256226550727,-3.21862958324598,0.00195996754723593));
#49746=CARTESIAN_POINT('',(-111.877773449273,-3.22275,5.46201577318104E-12));
#49747=CARTESIAN_POINT('Ctrl Pts',(-47.5027734492733,-3.22722180108715,
0.00150419546486084));
#49748=CARTESIAN_POINT('Ctrl Pts',(-47.4417104924145,-3.2215318458885,-0.983815348456214));
#49749=CARTESIAN_POINT('Ctrl Pts',(-47.3143563583233,-2.21183553277418,
-3.04890018572942));
#49750=CARTESIAN_POINT('Ctrl Pts',(-47.1207110469995,1.30583246036561,-3.5811371402032));
#49751=CARTESIAN_POINT('Ctrl Pts',(-46.9218375153022,3.71867225532388,-0.837387776942048));
#49752=CARTESIAN_POINT('Ctrl Pts',(-46.7229639836046,2.71478834664286,2.67575519515887));
#49753=CARTESIAN_POINT('Ctrl Pts',(-46.5240904519072,-0.783448669134082,
3.73040879989306));
#49754=CARTESIAN_POINT('Ctrl Pts',(-46.3673602737967,-2.97307922116837,
1.86038731633198));
#49755=CARTESIAN_POINT('Ctrl Pts',(-46.2769212729187,-3.22138732639628,
0.394390767735412));
#49756=CARTESIAN_POINT('Ctrl Pts',(-46.2527734492733,-3.21897007644484,
0.0021706558627849));
#49757=CARTESIAN_POINT('Ctrl Pts',(-47.256226550727,-3.21862958324598,0.00195996754723593));
#49758=CARTESIAN_POINT('Ctrl Pts',(-47.2151600379169,-3.21494169678062,
-0.665238231074718));
#49759=CARTESIAN_POINT('Ctrl Pts',(-47.1078023478743,-2.68699897644198,
-2.41480261420779));
#49760=CARTESIAN_POINT('Ctrl Pts',(-46.934153480599,0.183350639119669,-3.80737759811421));
#49761=CARTESIAN_POINT('Ctrl Pts',(-46.7352799489018,3.30219140325315,-1.90401511752624));
#49762=CARTESIAN_POINT('Ctrl Pts',(-46.5364064172041,3.3869719257786,1.74876036250685));
#49763=CARTESIAN_POINT('Ctrl Pts',(-46.3375328855069,0.3597956885221,3.79477123078697));
#49764=CARTESIAN_POINT('Ctrl Pts',(-46.1608062633476,-2.6240357574013,2.51456991883394));
#49765=CARTESIAN_POINT('Ctrl Pts',(-46.0503708184211,-3.21451842507627,
0.714099948302537));
#49766=CARTESIAN_POINT('Ctrl Pts',(-46.006226550727,-3.21969458294954,-0.0025062700251724));
#49767=CARTESIAN_POINT('Origin',(-111.877773449273,0.,0.));
#49768=CARTESIAN_POINT('',(-48.7527734492733,-3.22360668808134,-0.00290950365520015));
#49769=CARTESIAN_POINT('',(-48.506226550727,-3.22687206568905,0.00177085358160415));
#49770=CARTESIAN_POINT('',(-111.877773449273,-3.22275,5.46201577318104E-12));
#49771=CARTESIAN_POINT('Ctrl Pts',(-48.7527734492733,-3.22360668808134,
-0.00290950365519946));
#49772=CARTESIAN_POINT('Ctrl Pts',(-48.7390820663752,-3.22566447975376,
-0.224480681040578));
#49773=CARTESIAN_POINT('Ctrl Pts',(-48.6590995062447,-3.10364616015319,
-1.51660682019015));
#49774=CARTESIAN_POINT('Ctrl Pts',(-48.5128257688817,-1.35950374327106,
-3.56110814263194));
#49775=CARTESIAN_POINT('Ctrl Pts',(-48.3139522371842,2.26094423642121,-3.06885529005218));
#49776=CARTESIAN_POINT('Ctrl Pts',(-48.1150787054868,3.80403200935488,0.243068104223925));
#49777=CARTESIAN_POINT('Ctrl Pts',(-47.9162051737893,1.85196736137869,3.33166002525401));
#49778=CARTESIAN_POINT('Ctrl Pts',(-47.7173316420919,-1.80168870082603,
3.35911587427456));
#49779=CARTESIAN_POINT('Ctrl Pts',(-47.5795210672532,-3.1863951775648,1.23942860890804));
#49780=CARTESIAN_POINT('Ctrl Pts',(-47.508001669647,-3.22770897598377,0.0858674162971823));
#49781=CARTESIAN_POINT('Ctrl Pts',(-47.5027734492733,-3.22722180108715,
0.00150419546486084));
#49782=CARTESIAN_POINT('Ctrl Pts',(-48.506226550727,-3.22687206568905,0.00177085358160422));
#49783=CARTESIAN_POINT('Ctrl Pts',(-48.4462404346451,-3.22048116252823,
-0.966449641389064));
#49784=CARTESIAN_POINT('Ctrl Pts',(-48.3199631413307,-2.24154020220606,
-3.01586013407486));
#49785=CARTESIAN_POINT('Ctrl Pts',(-48.1273946707838,1.24751100295795,-3.60186867181274));
#49786=CARTESIAN_POINT('Ctrl Pts',(-47.9285211390864,3.7045847670046,-0.897659921999986));
#49787=CARTESIAN_POINT('Ctrl Pts',(-47.7296476073888,2.75787844060516,2.63132060728692));
#49788=CARTESIAN_POINT('Ctrl Pts',(-47.5307740756916,-0.722772259698463,
3.74263835978015));
#49789=CARTESIAN_POINT('Ctrl Pts',(-47.3729670568041,-2.95772977401545,
1.89581558441457));
#49790=CARTESIAN_POINT('Ctrl Pts',(-47.2814512151493,-3.22089482789791,
0.41177929506686));
#49791=CARTESIAN_POINT('Ctrl Pts',(-47.256226550727,-3.21862958324598,0.00195996754723593));
#49792=CARTESIAN_POINT('Origin',(-111.877773449273,0.,0.));
#49793=CARTESIAN_POINT('',(-50.0027734492733,-3.21741165506535,-0.000143917224426878));
#49794=CARTESIAN_POINT('',(-49.756226550727,-3.22413672240192,-0.00282835657440583));
#49795=CARTESIAN_POINT('',(-111.877773449273,-3.22275,5.46201577318104E-12));
#49796=CARTESIAN_POINT('Ctrl Pts',(-50.0027734492733,-3.21741165506535,
-0.000143917224427054));
#49797=CARTESIAN_POINT('Ctrl Pts',(-49.9701624631035,-3.21762205297516,
-0.5304684062323));
#49798=CARTESIAN_POINT('Ctrl Pts',(-49.8712602997012,-2.84224577629495,
-2.13854902871477));
#49799=CARTESIAN_POINT('Ctrl Pts',(-49.7060669590664,-0.302288193939447,
-3.79978466222657));
#49800=CARTESIAN_POINT('Ctrl Pts',(-49.507193427369,3.03326776036106,-2.30846882704571));
#49801=CARTESIAN_POINT('Ctrl Pts',(-49.3083198956714,3.58185106831631,1.3038729063405));
#49802=CARTESIAN_POINT('Ctrl Pts',(-49.1094463639741,0.839422260186034,
3.71821353617451));
#49803=CARTESIAN_POINT('Ctrl Pts',(-48.9242642151746,-2.43237049411793,
2.78523165147994));
#49804=CARTESIAN_POINT('Ctrl Pts',(-48.8053732436077,-3.2157010280353,0.848326521785803));
#49805=CARTESIAN_POINT('Ctrl Pts',(-48.7527734492733,-3.22360668808134,
-0.00290950365519946));
#49806=CARTESIAN_POINT('Ctrl Pts',(-49.756226550727,-3.22413672240192,-0.00282835657440569));
#49807=CARTESIAN_POINT('Ctrl Pts',(-49.7436120086058,-3.22601281988437,
-0.20688641167527));
#49808=CARTESIAN_POINT('Ctrl Pts',(-49.6647062892522,-3.11526915608657,
-1.48126866875651));
#49809=CARTESIAN_POINT('Ctrl Pts',(-49.519509392666,-1.41714857988236,-3.53856348452659));
#49810=CARTESIAN_POINT('Ctrl Pts',(-49.3206358609686,2.21081511742383,-3.10516314354943));
#49811=CARTESIAN_POINT('Ctrl Pts',(-49.1217623292711,3.80747734543496,0.181267469467265));
#49812=CARTESIAN_POINT('Ctrl Pts',(-48.9228887975737,1.90582157067163,3.30114915934591));
#49813=CARTESIAN_POINT('Ctrl Pts',(-48.7240152658761,-1.74690697639595,
3.3879282234585));
#49814=CARTESIAN_POINT('Ctrl Pts',(-48.5851278502606,-3.17693716528882,
1.27461962210879));
#49815=CARTESIAN_POINT('Ctrl Pts',(-48.5125316118776,-3.22754380504923,
0.103539226444708));
#49816=CARTESIAN_POINT('Ctrl Pts',(-48.506226550727,-3.22687206568905,0.00177085358160422));
#49817=CARTESIAN_POINT('Origin',(-111.877773449273,0.,0.));
#49818=CARTESIAN_POINT('',(-51.2527734492733,-3.223076684641,0.0029595821066306));
#49819=CARTESIAN_POINT('',(-51.006226550727,-3.2174581254241,-0.000432486719161296));
#49820=CARTESIAN_POINT('',(-111.877773449273,-3.22275,5.46201577318104E-12));
#49821=CARTESIAN_POINT('Ctrl Pts',(-51.2527734492733,-3.223076684641,0.00295958210663055));
#49822=CARTESIAN_POINT('Ctrl Pts',(-51.2012428598317,-3.21532624848516,
-0.831324944861402));
#49823=CARTESIAN_POINT('Ctrl Pts',(-51.0834210931577,-2.45815795239362,
-2.75134438455826));
#49824=CARTESIAN_POINT('Ctrl Pts',(-50.8993081492511,0.779366140619599,
-3.73126386769187));
#49825=CARTESIAN_POINT('Ctrl Pts',(-50.7004346175537,3.56036378015273,-1.36145193982897));
#49826=CARTESIAN_POINT('Ctrl Pts',(-50.5015610858562,3.07009186808429,2.25926482578078));
#49827=CARTESIAN_POINT('Ctrl Pts',(-50.3026875541588,-0.240986756115434,
3.80416443057663));
#49828=CARTESIAN_POINT('Ctrl Pts',(-50.1364250086311,-2.82400848125359,
2.17360945505402));
#49829=CARTESIAN_POINT('Ctrl Pts',(-50.036453640336,-3.21719435891352,0.547568133616722));
#49830=CARTESIAN_POINT('Ctrl Pts',(-50.0027734492733,-3.21741165506535,
-0.000143917224427054));
#49831=CARTESIAN_POINT('Ctrl Pts',(-51.006226550727,-3.2174581254241,-0.000432486719161573));
#49832=CARTESIAN_POINT('Ctrl Pts',(-50.9746924053341,-3.2180700033416,-0.513226776194044));
#49833=CARTESIAN_POINT('Ctrl Pts',(-50.8768670827086,-2.8602169712618,-2.10321212263254));
#49834=CARTESIAN_POINT('Ctrl Pts',(-50.7127505828507,-0.363947962184506,
-3.79437524663933));
#49835=CARTESIAN_POINT('Ctrl Pts',(-50.5138770511533,2.99538371751683,-2.35741765843947));
#49836=CARTESIAN_POINT('Ctrl Pts',(-50.3150035194558,3.60255068722456,1.24554011475546));
#49837=CARTESIAN_POINT('Ctrl Pts',(-50.1161299877584,0.899686688491969,
3.70409307307982));
#49838=CARTESIAN_POINT('Ctrl Pts',(-49.929870998182,-2.40593533673339,2.8192447831268));
#49839=CARTESIAN_POINT('Ctrl Pts',(-49.8099031858383,-3.21615366609824,
0.865467112255008));
#49840=CARTESIAN_POINT('Ctrl Pts',(-49.756226550727,-3.22413672240192,-0.00282835657440569));
#49841=CARTESIAN_POINT('Origin',(-111.877773449273,0.,0.));
#49842=CARTESIAN_POINT('',(-52.5027734492733,-3.22751885487476,-0.00122046435559179));
#49843=CARTESIAN_POINT('',(-52.256226550727,-3.22254425484652,0.00297929525483548));
#49844=CARTESIAN_POINT('',(-111.877773449273,-3.22275,5.46201577318104E-12));
#49845=CARTESIAN_POINT('Ctrl Pts',(-52.5027734492733,-3.22751885487476,
-0.00122046435559201));
#49846=CARTESIAN_POINT('Ctrl Pts',(-52.4986144337925,-3.22784327448082,
-0.0683144855938748));
#49847=CARTESIAN_POINT('Ctrl Pts',(-52.4281642410792,-3.19548702846004,
-1.20451144458635));
#49848=CARTESIAN_POINT('Ctrl Pts',(-52.2914228711333,-1.8556119748251,-3.32963148567123));
#49849=CARTESIAN_POINT('Ctrl Pts',(-52.0925493394359,1.79801185590047,-3.36108538980027));
#49850=CARTESIAN_POINT('Ctrl Pts',(-51.8936758077384,3.79961870161625,-0.304367136556382));
#49851=CARTESIAN_POINT('Ctrl Pts',(-51.694802276041,2.31012808263415,3.03200426670422));
#49852=CARTESIAN_POINT('Ctrl Pts',(-51.4959287443436,-1.30191296199484,
3.58256392418577));
#49853=CARTESIAN_POINT('Ctrl Pts',(-51.3485858020876,-3.09177951640618,
1.55171129825264));
#49854=CARTESIAN_POINT('Ctrl Pts',(-51.2675340370642,-3.22529674450323,
0.241934725538514));
#49855=CARTESIAN_POINT('Ctrl Pts',(-51.2527734492733,-3.223076684641,0.00295958210663055));
#49856=CARTESIAN_POINT('Ctrl Pts',(-52.256226550727,-3.22254425484652,0.00297929525483558));
#49857=CARTESIAN_POINT('Ctrl Pts',(-52.2057728020623,-3.21502087541627,
-0.814216185777217));
#49858=CARTESIAN_POINT('Ctrl Pts',(-52.0890278761651,-2.48366918414892,
-2.71710498222641));
#49859=CARTESIAN_POINT('Ctrl Pts',(-51.9059917730355,0.718676385120064,
-3.74342702412619));
#49860=CARTESIAN_POINT('Ctrl Pts',(-51.707118241338,3.53778758602515,-1.41908443288405));
#49861=CARTESIAN_POINT('Ctrl Pts',(-51.5082447096405,3.10637228884811,2.2091158490591));
#49862=CARTESIAN_POINT('Ctrl Pts',(-51.3093711779431,-0.179184245551611,
3.80757595296977));
#49863=CARTESIAN_POINT('Ctrl Pts',(-51.1420317916386,-2.80524068683852,
2.20889053097753));
#49864=CARTESIAN_POINT('Ctrl Pts',(-51.0409835825666,-3.21678371170541,
0.564770953054575));
#49865=CARTESIAN_POINT('Ctrl Pts',(-51.006226550727,-3.2174581254241,-0.000432486719161573));
#49866=CARTESIAN_POINT('Origin',(-111.877773449273,0.,0.));
#49867=CARTESIAN_POINT('',(-53.7527734492733,-3.21934317032028,-0.00235959395598513));
#49868=CARTESIAN_POINT('',(-53.506226550727,-3.22776089439009,-0.000918729460922529));
#49869=CARTESIAN_POINT('',(-111.877773449273,-3.22275,5.46201577318104E-12));
#49870=CARTESIAN_POINT('Ctrl Pts',(-53.7527734492733,-3.21934317032028,
-0.00235959395598572));
#49871=CARTESIAN_POINT('Ctrl Pts',(-53.7296948305207,-3.22187288607612,
-0.377104113301222));
#49872=CARTESIAN_POINT('Ctrl Pts',(-53.6403250345356,-2.98795702091302,
-1.82520830613947));
#49873=CARTESIAN_POINT('Ctrl Pts',(-53.484664061318,-0.843490472210508,
-3.71729275882027));
#49874=CARTESIAN_POINT('Ctrl Pts',(-53.2857905296207,2.67129554096001,-2.71917667030568));
#49875=CARTESIAN_POINT('Ctrl Pts',(-53.086916997923,3.73168972619857,0.777324526096578));
#49876=CARTESIAN_POINT('Ctrl Pts',(-52.8880434662258,1.36339972882987,3.55961835186216));
#49877=CARTESIAN_POINT('Ctrl Pts',(-52.6933289500089,-2.18185957656017,
3.08153908756355));
#49878=CARTESIAN_POINT('Ctrl Pts',(-52.5649056110249,-3.22267230127756,
1.00110727387197));
#49879=CARTESIAN_POINT('Ctrl Pts',(-52.5027734492733,-3.22751885487476,
-0.00122046435559201));
#49880=CARTESIAN_POINT('Ctrl Pts',(-53.506226550727,-3.22776089439009,-0.000918729460922746));
#49881=CARTESIAN_POINT('Ctrl Pts',(-53.503144376023,-3.22794811375422,-0.0506310245026929));
#49882=CARTESIAN_POINT('Ctrl Pts',(-53.4337710240866,-3.20434578131378,
-1.16936988671058));
#49883=CARTESIAN_POINT('Ctrl Pts',(-53.2981064949176,-1.90943276487233,
-3.29906170720093));
#49884=CARTESIAN_POINT('Ctrl Pts',(-53.0992329632202,1.74319863589507,-3.38983777595641));
#49885=CARTESIAN_POINT('Ctrl Pts',(-52.9003594315227,3.79417555074013,-0.366023935902194));
#49886=CARTESIAN_POINT('Ctrl Pts',(-52.7014858998253,2.35905617908858,2.99409344800579));
#49887=CARTESIAN_POINT('Ctrl Pts',(-52.5026123681278,-1.24356885369478,
3.60323162419618));
#49888=CARTESIAN_POINT('Ctrl Pts',(-52.3541925850951,-3.07949606830474,
1.58708207888242));
#49889=CARTESIAN_POINT('Ctrl Pts',(-52.2720639792948,-3.22490584318174,
0.259496905924056));
#49890=CARTESIAN_POINT('Ctrl Pts',(-52.256226550727,-3.22254425484652,0.00297929525483558));
#49891=CARTESIAN_POINT('Origin',(-111.877773449273,0.,0.));
#49892=CARTESIAN_POINT('',(-55.0027734492732,-3.2189220646149,0.00214340917629934));
#49893=CARTESIAN_POINT('',(-54.756226550727,-3.21975139093016,-0.00252752881742452));
#49894=CARTESIAN_POINT('',(-111.877773449273,-3.22275,5.46201577318104E-12));
#49895=CARTESIAN_POINT('Ctrl Pts',(-55.0027734492732,-3.2189220646149,0.00214340917629927));
#49896=CARTESIAN_POINT('Ctrl Pts',(-54.9607752272489,-3.21477455481245,
-0.680036647789328));
#49897=CARTESIAN_POINT('Ctrl Pts',(-54.8524858279921,-2.66831154574978,
-2.44506023208848));
#49898=CARTESIAN_POINT('Ctrl Pts',(-54.6779052515027,0.236823844100095,
-3.80442585659819));
#49899=CARTESIAN_POINT('Ctrl Pts',(-54.4790317198054,3.32861572061708,-1.857433448592));
#49900=CARTESIAN_POINT('Ctrl Pts',(-54.2801581881078,3.36206863847578,1.79617262579773));
#49901=CARTESIAN_POINT('Ctrl Pts',(-54.0812846564105,0.306445988059607,
3.7994516035725));
#49902=CARTESIAN_POINT('Ctrl Pts',(-53.9054897434655,-2.64347043160142,
2.48442526820891));
#49903=CARTESIAN_POINT('Ctrl Pts',(-53.7959860077532,-3.21460651379814,
0.699314524015979));
#49904=CARTESIAN_POINT('Ctrl Pts',(-53.7527734492733,-3.21934317032028,
-0.00235959395598572));
#49905=CARTESIAN_POINT('Ctrl Pts',(-54.756226550727,-3.21975139093016,-0.00252752881742448));
#49906=CARTESIAN_POINT('Ctrl Pts',(-54.7342247727513,-3.22235614149659,
-0.359672668312695));
#49907=CARTESIAN_POINT('Ctrl Pts',(-54.6459318175431,-3.00257958162626,
-1.78977856998388));
#49908=CARTESIAN_POINT('Ctrl Pts',(-54.4913476851023,-0.90373941289318,
-3.70310635886562));
#49909=CARTESIAN_POINT('Ctrl Pts',(-54.2924741534049,2.62679028492706,-2.76219377135282));
#49910=CARTESIAN_POINT('Ctrl Pts',(-54.0936006217074,3.74381967543987,0.71662812481567));
#49911=CARTESIAN_POINT('Ctrl Pts',(-53.89472709001,1.42101986107626,3.53701062847065));
#49912=CARTESIAN_POINT('Ctrl Pts',(-53.6989357330165,-2.15118182487284,
3.11423588293571));
#49913=CARTESIAN_POINT('Ctrl Pts',(-53.5694355532555,-3.2239214140241,1.01857720597386));
#49914=CARTESIAN_POINT('Ctrl Pts',(-53.506226550727,-3.22776089439009,-0.000918729460922746));
#49915=CARTESIAN_POINT('Origin',(-111.877773449273,0.,0.));
#49916=CARTESIAN_POINT('',(-56.2527734492733,-3.22717748004024,0.00154131605262783));
#49917=CARTESIAN_POINT('',(-56.006226550727,-3.21858653956579,0.00193011919197975));
#49918=CARTESIAN_POINT('',(-111.877773449273,-3.22275,5.46201577318104E-12));
#49919=CARTESIAN_POINT('Ctrl Pts',(-56.2527734492733,-3.22717748004024,
0.00154131605262783));
#49920=CARTESIAN_POINT('Ctrl Pts',(-56.1918556239772,-3.22138456848205,
-0.981472074920973));
#49921=CARTESIAN_POINT('Ctrl Pts',(-56.0646466214485,-2.2158673361632,-3.04445687931626));
#49922=CARTESIAN_POINT('Ctrl Pts',(-55.8711464416876,1.29799190468937,-3.58398641834039));
#49923=CARTESIAN_POINT('Ctrl Pts',(-55.67227290999,3.71683070089097,-0.845524199773049));
#49924=CARTESIAN_POINT('Ctrl Pts',(-55.4733993782926,2.7206378174474,2.66980738963741));
#49925=CARTESIAN_POINT('Ctrl Pts',(-55.2745258465951,-0.77528267887785,
3.73211446760674));
#49926=CARTESIAN_POINT('Ctrl Pts',(-55.117650536922,-2.97103196108619,1.86516234467601));
#49927=CARTESIAN_POINT('Ctrl Pts',(-55.0270664044814,-3.2213211011693,0.396735579248406));
#49928=CARTESIAN_POINT('Ctrl Pts',(-55.0027734492732,-3.2189220646149,0.00214340917629927));
#49929=CARTESIAN_POINT('Ctrl Pts',(-56.006226550727,-3.21858653956579,0.00193011919197968));
#49930=CARTESIAN_POINT('Ctrl Pts',(-55.9653051694795,-3.21497056641272,
-0.662932432587956));
#49931=CARTESIAN_POINT('Ctrl Pts',(-55.8580926109995,-2.68988099457248,
-2.41008537974996));
#49932=CARTESIAN_POINT('Ctrl Pts',(-55.6845888752871,0.175017637425035,
-3.80776974856381));
#49933=CARTESIAN_POINT('Ctrl Pts',(-55.4857153435897,3.29801649958808,-1.9112375048466));
#49934=CARTESIAN_POINT('Ctrl Pts',(-55.2868418118921,3.39079103020278,1.74134368261521));
#49935=CARTESIAN_POINT('Ctrl Pts',(-55.0879682801948,0.368099800048924,
3.79397471903694));
#49936=CARTESIAN_POINT('Ctrl Pts',(-54.9110965264729,-2.62097893908948,
2.5192607169782));
#49937=CARTESIAN_POINT('Ctrl Pts',(-54.8005159499837,-3.21450804932711,
0.716402718236941));
#49938=CARTESIAN_POINT('Ctrl Pts',(-54.756226550727,-3.21975139093016,-0.00252752881742448));
#49939=CARTESIAN_POINT('Origin',(-111.877773449273,0.,0.));
#49940=CARTESIAN_POINT('',(-57.5027734492733,-3.22367845862114,-0.00290036030699531));
#49941=CARTESIAN_POINT('',(-57.256226550727,-3.22682140413586,0.00180517358502927));
#49942=CARTESIAN_POINT('',(-111.877773449273,-3.22275,5.46201577318104E-12));
#49943=CARTESIAN_POINT('Ctrl Pts',(-57.5027734492733,-3.22367845862114,
-0.0029003603069952));
#49944=CARTESIAN_POINT('Ctrl Pts',(-57.4892271979379,-3.22571274738317,
-0.222110297568779));
#49945=CARTESIAN_POINT('Ctrl Pts',(-57.40938976937,-3.10523178828499,-1.51184308272459));
#49946=CARTESIAN_POINT('Ctrl Pts',(-57.2632611635696,-1.3672940818287,-3.55812429873996));
#49947=CARTESIAN_POINT('Ctrl Pts',(-57.0643876318723,2.25422253794341,-3.073796086424));
#49948=CARTESIAN_POINT('Ctrl Pts',(-56.8655141001747,3.80455486131976,0.234742281439464));
#49949=CARTESIAN_POINT('Ctrl Pts',(-56.6666405684773,1.85925436632751,3.32759895912643));
#49950=CARTESIAN_POINT('Ctrl Pts',(-56.4677670367798,-1.79433285800241,
3.3630508807005));
#49951=CARTESIAN_POINT('Ctrl Pts',(-56.3298113303785,-3.18513816811937,
1.24417006843104));
#49952=CARTESIAN_POINT('Ctrl Pts',(-56.2581468012097,-3.227688452853,0.0882495477107612));
#49953=CARTESIAN_POINT('Ctrl Pts',(-56.2527734492733,-3.22717748004024,
0.00154131605262783));
#49954=CARTESIAN_POINT('Ctrl Pts',(-57.256226550727,-3.22682140413586,0.00180517358502903));
#49955=CARTESIAN_POINT('Ctrl Pts',(-57.1963855662077,-3.22034692564174,
-0.964112732485139));
#49956=CARTESIAN_POINT('Ctrl Pts',(-57.070253404456,-2.24550654357098,-3.01139463839781));
#49957=CARTESIAN_POINT('Ctrl Pts',(-56.8778300654718,1.23962521535938,-3.60459026200378));
#49958=CARTESIAN_POINT('Ctrl Pts',(-56.6789565337743,3.70261133887159,-0.905765369589214));
#49959=CARTESIAN_POINT('Ctrl Pts',(-56.4800830020769,2.76363056175831,2.62527860418717));
#49960=CARTESIAN_POINT('Ctrl Pts',(-56.2812094703794,-0.714579649985331,
3.74421120602382));
#49961=CARTESIAN_POINT('Ctrl Pts',(-56.1232573199295,-2.9556327925769,1.9005901476665));
#49962=CARTESIAN_POINT('Ctrl Pts',(-56.031596346712,-3.22082831387507,0.41412117390532));
#49963=CARTESIAN_POINT('Ctrl Pts',(-56.006226550727,-3.21858653956579,0.00193011919197968));
#49964=CARTESIAN_POINT('Origin',(-111.877773449273,0.,0.));
#49965=CARTESIAN_POINT('',(-58.7527734492733,-3.21741520282347,-0.000182944744591371));
#49966=CARTESIAN_POINT('',(-58.5062265507269,-3.224207581543,-0.00281507645755574));
#49967=CARTESIAN_POINT('',(-111.877773449273,-3.22275,5.46201577318104E-12));
#49968=CARTESIAN_POINT('Ctrl Pts',(-58.7527734492732,-3.21741520282347,
-0.000182944744591441));
#49969=CARTESIAN_POINT('Ctrl Pts',(-58.7203075946661,-3.21768148241439,
-0.528145832653428));
#49970=CARTESIAN_POINT('Ctrl Pts',(-58.6215505628265,-2.84469095478287,
-2.13378793357218));
#49971=CARTESIAN_POINT('Ctrl Pts',(-58.4565023537544,-0.310603415235633,
-3.79911399538513));
#49972=CARTESIAN_POINT('Ctrl Pts',(-58.2576288220569,3.02820834138102,-2.3151016981286));
#49973=CARTESIAN_POINT('Ctrl Pts',(-58.0587552903595,3.58469605619972,1.29603079290335));
#49974=CARTESIAN_POINT('Ctrl Pts',(-57.859881758662,0.84755767422402,3.71636753031121));
#49975=CARTESIAN_POINT('Ctrl Pts',(-57.6745544783,-2.42883487841989,2.78982271261159));
#49976=CARTESIAN_POINT('Ctrl Pts',(-57.5555183751704,-3.21575756542716,
0.85063554497991));
#49977=CARTESIAN_POINT('Ctrl Pts',(-57.5027734492733,-3.22367845862114,
-0.0029003603069952));
#49978=CARTESIAN_POINT('Ctrl Pts',(-58.5062265507269,-3.224207581543,-0.00281507645755581));
#49979=CARTESIAN_POINT('Ctrl Pts',(-58.4937571401684,-3.22605800120511,
-0.204513997007941));
#49980=CARTESIAN_POINT('Ctrl Pts',(-58.4149965523774,-3.11681064543685,
-1.47650733819638));
#49981=CARTESIAN_POINT('Ctrl Pts',(-58.2699447873541,-1.42488944071483,
-3.53545353713309));
#49982=CARTESIAN_POINT('Ctrl Pts',(-58.0710712556564,2.20401407814638,-3.10999414385624));
#49983=CARTESIAN_POINT('Ctrl Pts',(-57.8721977239591,3.80786493656502,0.172934254461413));
#49984=CARTESIAN_POINT('Ctrl Pts',(-57.6733241922616,1.9130416726831,3.29697030469875));
#49985=CARTESIAN_POINT('Ctrl Pts',(-57.4744506605642,-1.73948820805607,
3.39174326940018));
#49986=CARTESIAN_POINT('Ctrl Pts',(-57.3354181133859,-3.1756391642871,1.27936435020756));
#49987=CARTESIAN_POINT('Ctrl Pts',(-57.2626767434402,-3.22751928092282,
0.105920383075324));
#49988=CARTESIAN_POINT('Ctrl Pts',(-57.256226550727,-3.22682140413586,0.00180517358502903));
#49989=CARTESIAN_POINT('Origin',(-111.877773449273,0.,0.));
#49990=CARTESIAN_POINT('',(-60.0027734492732,-3.22300473664784,0.00296403349578234));
#49991=CARTESIAN_POINT('',(-59.756226550727,-3.21746794082411,-0.000471133578089089));
#49992=CARTESIAN_POINT('',(-111.877773449273,-3.22275,5.46201577318104E-12));
#49993=CARTESIAN_POINT('Ctrl Pts',(-60.0027734492732,-3.22300473664784,
0.00296403349578239));
#49994=CARTESIAN_POINT('Ctrl Pts',(-59.9513879913943,-3.21528094263802,
-0.829018345407677));
#49995=CARTESIAN_POINT('Ctrl Pts',(-59.833711356283,-2.46162310557184,-2.74673607057375));
#49996=CARTESIAN_POINT('Ctrl Pts',(-59.6497435439391,0.77119828879821,-3.73296059861904));
#49997=CARTESIAN_POINT('Ctrl Pts',(-59.4508700122417,3.55737567435549,-1.36924064466089));
#49998=CARTESIAN_POINT('Ctrl Pts',(-59.2519964805442,3.07502898605303,2.25254042503595));
#49999=CARTESIAN_POINT('Ctrl Pts',(-59.0531229488468,-0.232660648507626,
3.80468272713029));
#50000=CARTESIAN_POINT('Ctrl Pts',(-58.8867152717565,-2.8215025518602,2.17836629560583));
#50001=CARTESIAN_POINT('Ctrl Pts',(-58.7865987718986,-3.21713777309984,
0.549887744409677));
#50002=CARTESIAN_POINT('Ctrl Pts',(-58.7527734492732,-3.21741520282347,
-0.000182944744591441));
#50003=CARTESIAN_POINT('Ctrl Pts',(-59.7562265507269,-3.21746794082411,
-0.000471133578089228));
#50004=CARTESIAN_POINT('Ctrl Pts',(-59.7248375368967,-3.21813154016163,
-0.510901476063965));
#50005=CARTESIAN_POINT('Ctrl Pts',(-59.6271573458339,-2.86260884250598,
-2.0984477708445));
#50006=CARTESIAN_POINT('Ctrl Pts',(-59.4631859775387,-0.372251197144022,
-3.79356964845936));
#50007=CARTESIAN_POINT('Ctrl Pts',(-59.2643124458413,2.99021726324463,-2.36396750190888));
#50008=CARTESIAN_POINT('Ctrl Pts',(-59.0654389141438,3.60526796243309,1.23765283926516));
#50009=CARTESIAN_POINT('Ctrl Pts',(-58.8665653824463,0.90779105514019,3.70211521048372));
#50010=CARTESIAN_POINT('Ctrl Pts',(-58.6801612613074,-2.40233678911353,
2.82381966648872));
#50011=CARTESIAN_POINT('Ctrl Pts',(-58.5600483174009,-3.21622060775338,
0.867778781152312));
#50012=CARTESIAN_POINT('Ctrl Pts',(-58.5062265507269,-3.224207581543,-0.00281507645755581));
#50013=CARTESIAN_POINT('Origin',(-111.877773449273,0.,0.));
#50014=CARTESIAN_POINT('',(-61.2527734492733,-3.22755496513108,-0.00118065924393767));
#50015=CARTESIAN_POINT('',(-61.006226550727,-3.22247286999595,0.00297960598500319));
#50016=CARTESIAN_POINT('',(-111.877773449273,-3.22275,5.46201577318104E-12));
#50017=CARTESIAN_POINT('Ctrl Pts',(-61.2527734492733,-3.22755496513108,
-0.00118065924393777));
#50018=CARTESIAN_POINT('Ctrl Pts',(-61.2487595653551,-3.22785919387834,
-0.065931465168597));
#50019=CARTESIAN_POINT('Ctrl Pts',(-61.1784545042045,-3.19669833842117,
-1.19977375893129));
#50020=CARTESIAN_POINT('Ctrl Pts',(-61.0418582658212,-1.86289453152446,
-3.32556244805351));
#50021=CARTESIAN_POINT('Ctrl Pts',(-60.8429847341239,1.79065171153737,-3.3650123446216));
#50022=CARTESIAN_POINT('Ctrl Pts',(-60.6441112024263,3.79894348534265,-0.312681989663811));
#50023=CARTESIAN_POINT('Ctrl Pts',(-60.445237670729,2.31675818454863,3.02694121941845));
#50024=CARTESIAN_POINT('Ctrl Pts',(-60.2463641390315,-1.29406929314464,
3.58540462096363));
#50025=CARTESIAN_POINT('Ctrl Pts',(-60.0988760652129,-3.0901435215559,1.55647752678745));
#50026=CARTESIAN_POINT('Ctrl Pts',(-60.0176791686268,-3.22524522861985,
0.244302660394943));
#50027=CARTESIAN_POINT('Ctrl Pts',(-60.0027734492732,-3.22300473664784,
0.00296403349578239));
#50028=CARTESIAN_POINT('Ctrl Pts',(-61.006226550727,-3.22247286999594,0.00297960598500333));
#50029=CARTESIAN_POINT('Ctrl Pts',(-60.9559179336249,-3.21498508007288,
-0.811911263580403));
#50030=CARTESIAN_POINT('Ctrl Pts',(-60.8393181392904,-2.48707231186256,
-2.71248222746116));
#50031=CARTESIAN_POINT('Ctrl Pts',(-60.6564271677235,0.71048205919978,-3.74499090453405));
#50032=CARTESIAN_POINT('Ctrl Pts',(-60.4575536360259,3.53467340381617,-1.42682359100281));
#50033=CARTESIAN_POINT('Ctrl Pts',(-60.2586801043286,3.1111995673583,2.20231216759956));
#50034=CARTESIAN_POINT('Ctrl Pts',(-60.059806572631,-0.170850819729117,
3.80795898466428));
#50035=CARTESIAN_POINT('Ctrl Pts',(-59.8923220547639,-2.80268032222874,
2.21364306226118));
#50036=CARTESIAN_POINT('Ctrl Pts',(-59.7911287141292,-3.21673006952186,
0.567088054971965));
#50037=CARTESIAN_POINT('Ctrl Pts',(-59.7562265507269,-3.21746794082411,
-0.000471133578089228));
#50038=CARTESIAN_POINT('Origin',(-111.877773449273,0.,0.));
#50039=CARTESIAN_POINT('',(-62.5027734492733,-3.21939635421877,-0.002383576536604));
#50040=CARTESIAN_POINT('',(-62.256226550727,-3.22778876783897,-0.000877024610755894));
#50041=CARTESIAN_POINT('',(-111.877773449273,-3.22275,5.46201577318104E-12));
#50042=CARTESIAN_POINT('Ctrl Pts',(-62.5027734492733,-3.21939635421877,
-0.00238357653660443));
#50043=CARTESIAN_POINT('Ctrl Pts',(-62.4798399620833,-3.22193840446921,
-0.37475602650426));
#50044=CARTESIAN_POINT('Ctrl Pts',(-62.3906152976609,-2.98994884724002,
-1.82043316881518));
#50045=CARTESIAN_POINT('Ctrl Pts',(-62.2350994560059,-0.851623861356168,
-3.71543785175534));
#50046=CARTESIAN_POINT('Ctrl Pts',(-62.0362259243087,2.66533814213779,-2.72501637051098));
#50047=CARTESIAN_POINT('Ctrl Pts',(-61.837352392611,3.73338198796987,0.76915574716017));
#50048=CARTESIAN_POINT('Ctrl Pts',(-61.6384788609137,1.37118679760446,3.5566259850542));
#50049=CARTESIAN_POINT('Ctrl Pts',(-61.4436192131343,-2.17775356114322,
3.08595621928119));
#50050=CARTESIAN_POINT('Ctrl Pts',(-61.3150507425876,-3.22283471329673,
1.00345849204261));
#50051=CARTESIAN_POINT('Ctrl Pts',(-61.2527734492733,-3.22755496513108,
-0.00118065924393777));
#50052=CARTESIAN_POINT('Ctrl Pts',(-62.256226550727,-3.22778876783897,-0.00087702461075625));
#50053=CARTESIAN_POINT('Ctrl Pts',(-62.2532895075857,-3.22795988649932,
-0.0482474052521493));
#50054=CARTESIAN_POINT('Ctrl Pts',(-62.1840612872119,-3.20551702323328,
-1.16463561095075));
#50055=CARTESIAN_POINT('Ctrl Pts',(-62.0485418896055,-1.91664828978265,
-3.29487495434361));
#50056=CARTESIAN_POINT('Ctrl Pts',(-61.8496683579083,1.73577569732174,-3.39364470150818));
#50057=CARTESIAN_POINT('Ctrl Pts',(-61.6507948262106,3.79336540970629,-0.374326728849534));
#50058=CARTESIAN_POINT('Ctrl Pts',(-61.4519212945133,2.36560319483962,2.9889234108709));
#50059=CARTESIAN_POINT('Ctrl Pts',(-61.2530477628157,-1.23568009267388,
3.6059445836087));
#50060=CARTESIAN_POINT('Ctrl Pts',(-61.1044828482204,-3.07781487847321,
1.59185030130126));
#50061=CARTESIAN_POINT('Ctrl Pts',(-61.0222091108574,-3.224851668293,0.261862538429334));
#50062=CARTESIAN_POINT('Ctrl Pts',(-61.006226550727,-3.22247286999594,0.00297960598500333));
#50063=CARTESIAN_POINT('Origin',(-111.877773449273,0.,0.));
#50064=CARTESIAN_POINT('',(-63.7527734492732,-3.21887470245503,0.0021157953170018));
#50065=CARTESIAN_POINT('',(-63.506226550727,-3.21980873461777,-0.00254834726308467));
#50066=CARTESIAN_POINT('',(-111.877773449273,-3.22275,5.46201577318104E-12));
#50067=CARTESIAN_POINT('Ctrl Pts',(-63.7527734492732,-3.21887470245503,
0.00211579531700205));
#50068=CARTESIAN_POINT('Ctrl Pts',(-63.7109203588115,-3.21479847498223,
-0.677731968031492));
#50069=CARTESIAN_POINT('Ctrl Pts',(-63.6027760911173,-2.67124363934922,
-2.4403500396236));
#50070=CARTESIAN_POINT('Ctrl Pts',(-63.4283406461908,0.228497174322965,
-3.80493504186522));
#50071=CARTESIAN_POINT('Ctrl Pts',(-63.2294671144933,3.32454269908083,-1.8647137778962));
#50072=CARTESIAN_POINT('Ctrl Pts',(-63.0305935827958,3.36599156573087,1.78881033396948));
#50073=CARTESIAN_POINT('Ctrl Pts',(-62.8317200510984,0.314760470489306,
3.79877183806881));
#50074=CARTESIAN_POINT('Ctrl Pts',(-62.6557800065908,-2.64046460203817,
2.48912431653265));
#50075=CARTESIAN_POINT('Ctrl Pts',(-62.5461311393158,-3.21459039401224,
0.701617918411942));
#50076=CARTESIAN_POINT('Ctrl Pts',(-62.5027734492733,-3.21939635421877,
-0.00238357653660443));
#50077=CARTESIAN_POINT('Ctrl Pts',(-63.506226550727,-3.21980873461777,-0.00254834726308481));
#50078=CARTESIAN_POINT('Ctrl Pts',(-63.4843699043139,-3.22242070748555,
-0.35732171994346));
#50079=CARTESIAN_POINT('Ctrl Pts',(-63.3962220806684,-3.00452281277026,
-1.78500368537475));
#50080=CARTESIAN_POINT('Ctrl Pts',(-63.2417830797903,-0.911841610381489,
-3.70111962912095));
#50081=CARTESIAN_POINT('Ctrl Pts',(-63.0429095480929,2.62073884844303,-2.7679359674221));
#50082=CARTESIAN_POINT('Ctrl Pts',(-62.8440360163953,3.74537907222691,0.708432944471117));
#50083=CARTESIAN_POINT('Ctrl Pts',(-62.6451624846981,1.42875731416466,3.53389221237837));
#50084=CARTESIAN_POINT('Ctrl Pts',(-62.4492259961417,-2.14700966869485,
3.11862876361037));
#50085=CARTESIAN_POINT('Ctrl Pts',(-62.3195806848181,-3.22409761519604,
1.02093617415114));
#50086=CARTESIAN_POINT('Ctrl Pts',(-62.256226550727,-3.22778876783897,-0.00087702461075625));
#50087=CARTESIAN_POINT('Origin',(-111.877773449273,0.,0.));
#50088=CARTESIAN_POINT('',(-65.0027734492732,-3.22713225326276,0.00157808088591664));
#50089=CARTESIAN_POINT('',(-64.756226550727,-3.21854419053207,0.00189994234605001));
#50090=CARTESIAN_POINT('',(-111.877773449273,-3.22275,5.46201577318104E-12));
#50091=CARTESIAN_POINT('Ctrl Pts',(-65.0027734492732,-3.22713225326276,
0.00157808088591662));
#50092=CARTESIAN_POINT('Ctrl Pts',(-64.9420007555398,-3.2212390697275,-0.979129695932009));
#50093=CARTESIAN_POINT('Ctrl Pts',(-64.8149368845739,-2.219890297518,-3.04001052674665));
#50094=CARTESIAN_POINT('Ctrl Pts',(-64.6215818363755,1.29014513205747,-3.5868185303575));
#50095=CARTESIAN_POINT('Ctrl Pts',(-64.422708304678,3.71497134405747,-0.853656572820322));
#50096=CARTESIAN_POINT('Ctrl Pts',(-64.2238347729806,2.72647425728869,2.66384679661379));
#50097=CARTESIAN_POINT('Ctrl Pts',(-64.024961241283,-0.767112975271716,
3.73380225971558));
#50098=CARTESIAN_POINT('Ctrl Pts',(-63.8679408000473,-2.96897803075723,
1.86993733095529));
#50099=CARTESIAN_POINT('Ctrl Pts',(-63.777211536044,-3.22125481822615,0.399079996726682));
#50100=CARTESIAN_POINT('Ctrl Pts',(-63.7527734492732,-3.21887470245503,
0.00211579531700205));
#50101=CARTESIAN_POINT('Ctrl Pts',(-64.756226550727,-3.21854419053207,0.00189994234605008));
#50102=CARTESIAN_POINT('Ctrl Pts',(-64.7154503010421,-3.2150001780999,-0.660626443449188));
#50103=CARTESIAN_POINT('Ctrl Pts',(-64.6083828741248,-2.69275524640072,
-2.40536709103522));
#50104=CARTESIAN_POINT('Ctrl Pts',(-64.435024269975,0.16668379745318,-3.80814366104459));
#50105=CARTESIAN_POINT('Ctrl Pts',(-64.2361507382776,3.2938257995051,-1.91845073796596));
#50106=CARTESIAN_POINT('Ctrl Pts',(-64.0372772065801,3.39459389384955,1.73391866225805));
#50107=CARTESIAN_POINT('Ctrl Pts',(-63.8384036748827,0.376402148498568,
3.79316003539174));
#50108=CARTESIAN_POINT('Ctrl Pts',(-63.6613867895983,-2.6179141453899,2.52395018421684));
#50109=CARTESIAN_POINT('Ctrl Pts',(-63.5506610815464,-3.21449859752266,
0.71870541071796));
#50110=CARTESIAN_POINT('Ctrl Pts',(-63.506226550727,-3.21980873461777,-0.00254834726308481));
#50111=CARTESIAN_POINT('Origin',(-111.877773449273,0.,0.));
#50112=CARTESIAN_POINT('',(-66.2527734492732,-3.22375014837333,-0.00289065711299991));
#50113=CARTESIAN_POINT('',(-66.0062265507269,-3.22676995476309,0.00183908904011605));
#50114=CARTESIAN_POINT('',(-111.877773449273,-3.22275,5.46201577318104E-12));
#50115=CARTESIAN_POINT('Ctrl Pts',(-66.2527734492732,-3.22375014837333,
-0.00289065711299982));
#50116=CARTESIAN_POINT('Ctrl Pts',(-66.2393723295005,-3.22576060998705,
-0.219739632465005));
#50117=CARTESIAN_POINT('Ctrl Pts',(-66.1596800324953,-3.10681143896077,
-1.50707965918289));
#50118=CARTESIAN_POINT('Ctrl Pts',(-66.0136965582577,-1.37507787149593,
-3.555123412599));
#50119=CARTESIAN_POINT('Ctrl Pts',(-65.8148230265601,2.24749004247856,-3.07872216032026));
#50120=CARTESIAN_POINT('Ctrl Pts',(-65.6159494948628,3.80505949071416,0.22641533431646));
#50121=CARTESIAN_POINT('Ctrl Pts',(-65.4170759631652,1.8665324660573,3.32352195489086));
#50122=CARTESIAN_POINT('Ctrl Pts',(-65.2182024314679,-1.78696842091292,
3.36696977921506));
#50123=CARTESIAN_POINT('Ctrl Pts',(-65.0801015935038,-3.18387565979518,
1.24891197307991));
#50124=CARTESIAN_POINT('Ctrl Pts',(-65.0082919327723,-3.22766738564045,
0.0906315578881633));
#50125=CARTESIAN_POINT('Ctrl Pts',(-65.0027734492732,-3.22713225326276,
0.00157808088591662));
#50126=CARTESIAN_POINT('Ctrl Pts',(-66.0062265507269,-3.22676995476309,
0.00183908904011598));
#50127=CARTESIAN_POINT('Ctrl Pts',(-65.9465306977704,-3.22021441834723,
-0.961776633740155));
#50128=CARTESIAN_POINT('Ctrl Pts',(-65.8205436675812,-2.24946408802035,
-3.00692622463982));
#50129=CARTESIAN_POINT('Ctrl Pts',(-65.6282654601599,1.23173349036234,-3.60729458738919));
#50130=CARTESIAN_POINT('Ctrl Pts',(-65.4293919284621,3.70062017644406,-0.913866478859252));
#50131=CARTESIAN_POINT('Ctrl Pts',(-65.230518396765,2.76936944602707,2.61922402686354));
#50132=CARTESIAN_POINT('Ctrl Pts',(-65.0316448650673,-0.706383617669903,
3.74576611872324));
#50133=CARTESIAN_POINT('Ctrl Pts',(-64.8735475830548,-2.95352906927565,
1.9053646207508));
#50134=CARTESIAN_POINT('Ctrl Pts',(-64.7817414782746,-3.22076178585125,
0.416462656245822));
#50135=CARTESIAN_POINT('Ctrl Pts',(-64.756226550727,-3.21854419053207,0.00189994234605008));
#50136=CARTESIAN_POINT('Origin',(-111.877773449273,0.,0.));
#50137=CARTESIAN_POINT('',(-67.5027734492732,-3.21741959772868,-0.000221941790678977));
#50138=CARTESIAN_POINT('',(-67.256226550727,-3.22427826197944,-0.00280124290513745));
#50139=CARTESIAN_POINT('',(-111.877773449273,-3.22275,5.46201577318104E-12));
#50140=CARTESIAN_POINT('Ctrl Pts',(-67.5027734492732,-3.21741959772868,
-0.000221941790679026));
#50141=CARTESIAN_POINT('Ctrl Pts',(-67.4704527262287,-3.21774121840307,
-0.525822896622257));
#50142=CARTESIAN_POINT('Ctrl Pts',(-67.3718408259518,-2.84712891776362,
-2.12902637166851));
#50143=CARTESIAN_POINT('Ctrl Pts',(-67.2069377484423,-0.318917148843096,
-3.79842513203319));
#50144=CARTESIAN_POINT('Ctrl Pts',(-67.008064216745,3.02313441827591,-2.32172348063307));
#50145=CARTESIAN_POINT('Ctrl Pts',(-66.8091906850474,3.58752387456407,1.28818247190379));
#50146=CARTESIAN_POINT('Ctrl Pts',(-66.61031715335,0.855689028738441,3.71450372426576));
#50147=CARTESIAN_POINT('Ctrl Pts',(-66.4248447414253,-2.42529080533395,
2.79441164195831));
#50148=CARTESIAN_POINT('Ctrl Pts',(-66.305663506733,-3.21581548081763,0.852944897003651));
#50149=CARTESIAN_POINT('Ctrl Pts',(-66.2527734492732,-3.22375014837333,
-0.00289065711299982));
#50150=CARTESIAN_POINT('Ctrl Pts',(-67.256226550727,-3.22427826197944,-0.00280124290513738));
#50151=CARTESIAN_POINT('Ctrl Pts',(-67.2439022717311,-3.22610275259481,
-0.202141319110646));
#50152=CARTESIAN_POINT('Ctrl Pts',(-67.1652868155028,-3.11834622337749,
-1.4717463453671));
#50153=CARTESIAN_POINT('Ctrl Pts',(-67.0203801820419,-1.43262347679405,
-3.53232665607612));
#50154=CARTESIAN_POINT('Ctrl Pts',(-66.8215066503446,2.19720248236392,-3.11481024831069));
#50155=CARTESIAN_POINT('Ctrl Pts',(-66.6226331186469,3.80823428927037,0.164600211157061));
#50156=CARTESIAN_POINT('Ctrl Pts',(-66.4237595869497,1.92025261185217,3.29277565864461));
#50157=CARTESIAN_POINT('Ctrl Pts',(-66.2248860552521,-1.73206110813779,
3.39554207000353));
#50158=CARTESIAN_POINT('Ctrl Pts',(-66.0857083765112,-3.17433560462667,
1.28410951244796));
#50159=CARTESIAN_POINT('Ctrl Pts',(-66.0128218750029,-3.22749422431154,
0.108301395119127));
#50160=CARTESIAN_POINT('Ctrl Pts',(-66.0062265507269,-3.22676995476309,
0.00183908904011598));
#50161=CARTESIAN_POINT('Origin',(-111.877773449273,0.,0.));
#50162=CARTESIAN_POINT('',(-68.7527734492732,-3.22293282582728,0.00296792478262312));
#50163=CARTESIAN_POINT('',(-68.5062265507269,-3.21747859664537,-0.000509701883559255));
#50164=CARTESIAN_POINT('',(-111.877773449273,-3.22275,5.46201577318104E-12));
#50165=CARTESIAN_POINT('Ctrl Pts',(-68.7527734492732,-3.22293282582728,
0.00296792478262326));
#50166=CARTESIAN_POINT('Ctrl Pts',(-68.701533122957,-3.21523694329641,-0.826711997340943));
#50167=CARTESIAN_POINT('Ctrl Pts',(-68.5840016194083,-2.4650798738634,-2.74212576371246));
#50168=CARTESIAN_POINT('Ctrl Pts',(-68.4001789386271,0.76302674318989,-3.73463944988864));
#50169=CARTESIAN_POINT('Ctrl Pts',(-68.2013054069296,3.55437052989495,-1.37702279127899));
#50170=CARTESIAN_POINT('Ctrl Pts',(-68.0024318752321,3.07995137564101,2.24580523536093));
#50171=CARTESIAN_POINT('Ctrl Pts',(-67.8035583435348,-0.224333426531556,
3.80518280050091));
#50172=CARTESIAN_POINT('Ctrl Pts',(-67.6370055348817,-2.81898931674464,
2.18312258522133));
#50173=CARTESIAN_POINT('Ctrl Pts',(-67.5367439034612,-3.21708156072468,
0.552207010145866));
#50174=CARTESIAN_POINT('Ctrl Pts',(-67.5027734492732,-3.21741959772868,
-0.000221941790679026));
#50175=CARTESIAN_POINT('Ctrl Pts',(-68.5062265507269,-3.21747859664537,
-0.000509701883559047));
#50176=CARTESIAN_POINT('Ctrl Pts',(-68.4749826684593,-3.2181933316529,-0.508575802308148));
#50177=CARTESIAN_POINT('Ctrl Pts',(-68.3774476089592,-2.86499356994955,
-2.09368301619967));
#50178=CARTESIAN_POINT('Ctrl Pts',(-68.2136213722266,-0.380552649142222,
-3.79274588032446));
#50179=CARTESIAN_POINT('Ctrl Pts',(-68.0147478405293,2.98503648681207,-2.37050602274877));
#50180=CARTESIAN_POINT('Ctrl Pts',(-67.8158743088317,3.6079679695899,1.22975963582352));
#50181=CARTESIAN_POINT('Ctrl Pts',(-67.6170007771343,0.915891073766863,
3.70011961596942));
#50182=CARTESIAN_POINT('Ctrl Pts',(-67.4304515244327,-2.39872972824626,
2.82839230532065));
#50183=CARTESIAN_POINT('Ctrl Pts',(-67.3101934489636,-3.21628898330386,
0.8700908435767));
#50184=CARTESIAN_POINT('Ctrl Pts',(-67.256226550727,-3.22427826197944,-0.00280124290513738));
#50185=CARTESIAN_POINT('Origin',(-111.877773449273,0.,0.));
#50186=CARTESIAN_POINT('',(-70.0027734492732,-3.22759001795114,-0.00114057037762329));
#50187=CARTESIAN_POINT('',(-69.7562265507269,-3.22240161101842,0.00297936229024562));
#50188=CARTESIAN_POINT('',(-111.877773449273,-3.22275,5.46201577318104E-12));
#50189=CARTESIAN_POINT('Ctrl Pts',(-70.0027734492732,-3.22759001795114,
-0.00114057037762324));
#50190=CARTESIAN_POINT('Ctrl Pts',(-69.9989046969177,-3.22787455754374,
-0.0635483535897433));
#50191=CARTESIAN_POINT('Ctrl Pts',(-69.9287447673297,-3.19790422336463,
-1.19503652969521));
#50192=CARTESIAN_POINT('Ctrl Pts',(-69.7922936605092,-1.8701681655698,-3.32147748208183));
#50193=CARTESIAN_POINT('Ctrl Pts',(-69.5934201288118,1.78328299053953,-3.36892318213695));
#50194=CARTESIAN_POINT('Ctrl Pts',(-69.3945465971144,3.79825007337514,-0.320995345127123));
#50195=CARTESIAN_POINT('Ctrl Pts',(-69.1956730654169,2.32337718995098,3.02186367407648));
#50196=CARTESIAN_POINT('Ctrl Pts',(-68.9967995337195,-1.2862194261268,3.58822814482881));
#50197=CARTESIAN_POINT('Ctrl Pts',(-68.8491663283382,-3.0885014647762,1.56124403622359));
#50198=CARTESIAN_POINT('Ctrl Pts',(-68.7678243001894,-3.22519334188891,
0.246670291918771));
#50199=CARTESIAN_POINT('Ctrl Pts',(-68.7527734492732,-3.22293282582728,
0.00296792478262326));
#50200=CARTESIAN_POINT('Ctrl Pts',(-69.7562265507269,-3.22240161101842,
0.00297936229024551));
#50201=CARTESIAN_POINT('Ctrl Pts',(-69.7060630651875,-3.21495053399222,
-0.809606534766093));
#50202=CARTESIAN_POINT('Ctrl Pts',(-69.5896084024157,-2.49046711360947,
-2.70785758711506));
#50203=CARTESIAN_POINT('Ctrl Pts',(-69.4068625624114,0.702284330303311,
-3.74653684766316));
#50204=CARTESIAN_POINT('Ctrl Pts',(-69.2079890307139,3.53154229168029,-1.43455591510438));
#50205=CARTESIAN_POINT('Ctrl Pts',(-69.0091154990165,3.11601194424255,2.19549793778661));
#50206=CARTESIAN_POINT('Ctrl Pts',(-68.810241967319,-0.162516575587105,
3.8083237774836));
#50207=CARTESIAN_POINT('Ctrl Pts',(-68.6426123178892,-2.80011258075798,
2.21839497315072));
#50208=CARTESIAN_POINT('Ctrl Pts',(-68.5412738456918,-3.21667685477425,
0.569404828286875));
#50209=CARTESIAN_POINT('Ctrl Pts',(-68.5062265507269,-3.21747859664537,
-0.000509701883559047));
#50210=CARTESIAN_POINT('Origin',(-111.877773449273,0.,0.));
#50211=CARTESIAN_POINT('',(-71.2527734492732,-3.21945012312131,-0.00240714690090972));
#50212=CARTESIAN_POINT('',(-71.0062265507269,-3.22781546179181,-0.00083510151203281));
#50213=CARTESIAN_POINT('',(-111.877773449273,-3.22275,5.46201577318104E-12));
#50214=CARTESIAN_POINT('Ctrl Pts',(-71.2527734492732,-3.21945012312131,
-0.00240714690090973));
#50215=CARTESIAN_POINT('Ctrl Pts',(-71.2299850936459,-3.22200381206688,
-0.372407551372853));
#50216=CARTESIAN_POINT('Ctrl Pts',(-71.1409055607861,-2.99193409339074,
-1.81565804682397));
#50217=CARTESIAN_POINT('Ctrl Pts',(-70.9855348506941,-0.859753171502819,
-3.71356514896109));
#50218=CARTESIAN_POINT('Ctrl Pts',(-70.7866613189964,2.65936797721959,-2.73084301878126));
#50219=CARTESIAN_POINT('Ctrl Pts',(-70.5877877872991,3.73505636806534,0.760983284219782));
#50220=CARTESIAN_POINT('Ctrl Pts',(-70.3889142556016,1.37896729884392,3.55361658317363));
#50221=CARTESIAN_POINT('Ctrl Pts',(-70.1939094762596,-2.17363864940172,
3.09037013995876));
#50222=CARTESIAN_POINT('Ctrl Pts',(-70.0651958741502,-3.22299896385633,
1.00581071554859));
#50223=CARTESIAN_POINT('Ctrl Pts',(-70.0027734492732,-3.22759001795114,
-0.00114057037762324));
#50224=CARTESIAN_POINT('Ctrl Pts',(-71.0062265507269,-3.22781546179181,
-0.000835101512032888));
#50225=CARTESIAN_POINT('Ctrl Pts',(-71.0034346391483,-3.22797109666668,
-0.0458637190486939));
#50226=CARTESIAN_POINT('Ctrl Pts',(-70.9343515503372,-3.20668289731449,
-1.15990179856474));
#50227=CARTESIAN_POINT('Ctrl Pts',(-70.7989772842935,-1.92385463457588,
-3.29067242011544));
#50228=CARTESIAN_POINT('Ctrl Pts',(-70.6001037525962,1.72834444495199,-3.39743537261432));
#50229=CARTESIAN_POINT('Ctrl Pts',(-70.4012302208986,3.79253709969573,-0.382627728894362));
#50230=CARTESIAN_POINT('Ctrl Pts',(-70.2023566892013,2.3721388801267,2.98373905777277));
#50231=CARTESIAN_POINT('Ctrl Pts',(-70.0034831575037,-1.22778541315046,
3.60864027172874));
#50232=CARTESIAN_POINT('Ctrl Pts',(-69.8547731113456,-3.07612755899721,
1.59661877607581));
#50233=CARTESIAN_POINT('Ctrl Pts',(-69.77235424242,-3.22479715175424,0.264227851724424));
#50234=CARTESIAN_POINT('Ctrl Pts',(-69.7562265507269,-3.22240161101842,
0.00297936229024551));
#50235=CARTESIAN_POINT('Origin',(-111.877773449273,0.,0.));
#50236=CARTESIAN_POINT('',(-72.5027734492732,-3.21882799635161,0.00208781935145901));
#50237=CARTESIAN_POINT('',(-72.2562265507269,-3.21986660597496,-0.00256872119734103));
#50238=CARTESIAN_POINT('',(-111.877773449273,-3.22275,5.46201577318104E-12));
#50239=CARTESIAN_POINT('Ctrl Pts',(-72.5027734492732,-3.21882799635161,
0.00208781935145931));
#50240=CARTESIAN_POINT('Ctrl Pts',(-72.4610654903742,-3.2148231872832,-0.675427126265385));
#50241=CARTESIAN_POINT('Ctrl Pts',(-72.3530663542426,-2.67416790804054,
-2.43563871880424));
#50242=CARTESIAN_POINT('Ctrl Pts',(-72.1787760408787,0.220169410119124,
-3.80542600274073));
#50243=CARTESIAN_POINT('Ctrl Pts',(-71.9799025091812,3.3204537540748,-1.87198517583289));
#50244=CARTESIAN_POINT('Ctrl Pts',(-71.7810289774838,3.36989837098991,1.78143947432599));
#50245=CARTESIAN_POINT('Ctrl Pts',(-71.5821554457863,0.323073445319674,
3.79807387769336));
#50246=CARTESIAN_POINT('Ctrl Pts',(-71.4060702697162,-2.63745085413309,
2.49382211291307));
#50247=CARTESIAN_POINT('Ctrl Pts',(-71.2962762708784,-3.21457514765352,
0.70392120135233));
#50248=CARTESIAN_POINT('Ctrl Pts',(-71.2527734492732,-3.21945012312131,
-0.00240714690090973));
#50249=CARTESIAN_POINT('Ctrl Pts',(-72.2562265507269,-3.21986660597496,
-0.00256872119734103));
#50250=CARTESIAN_POINT('Ctrl Pts',(-72.2345150358765,-3.22248512237309,
-0.354970389721529));
#50251=CARTESIAN_POINT('Ctrl Pts',(-72.1465123437936,-3.00645953474252,
-1.780228858952));
#50252=CARTESIAN_POINT('Ctrl Pts',(-71.9922184744782,-0.919939440447408,
-3.69911517222657));
#50253=CARTESIAN_POINT('Ctrl Pts',(-71.7933449427809,2.61467485947912,-2.77366490598547));
#50254=CARTESIAN_POINT('Ctrl Pts',(-71.5944714110833,3.74692052987602,0.700234370965129));
#50255=CARTESIAN_POINT('Ctrl Pts',(-71.3955978793859,1.43648792397377,3.53075687010093));
#50256=CARTESIAN_POINT('Ctrl Pts',(-71.1995162592671,-2.14282857537852,
3.12301830014379));
#50257=CARTESIAN_POINT('Ctrl Pts',(-71.0697258163808,-3.2242757005974,1.02329623877626));
#50258=CARTESIAN_POINT('Ctrl Pts',(-71.0062265507269,-3.22781546179181,
-0.000835101512032888));
#50259=CARTESIAN_POINT('Origin',(-111.877773449273,0.,0.));
#50260=CARTESIAN_POINT('',(-73.7527734492733,-3.22708613677034,0.00161448296875132));
#50261=CARTESIAN_POINT('',(-73.5062265507269,-3.21850254177831,0.00186944240760517));
#50262=CARTESIAN_POINT('',(-111.877773449273,-3.22275,5.46201577318104E-12));
#50263=CARTESIAN_POINT('Ctrl Pts',(-73.7527734492733,-3.22708613677034,
0.00161448296875113));
#50264=CARTESIAN_POINT('Ctrl Pts',(-73.6921458871025,-3.22109534309337,
-0.976788199942429));
#50265=CARTESIAN_POINT('Ctrl Pts',(-73.565227147699,-2.22390442281198,-3.03556114541307));
#50266=CARTESIAN_POINT('Ctrl Pts',(-73.3720172310635,1.28229218005324,-3.5896334626897));
#50267=CARTESIAN_POINT('Ctrl Pts',(-73.1731436993659,3.71309419372906,-0.861784857132571));
#50268=CARTESIAN_POINT('Ctrl Pts',(-72.9742701676686,2.73229763821218,2.65787344463722));
#50269=CARTESIAN_POINT('Ctrl Pts',(-72.7753966359709,-0.758939597445834,
3.73547216813566));
#50270=CARTESIAN_POINT('Ctrl Pts',(-72.6182310631726,-2.96691742054202,
1.87471226882313));
#50271=CARTESIAN_POINT('Ctrl Pts',(-72.5273566676067,-3.22118848337403,
0.401424019730246));
#50272=CARTESIAN_POINT('Ctrl Pts',(-72.5027734492732,-3.21882799635161,
0.00208781935145931));
#50273=CARTESIAN_POINT('Ctrl Pts',(-73.5062265507269,-3.21850254177831,
0.00186944240760538));
#50274=CARTESIAN_POINT('Ctrl Pts',(-73.4655954326047,-3.21503052406492,
-0.658320259377352));
#50275=CARTESIAN_POINT('Ctrl Pts',(-73.3586731372501,-2.69562174110393,
-2.40064775943804));
#50276=CARTESIAN_POINT('Ctrl Pts',(-73.185459664663,0.158349159120692,-3.80849933376564));
#50277=CARTESIAN_POINT('Ctrl Pts',(-72.9865861329655,3.28961932307638,-1.92565478233509));
#50278=CARTESIAN_POINT('Ctrl Pts',(-72.7877126012682,3.39838049850435,1.72648533699904));
#50279=CARTESIAN_POINT('Ctrl Pts',(-72.5888390695705,0.384702694105128,
3.79232718375349));
#50280=CARTESIAN_POINT('Ctrl Pts',(-72.4116770527236,-2.61484136747631,
2.52863830808241));
#50281=CARTESIAN_POINT('Ctrl Pts',(-72.300806213109,-3.21449007753948,0.721008031228958));
#50282=CARTESIAN_POINT('Ctrl Pts',(-72.2562265507269,-3.21986660597496,
-0.00256872119734103));
#50283=CARTESIAN_POINT('Origin',(-111.877773449273,0.,0.));
#50284=CARTESIAN_POINT('',(-75.0027734492731,-3.22382174436618,-0.00288039460979974));
#50285=CARTESIAN_POINT('',(-74.7562265507269,-3.22671773329219,0.00187259391569501));
#50286=CARTESIAN_POINT('',(-111.877773449273,-3.22275,5.46201577318104E-12));
#50287=CARTESIAN_POINT('Ctrl Pts',(-75.0027734492731,-3.22382174436618,
-0.00288039460980015));
#50288=CARTESIAN_POINT('Ctrl Pts',(-74.9895174610631,-3.2258080640962,-0.217368688148813));
#50289=CARTESIAN_POINT('Ctrl Pts',(-74.9099702956205,-3.10838512112799,
-1.50231655289377));
#50290=CARTESIAN_POINT('Ctrl Pts',(-74.7641319529457,-1.38285507499101,
-3.55210549858237));
#50291=CARTESIAN_POINT('Ctrl Pts',(-74.5652584212481,2.24074678227322,-3.08363348814666));
#50292=CARTESIAN_POINT('Ctrl Pts',(-74.3663848895507,3.80554589512093,0.218087302738192));
#50293=CARTESIAN_POINT('Ctrl Pts',(-74.1675113578533,1.87380162570858,3.31942903207455));
#50294=CARTESIAN_POINT('Ctrl Pts',(-73.9686378261556,-1.77959542483032,
3.37087255104825));
#50295=CARTESIAN_POINT('Ctrl Pts',(-73.8303918566292,-3.18260764459991,
1.25365432148051));
#50296=CARTESIAN_POINT('Ctrl Pts',(-73.758437064335,-3.22764577578741,0.0930134436550926));
#50297=CARTESIAN_POINT('Ctrl Pts',(-73.7527734492733,-3.22708613677034,
0.00161448296875113));
#50298=CARTESIAN_POINT('Ctrl Pts',(-74.7562265507269,-3.22671773329219,
0.00187259391569496));
#50299=CARTESIAN_POINT('Ctrl Pts',(-74.696675829333,-3.22008363392945,-0.959441334008879));
#50300=CARTESIAN_POINT('Ctrl Pts',(-74.5708339307065,-2.2534128417743,-3.00245490988977));
#50301=CARTESIAN_POINT('Ctrl Pts',(-74.3787008548478,1.22383586576573,-3.60998163501602));
#50302=CARTESIAN_POINT('Ctrl Pts',(-74.1798273231502,3.69861128925905,-0.921963211008446));
#50303=CARTESIAN_POINT('Ctrl Pts',(-73.9809537914529,2.77509506592403,2.61315690431547));
#50304=CARTESIAN_POINT('Ctrl Pts',(-73.7820802597554,-0.698184202008545,
3.74730309043091));
#50305=CARTESIAN_POINT('Ctrl Pts',(-73.6238378461801,-2.95141859444466,
1.910138997005));
#50306=CARTESIAN_POINT('Ctrl Pts',(-73.5318866098372,-3.22069524982759,
0.418803741899784));
#50307=CARTESIAN_POINT('Ctrl Pts',(-73.5062265507269,-3.21850254177831,
0.00186944240760538));
#50308=CARTESIAN_POINT('Origin',(-111.877773449273,0.,0.));
#50309=CARTESIAN_POINT('',(-76.2527734492732,-3.21742483922095,-0.000260901863258924));
#50310=CARTESIAN_POINT('',(-76.0062265507269,-3.22434875022485,-0.00278685721651517));
#50311=CARTESIAN_POINT('',(-111.877773449273,-3.22275,5.46201577318104E-12));
#50312=CARTESIAN_POINT('Ctrl Pts',(-76.2527734492732,-3.21742483922095,
-0.000260901863258847));
#50313=CARTESIAN_POINT('Ctrl Pts',(-76.2205978577914,-3.21780125389046,
-0.523499596499799));
#50314=CARTESIAN_POINT('Ctrl Pts',(-76.122131089077,-2.84955967489057,-2.1242643517588));
#50315=CARTESIAN_POINT('Ctrl Pts',(-75.9573731431304,-0.327229354942119,
-3.79771807547001));
#50316=CARTESIAN_POINT('Ctrl Pts',(-75.7584996114328,3.01804601534794,-2.32833414284333));
#50317=CARTESIAN_POINT('Ctrl Pts',(-75.5596260797355,3.59033450986518,1.28032798093242));
#50318=CARTESIAN_POINT('Ctrl Pts',(-75.3607525480379,0.863816284783001,
3.71262212696513));
#50319=CARTESIAN_POINT('Ctrl Pts',(-75.1751350045506,-2.42173826724886,
2.79899842446453));
#50320=CARTESIAN_POINT('Ctrl Pts',(-75.0558086382956,-3.21587478178058,
0.855254586403673));
#50321=CARTESIAN_POINT('Ctrl Pts',(-75.0027734492731,-3.22382174436618,
-0.00288039460980015));
#50322=CARTESIAN_POINT('Ctrl Pts',(-76.0062265507269,-3.22434875022485,
-0.00278685721651517));
#50323=CARTESIAN_POINT('Ctrl Pts',(-75.9940474032937,-3.22614707084526,
-0.199768380540557));
#50324=CARTESIAN_POINT('Ctrl Pts',(-75.915577078628,-3.11987589874836,-1.4669856933204));
#50325=CARTESIAN_POINT('Ctrl Pts',(-75.77081557673,-1.4403506510764,-3.52918285633249));
#50326=CARTESIAN_POINT('Ctrl Pts',(-75.5719420450324,2.19038036270197,-3.1196114338451));
#50327=CARTESIAN_POINT('Ctrl Pts',(-75.373068513335,3.80858540178188,0.156265379471771));
#50328=CARTESIAN_POINT('Ctrl Pts',(-75.1741949816376,1.92745435364065,3.28856524127456));
#50329=CARTESIAN_POINT('Ctrl Pts',(-74.9753214499401,-1.72462571221478,
3.39932460707347));
#50330=CARTESIAN_POINT('Ctrl Pts',(-74.8359986396366,-3.17302647816718,
1.28885510720927));
#50331=CARTESIAN_POINT('Ctrl Pts',(-74.7629670065655,-3.22746863693763,
0.110682259466689));
#50332=CARTESIAN_POINT('Ctrl Pts',(-74.7562265507269,-3.22671773329219,
0.00187259391569496));
#50333=CARTESIAN_POINT('Origin',(-111.877773449273,0.,0.));
#50334=CARTESIAN_POINT('',(-77.5027734492732,-3.22286096438354,0.00297125643594199));
#50335=CARTESIAN_POINT('',(-77.2562265507269,-3.2174900915274,-0.00054818518968075));
#50336=CARTESIAN_POINT('',(-111.877773449273,-3.22275,5.46201577318104E-12));
#50337=CARTESIAN_POINT('Ctrl Pts',(-77.5027734492732,-3.22286096438354,
0.00297125643594204));
#50338=CARTESIAN_POINT('Ctrl Pts',(-77.4516782545196,-3.21519424277418,
-0.824405892672294));
#50339=CARTESIAN_POINT('Ctrl Pts',(-77.3342918825336,-2.46852826513399,
-2.73751347857648));
#50340=CARTESIAN_POINT('Ctrl Pts',(-77.150614333315,0.754851542933501,-3.73630041345961));
#50341=CARTESIAN_POINT('Ctrl Pts',(-76.9517408016175,3.55134836116475,-1.38479834240944));
#50342=CARTESIAN_POINT('Ctrl Pts',(-76.7528672699202,3.08485901327164,2.23905928901498));
#50343=CARTESIAN_POINT('Ctrl Pts',(-76.5539937382226,-0.216005130071836,
3.80566464829338));
#50344=CARTESIAN_POINT('Ctrl Pts',(-76.3872957980071,-2.81646876630082,
2.18787831468303));
#50345=CARTESIAN_POINT('Ctrl Pts',(-76.2868890350239,-3.21702572901523,
0.554525932903884));
#50346=CARTESIAN_POINT('Ctrl Pts',(-76.2527734492732,-3.21742483922095,
-0.000260901863258847));
#50347=CARTESIAN_POINT('Ctrl Pts',(-77.2562265507269,-3.2174900915274,-0.000548185189681097));
#50348=CARTESIAN_POINT('Ctrl Pts',(-77.225127800022,-3.21825537090246,-0.506249753593985));
#50349=CARTESIAN_POINT('Ctrl Pts',(-77.1277378720846,-2.86737116326948,
-2.08891786712429));
#50350=CARTESIAN_POINT('Ctrl Pts',(-76.9640567669146,-0.388852278417899,
-3.79190394618015));
#50351=CARTESIAN_POINT('Ctrl Pts',(-76.7651832352172,2.9798414130333,-2.37703318964188));
#50352=CARTESIAN_POINT('Ctrl Pts',(-76.5663097035197,3.61065069576294,1.22186054223637));
#50353=CARTESIAN_POINT('Ctrl Pts',(-76.3674361718222,0.923986705575531,
3.69810629909514));
#50354=CARTESIAN_POINT('Ctrl Pts',(-76.1807417875581,-2.39511414671302,
2.83296268424476));
#50355=CARTESIAN_POINT('Ctrl Pts',(-76.0603385805262,-3.21635880022759,
0.872403308475266));
#50356=CARTESIAN_POINT('Ctrl Pts',(-76.0062265507269,-3.22434875022485,
-0.00278685721651517));
#50357=CARTESIAN_POINT('Origin',(-111.877773449273,0.,0.));
#50358=CARTESIAN_POINT('',(-78.7527734492732,-3.2276239969737,-0.00110020614287963));
#50359=CARTESIAN_POINT('',(-78.5062265507269,-3.22233048953625,0.00297856531753751));
#50360=CARTESIAN_POINT('',(-111.877773449273,-3.22275,5.46201577318104E-12));
#50361=CARTESIAN_POINT('Ctrl Pts',(-78.7527734492731,-3.2276239969737,-0.00110020614287983));
#50362=CARTESIAN_POINT('Ctrl Pts',(-78.7490498284803,-3.22788936443132,
-0.0611651541018486));
#50363=CARTESIAN_POINT('Ctrl Pts',(-78.679035030455,-3.19910469106636,-1.19029975791683));
#50364=CARTESIAN_POINT('Ctrl Pts',(-78.5427290551972,-1.87743284212275,
-3.31737660732185));
#50365=CARTESIAN_POINT('Ctrl Pts',(-78.3438555234997,1.77590572820074,-3.3728178836147));
#50366=CARTESIAN_POINT('Ctrl Pts',(-78.1449819918024,3.79753846903493,-0.329307163127962));
#50367=CARTESIAN_POINT('Ctrl Pts',(-77.9461084601048,2.32998506713825,3.01677165499815));
#50368=CARTESIAN_POINT('Ctrl Pts',(-77.7472349284074,-1.27836339853949,
3.59103448225746));
#50369=CARTESIAN_POINT('Ctrl Pts',(-77.5994565914635,-3.08685333698085,
1.56601082283768));
#50370=CARTESIAN_POINT('Ctrl Pts',(-77.5179694317521,-3.22514108813702,
0.24903761790008));
#50371=CARTESIAN_POINT('Ctrl Pts',(-77.5027734492732,-3.22286096438354,
0.00297125643594204));
#50372=CARTESIAN_POINT('Ctrl Pts',(-78.5062265507269,-3.22233048953625,
0.00297856531753734));
#50373=CARTESIAN_POINT('Ctrl Pts',(-78.4562081967502,-3.21491722942411,
-0.807301991740865));
#50374=CARTESIAN_POINT('Ctrl Pts',(-78.339898665541,-2.49385359742783,-2.70323107546322));
#50375=CARTESIAN_POINT('Ctrl Pts',(-78.1572979570994,0.694083237695167,
-3.74806484610899));
#50376=CARTESIAN_POINT('Ctrl Pts',(-77.9584244254018,3.52839426461459,-1.44228136815333));
#50377=CARTESIAN_POINT('Ctrl Pts',(-77.7595508937045,3.12080939645103,2.18867319225837));
#50378=CARTESIAN_POINT('Ctrl Pts',(-77.560677362007,-0.154181553044083,
3.80867032968048));
#50379=CARTESIAN_POINT('Ctrl Pts',(-77.3929025810144,-2.79753745286427,
2.22314625409605));
#50380=CARTESIAN_POINT('Ctrl Pts',(-77.2914189772544,-3.21662407480424,
0.571721275400419));
#50381=CARTESIAN_POINT('Ctrl Pts',(-77.2562265507269,-3.2174900915274,-0.000548185189681097));
#50382=CARTESIAN_POINT('Origin',(-111.877773449273,0.,0.));
#50383=CARTESIAN_POINT('',(-80.0027734492731,-3.21950446961254,-0.00243030051328978));
#50384=CARTESIAN_POINT('',(-79.7562265507269,-3.2278409596885,-0.000792969578133351));
#50385=CARTESIAN_POINT('',(-111.877773449273,-3.22275,5.46201577318104E-12));
#50386=CARTESIAN_POINT('Ctrl Pts',(-80.0027734492731,-3.21950446961254,
-0.00243030051328971));
#50387=CARTESIAN_POINT('Ctrl Pts',(-79.9801302252086,-3.22206910334583,
-0.370058688680998));
#50388=CARTESIAN_POINT('Ctrl Pts',(-79.8911958239115,-2.99391276895397,
-1.81088294607542));
#50389=CARTESIAN_POINT('Ctrl Pts',(-79.7359702453819,-0.867878363713628,
-3.71167465940716));
#50390=CARTESIAN_POINT('Ctrl Pts',(-79.5370967136845,2.65338507480061,-2.73665658720871));
#50391=CARTESIAN_POINT('Ctrl Pts',(-79.338223181987,3.73671285846524,0.752807176418981));
#50392=CARTESIAN_POINT('Ctrl Pts',(-79.1393496502896,1.38674119528204,3.55059016063458));
#50393=CARTESIAN_POINT('Ctrl Pts',(-78.944199739385,-2.16951483572038,3.09478083178531));
#50394=CARTESIAN_POINT('Ctrl Pts',(-78.8153410057128,-3.2231650592069,1.00816395649729));
#50395=CARTESIAN_POINT('Ctrl Pts',(-78.7527734492731,-3.2276239969737,-0.00110020614287983));
#50396=CARTESIAN_POINT('Ctrl Pts',(-79.7562265507269,-3.2278409596885,-0.00079296957813336));
#50397=CARTESIAN_POINT('Ctrl Pts',(-79.7535797707109,-3.22798174349532,
-0.0434799691742248));
#50398=CARTESIAN_POINT('Ctrl Pts',(-79.6846418134625,-3.2078434111715,-1.15516845035792));
#50399=CARTESIAN_POINT('Ctrl Pts',(-79.5494126789815,-1.9310517647361,-3.28645412464514));
#50400=CARTESIAN_POINT('Ctrl Pts',(-79.3505391472841,1.72090491437897,-3.40120977111878));
#50401=CARTESIAN_POINT('Ctrl Pts',(-79.1516656155866,3.79169062467575,-0.39092689627776));
#50402=CARTESIAN_POINT('Ctrl Pts',(-78.9527920838892,2.37866320364617,2.9785404135427));
#50403=CARTESIAN_POINT('Ctrl Pts',(-78.7539185521916,-1.21988485293742,
3.61131867564487));
#50404=CARTESIAN_POINT('Ctrl Pts',(-78.605063374471,-3.07443410069902,1.60138749919574));
#50405=CARTESIAN_POINT('Ctrl Pts',(-78.5224993739827,-3.22474229764194,
0.266592843763458));
#50406=CARTESIAN_POINT('Ctrl Pts',(-78.5062265507269,-3.22233048953625,
0.00297856531753734));
#50407=CARTESIAN_POINT('Origin',(-111.877773449273,0.,0.));
#50408=CARTESIAN_POINT('',(-81.2527734492731,-3.21878195259031,0.00205948639376733));
#50409=CARTESIAN_POINT('',(-81.0062265507269,-3.21992499686852,-0.002588646514457));
#50410=CARTESIAN_POINT('',(-111.877773449273,-3.22275,5.46201577318104E-12));
#50411=CARTESIAN_POINT('Ctrl Pts',(-81.2527734492731,-3.21878195259031,
0.00205948639376698));
#50412=CARTESIAN_POINT('Ctrl Pts',(-81.2112106219368,-3.21484868389951,
-0.673122117896321));
#50413=CARTESIAN_POINT('Ctrl Pts',(-81.1033566173679,-2.6770843609167,-2.43092628129503));
#50414=CARTESIAN_POINT('Ctrl Pts',(-80.9292114355667,0.211840591375986,
-3.8058987368732));
#50415=CARTESIAN_POINT('Ctrl Pts',(-80.7303379038692,3.31634890518381,-1.87924760757427));
#50416=CARTESIAN_POINT('Ctrl Pts',(-80.5314643721718,3.3737890355405,1.77406008217146));
#50417=CARTESIAN_POINT('Ctrl Pts',(-80.3325908404742,0.331384872734104,
3.79735772578913));
#50418=CARTESIAN_POINT('Ctrl Pts',(-80.1563605328414,-2.63442917895774,
2.49851864517239));
#50419=CARTESIAN_POINT('Ctrl Pts',(-80.046421402441,-3.2145607825844,0.706224377997202));
#50420=CARTESIAN_POINT('Ctrl Pts',(-80.0027734492731,-3.21950446961254,
-0.00243030051328971));
#50421=CARTESIAN_POINT('Ctrl Pts',(-81.0062265507269,-3.21992499686852,
-0.0025886465144568));
#50422=CARTESIAN_POINT('Ctrl Pts',(-80.9846601674391,-3.22254938084776,
-0.352618678648645));
#50423=CARTESIAN_POINT('Ctrl Pts',(-80.8968026069189,-3.00838975708643,
-1.77545409631581));
#50424=CARTESIAN_POINT('Ctrl Pts',(-80.7426538691663,-0.92803286430498,
-3.69709299778318));
#50425=CARTESIAN_POINT('Ctrl Pts',(-80.5437803374688,2.60859834707974,-2.77938055960323));
#50426=CARTESIAN_POINT('Ctrl Pts',(-80.3449068057714,3.74844404100414,0.692032443566012));
#50427=CARTESIAN_POINT('Ctrl Pts',(-80.1460332740739,1.44421165347667,3.52760461665555));
#50428=CARTESIAN_POINT('Ctrl Pts',(-79.9498065223924,-2.13863853957505,
3.1274044744303));
#50429=CARTESIAN_POINT('Ctrl Pts',(-79.8198709479434,-3.22445567626158,
1.0256574123546));
#50430=CARTESIAN_POINT('Ctrl Pts',(-79.7562265507269,-3.2278409596885,-0.00079296957813336));
#50431=CARTESIAN_POINT('Origin',(-111.877773449273,0.,0.));
#50432=CARTESIAN_POINT('',(-82.5027734492731,-3.2270391465412,0.00165051543764288));
#50433=CARTESIAN_POINT('',(-82.2562265507269,-3.21846159883558,0.00183862481499944));
#50434=CARTESIAN_POINT('',(-111.877773449273,-3.22275,5.46201577318104E-12));
#50435=CARTESIAN_POINT('Ctrl Pts',(-82.5027734492731,-3.2270391465412,0.00165051543764267));
#50436=CARTESIAN_POINT('Ctrl Pts',(-82.4422910186651,-3.22095338202291,
-0.974447575458847));
#50437=CARTESIAN_POINT('Ctrl Pts',(-82.3155174108245,-2.22790971805254,
-3.03110875266732));
#50438=CARTESIAN_POINT('Ctrl Pts',(-82.1224526257514,1.27443308628981,-3.59243120185442));
#50439=CARTESIAN_POINT('Ctrl Pts',(-81.9235790940539,3.71119925889672,-0.86990901377786));
#50440=CARTESIAN_POINT('Ctrl Pts',(-81.7247055623564,2.73810793232568,2.65188736231815));
#50441=CARTESIAN_POINT('Ctrl Pts',(-81.525832030659,-0.750762584548115,
3.73712418486865));
#50442=CARTESIAN_POINT('Ctrl Pts',(-81.368521326298,-2.96485012079678,1.87948715189045));
#50443=CARTESIAN_POINT('Ctrl Pts',(-81.2775017991693,-3.22112210244669,
0.403767647852714));
#50444=CARTESIAN_POINT('Ctrl Pts',(-81.2527734492731,-3.21878195259031,
0.00205948639376698));
#50445=CARTESIAN_POINT('Ctrl Pts',(-82.2562265507268,-3.21846159883558,
0.00183862481499927));
#50446=CARTESIAN_POINT('Ctrl Pts',(-82.2157405641674,-3.21506159653712,
-0.656013876140592));
#50447=CARTESIAN_POINT('Ctrl Pts',(-82.1089634003754,-2.69848048787162,
-2.39592739628771));
#50448=CARTESIAN_POINT('Ctrl Pts',(-81.9358950593511,0.150013762347644,
-3.80883676502338));
#50449=CARTESIAN_POINT('Ctrl Pts',(-81.7370215276534,3.28539709044952,-1.93284960344911));
#50450=CARTESIAN_POINT('Ctrl Pts',(-81.5381479959562,3.40215082603064,1.7190437424413));
#50451=CARTESIAN_POINT('Ctrl Pts',(-81.3392744642585,0.393001397111847,
3.79147616811124));
#50452=CARTESIAN_POINT('Ctrl Pts',(-81.161967315849,-2.61176059653824,2.53332507606297));
#50453=CARTESIAN_POINT('Ctrl Pts',(-81.0509513446717,-3.21448249725523,
0.723310585305127));
#50454=CARTESIAN_POINT('Ctrl Pts',(-81.0062265507269,-3.21992499686852,
-0.0025886465144568));
#50455=CARTESIAN_POINT('Origin',(-111.877773449273,0.,0.));
#50456=CARTESIAN_POINT('',(-83.7527734492731,-3.2238932335569,-0.0028695734350786));
#50457=CARTESIAN_POINT('',(-83.5062265507268,-3.22666475540204,0.00190568230792103));
#50458=CARTESIAN_POINT('',(-111.877773449273,-3.22275,5.46201577318104E-12));
#50459=CARTESIAN_POINT('Ctrl Pts',(-83.7527734492731,-3.2238932335569,-0.00286957343507855));
#50460=CARTESIAN_POINT('Ctrl Pts',(-83.7396625926257,-3.22585510627631,
-0.214997467059213));
#50461=CARTESIAN_POINT('Ctrl Pts',(-83.6602605587458,-3.10995284371994,
-1.49755376714856));
#50462=CARTESIAN_POINT('Ctrl Pts',(-83.5145673476336,-1.39062565506363,
-3.54907057114484));
#50463=CARTESIAN_POINT('Ctrl Pts',(-83.3156938159361,2.23399278962533,-3.08853004637957));
#50464=CARTESIAN_POINT('Ctrl Pts',(-83.1168202842386,3.80601407221043,0.209758226593208));
#50465=CARTESIAN_POINT('Ctrl Pts',(-82.9179467525413,1.88106181046435,3.31532021028137));
#50466=CARTESIAN_POINT('Ctrl Pts',(-82.7190732208437,-1.77221390506902,
3.37475917750697));
#50467=CARTESIAN_POINT('Ctrl Pts',(-82.5806821197544,-3.18133411452089,
1.25839711222566));
#50468=CARTESIAN_POINT('Ctrl Pts',(-82.5085821958975,-3.2276236247731,0.0953952018457218));
#50469=CARTESIAN_POINT('Ctrl Pts',(-82.5027734492731,-3.2270391465412,0.00165051543764267));
#50470=CARTESIAN_POINT('Ctrl Pts',(-83.5062265507268,-3.22666475540204,
0.00190568230792082));
#50471=CARTESIAN_POINT('Ctrl Pts',(-83.4468209608956,-3.21995456564922,
-0.957106822200469));
#50472=CARTESIAN_POINT('Ctrl Pts',(-83.321124193832,-2.25735281108562,-2.99798071119528));
#50473=CARTESIAN_POINT('Ctrl Pts',(-83.1291362495355,1.21593237939653,-3.61265139201427));
#50474=CARTESIAN_POINT('Ctrl Pts',(-82.9302627178384,3.69658468693845,-0.930055527256101));
#50475=CARTESIAN_POINT('Ctrl Pts',(-82.7313891861407,2.78080739402538,2.60707726560248));
#50476=CARTESIAN_POINT('Ctrl Pts',(-82.5325156544434,-0.689981442273743,
3.74882211378524));
#50477=CARTESIAN_POINT('Ctrl Pts',(-82.3741281093054,-2.94930135841404,
1.91491326972369));
#50478=CARTESIAN_POINT('Ctrl Pts',(-82.2820317413998,-3.22062871183087,
0.421144430712464));
#50479=CARTESIAN_POINT('Ctrl Pts',(-82.2562265507268,-3.21846159883558,
0.00183862481499927));
#50480=CARTESIAN_POINT('Origin',(-111.877773449273,0.,0.));
#50481=CARTESIAN_POINT('',(-85.0027734492731,-3.21743092663228,-0.000299818468146348));
#50482=CARTESIAN_POINT('',(-84.756226550727,-3.2244190327258,-0.00277192079580268));
#50483=CARTESIAN_POINT('',(-111.877773449273,-3.22275,5.46201577318104E-12));
#50484=CARTESIAN_POINT('Ctrl Pts',(-85.0027734492731,-3.21743092663228,
-0.000299818468146203));
#50485=CARTESIAN_POINT('Ctrl Pts',(-84.970742989354,-3.21786158184376,-0.521175930689154));
#50486=CARTESIAN_POINT('Ctrl Pts',(-84.8724213522023,-2.85198323582054,
-2.11950188255398));
#50487=CARTESIAN_POINT('Ctrl Pts',(-84.7078085378184,-0.335539993719798,
-3.79699282908225));
#50488=CARTESIAN_POINT('Ctrl Pts',(-84.5089350061207,3.01294315696887,-2.33493365309634));
#50489=CARTESIAN_POINT('Ctrl Pts',(-84.3100614744234,3.59312794864103,1.27246735760964));
#50490=CARTESIAN_POINT('Ctrl Pts',(-84.1111879427259,0.871939403430806,
3.71072274742162));
#50491=CARTESIAN_POINT('Ctrl Pts',(-83.9254252676759,-2.41817725657903,
2.80358304503091));
#50492=CARTESIAN_POINT('Ctrl Pts',(-83.8059537698582,-3.2159354758778,0.857564621780238));
#50493=CARTESIAN_POINT('Ctrl Pts',(-83.7527734492731,-3.2238932335569,-0.00286957343507855));
#50494=CARTESIAN_POINT('Ctrl Pts',(-84.7562265507269,-3.2244190327258,-0.00277192079580251));
#50495=CARTESIAN_POINT('Ctrl Pts',(-84.7441925348564,-3.2261909527838,-0.197395183872092));
#50496=CARTESIAN_POINT('Ctrl Pts',(-84.6658673417535,-3.1213996803745,-1.46222538507072));
#50497=CARTESIAN_POINT('Ctrl Pts',(-84.5212509714179,-1.44807092655128,
-3.52602215295995));
#50498=CARTESIAN_POINT('Ctrl Pts',(-84.3223774397204,2.18354775183615,-3.1243976774634));
#50499=CARTESIAN_POINT('Ctrl Pts',(-84.123503908023,3.80891827241787,0.147929799326536));
#50500=CARTESIAN_POINT('Ctrl Pts',(-83.9246303763255,1.93464686355464,3.28433907275508));
#50501=CARTESIAN_POINT('Ctrl Pts',(-83.7257568446282,-1.71718205589994,
3.40309086249292));
#50502=CARTESIAN_POINT('Ctrl Pts',(-83.5862889027618,-3.17171177674872,
1.29360113283735));
#50503=CARTESIAN_POINT('Ctrl Pts',(-83.5131121381281,-3.22744252056106,
0.113062973018134));
#50504=CARTESIAN_POINT('Ctrl Pts',(-83.5062265507268,-3.22666475540204,
0.00190568230792082));
#50505=CARTESIAN_POINT('Origin',(-111.877773449273,0.,0.));
#50506=CARTESIAN_POINT('',(-86.2527734492731,-3.22278916444396,0.00297402901880627));
#50507=CARTESIAN_POINT('',(-86.0062265507268,-3.217502424002,-0.000586577060036064));
#50508=CARTESIAN_POINT('',(-111.877773449273,-3.22275,5.46201577318104E-12));
#50509=CARTESIAN_POINT('Ctrl Pts',(-86.2527734492731,-3.22278916444396,
0.00297402901880631));
#50510=CARTESIAN_POINT('Ctrl Pts',(-86.2018233860822,-3.21515283337601,
-0.822100023465869));
#50511=CARTESIAN_POINT('Ctrl Pts',(-86.0845821456587,-2.4719682872732,-2.73289922972401));
#50512=CARTESIAN_POINT('Ctrl Pts',(-85.9010497280032,0.746672727185684,
-3.73794348137644));
#50513=CARTESIAN_POINT('Ctrl Pts',(-85.7021761963054,3.54830918264012,-1.3925672608098));
#50514=CARTESIAN_POINT('Ctrl Pts',(-85.5033026646083,3.08975187543889,2.23230261830901));
#50515=CARTESIAN_POINT('Ctrl Pts',(-85.3044291329105,-0.20767579901831,
3.80612826819978));
#50516=CARTESIAN_POINT('Ctrl Pts',(-85.1375860611324,-2.81394089092827,
2.19263347472861));
#50517=CARTESIAN_POINT('Ctrl Pts',(-85.0370341665865,-3.21697028521478,
0.556844514805024));
#50518=CARTESIAN_POINT('Ctrl Pts',(-85.0027734492731,-3.21743092663228,
-0.000299818468146203));
#50519=CARTESIAN_POINT('Ctrl Pts',(-86.0062265507269,-3.217502424002,-0.000586577060035821));
#50520=CARTESIAN_POINT('Ctrl Pts',(-85.9752729315846,-3.2183176510168,-0.503923328628746));
#50521=CARTESIAN_POINT('Ctrl Pts',(-85.8780281352097,-2.86974163214569,
-2.08415233200003));
#50522=CARTESIAN_POINT('Ctrl Pts',(-85.7144921616027,-0.397150045218662,
-3.79104385005903));
#50523=CARTESIAN_POINT('Ctrl Pts',(-85.5156186299052,2.97463206679106,-2.38354897132526));
#50524=CARTESIAN_POINT('Ctrl Pts',(-85.3167450982077,3.61331612810275,1.21395559633781));
#50525=CARTESIAN_POINT('Ctrl Pts',(-85.1178715665104,0.932077911790798,
3.69607526950402));
#50526=CARTESIAN_POINT('Ctrl Pts',(-84.9310320506832,-2.39149003712163,
2.83753078784002));
#50527=CARTESIAN_POINT('Ctrl Pts',(-84.8104837120889,-3.21643006598832,
0.874716184849638));
#50528=CARTESIAN_POINT('Ctrl Pts',(-84.7562265507269,-3.2244190327258,-0.00277192079580251));
#50529=CARTESIAN_POINT('Origin',(-111.877773449273,0.,0.));
#50530=CARTESIAN_POINT('',(-87.5027734492732,-3.22765688580833,-0.00105957506344378));
#50531=CARTESIAN_POINT('',(-87.2562265507268,-3.22225951709131,0.0029772163012047));
#50532=CARTESIAN_POINT('',(-111.877773449273,-3.22275,5.46201577318104E-12));
#50533=CARTESIAN_POINT('Ctrl Pts',(-87.5027734492732,-3.22765688580833,
-0.00105957506344349));
#50534=CARTESIAN_POINT('Ctrl Pts',(-87.499194960043,-3.2279036135337,-0.0587818699554488));
#50535=CARTESIAN_POINT('Ctrl Pts',(-87.4293252935804,-3.20029974928073,
-1.18556344460323));
#50536=CARTESIAN_POINT('Ctrl Pts',(-87.2931644498851,-1.88468852638785,
-3.31325984341546));
#50537=CARTESIAN_POINT('Ctrl Pts',(-87.0942909181878,1.76851995985574,-3.37669643040047));
#50538=CARTESIAN_POINT('Ctrl Pts',(-86.8954173864903,3.79680867573037,-0.337617403855405));
#50539=CARTESIAN_POINT('Ctrl Pts',(-86.6965438547928,2.33658178446086,3.01166518657256));
#50540=CARTESIAN_POINT('Ctrl Pts',(-86.4976703230953,-1.27050124801057,
3.59382361980817));
#50541=CARTESIAN_POINT('Ctrl Pts',(-86.3497468545889,-3.08519912907081,
1.57077788286796));
#50542=CARTESIAN_POINT('Ctrl Pts',(-86.2681145633147,-3.22508847122468,
0.251404636150737));
#50543=CARTESIAN_POINT('Ctrl Pts',(-86.2527734492731,-3.22278916444396,
0.00297402901880631));
#50544=CARTESIAN_POINT('Ctrl Pts',(-87.2562265507268,-3.22225951709131,
0.0029772163012047));
#50545=CARTESIAN_POINT('Ctrl Pts',(-87.2063533283128,-3.21488515861041,
-0.80499762696524));
#50546=CARTESIAN_POINT('Ctrl Pts',(-87.0901889286664,-2.49723177137797,
-2.6986027067367));
#50547=CARTESIAN_POINT('Ctrl Pts',(-86.9077333517873,0.685878820655876,
-3.74957489255291));
#50548=CARTESIAN_POINT('Ctrl Pts',(-86.70885982009,3.52522933769711,-1.44999991314728));
#50549=CARTESIAN_POINT('Ctrl Pts',(-86.5099862883923,3.12559190100552,2.1818379637031));
#50550=CARTESIAN_POINT('Ctrl Pts',(-86.311112756695,-0.145845792021992,
3.80899863959504));
#50551=CARTESIAN_POINT('Ctrl Pts',(-86.1431928441399,-2.79495492899174,
2.22789689550261));
#50552=CARTESIAN_POINT('Ctrl Pts',(-86.0415641088171,-3.21657173696795,
0.574037398758534));
#50553=CARTESIAN_POINT('Ctrl Pts',(-86.0062265507269,-3.217502424002,-0.000586577060035821));
#50554=CARTESIAN_POINT('Origin',(-111.877773449273,0.,0.));
#50555=CARTESIAN_POINT('',(-88.7527734492731,-3.21955938617937,-0.00245303289388847));
#50556=CARTESIAN_POINT('',(-88.5062265507269,-3.22786524494525,-0.00075063836163014));
#50557=CARTESIAN_POINT('',(-111.877773449273,-3.22275,5.46201577318104E-12));
#50558=CARTESIAN_POINT('Ctrl Pts',(-88.7527734492731,-3.21955938617937,
-0.00245303289388835));
#50559=CARTESIAN_POINT('Ctrl Pts',(-88.7302753567712,-3.22213427281091,
-0.367709439234079));
#50560=CARTESIAN_POINT('Ctrl Pts',(-88.6414860870369,-2.99588488351278,
-1.80610787243726));
#50561=CARTESIAN_POINT('Ctrl Pts',(-88.4864056400698,-0.875999399071568,
-3.70976639214839));
#50562=CARTESIAN_POINT('Ctrl Pts',(-88.2875321083726,2.64738946353692,-2.74245704794827));
#50563=CARTESIAN_POINT('Ctrl Pts',(-88.0886585766749,3.73835145123555,0.744627462918542));
#50564=CARTESIAN_POINT('Ctrl Pts',(-87.8897850449776,1.39450844968449,3.54754673193265));
#50565=CARTESIAN_POINT('Ctrl Pts',(-87.6944900025101,-2.16538211451947,
3.09918827690999));
#50566=CARTESIAN_POINT('Ctrl Pts',(-87.5654861372755,-3.22333300557069,
1.01051822704953));
#50567=CARTESIAN_POINT('Ctrl Pts',(-87.5027734492732,-3.22765688580833,
-0.00105957506344349));
#50568=CARTESIAN_POINT('Ctrl Pts',(-88.5062265507269,-3.22786524494525,
-0.000750638361630088));
#50569=CARTESIAN_POINT('Ctrl Pts',(-88.5037249022736,-3.2279918262627,-0.041096158914104));
#50570=CARTESIAN_POINT('Ctrl Pts',(-88.4349320765878,-3.20899857239634,
-1.15043556710435));
#50571=CARTESIAN_POINT('Ctrl Pts',(-88.2998480736696,-1.93823964579142,
-3.28222008813697));
#50572=CARTESIAN_POINT('Ctrl Pts',(-88.1009745419719,1.71345714123552,-3.40496787894343));
#50573=CARTESIAN_POINT('Ctrl Pts',(-87.9021010102748,3.79082598870071,-0.399224191249501));
#50574=CARTESIAN_POINT('Ctrl Pts',(-87.703227478577,2.38517613414864,2.97332750308055));
#50575=CARTESIAN_POINT('Ctrl Pts',(-87.5043539468798,-1.2119784498759,3.61397978252837));
#50576=CARTESIAN_POINT('Ctrl Pts',(-87.3553536375962,-3.07273449438949,
1.60615646661143));
#50577=CARTESIAN_POINT('Ctrl Pts',(-87.2726445055453,-3.22468711006595,
0.268957512522698));
#50578=CARTESIAN_POINT('Ctrl Pts',(-87.2562265507268,-3.22225951709131,
0.0029772163012047));
#50579=CARTESIAN_POINT('Origin',(-111.877773449273,0.,0.));
#50580=CARTESIAN_POINT('',(-90.0027734492731,-3.21873657735583,0.00203080160484108));
#50581=CARTESIAN_POINT('',(-89.7562265507268,-3.21998389906979,-0.00260811917007442));
#50582=CARTESIAN_POINT('',(-111.877773449273,-3.22275,5.46201577318104E-12));
#50583=CARTESIAN_POINT('Ctrl Pts',(-90.0027734492731,-3.21873657735583,
0.00203080160484068));
#50584=CARTESIAN_POINT('Ctrl Pts',(-89.9613557534995,-3.21487495702084,
-0.670816938378399));
#50585=CARTESIAN_POINT('Ctrl Pts',(-89.8536468804933,-2.67999300708434,
-2.42621273871526));
#50586=CARTESIAN_POINT('Ctrl Pts',(-89.6796468302546,0.203510757985896,
-3.80635324199837));
#50587=CARTESIAN_POINT('Ctrl Pts',(-89.4807732985572,3.31222817206875,-1.88650103833566));
#50588=CARTESIAN_POINT('Ctrl Pts',(-89.2818997668597,3.37766354074761,1.76667219285066));
#50589=CARTESIAN_POINT('Ctrl Pts',(-89.0830262351624,0.339694712923688,
3.79662338578627));
#50590=CARTESIAN_POINT('Ctrl Pts',(-88.9066507959666,-2.63139956759911,
2.50321390108784));
#50591=CARTESIAN_POINT('Ctrl Pts',(-88.7965665340037,-3.21454730667008,
0.708527453556772));
#50592=CARTESIAN_POINT('Ctrl Pts',(-88.7527734492731,-3.21955938617937,
-0.00245303289388835));
#50593=CARTESIAN_POINT('Ctrl Pts',(-89.7562265507268,-3.21998389906979,
-0.00260811917007466));
#50594=CARTESIAN_POINT('Ctrl Pts',(-89.7348052990017,-3.22261347762718,
-0.350266587756745));
#50595=CARTESIAN_POINT('Ctrl Pts',(-89.6470928700442,-3.01031348933854,
-1.77067940302499));
#50596=CARTESIAN_POINT('Ctrl Pts',(-89.4930892638543,-0.936121843189332,
-3.69505311547631));
#50597=CARTESIAN_POINT('Ctrl Pts',(-89.2942157321568,2.60250934034945,-2.78508290089926));
#50598=CARTESIAN_POINT('Ctrl Pts',(-89.0953422004592,3.74994959831413,0.683827201558385));
#50599=CARTESIAN_POINT('Ctrl Pts',(-88.896468668762,1.45192846567913,3.52443546714054));
#50600=CARTESIAN_POINT('Ctrl Pts',(-88.7000967855176,-2.13443955597185,
3.13178726832469));
#50601=CARTESIAN_POINT('Ctrl Pts',(-88.5700160795061,-3.22463754819128,
1.02801970744573));
#50602=CARTESIAN_POINT('Ctrl Pts',(-88.5062265507269,-3.22786524494525,
-0.000750638361630088));
#50603=CARTESIAN_POINT('Origin',(-111.877773449273,0.,0.));
#50604=CARTESIAN_POINT('',(-91.2527734492731,-3.22699129851545,0.00168617155983299));
#50605=CARTESIAN_POINT('',(-91.0062265507269,-3.21842136713232,0.00180749504835861));
#50606=CARTESIAN_POINT('',(-111.877773449273,-3.22275,5.46201577318104E-12));
#50607=CARTESIAN_POINT('Ctrl Pts',(-91.2527734492731,-3.22699129851545,
0.00168617155983283));
#50608=CARTESIAN_POINT('Ctrl Pts',(-91.1924361502277,-3.22081317993391,
-0.972107811042261));
#50609=CARTESIAN_POINT('Ctrl Pts',(-91.0658076739498,-2.23190618928049,
-3.02665336582039));
#50610=CARTESIAN_POINT('Ctrl Pts',(-90.8728880204393,1.26656788840972,-3.59521173445138));
#50611=CARTESIAN_POINT('Ctrl Pts',(-90.6740144887419,3.70928654863654,-0.878029003844108));
#50612=CARTESIAN_POINT('Ctrl Pts',(-90.4751409570445,2.74390511179979,2.64588857832797));
#50613=CARTESIAN_POINT('Ctrl Pts',(-90.276267425347,-0.742581975743678,
3.73875830200189));
#50614=CARTESIAN_POINT('Ctrl Pts',(-90.1188115894232,-2.96277612187353,
1.88426197372598));
#50615=CARTESIAN_POINT('Ctrl Pts',(-90.0276469307319,-3.22105568130425,
0.406110880721617));
#50616=CARTESIAN_POINT('Ctrl Pts',(-90.0027734492731,-3.21873657735583,
0.00203080160484068));
#50617=CARTESIAN_POINT('Ctrl Pts',(-91.0062265507269,-3.21842136713232,
0.00180749504835851));
#50618=CARTESIAN_POINT('Ctrl Pts',(-90.9658856957301,-3.21509338775306,
-0.65370728955473));
#50619=CARTESIAN_POINT('Ctrl Pts',(-90.8592536635008,-2.70133149590602,
-2.39120601286823));
#50620=CARTESIAN_POINT('Ctrl Pts',(-90.6863304540388,0.141677647057878,
-3.80915595320164));
#50621=CARTESIAN_POINT('Ctrl Pts',(-90.4874569223416,3.28115912184763,-1.94003516684714));
#50622=CARTESIAN_POINT('Ctrl Pts',(-90.288583390644,3.40590485836977,1.71159391422753));
#50623=CARTESIAN_POINT('Ctrl Pts',(-90.0897098589466,0.401298217770733,
3.79060699254111));
#50624=CARTESIAN_POINT('Ctrl Pts',(-89.9122575789742,-2.60867182378199,
2.53801047560143));
#50625=CARTESIAN_POINT('Ctrl Pts',(-89.8010964762342,-3.21447586454873,
0.725613078532235));
#50626=CARTESIAN_POINT('Ctrl Pts',(-89.7562265507268,-3.21998389906979,
-0.00260811917007466));
#50627=CARTESIAN_POINT('Origin',(-111.877773449273,0.,0.));
#50628=CARTESIAN_POINT('',(-92.5027734492732,-3.22396460283213,-0.00285819432760913));
#50629=CARTESIAN_POINT('',(-92.2562265507269,-3.22661103672827,0.00193834844061623));
#50630=CARTESIAN_POINT('',(-111.877773449273,-3.22275,5.46201577318104E-12));
#50631=CARTESIAN_POINT('Ctrl Pts',(-92.5027734492732,-3.22396460283213,
-0.00285819432760914));
#50632=CARTESIAN_POINT('Ctrl Pts',(-92.4898077241885,-3.22590173312812,
-0.212625971653954));
#50633=CARTESIAN_POINT('Ctrl Pts',(-92.4105508218713,-3.11151461565573,
-1.49279130520091));
#50634=CARTESIAN_POINT('Ctrl Pts',(-92.2650027423214,-1.39838957449524,
-3.54601864482274));
#50635=CARTESIAN_POINT('Ctrl Pts',(-92.0661292106243,2.22722809688435,-3.09341181156606));
#50636=CARTESIAN_POINT('Ctrl Pts',(-91.8672556789264,3.80646401974024,0.201428145775125));
#50637=CARTESIAN_POINT('Ctrl Pts',(-91.6683821472293,1.88831298555067,3.31119550919123));
#50638=CARTESIAN_POINT('Ctrl Pts',(-91.4695086155316,-1.7648238969841,3.37862963997555));
#50639=CARTESIAN_POINT('Ctrl Pts',(-91.3309723828797,-3.18005506152525,
1.26314034387524));
#50640=CARTESIAN_POINT('Ctrl Pts',(-91.2587273274602,-3.22760093411468,
0.0977768293023363));
#50641=CARTESIAN_POINT('Ctrl Pts',(-91.2527734492731,-3.22699129851545,
0.00168617155983283));
#50642=CARTESIAN_POINT('Ctrl Pts',(-92.2562265507269,-3.22661103672827,
0.00193834844061606));
#50643=CARTESIAN_POINT('Ctrl Pts',(-92.1969660924583,-3.219827206744,-0.954773087278188));
#50644=CARTESIAN_POINT('Ctrl Pts',(-92.0714144569572,-2.26128400223956,
-2.99350364556276));
#50645=CARTESIAN_POINT('Ctrl Pts',(-91.8795716442237,1.2080230691099,-3.61530384559662));
#50646=CARTESIAN_POINT('Ctrl Pts',(-91.6806981125261,3.69454037918903,-0.938143388842634));
#50647=CARTESIAN_POINT('Ctrl Pts',(-91.4818245808289,2.78650640297092,2.60098513984405));
#50648=CARTESIAN_POINT('Ctrl Pts',(-91.2829510491313,-0.681775377754059,
3.75032318151061));
#50649=CARTESIAN_POINT('Ctrl Pts',(-91.1244183724306,-2.94717735151063,
1.91968743215883));
#50650=CARTESIAN_POINT('Ctrl Pts',(-91.0321768729625,-3.22056217791316,
0.423484722564532));
#50651=CARTESIAN_POINT('Ctrl Pts',(-91.0062265507269,-3.21842136713232,
0.00180749504835851));
#50652=CARTESIAN_POINT('Origin',(-111.877773449273,0.,0.));
#50653=CARTESIAN_POINT('',(-93.7527734492732,-3.21743785918669,-0.000338685115544857));
#50654=CARTESIAN_POINT('',(-93.5062265507269,-3.22448909586232,-0.00275643515406654));
#50655=CARTESIAN_POINT('',(-111.877773449273,-3.22275,5.46201577318104E-12));
#50656=CARTESIAN_POINT('Ctrl Pts',(-93.7527734492731,-3.21743785918669,
-0.000338685115544891));
#50657=CARTESIAN_POINT('Ctrl Pts',(-93.7208881209167,-3.2179221952485,-0.518851897634327));
#50658=CARTESIAN_POINT('Ctrl Pts',(-93.6227116153277,-2.85439961021422,
-2.11473897272031));
#50659=CARTESIAN_POINT('Ctrl Pts',(-93.4582439325062,-0.343849025370891,
-3.79624939634358));
#50660=CARTESIAN_POINT('Ctrl Pts',(-93.2593704008088,3.00782586757985,-2.34152197978259));
#50661=CARTESIAN_POINT('Ctrl Pts',(-93.0604968691114,3.59590417751189,1.26460063958548));
#50662=CARTESIAN_POINT('Ctrl Pts',(-92.8616233374138,0.880058345774601,
3.70880559473261));
#50663=CARTESIAN_POINT('Ctrl Pts',(-92.6757155308011,-2.41460776576439,
2.8081654885147));
#50664=CARTESIAN_POINT('Ctrl Pts',(-92.556098901421,-3.21599757065862,0.859875011787762));
#50665=CARTESIAN_POINT('Ctrl Pts',(-92.5027734492732,-3.22396460283213,
-0.00285819432760914));
#50666=CARTESIAN_POINT('Ctrl Pts',(-93.5062265507269,-3.22448909586232,
-0.00275643515406668));
#50667=CARTESIAN_POINT('Ctrl Pts',(-93.4943376664191,-3.22623439527328,
-0.195021731697769));
#50668=CARTESIAN_POINT('Ctrl Pts',(-93.4161576048787,-3.12291757706562,
-1.45746542359579));
#50669=CARTESIAN_POINT('Ctrl Pts',(-93.2716863661057,-1.45578426624114,
-3.52284456109722));
#50670=CARTESIAN_POINT('Ctrl Pts',(-93.0728128344086,2.17670468249244,-3.12916895624107));
#50671=CARTESIAN_POINT('Ctrl Pts',(-92.8739393027108,3.80923289958397,0.139593510646091));
#50672=CARTESIAN_POINT('Ctrl Pts',(-92.6750657710136,1.94183010714438,3.28009717332813));
#50673=CARTESIAN_POINT('Ctrl Pts',(-92.476192239316,-1.70973017484599,3.40684081822274));
#50674=CARTESIAN_POINT('Ctrl Pts',(-92.3365791658872,-3.170391492192,1.29834758764436));
#50675=CARTESIAN_POINT('Ctrl Pts',(-92.2632572696908,-3.22741587697946,
0.115443532683487));
#50676=CARTESIAN_POINT('Ctrl Pts',(-92.2562265507269,-3.22661103672827,
0.00193834844061606));
#50677=CARTESIAN_POINT('Origin',(-111.877773449273,0.,0.));
#50678=CARTESIAN_POINT('',(-95.0027734492731,-3.22271743805854,0.00297624318753977));
#50679=CARTESIAN_POINT('',(-94.7562265507269,-3.21751559249332,-0.000624871069029309));
#50680=CARTESIAN_POINT('',(-111.877773449273,-3.22275,5.46201577318104E-12));
#50681=CARTESIAN_POINT('Ctrl Pts',(-95.0027734492731,-3.22271743805854,
0.00297624318753967));
#50682=CARTESIAN_POINT('Ctrl Pts',(-94.9519685176449,-3.21511270739749,
-0.819794381838916));
#50683=CARTESIAN_POINT('Ctrl Pts',(-94.8348724087843,-2.47539994819433,
-2.72828303166915));
#50684=CARTESIAN_POINT('Ctrl Pts',(-94.6514851226908,0.738490335120334,
-3.73956864576937));
#50685=CARTESIAN_POINT('Ctrl Pts',(-94.4526115909935,3.54525300887773,-1.40032950926946));
#50686=CARTESIAN_POINT('Ctrl Pts',(-94.2537380592961,3.09462993870752,2.22553525560538));
#50687=CARTESIAN_POINT('Ctrl Pts',(-94.0548645275986,-0.199345473265892,
3.80657365799952));
#50688=CARTESIAN_POINT('Ctrl Pts',(-93.8878763242577,-2.8114056810318,2.19738805605108));
#50689=CARTESIAN_POINT('Ctrl Pts',(-93.7871792981492,-3.21691523658229,
0.559162758014472));
#50690=CARTESIAN_POINT('Ctrl Pts',(-93.7527734492731,-3.21743785918669,
-0.000338685115544891));
#50691=CARTESIAN_POINT('Ctrl Pts',(-94.7562265507269,-3.21751559249332,
-0.000624871069029309));
#50692=CARTESIAN_POINT('Ctrl Pts',(-94.7254180631473,-3.21838016512199,
-0.501596526159939));
#50693=CARTESIAN_POINT('Ctrl Pts',(-94.6283183983351,-2.87210498626068,
-2.07938641916441));
#50694=CARTESIAN_POINT('Ctrl Pts',(-94.4649275562905,-0.40544590980093,
-3.79016559608063));
#50695=CARTESIAN_POINT('Ctrl Pts',(-94.2660540245932,2.96940847303638,-2.39005333659048));
#50696=CARTESIAN_POINT('Ctrl Pts',(-94.0671804928955,3.61596425384286,1.20604483598993));
#50697=CARTESIAN_POINT('Ctrl Pts',(-93.8683069611984,0.940164653658382,
3.69402653692401));
#50698=CARTESIAN_POINT('Ctrl Pts',(-93.6813223138085,-2.38785739210696,
2.84209660064214));
#50699=CARTESIAN_POINT('Ctrl Pts',(-93.5606288436515,-3.21650278803584,
0.877029481754939));
#50700=CARTESIAN_POINT('Ctrl Pts',(-93.5062265507269,-3.22448909586232,
-0.00275643515406668));
#50701=CARTESIAN_POINT('Origin',(-111.877773449273,0.,0.));
#50702=CARTESIAN_POINT('',(-96.2527734492731,-3.22768866803615,-0.00101868579972961));
#50703=CARTESIAN_POINT('',(-96.0062265507269,-3.22218870514462,0.00297531656463582));
#50704=CARTESIAN_POINT('',(-111.877773449273,-3.22275,5.46201577318104E-12));
#50705=CARTESIAN_POINT('Ctrl Pts',(-96.2527734492731,-3.22768866803615,
-0.00101868579972937));
#50706=CARTESIAN_POINT('Ctrl Pts',(-96.2493400916056,-3.22791730388182,
-0.0563985044060784));
#50707=CARTESIAN_POINT('Ctrl Pts',(-96.1796155567056,-3.20148940574067,
-1.18082759072959));
#50708=CARTESIAN_POINT('Ctrl Pts',(-96.0435998445732,-1.89193518361277,
-3.30912721008056));
#50709=CARTESIAN_POINT('Ctrl Pts',(-95.8447263128756,1.76112572087986,-3.38055880391732));
#50710=CARTESIAN_POINT('Ctrl Pts',(-95.6458527811783,3.79606069695695,-0.345926027506187));
#50711=CARTESIAN_POINT('Ctrl Pts',(-95.4469792494807,2.3431673103227,3.00654429325805));
#50712=CARTESIAN_POINT('Ctrl Pts',(-95.2481057177834,-1.26263301219719,
3.59659554412187));
#50713=CARTESIAN_POINT('Ctrl Pts',(-95.100037117714,-3.0835388319343,1.57554521251432));
#50714=CARTESIAN_POINT('Ctrl Pts',(-95.0182596948773,-3.22503549504625,
0.253771344504622));
#50715=CARTESIAN_POINT('Ctrl Pts',(-95.0027734492731,-3.22271743805854,
0.00297624318753967));
#50716=CARTESIAN_POINT('Ctrl Pts',(-96.0062265507269,-3.22218870514462,
0.00297531656463585));
#50717=CARTESIAN_POINT('Ctrl Pts',(-95.9564984598755,-3.21485431378588,
-0.802693432952016));
#50718=CARTESIAN_POINT('Ctrl Pts',(-95.8404791917917,-2.50060164354313,
-2.69397249512217));
#50719=CARTESIAN_POINT('Ctrl Pts',(-95.6581687464753,0.677671118481855,
-3.7510669797623));
#50720=CARTESIAN_POINT('Ctrl Pts',(-95.4592952147778,3.52204752608671,-1.45771151311705));
#50721=CARTESIAN_POINT('Ctrl Pts',(-95.2604216830804,3.13035943499951,2.17499228485918));
#50722=CARTESIAN_POINT('Ctrl Pts',(-95.0615481513829,-0.137509332446344,
3.80930870565481));
#50723=CARTESIAN_POINT('Ctrl Pts',(-94.8934831072652,-2.79236499959111,
2.23264688773096));
#50724=CARTESIAN_POINT('Ctrl Pts',(-94.7917092403798,-3.21651984863585,
0.576353200851608));
#50725=CARTESIAN_POINT('Ctrl Pts',(-94.7562265507269,-3.21751559249332,
-0.000624871069029309));
#50726=CARTESIAN_POINT('Origin',(-111.877773449273,0.,0.));
#50727=CARTESIAN_POINT('',(-97.5027734492731,-3.2196148652113,-0.00247533961895227));
#50728=CARTESIAN_POINT('',(-97.2562265507269,-3.2278883009554,-0.000708117556544874));
#50729=CARTESIAN_POINT('',(-111.877773449273,-3.22275,5.46201577318104E-12));
#50730=CARTESIAN_POINT('Ctrl Pts',(-97.5027734492731,-3.2196148652113,-0.00247533961895269));
#50731=CARTESIAN_POINT('Ctrl Pts',(-97.4804204883339,-3.22219931499525,
-0.365359803868385));
#50732=CARTESIAN_POINT('Ctrl Pts',(-97.3917763501621,-2.99785044664452,
-1.8013328317353));
#50733=CARTESIAN_POINT('Ctrl Pts',(-97.236841034758,-0.884116238679596,
-3.70784035632476));
#50734=CARTESIAN_POINT('Ctrl Pts',(-97.0379675030604,2.6413811721456,-2.74824437321759));
#50735=CARTESIAN_POINT('Ctrl Pts',(-96.8390939713629,3.73997213852792,0.736444182896666));
#50736=CARTESIAN_POINT('Ctrl Pts',(-96.6402204396655,1.4022690248486,3.54448631164484));
#50737=CARTESIAN_POINT('Ctrl Pts',(-96.4447802656356,-2.16124048025456,
3.10359245744214));
#50738=CARTESIAN_POINT('Ctrl Pts',(-96.3156312688381,-3.22350280914098,
1.01287353942035));
#50739=CARTESIAN_POINT('Ctrl Pts',(-96.2527734492731,-3.22768866803615,
-0.00101868579972937));
#50740=CARTESIAN_POINT('Ctrl Pts',(-97.2562265507269,-3.2278883009554,-0.000708117556544644));
#50741=CARTESIAN_POINT('Ctrl Pts',(-97.2538700338363,-3.22800134428475,
-0.0387122915581514));
#50742=CARTESIAN_POINT('Ctrl Pts',(-97.1852223397131,-3.21014838855854,
-1.14570314954745));
#50743=CARTESIAN_POINT('Ctrl Pts',(-97.0502834683574,-1.94541824331421,
-3.27797033087057));
#50744=CARTESIAN_POINT('Ctrl Pts',(-96.8514099366601,1.70600116119408,-3.40870967808817));
#50745=CARTESIAN_POINT('Ctrl Pts',(-96.6525364049625,3.78994319591188,-0.407519574068266));
#50746=CARTESIAN_POINT('Ctrl Pts',(-96.4536628732652,2.39167764043941,2.96810035135433));
#50747=CARTESIAN_POINT('Ctrl Pts',(-96.2547893415676,-1.20406624183485,
3.6166235796335));
#50748=CARTESIAN_POINT('Ctrl Pts',(-96.1056439007216,-3.07102873086741,
1.6109256742346));
#50749=CARTESIAN_POINT('Ctrl Pts',(-96.022789637108,-3.22463159316923,0.271321856002311));
#50750=CARTESIAN_POINT('Ctrl Pts',(-96.0062265507269,-3.22218870514462,
0.00297531656463585));
#50751=CARTESIAN_POINT('Origin',(-111.877773449273,0.,0.));
#50752=CARTESIAN_POINT('',(-98.7527734492732,-3.21869187673167,0.00200177019059543));
#50753=CARTESIAN_POINT('',(-98.5062265507269,-3.22004330425499,-0.00262713518237062));
#50754=CARTESIAN_POINT('',(-111.877773449273,-3.22275,5.46201577318104E-12));
#50755=CARTESIAN_POINT('Ctrl Pts',(-98.7527734492732,-3.21869187673167,
0.00200177019059538));
#50756=CARTESIAN_POINT('Ctrl Pts',(-98.7115008850621,-3.21490199884244,
-0.668511583215047));
#50757=CARTESIAN_POINT('Ctrl Pts',(-98.6039371436185,-2.68289385566343,
-2.42149810263904));
#50758=CARTESIAN_POINT('Ctrl Pts',(-98.4300822249426,0.195179949845956,
-3.80678951593933));
#50759=CARTESIAN_POINT('Ctrl Pts',(-98.2312086932451,3.30809157446657,-1.89374543337553));
#50760=CARTESIAN_POINT('Ctrl Pts',(-98.0323351615477,3.38152186805364,1.75927584174923));
#50761=CARTESIAN_POINT('Ctrl Pts',(-97.8334616298501,0.348002926086945,
3.795870861202));
#50762=CARTESIAN_POINT('Ctrl Pts',(-97.6569410590921,-2.62836201115969,
2.50790786839153));
#50763=CARTESIAN_POINT('Ctrl Pts',(-97.5467116655664,-3.2145347277783,0.710830433291791));
#50764=CARTESIAN_POINT('Ctrl Pts',(-97.5027734492731,-3.2196148652113,-0.00247533961895269));
#50765=CARTESIAN_POINT('Ctrl Pts',(-98.5062265507269,-3.22004330425499,
-0.00262713518237034));
#50766=CARTESIAN_POINT('Ctrl Pts',(-98.4849504305645,-3.22267740745809,
-0.347914118107918));
#50767=CARTESIAN_POINT('Ctrl Pts',(-98.3973831331696,-3.01223074102848,
-1.76590478459706));
#50768=CARTESIAN_POINT('Ctrl Pts',(-98.2435246585422,-0.94420633835697,
-3.69299553507636));
#50769=CARTESIAN_POINT('Ctrl Pts',(-98.0446511268448,2.59640786845259,-2.79077190256118));
#50770=CARTESIAN_POINT('Ctrl Pts',(-97.8457775951473,3.75143719459486,0.675618684242606));
#50771=CARTESIAN_POINT('Ctrl Pts',(-97.6469040634498,1.45963832362029,3.52124943673499));
#50772=CARTESIAN_POINT('Ctrl Pts',(-97.450387048643,-2.13023161929317,3.13616666364257));
#50773=CARTESIAN_POINT('Ctrl Pts',(-97.3201612110688,-3.22482132235888,
1.03038313666224));
#50774=CARTESIAN_POINT('Ctrl Pts',(-97.2562265507269,-3.2278883009554,-0.000708117556544644));
#50775=CARTESIAN_POINT('Origin',(-111.877773449273,0.,0.));
#50776=CARTESIAN_POINT('',(-100.002773449273,-3.22694260859439,0.00172144473337393));
#50777=CARTESIAN_POINT('',(-99.7562265507269,-3.21838185199414,0.00177605862614089));
#50778=CARTESIAN_POINT('',(-111.877773449273,-3.22275,5.46201577318104E-12));
#50779=CARTESIAN_POINT('Ctrl Pts',(-100.002773449273,-3.22694260859439,
0.001721444733374));
#50780=CARTESIAN_POINT('Ctrl Pts',(-99.9425812817904,-3.22067473021912,
-0.969768895307658));
#50781=CARTESIAN_POINT('Ctrl Pts',(-99.8160979370751,-2.23589384257021,
-3.02219500214244));
#50782=CARTESIAN_POINT('Ctrl Pts',(-99.6233234151273,1.25869662408462,-3.5979750471627));
#50783=CARTESIAN_POINT('Ctrl Pts',(-99.4244498834298,3.70735607210978,-0.886144788439325));
#50784=CARTESIAN_POINT('Ctrl Pts',(-99.2255763517325,2.74968914886796,2.63987712139888));
#50785=CARTESIAN_POINT('Ctrl Pts',(-99.0267028200349,-0.734397810215034,
3.74037451170853));
#50786=CARTESIAN_POINT('Ctrl Pts',(-98.8691018525486,-2.96069541412064,
1.88903672785569));
#50787=CARTESIAN_POINT('Ctrl Pts',(-98.7777920622946,-3.22098922583323,
0.40845371799762));
#50788=CARTESIAN_POINT('Ctrl Pts',(-98.7527734492732,-3.21869187673167,
0.00200177019059538));
#50789=CARTESIAN_POINT('Ctrl Pts',(-99.7562265507269,-3.21838185199414,
0.0017760586261405));
#50790=CARTESIAN_POINT('Ctrl Pts',(-99.7160308272927,-3.21512588995624,
-0.651400495484813));
#50791=CARTESIAN_POINT('Ctrl Pts',(-99.6095439266259,-2.70417477442122,
-2.38648362041853));
#50792=CARTESIAN_POINT('Ctrl Pts',(-99.4367658487271,0.133340853178626,
-3.80945689677165));
#50793=CARTESIAN_POINT('Ctrl Pts',(-99.2378923170293,3.2769054375692,-1.94721143811269));
#50794=CARTESIAN_POINT('Ctrl Pts',(-99.0390187853321,3.40964257754116,1.70413588804003));
#50795=CARTESIAN_POINT('Ctrl Pts',(-98.8401452536345,0.409593116342725,
3.78971966120611));
#50796=CARTESIAN_POINT('Ctrl Pts',(-98.6625478420995,-2.60557504043074,
2.5426944940956));
#50797=CARTESIAN_POINT('Ctrl Pts',(-98.551241607797,-3.21447018729988,0.72791551654661));
#50798=CARTESIAN_POINT('Ctrl Pts',(-98.5062265507269,-3.22004330425499,
-0.00262713518237034));
#50799=CARTESIAN_POINT('Origin',(-111.877773449273,0.,0.));
#50800=CARTESIAN_POINT('',(-101.252773449273,-3.22403583900848,-0.00284625812878155));
#50801=CARTESIAN_POINT('',(-101.006226550727,-3.22655659286261,0.00197058666357074));
#50802=CARTESIAN_POINT('',(-111.877773449273,-3.22275,5.46201577318104E-12));
#50803=CARTESIAN_POINT('Ctrl Pts',(-101.252773449273,-3.22403583900848,
-0.00284625812878147));
#50804=CARTESIAN_POINT('Ctrl Pts',(-101.239952855751,-3.22594794128741,
-0.210254204409943));
#50805=CARTESIAN_POINT('Ctrl Pts',(-101.160841084997,-3.11307044583999,
-1.48802917026718));
#50806=CARTESIAN_POINT('Ctrl Pts',(-101.015438137009,-1.40614679609923,
-3.54294973423381));
#50807=CARTESIAN_POINT('Ctrl Pts',(-100.816564605312,2.22045273645088,-3.09827876032406));
#50808=CARTESIAN_POINT('Ctrl Pts',(-100.617691073615,3.80689573555524,0.193097100182191));
#50809=CARTESIAN_POINT('Ctrl Pts',(-100.418817541917,1.89555511623687,3.30705494856008));
#50810=CARTESIAN_POINT('Ctrl Pts',(-100.21994401022,-1.75742543597124,3.38248391991576));
#50811=CARTESIAN_POINT('Ctrl Pts',(-100.081262646005,-3.17877047756002,
1.26788401495614));
#50812=CARTESIAN_POINT('Ctrl Pts',(-100.008872459023,-3.22757770536726,
0.100158322875876));
#50813=CARTESIAN_POINT('Ctrl Pts',(-100.002773449273,-3.22694260859439,
0.001721444733374));
#50814=CARTESIAN_POINT('Ctrl Pts',(-101.006226550727,-3.22655659286261,
0.00197058666357072));
#50815=CARTESIAN_POINT('Ctrl Pts',(-100.947111224021,-3.21970155042776,
-0.952440118260013));
#50816=CARTESIAN_POINT('Ctrl Pts',(-100.821704720082,-2.26520642155357,
-2.98902372995717));
#50817=CARTESIAN_POINT('Ctrl Pts',(-100.630007038912,1.20010797278872,-3.61793898305879));
#50818=CARTESIAN_POINT('Ctrl Pts',(-100.431133507214,3.69247837580237,-0.946226757029911));
#50819=CARTESIAN_POINT('Ctrl Pts',(-100.232259975517,2.79219206546425,2.59488055621948));
#50820=CARTESIAN_POINT('Ctrl Pts',(-100.033386443819,-0.673566047753791,
3.75180628641736));
#50821=CARTESIAN_POINT('Ctrl Pts',(-99.8747086355561,-2.94504656405884,
1.92446147751931));
#50822=CARTESIAN_POINT('Ctrl Pts',(-99.7823220045252,-3.22049565415193,
0.425824617370613));
#50823=CARTESIAN_POINT('Ctrl Pts',(-99.7562265507269,-3.21838185199414,
0.0017760586261405));
#50824=CARTESIAN_POINT('Origin',(-111.877773449273,0.,0.));
#50825=CARTESIAN_POINT('',(-102.502773449273,-3.21744563600034,-0.000377495323892581));
#50826=CARTESIAN_POINT('',(-102.256226550727,-3.22455892594853,-0.00274040190877844));
#50827=CARTESIAN_POINT('',(-111.877773449273,-3.22275,5.46201577318104E-12));
#50828=CARTESIAN_POINT('Ctrl Pts',(-102.502773449273,-3.21744563600034,
-0.000377495323892994));
#50829=CARTESIAN_POINT('Ctrl Pts',(-102.471033252479,-3.21798308710835,
-0.516527495821932));
#50830=CARTESIAN_POINT('Ctrl Pts',(-102.373001878453,-2.85680880773506,
-2.10997563087918));
#50831=CARTESIAN_POINT('Ctrl Pts',(-102.208679327194,-0.352156410097993,
-3.79548778081539));
#50832=CARTESIAN_POINT('Ctrl Pts',(-102.009805795497,3.00269417169098,-2.34809909134587));
#50833=CARTESIAN_POINT('Ctrl Pts',(-101.810932263799,3.59866318318054,1.25672786453859));
#50834=CARTESIAN_POINT('Ctrl Pts',(-101.612058732102,0.888173072927529,
3.70687067808071));
#50835=CARTESIAN_POINT('Ctrl Pts',(-101.426005793926,-2.41102978727076,
2.81274573972963));
#50836=CARTESIAN_POINT('Ctrl Pts',(-101.306244032984,-3.21606107365988,
0.862185765134263));
#50837=CARTESIAN_POINT('Ctrl Pts',(-101.252773449273,-3.22403583900848,
-0.00284625812878147));
#50838=CARTESIAN_POINT('Ctrl Pts',(-102.256226550727,-3.22455892594853,
-0.0027404019087786));
#50839=CARTESIAN_POINT('Ctrl Pts',(-102.244482797982,-3.22627739521217,
-0.192648026627219));
#50840=CARTESIAN_POINT('Ctrl Pts',(-102.166447868004,-3.1244295976162,-1.45270581183642));
#50841=CARTESIAN_POINT('Ctrl Pts',(-102.022121760794,-1.46349063320167,
-3.51965009596396));
#50842=CARTESIAN_POINT('Ctrl Pts',(-101.823248229096,2.16985118744687,-3.13392524732525));
#50843=CARTESIAN_POINT('Ctrl Pts',(-101.624374697399,3.80952928177325,0.131256553358462));
#50844=CARTESIAN_POINT('Ctrl Pts',(-101.425501165701,1.94900405000445,3.27583956331103));
#50845=CARTESIAN_POINT('Ctrl Pts',(-101.226627634004,-1.70227010474501,
3.41057445630188));
#50846=CARTESIAN_POINT('Ctrl Pts',(-101.086869429013,-3.16906561629859,
1.30309446990841));
#50847=CARTESIAN_POINT('Ctrl Pts',(-101.013402401253,-3.22738870802812,
0.117823935382279));
#50848=CARTESIAN_POINT('Ctrl Pts',(-101.006226550727,-3.22655659286261,
0.00197058666357072));
#50849=CARTESIAN_POINT('Origin',(-111.877773449273,0.,0.));
#50850=CARTESIAN_POINT('',(-103.752773449273,-3.22264579720397,0.00297789965849656));
#50851=CARTESIAN_POINT('',(-103.506226550727,-3.21752959531867,-0.000663060806946891));
#50852=CARTESIAN_POINT('',(-111.877773449273,-3.22275,5.46201577318104E-12));
#50853=CARTESIAN_POINT('Ctrl Pts',(-103.752773449273,-3.22264579720397,
0.00297789965849664));
#50854=CARTESIAN_POINT('Ctrl Pts',(-103.702113649208,-3.21507385712874,
-0.817488959989247));
#50855=CARTESIAN_POINT('Ctrl Pts',(-103.58516267191,-2.47882325582672,-2.72366489883768));
#50856=CARTESIAN_POINT('Ctrl Pts',(-103.401920517379,0.730304405924223,
-3.74117589888118));
#50857=CARTESIAN_POINT('Ctrl Pts',(-103.203046985682,3.5421798545178,-1.40808505059571));
#50858=CARTESIAN_POINT('Ctrl Pts',(-103.004173453984,3.09949317971213,2.2187572333099));
#50859=CARTESIAN_POINT('Ctrl Pts',(-102.805299922287,-0.191014192713332,
3.80700081556329));
#50860=CARTESIAN_POINT('Ctrl Pts',(-102.638166587383,-2.8088631270226,2.20214204929746));
#50861=CARTESIAN_POINT('Ctrl Pts',(-102.537324429712,-3.21686059039271,
0.561480664739076));
#50862=CARTESIAN_POINT('Ctrl Pts',(-102.502773449273,-3.21744563600034,
-0.000377495323892994));
#50863=CARTESIAN_POINT('Ctrl Pts',(-103.506226550727,-3.21752959531867,
-0.000663060806946926));
#50864=CARTESIAN_POINT('Ctrl Pts',(-103.47556319471,-3.21844290636372,-0.499269344977216));
#50865=CARTESIAN_POINT('Ctrl Pts',(-103.37860866146,-2.87446123529701,-2.0746201369058));
#50866=CARTESIAN_POINT('Ctrl Pts',(-103.215362950979,-0.413739832431433,
-3.78926918845535));
#50867=CARTESIAN_POINT('Ctrl Pts',(-103.016489419281,2.96417065678915,-2.39654625428174));
#50868=CARTESIAN_POINT('Ctrl Pts',(-102.817615887584,3.61859506029929,1.19812829908153));
#50869=CARTESIAN_POINT('Ctrl Pts',(-102.618742355886,0.948246892445682,
3.69196011116847));
#50870=CARTESIAN_POINT('Ctrl Pts',(-102.431612576934,-2.38421620433085,
2.84666010714341));
#50871=CARTESIAN_POINT('Ctrl Pts',(-102.310773975214,-3.21657697380546,
0.879343208300523));
#50872=CARTESIAN_POINT('Ctrl Pts',(-102.256226550727,-3.22455892594853,
-0.0027404019087786));
#50873=CARTESIAN_POINT('Origin',(-111.877773449273,0.,0.));
#50874=CARTESIAN_POINT('',(-105.002773449273,-3.22771932735903,-0.000977548123388087));
#50875=CARTESIAN_POINT('',(-104.756226550727,-3.22211806513786,0.00297286732293386));
#50876=CARTESIAN_POINT('',(-111.877773449273,-3.22275,5.46201577318104E-12));
#50877=CARTESIAN_POINT('Ctrl Pts',(-105.002773449273,-3.22771932735903,
-0.000977548123388232));
#50878=CARTESIAN_POINT('Ctrl Pts',(-104.999485223168,-3.22793043470303,
-0.0540150617505775));
#50879=CARTESIAN_POINT('Ctrl Pts',(-104.929905819831,-3.20267366849749,
-1.17609219946835));
#50880=CARTESIAN_POINT('Ctrl Pts',(-104.794035239261,-1.89917277873868,
-3.30497872482143));
#50881=CARTESIAN_POINT('Ctrl Pts',(-104.595161707564,1.75372304650391,-3.38440498687836));
#50882=CARTESIAN_POINT('Ctrl Pts',(-104.396288175866,3.79529453639531,-0.354232993642497));
#50883=CARTESIAN_POINT('Ctrl Pts',(-104.197414644169,2.34974161312935,3.00140899924184));
#50884=CARTESIAN_POINT('Ctrl Pts',(-103.998541112471,-1.25475872875807,
3.59935024210211));
#50885=CARTESIAN_POINT('Ctrl Pts',(-103.850327380839,-3.08187243645139,
1.58031280791233));
#50886=CARTESIAN_POINT('Ctrl Pts',(-103.76840482644,-3.22498216353482,0.256137740784716));
#50887=CARTESIAN_POINT('Ctrl Pts',(-103.752773449273,-3.22264579720397,
0.00297789965849664));
#50888=CARTESIAN_POINT('Ctrl Pts',(-104.756226550727,-3.22211806513786,
0.00297286732293373));
#50889=CARTESIAN_POINT('Ctrl Pts',(-104.706643591438,-3.21482468722874,
-0.800389402427977));
#50890=CARTESIAN_POINT('Ctrl Pts',(-104.590769454917,-2.50396322193643,
-2.68934045447677));
#50891=CARTESIAN_POINT('Ctrl Pts',(-104.408604141163,0.66946017042967,-3.75254110076405));
#50892=CARTESIAN_POINT('Ctrl Pts',(-104.209730609466,3.51884884505274,-1.46541613103467));
#50893=CARTESIAN_POINT('Ctrl Pts',(-104.010857077768,3.1351119755824,2.16813618846657));
#50894=CARTESIAN_POINT('Ctrl Pts',(-103.811983546071,-0.129172214237829,
3.80960052640045));
#50895=CARTESIAN_POINT('Ctrl Pts',(-103.64377337039,-2.78976765512291,2.23739622108886));
#50896=CARTESIAN_POINT('Ctrl Pts',(-103.541854371942,-3.21646841719422,
0.57866868420927));
#50897=CARTESIAN_POINT('Ctrl Pts',(-103.506226550727,-3.21752959531867,
-0.000663060806946926));
#50898=CARTESIAN_POINT('Origin',(-111.877773449273,0.,0.));
#50899=CARTESIAN_POINT('',(-106.252773449273,-3.21967089505607,-0.00249719049460675));
#50900=CARTESIAN_POINT('',(-106.006226550727,-3.22791011323673,-0.000665423688525069));
#50901=CARTESIAN_POINT('',(-111.877773449273,-3.22275,5.46201577318104E-12));
#50902=CARTESIAN_POINT('Ctrl Pts',(-106.252773449273,-3.21967089505607,
-0.00249719049460629));
#50903=CARTESIAN_POINT('Ctrl Pts',(-106.230565619897,-3.22226422533865,
-0.36300978920333));
#50904=CARTESIAN_POINT('Ctrl Pts',(-106.142066613287,-2.99980948769902,
-1.79655795925824));
#50905=CARTESIAN_POINT('Ctrl Pts',(-105.987276429446,-0.89222882781209,
-3.70589645739097));
#50906=CARTESIAN_POINT('Ctrl Pts',(-105.788402897748,2.63536022101092,-2.75401859025452));
#50907=CARTESIAN_POINT('Ctrl Pts',(-105.589529366051,3.74157491702501,0.728257404654141));
#50908=CARTESIAN_POINT('Ctrl Pts',(-105.390655834353,1.41002288124958,3.54140889901514));
#50909=CARTESIAN_POINT('Ctrl Pts',(-105.195070528761,-2.15708992623015,
3.10799336322487));
#50910=CARTESIAN_POINT('Ctrl Pts',(-105.065776400401,-3.22367447604636,
1.01522990611466));
#50911=CARTESIAN_POINT('Ctrl Pts',(-105.002773449273,-3.22771932735903,
-0.000977548123388232));
#50912=CARTESIAN_POINT('Ctrl Pts',(-106.006226550727,-3.22791011323674,
-0.000665423688524592));
#50913=CARTESIAN_POINT('Ctrl Pts',(-106.004015165399,-3.22801029914443,
-0.0363283773460198));
#50914=CARTESIAN_POINT('Ctrl Pts',(-105.935512602838,-3.21129287176671,
-1.14097121261763));
#50915=CARTESIAN_POINT('Ctrl Pts',(-105.800718863045,-1.95258751815794,
-3.27370485835312));
#50916=CARTESIAN_POINT('Ctrl Pts',(-105.601845331348,1.69853700744364,-3.41243515849443));
#50917=CARTESIAN_POINT('Ctrl Pts',(-105.402971799651,3.78904225187362,-0.415813000837348));
#50918=CARTESIAN_POINT('Ctrl Pts',(-105.204098267953,2.39816769067077,2.96285898119487));
#50919=CARTESIAN_POINT('Ctrl Pts',(-105.005224736256,-1.19614826633649,
3.61925005546539));
#50920=CARTESIAN_POINT('Ctrl Pts',(-104.855934163847,-3.0693168009762,1.61569511776405));
#50921=CARTESIAN_POINT('Ctrl Pts',(-104.772934768671,-3.22457575119371,
0.273685872019571));
#50922=CARTESIAN_POINT('Ctrl Pts',(-104.756226550727,-3.22211806513786,
0.00297286732293373));
#50923=CARTESIAN_POINT('Origin',(-111.877773449273,0.,0.));
#50924=CARTESIAN_POINT('',(-107.502773449273,-3.21864717840401,0.00197683862682141));
#50925=CARTESIAN_POINT('',(-107.256226550727,-3.22010315981886,-0.00264555290059448));
#50926=CARTESIAN_POINT('',(-111.877773449273,-3.22275,5.46201577318104E-12));
#50927=CARTESIAN_POINT('Ctrl Pts',(-107.502773449273,-3.21864717840401,
0.00197683862682117));
#50928=CARTESIAN_POINT('Ctrl Pts',(-107.461646016625,-3.21492939379356,
-0.66620337802367));
#50929=CARTESIAN_POINT('Ctrl Pts',(-107.354227406744,-2.68578800952235,
-2.41678954596452));
#50930=CARTESIAN_POINT('Ctrl Pts',(-107.180517619631,0.186848925119125,
-3.80720285370364));
#50931=CARTESIAN_POINT('Ctrl Pts',(-106.981644087933,3.3039387517963,-1.90098324867159));
#50932=CARTESIAN_POINT('Ctrl Pts',(-106.782770556236,3.3853642004366,1.75187238336515));
#50933=CARTESIAN_POINT('Ctrl Pts',(-106.583897024538,0.356309365737235,
3.79509945705497));
#50934=CARTESIAN_POINT('Ctrl Pts',(-106.407231322217,-2.62531646247706,
2.51260078542008));
#50935=CARTESIAN_POINT('Ctrl Pts',(-106.296856797129,-3.21452304026067,
0.713133411027618));
#50936=CARTESIAN_POINT('Ctrl Pts',(-106.252773449273,-3.21967089505607,
-0.00249719049460629));
#50937=CARTESIAN_POINT('Ctrl Pts',(-107.256226550727,-3.22010315981886,
-0.00264555290059414));
#50938=CARTESIAN_POINT('Ctrl Pts',(-107.235095562127,-3.22274118326769,
-0.345561327371345));
#50939=CARTESIAN_POINT('Ctrl Pts',(-107.147673396295,-3.01414178771879,
-1.76113107576296));
#50940=CARTESIAN_POINT('Ctrl Pts',(-106.99396005323,-0.952286095205662,
-3.69091959353343));
#50941=CARTESIAN_POINT('Ctrl Pts',(-106.795086521533,2.59029384628224,-2.79644789371376));
#50942=CARTESIAN_POINT('Ctrl Pts',(-106.596212989835,3.75290688327137,0.667407119671472));
#50943=CARTESIAN_POINT('Ctrl Pts',(-106.397339458138,1.46734115830479,3.5180464407433));
#50944=CARTESIAN_POINT('Ctrl Pts',(-106.200677311768,-2.12601470786238,
3.14054269339691));
#50945=CARTESIAN_POINT('Ctrl Pts',(-106.070306342631,-3.22500700447711,
1.03274771338295));
#50946=CARTESIAN_POINT('Ctrl Pts',(-106.006226550727,-3.22791011323674,
-0.000665423688524592));
#50947=CARTESIAN_POINT('Origin',(-111.877773449273,0.,0.));
#50948=CARTESIAN_POINT('',(-108.752773449273,-3.22685723674299,0.00199079345700962));
#50949=CARTESIAN_POINT('',(-108.506226550727,-3.21833411702487,0.00177219254916039));
#50950=CARTESIAN_POINT('',(-111.877773449273,-3.22275,5.46201577318104E-12));
#50951=CARTESIAN_POINT('Ctrl Pts',(-108.752773449273,-3.22685723674299,
0.00199079345700971));
#50952=CARTESIAN_POINT('Ctrl Pts',(-108.692726413353,-3.22049187575973,
-0.967128193374095));
#50953=CARTESIAN_POINT('Ctrl Pts',(-108.5663882002,-2.23993119932473,-3.01811690972611));
#50954=CARTESIAN_POINT('Ctrl Pts',(-108.373758809815,1.25085188316156,-3.60050797555933));
#50955=CARTESIAN_POINT('Ctrl Pts',(-108.174885278118,3.70539059895966,-0.894369208581839));
#50956=CARTESIAN_POINT('Ctrl Pts',(-107.97601174642,2.7554691459713,2.63391280124896));
#50957=CARTESIAN_POINT('Ctrl Pts',(-107.777138214723,-0.726214962520435,
3.74194114611939));
#50958=CARTESIAN_POINT('Ctrl Pts',(-107.619392115674,-2.95860695660328,
1.89381816019148));
#50959=CARTESIAN_POINT('Ctrl Pts',(-107.527937193857,-3.22092189813076,
0.410801684361577));
#50960=CARTESIAN_POINT('Ctrl Pts',(-107.502773449273,-3.21864717840401,
0.00197683862682117));
#50961=CARTESIAN_POINT('Ctrl Pts',(-108.506226550727,-3.21833411702487,
0.00177219254916029));
#50962=CARTESIAN_POINT('Ctrl Pts',(-108.466175958855,-3.2151539473228,-0.649077442870454));
#50963=CARTESIAN_POINT('Ctrl Pts',(-108.359834189751,-2.70702507792134,
-2.38180619169885));
#50964=CARTESIAN_POINT('Ctrl Pts',(-108.187201243415,0.125013204392657,
-3.80970909802013));
#50965=CARTESIAN_POINT('Ctrl Pts',(-107.988327711718,3.27263087647587,-1.95439453380991));
#50966=CARTESIAN_POINT('Ctrl Pts',(-107.78945418002,3.41336670979149,1.69667825319885));
#50967=CARTESIAN_POINT('Ctrl Pts',(-107.590580648323,0.417884599785739,
3.78880964833669));
#50968=CARTESIAN_POINT('Ctrl Pts',(-107.412838105225,-2.60246970424512,
2.54737878177037));
#50969=CARTESIAN_POINT('Ctrl Pts',(-107.30138673936,-3.21446529597712,0.730218458034701));
#50970=CARTESIAN_POINT('Ctrl Pts',(-107.256226550727,-3.22010315981886,
-0.00264555290059414));
#50971=CARTESIAN_POINT('Ctrl Pts',(-109.977063028692,-1.43290239521125,
2.88667772504966));
#50972=CARTESIAN_POINT('Ctrl Pts',(-109.910771851459,-2.39478902451357,
2.4092120062101));
#50973=CARTESIAN_POINT('Ctrl Pts',(-109.778189496994,-3.78690710807203,
0.425397354299135));
#50974=CARTESIAN_POINT('Ctrl Pts',(-109.579315965297,-2.40225732364717,
-2.962905510084));
#50975=CARTESIAN_POINT('Ctrl Pts',(-109.3804424336,1.19263195710595,-3.61916700220439));
#50976=CARTESIAN_POINT('Ctrl Pts',(-109.181568901902,3.6901636846244,-0.955038498682453));
#50977=CARTESIAN_POINT('Ctrl Pts',(-108.982695370205,2.7979887412231,2.58915131051891));
#50978=CARTESIAN_POINT('Ctrl Pts',(-108.783821838507,-0.665419358724505,
3.75306610556087));
#50979=CARTESIAN_POINT('Ctrl Pts',(-108.58494830681,-3.51720830079989,1.4693745407153));
#50980=CARTESIAN_POINT('Ctrl Pts',(-108.386074775112,-3.13750109000173,
-2.16476182736599));
#50981=CARTESIAN_POINT('Ctrl Pts',(-108.187201243415,0.125013204392657,
-3.80970909802013));
#50982=CARTESIAN_POINT('Ctrl Pts',(-107.988327711718,3.27263087647587,-1.95439453380991));
#50983=CARTESIAN_POINT('Ctrl Pts',(-107.78945418002,3.41336670979149,1.69667825319885));
#50984=CARTESIAN_POINT('Ctrl Pts',(-107.590580648323,0.417884599785739,
3.78880964833669));
#50985=CARTESIAN_POINT('Ctrl Pts',(-107.391707116625,-2.96154565338688,
2.39979080968668));
#50986=CARTESIAN_POINT('Ctrl Pts',(-107.192833584928,-3.61990437248132,
-1.19416914684889));
#50987=CARTESIAN_POINT('Ctrl Pts',(-106.99396005323,-0.952286095205662,
-3.69091959353343));
#50988=CARTESIAN_POINT('Ctrl Pts',(-106.795086521533,2.59029384628224,-2.79644789371376));
#50989=CARTESIAN_POINT('Ctrl Pts',(-106.596212989835,3.75290688327137,0.667407119671472));
#50990=CARTESIAN_POINT('Ctrl Pts',(-106.397339458138,1.46734115830479,3.5180464407433));
#50991=CARTESIAN_POINT('Ctrl Pts',(-106.19846592644,-2.16642052355891,3.13629781829738));
#50992=CARTESIAN_POINT('Ctrl Pts',(-105.999592394743,-3.80967063954889,
-0.127087864501012));
#50993=CARTESIAN_POINT('Ctrl Pts',(-105.800718863045,-1.95258751815794,
-3.27370485835312));
#50994=CARTESIAN_POINT('Ctrl Pts',(-105.601845331348,1.69853700744364,-3.41243515849443));
#50995=CARTESIAN_POINT('Ctrl Pts',(-105.402971799651,3.78904225187362,-0.415813000837348));
#50996=CARTESIAN_POINT('Ctrl Pts',(-105.204098267953,2.39816769067077,2.96285898119487));
#50997=CARTESIAN_POINT('Ctrl Pts',(-105.005224736256,-1.19614826633649,
3.61925005546539));
#50998=CARTESIAN_POINT('Ctrl Pts',(-104.806351204558,-3.69144074152657,
0.950266743380403));
#50999=CARTESIAN_POINT('Ctrl Pts',(-104.607477672861,-2.79502988317361,
-2.59182360151461));
#51000=CARTESIAN_POINT('Ctrl Pts',(-104.408604141163,0.66946017042967,-3.75254110076405));
#51001=CARTESIAN_POINT('Ctrl Pts',(-104.209730609466,3.51884884505274,-1.46541613103467));
#51002=CARTESIAN_POINT('Ctrl Pts',(-104.010857077768,3.1351119755824,2.16813618846657));
#51003=CARTESIAN_POINT('Ctrl Pts',(-103.811983546071,-0.129172214237829,
3.80960052640045));
#51004=CARTESIAN_POINT('Ctrl Pts',(-103.613110014373,-3.27477270841952,
1.95079607843917));
#51005=CARTESIAN_POINT('Ctrl Pts',(-103.414236482676,-3.41150531408905,
-1.70040381186034));
#51006=CARTESIAN_POINT('Ctrl Pts',(-103.215362950979,-0.413739832431433,
-3.78926918845535));
#51007=CARTESIAN_POINT('Ctrl Pts',(-103.016489419281,2.96417065678915,-2.39654625428174));
#51008=CARTESIAN_POINT('Ctrl Pts',(-102.817615887584,3.61859506029929,1.19812829908153));
#51009=CARTESIAN_POINT('Ctrl Pts',(-102.618742355886,0.948246892445682,
3.69196011116847));
#51010=CARTESIAN_POINT('Ctrl Pts',(-102.419868824189,-2.59335246719697,
2.79361139251142));
#51011=CARTESIAN_POINT('Ctrl Pts',(-102.220995292491,-3.75217425511925,
-0.671513209629694));
#51012=CARTESIAN_POINT('Ctrl Pts',(-102.022121760794,-1.46349063320167,
-3.51965009596396));
#51013=CARTESIAN_POINT('Ctrl Pts',(-101.823248229096,2.16985118744687,-3.13392524732525));
#51014=CARTESIAN_POINT('Ctrl Pts',(-101.624374697399,3.80952928177325,0.131256553358462));
#51015=CARTESIAN_POINT('Ctrl Pts',(-101.425501165701,1.94900405000445,3.27583956331103));
#51016=CARTESIAN_POINT('Ctrl Pts',(-101.226627634004,-1.70227010474501,
3.41057445630188));
#51017=CARTESIAN_POINT('Ctrl Pts',(-101.027754102307,-3.78949499203023,
0.411666536003608));
#51018=CARTESIAN_POINT('Ctrl Pts',(-100.828880570609,-2.39492409977199,
-2.96548144283838));
#51019=CARTESIAN_POINT('Ctrl Pts',(-100.630007038912,1.20010797278872,-3.61793898305879));
#51020=CARTESIAN_POINT('Ctrl Pts',(-100.431133507214,3.69247837580237,-0.946226757029911));
#51021=CARTESIAN_POINT('Ctrl Pts',(-100.232259975517,2.79219206546425,2.59488055621948));
#51022=CARTESIAN_POINT('Ctrl Pts',(-100.033386443819,-0.673566047753791,
3.75180628641736));
#51023=CARTESIAN_POINT('Ctrl Pts',(-99.834512912122,-3.52045029328096,1.46156469717404));
#51024=CARTESIAN_POINT('Ctrl Pts',(-99.6356393804242,-3.13273758089758,
-2.17156553682348));
#51025=CARTESIAN_POINT('Ctrl Pts',(-99.4367658487271,0.133340853178626,
-3.80945689677165));
#51026=CARTESIAN_POINT('Ctrl Pts',(-99.2378923170293,3.2769054375692,-1.94721143811269));
#51027=CARTESIAN_POINT('Ctrl Pts',(-99.0390187853321,3.40964257754116,1.70413588804003));
#51028=CARTESIAN_POINT('Ctrl Pts',(-98.8401452536345,0.409593116342725,
3.78971966120611));
#51029=CARTESIAN_POINT('Ctrl Pts',(-98.6412717219371,-2.9667913411577,2.39330122832859));
#51030=CARTESIAN_POINT('Ctrl Pts',(-98.4423981902396,-3.61728182277116,
-1.20208728723698));
#51031=CARTESIAN_POINT('Ctrl Pts',(-98.2435246585422,-0.94420633835697,
-3.69299553507636));
#51032=CARTESIAN_POINT('Ctrl Pts',(-98.0446511268448,2.59640786845259,-2.79077190256118));
#51033=CARTESIAN_POINT('Ctrl Pts',(-97.8457775951473,3.75143719459486,0.675618684242606));
#51034=CARTESIAN_POINT('Ctrl Pts',(-97.6469040634498,1.45963832362029,3.52124943673499));
#51035=CARTESIAN_POINT('Ctrl Pts',(-97.4480305317524,-2.17327923613194,
3.13154897667037));
#51036=CARTESIAN_POINT('Ctrl Pts',(-97.249157000055,-3.80938337139148,-0.135425113082561));
#51037=CARTESIAN_POINT('Ctrl Pts',(-97.0502834683574,-1.94541824331421,
-3.27797033087057));
#51038=CARTESIAN_POINT('Ctrl Pts',(-96.8514099366601,1.70600116119408,-3.40870967808817));
#51039=CARTESIAN_POINT('Ctrl Pts',(-96.6525364049625,3.78994319591188,-0.407519574068266));
#51040=CARTESIAN_POINT('Ctrl Pts',(-96.4536628732652,2.39167764043941,2.96810035135433));
#51041=CARTESIAN_POINT('Ctrl Pts',(-96.2547893415676,-1.20406624183485,
3.6166235796335));
#51042=CARTESIAN_POINT('Ctrl Pts',(-96.0559158098702,-3.69351158883507,
0.94218563703149));
#51043=CARTESIAN_POINT('Ctrl Pts',(-95.8570422781728,-2.78935090422765,
-2.59793440343899));
#51044=CARTESIAN_POINT('Ctrl Pts',(-95.6581687464753,0.677671118481855,
-3.7510669797623));
#51045=CARTESIAN_POINT('Ctrl Pts',(-95.4592952147778,3.52204752608671,-1.45771151311705));
#51046=CARTESIAN_POINT('Ctrl Pts',(-95.2604216830804,3.13035943499951,2.17499228485918));
#51047=CARTESIAN_POINT('Ctrl Pts',(-95.0615481513829,-0.137509332446344,
3.80930870565481));
#51048=CARTESIAN_POINT('Ctrl Pts',(-94.8626746196855,-3.27903424289638,
1.94362446614579));
#51049=CARTESIAN_POINT('Ctrl Pts',(-94.663801087988,-3.40777575822217,-1.70786592364882));
#51050=CARTESIAN_POINT('Ctrl Pts',(-94.4649275562905,-0.40544590980093,
-3.79016559608063));
#51051=CARTESIAN_POINT('Ctrl Pts',(-94.2660540245932,2.96940847303638,-2.39005333659048));
#51052=CARTESIAN_POINT('Ctrl Pts',(-94.0671804928955,3.61596425384286,1.20604483598993));
#51053=CARTESIAN_POINT('Ctrl Pts',(-93.8683069611984,0.940164653658382,
3.69402653692401));
#51054=CARTESIAN_POINT('Ctrl Pts',(-93.6694334295006,-2.59946016072173,
2.78792907088901));
#51055=CARTESIAN_POINT('Ctrl Pts',(-93.4705598978035,-3.75069564203049,
-0.679723349857117));
#51056=CARTESIAN_POINT('Ctrl Pts',(-93.2716863661057,-1.45578426624114,
-3.52284456109722));
#51057=CARTESIAN_POINT('Ctrl Pts',(-93.0728128344086,2.17670468249244,-3.12916895624107));
#51058=CARTESIAN_POINT('Ctrl Pts',(-92.8739393027108,3.80923289958397,0.139593510646091));
#51059=CARTESIAN_POINT('Ctrl Pts',(-92.6750657710136,1.94183010714438,3.28009717332813));
#51060=CARTESIAN_POINT('Ctrl Pts',(-92.476192239316,-1.70973017484599,3.40684081822274));
#51061=CARTESIAN_POINT('Ctrl Pts',(-92.2773187076186,-3.79038686164578,
0.403372124161483));
#51062=CARTESIAN_POINT('Ctrl Pts',(-92.0784451759211,-2.38842831726804,
-2.97071570581227));
#51063=CARTESIAN_POINT('Ctrl Pts',(-91.8795716442237,1.2080230691099,-3.61530384559662));
#51064=CARTESIAN_POINT('Ctrl Pts',(-91.6806981125261,3.69454037918903,-0.938143388842634));
#51065=CARTESIAN_POINT('Ctrl Pts',(-91.4818245808289,2.78650640297092,2.60098513984405));
#51066=CARTESIAN_POINT('Ctrl Pts',(-91.2829510491313,-0.681775377754059,
3.75032318151061));
#51067=CARTESIAN_POINT('Ctrl Pts',(-91.0840775174338,-3.52364054152792,
1.45385658356948));
#51068=CARTESIAN_POINT('Ctrl Pts',(-90.8852039857365,-3.12797754075145,
-2.17841642851909));
#51069=CARTESIAN_POINT('Ctrl Pts',(-90.6863304540388,0.141677647057878,
-3.80915595320164));
#51070=CARTESIAN_POINT('Ctrl Pts',(-90.4874569223416,3.28115912184763,-1.94003516684714));
#51071=CARTESIAN_POINT('Ctrl Pts',(-90.288583390644,3.40590485836977,1.71159391422753));
#51072=CARTESIAN_POINT('Ctrl Pts',(-90.0897098589466,0.401298217770733,
3.79060699254111));
#51073=CARTESIAN_POINT('Ctrl Pts',(-89.8908363272491,-2.97202204929068,
2.38680258295854));
#51074=CARTESIAN_POINT('Ctrl Pts',(-89.6919627955516,-3.61464235509244,
-1.21000094060259));
#51075=CARTESIAN_POINT('Ctrl Pts',(-89.4930892638543,-0.936121843189332,
-3.69505311547631));
#51076=CARTESIAN_POINT('Ctrl Pts',(-89.2942157321568,2.60250934034945,-2.78508290089926));
#51077=CARTESIAN_POINT('Ctrl Pts',(-89.0953422004592,3.74994959831413,0.683827201558385));
#51078=CARTESIAN_POINT('Ctrl Pts',(-88.896468668762,1.45192846567913,3.52443546714054));
#51079=CARTESIAN_POINT('Ctrl Pts',(-88.6975951370643,-2.18012752242672,
3.12678518888728));
#51080=CARTESIAN_POINT('Ctrl Pts',(-88.498721605367,-3.80907786653088,-0.143761741057804));
#51081=CARTESIAN_POINT('Ctrl Pts',(-88.2998480736696,-1.93823964579142,
-3.28222008813697));
#51082=CARTESIAN_POINT('Ctrl Pts',(-88.1009745419719,1.71345714123552,-3.40496787894343));
#51083=CARTESIAN_POINT('Ctrl Pts',(-87.9021010102748,3.79082598870071,-0.399224191249501));
#51084=CARTESIAN_POINT('Ctrl Pts',(-87.703227478577,2.38517613414864,2.97332750308055));
#51085=CARTESIAN_POINT('Ctrl Pts',(-87.5043539468798,-1.2119784498759,3.61397978252837));
#51086=CARTESIAN_POINT('Ctrl Pts',(-87.3054804151821,-3.69556474563236,
0.934100017303625));
#51087=CARTESIAN_POINT('Ctrl Pts',(-87.1066068834849,-2.78365856510014,
-2.60403276178164));
#51088=CARTESIAN_POINT('Ctrl Pts',(-86.9077333517873,0.685878820655876,
-3.74957489255291));
#51089=CARTESIAN_POINT('Ctrl Pts',(-86.70885982009,3.52522933769711,-1.44999991314728));
#51090=CARTESIAN_POINT('Ctrl Pts',(-86.5099862883923,3.12559190100552,2.1818379637031));
#51091=CARTESIAN_POINT('Ctrl Pts',(-86.311112756695,-0.145845792021992,
3.80899863959504));
#51092=CARTESIAN_POINT('Ctrl Pts',(-86.1122392249976,-3.28328007187856,
1.93644354451469));
#51093=CARTESIAN_POINT('Ctrl Pts',(-85.9133656932999,-3.40402988022421,
-1.71531985531219));
#51094=CARTESIAN_POINT('Ctrl Pts',(-85.7144921616027,-0.397150045218662,
-3.79104385005903));
#51095=CARTESIAN_POINT('Ctrl Pts',(-85.5156186299052,2.97463206679106,-2.38354897132526));
#51096=CARTESIAN_POINT('Ctrl Pts',(-85.3167450982077,3.61331612810275,1.21395559633781));
#51097=CARTESIAN_POINT('Ctrl Pts',(-85.1178715665104,0.932077911790798,
3.69607526950402));
#51098=CARTESIAN_POINT('Ctrl Pts',(-84.9189980348126,-2.60555540368459,
2.78223339599998));
#51099=CARTESIAN_POINT('Ctrl Pts',(-84.7201245031155,-3.74919906433912,
-0.687930234432375));
#51100=CARTESIAN_POINT('Ctrl Pts',(-84.5212509714179,-1.44807092655128,
-3.52602215295995));
#51101=CARTESIAN_POINT('Ctrl Pts',(-84.3223774397204,2.18354775183615,-3.1243976774634));
#51102=CARTESIAN_POINT('Ctrl Pts',(-84.123503908023,3.80891827241787,0.147929799326536));
#51103=CARTESIAN_POINT('Ctrl Pts',(-83.9246303763255,1.93464686355464,3.28433907275508));
#51104=CARTESIAN_POINT('Ctrl Pts',(-83.7257568446282,-1.71718205589994,
3.40309086249292));
#51105=CARTESIAN_POINT('Ctrl Pts',(-83.5268833129305,-3.79126057655081,
0.395075780299149));
#51106=CARTESIAN_POINT('Ctrl Pts',(-83.3280097812333,-2.38192109497551,
-2.97593574003171));
#51107=CARTESIAN_POINT('Ctrl Pts',(-83.1291362495355,1.21593237939653,-3.61265139201427));
#51108=CARTESIAN_POINT('Ctrl Pts',(-82.9302627178384,3.69658468693845,-0.930055527256101));
#51109=CARTESIAN_POINT('Ctrl Pts',(-82.7313891861407,2.78080739402538,2.60707726560248));
#51110=CARTESIAN_POINT('Ctrl Pts',(-82.5325156544434,-0.689981442273743,
3.74882211378524));
#51111=CARTESIAN_POINT('Ctrl Pts',(-82.3336421227459,-3.52681391269177,
1.44614150646857));
#51112=CARTESIAN_POINT('Ctrl Pts',(-82.1347685910484,-3.12320251861839,
-2.18525688631411));
#51113=CARTESIAN_POINT('Ctrl Pts',(-81.9358950593511,0.150013762347644,
-3.80883676502338));
#51114=CARTESIAN_POINT('Ctrl Pts',(-81.7370215276534,3.28539709044952,-1.93284960344911));
#51115=CARTESIAN_POINT('Ctrl Pts',(-81.5381479959562,3.40215082603064,1.7190437424413));
#51116=CARTESIAN_POINT('Ctrl Pts',(-81.3392744642585,0.393001397111847,
3.79147616811124));
#51117=CARTESIAN_POINT('Ctrl Pts',(-81.1404009325613,-2.97723852241226,
2.38029250558662));
#51118=CARTESIAN_POINT('Ctrl Pts',(-80.9415274008636,-3.61198557446186,
-1.21790879846029));
#51119=CARTESIAN_POINT('Ctrl Pts',(-80.7426538691663,-0.92803286430498,
-3.69709299778318));
#51120=CARTESIAN_POINT('Ctrl Pts',(-80.5437803374688,2.60859834707974,-2.77938055960323));
#51121=CARTESIAN_POINT('Ctrl Pts',(-80.3449068057714,3.74844404100414,0.692032443566012));
#51122=CARTESIAN_POINT('Ctrl Pts',(-80.1460332740739,1.44421165347667,3.52760461665555));
#51123=CARTESIAN_POINT('Ctrl Pts',(-79.9471597423764,-2.18696536662534,
3.12200642482824));
#51124=CARTESIAN_POINT('Ctrl Pts',(-79.748286210679,-3.80875411743601,-0.152097680461436));
#51125=CARTESIAN_POINT('Ctrl Pts',(-79.5494126789815,-1.9310517647361,-3.28645412464514));
#51126=CARTESIAN_POINT('Ctrl Pts',(-79.3505391472841,1.72090491437897,-3.40120977111878));
#51127=CARTESIAN_POINT('Ctrl Pts',(-79.1516656155866,3.79169062467575,-0.39092689627776));
#51128=CARTESIAN_POINT('Ctrl Pts',(-78.9527920838892,2.37866320364617,2.9785404135427));
#51129=CARTESIAN_POINT('Ctrl Pts',(-78.7539185521916,-1.21988485293742,
3.61131867564487));
#51130=CARTESIAN_POINT('Ctrl Pts',(-78.5550450204943,-3.69760020188601,
0.926009923542931));
#51131=CARTESIAN_POINT('Ctrl Pts',(-78.3561714887968,-2.77795289316067,
-2.61011864766102));
#51132=CARTESIAN_POINT('Ctrl Pts',(-78.1572979570994,0.694083237695167,
-3.74806484610899));
#51133=CARTESIAN_POINT('Ctrl Pts',(-77.9584244254018,3.52839426461459,-1.44228136815333));
#51134=CARTESIAN_POINT('Ctrl Pts',(-77.7595508937045,3.12080939645103,2.18867319225837));
#51135=CARTESIAN_POINT('Ctrl Pts',(-77.560677362007,-0.154181553044083,
3.80867032968048));
#51136=CARTESIAN_POINT('Ctrl Pts',(-77.3618038303095,-3.28751017502554,
1.92925334795383));
#51137=CARTESIAN_POINT('Ctrl Pts',(-77.1629302986122,-3.40026769803905,
-1.72276557115579));
#51138=CARTESIAN_POINT('Ctrl Pts',(-76.9640567669146,-0.388852278417899,
-3.79190394618015));
#51139=CARTESIAN_POINT('Ctrl Pts',(-76.7651832352172,2.9798414130333,-2.37703318964188));
#51140=CARTESIAN_POINT('Ctrl Pts',(-76.5663097035197,3.61065069576294,1.22186054223637));
#51141=CARTESIAN_POINT('Ctrl Pts',(-76.3674361718222,0.923986705575531,
3.69810629909514));
#51142=CARTESIAN_POINT('Ctrl Pts',(-76.1685626401249,-2.61163816689122,
2.77652439512505));
#51143=CARTESIAN_POINT('Ctrl Pts',(-75.9696891084273,-3.74768452921329,
-0.696133824047293));
#51144=CARTESIAN_POINT('Ctrl Pts',(-75.77081557673,-1.4403506510764,-3.52918285633249));
#51145=CARTESIAN_POINT('Ctrl Pts',(-75.5719420450324,2.19038036270197,-3.1196114338451));
#51146=CARTESIAN_POINT('Ctrl Pts',(-75.373068513335,3.80858540178188,0.156265379471771));
#51147=CARTESIAN_POINT('Ctrl Pts',(-75.1741949816376,1.92745435364065,3.28856524127456));
#51148=CARTESIAN_POINT('Ctrl Pts',(-74.9753214499401,-1.72462571221478,
3.39932460707347));
#51149=CARTESIAN_POINT('Ctrl Pts',(-74.7764479182427,-3.79211613256056,
0.386777544153313));
#51150=CARTESIAN_POINT('Ctrl Pts',(-74.5775743865451,-2.37540246406173,
-2.9811415204946));
#51151=CARTESIAN_POINT('Ctrl Pts',(-74.3787008548478,1.22383586576573,-3.60998163501602));
#51152=CARTESIAN_POINT('Ctrl Pts',(-74.1798273231502,3.69861128925905,-0.921963211008446));
#51153=CARTESIAN_POINT('Ctrl Pts',(-73.9809537914529,2.77509506592403,2.61315690431547));
#51154=CARTESIAN_POINT('Ctrl Pts',(-73.7820802597554,-0.698184202008545,
3.74730309043091));
#51155=CARTESIAN_POINT('Ctrl Pts',(-73.5832067280579,-3.52997039157319,
1.43841950282384));
#51156=CARTESIAN_POINT('Ctrl Pts',(-73.3843331963604,-3.11841253736907,
-2.19208687744507));
#51157=CARTESIAN_POINT('Ctrl Pts',(-73.185459664663,0.158349159120692,-3.80849933376564));
#51158=CARTESIAN_POINT('Ctrl Pts',(-72.9865861329655,3.28961932307638,-1.92565478233509));
#51159=CARTESIAN_POINT('Ctrl Pts',(-72.7877126012682,3.39838049850435,1.72648533699904));
#51160=CARTESIAN_POINT('Ctrl Pts',(-72.5888390695705,0.384702694105128,
3.79232718375349));
#51161=CARTESIAN_POINT('Ctrl Pts',(-72.3899655378733,-2.9824407355374,2.3737710273939));
#51162=CARTESIAN_POINT('Ctrl Pts',(-72.1910920061757,-3.60931149360442,
-1.22581082293416));
#51163=CARTESIAN_POINT('Ctrl Pts',(-71.9922184744782,-0.919939440447408,
-3.69911517222657));
#51164=CARTESIAN_POINT('Ctrl Pts',(-71.7933449427809,2.61467485947912,-2.77366490598547));
#51165=CARTESIAN_POINT('Ctrl Pts',(-71.5944714110833,3.74692052987602,0.700234370965129));
#51166=CARTESIAN_POINT('Ctrl Pts',(-71.3955978793859,1.43648792397377,3.53075687010093));
#51167=CARTESIAN_POINT('Ctrl Pts',(-71.1967243476885,-2.19379273597684,
3.11721270738183));
#51168=CARTESIAN_POINT('Ctrl Pts',(-70.997850815991,-3.80841212565751,-0.160432891367063));
#51169=CARTESIAN_POINT('Ctrl Pts',(-70.7989772842935,-1.92385463457588,
-3.29067242011544));
#51170=CARTESIAN_POINT('Ctrl Pts',(-70.6001037525962,1.72834444495199,-3.39743537261432));
#51171=CARTESIAN_POINT('Ctrl Pts',(-70.4012302208986,3.79253709969573,-0.382627728894362));
#51172=CARTESIAN_POINT('Ctrl Pts',(-70.2023566892013,2.3721388801267,2.98373905777277));
#51173=CARTESIAN_POINT('Ctrl Pts',(-70.0034831575037,-1.22778541315046,
3.60864027172874));
#51174=CARTESIAN_POINT('Ctrl Pts',(-69.8046096258063,-3.69961794784686,
0.91791539449824));
#51175=CARTESIAN_POINT('Ctrl Pts',(-69.6057360941088,-2.7722339157375,-2.61619203192775));
#51176=CARTESIAN_POINT('Ctrl Pts',(-69.4068625624114,0.702284330303311,
-3.74653684766316));
#51177=CARTESIAN_POINT('Ctrl Pts',(-69.2079890307139,3.53154229168029,-1.43455591510438));
#51178=CARTESIAN_POINT('Ctrl Pts',(-69.0091154990165,3.11601194424255,2.19549793778661));
#51179=CARTESIAN_POINT('Ctrl Pts',(-68.810241967319,-0.162516575587105,
3.8083237774836));
#51180=CARTESIAN_POINT('Ctrl Pts',(-68.6113684356216,-3.29172453207651,
1.92205391090189));
#51181=CARTESIAN_POINT('Ctrl Pts',(-68.4124949039241,-3.3964892296863,-1.73020303551702));
#51182=CARTESIAN_POINT('Ctrl Pts',(-68.2136213722266,-0.380552649142222,
-3.79274588032446));
#51183=CARTESIAN_POINT('Ctrl Pts',(-68.0147478405293,2.98503648681207,-2.37050602274877));
#51184=CARTESIAN_POINT('Ctrl Pts',(-67.8158743088317,3.6079679695899,1.22975963582352));
#51185=CARTESIAN_POINT('Ctrl Pts',(-67.6170007771343,0.915891073766863,
3.70011961596942));
#51186=CARTESIAN_POINT('Ctrl Pts',(-67.4181272454368,-2.61770842120721,
2.77080209560849));
#51187=CARTESIAN_POINT('Ctrl Pts',(-67.2192537137395,-3.74615204390717,
-0.70433407940944));
#51188=CARTESIAN_POINT('Ctrl Pts',(-67.0203801820419,-1.43262347679405,
-3.53232665607612));
#51189=CARTESIAN_POINT('Ctrl Pts',(-66.8215066503446,2.19720248236392,-3.11481024831069));
#51190=CARTESIAN_POINT('Ctrl Pts',(-66.6226331186469,3.80823428927037,0.164600211157061));
#51191=CARTESIAN_POINT('Ctrl Pts',(-66.4237595869497,1.92025261185217,3.29277565864461));
#51192=CARTESIAN_POINT('Ctrl Pts',(-66.2248860552521,-1.73206110813779,
3.39554207000353));
#51193=CARTESIAN_POINT('Ctrl Pts',(-66.0260125235547,-3.79295352557719,
0.378477455469882));
#51194=CARTESIAN_POINT('Ctrl Pts',(-65.8271389918571,-2.3688724557489,-2.98633302226689));
#51195=CARTESIAN_POINT('Ctrl Pts',(-65.6282654601599,1.23173349036234,-3.60729458738919));
#51196=CARTESIAN_POINT('Ctrl Pts',(-65.4293919284621,3.70062017644406,-0.913866478859252));
#51197=CARTESIAN_POINT('Ctrl Pts',(-65.230518396765,2.76936944602707,2.61922402686354));
#51198=CARTESIAN_POINT('Ctrl Pts',(-65.0316448650673,-0.706383617669903,
3.74576611872324));
#51199=CARTESIAN_POINT('Ctrl Pts',(-64.83277133337,-3.53310996305364,1.43069060962126));
#51200=CARTESIAN_POINT('Ctrl Pts',(-64.6338978016725,-3.11360761994599,
-2.19890636919852));
#51201=CARTESIAN_POINT('Ctrl Pts',(-64.435024269975,0.16668379745318,-3.80814366104459));
#51202=CARTESIAN_POINT('Ctrl Pts',(-64.2361507382776,3.2938257995051,-1.91845073796596));
#51203=CARTESIAN_POINT('Ctrl Pts',(-64.0372772065801,3.39459389384955,1.73391866225805));
#51204=CARTESIAN_POINT('Ctrl Pts',(-63.8384036748827,0.376402148498568,
3.79316003539174));
#51205=CARTESIAN_POINT('Ctrl Pts',(-63.6395301431853,-2.98762866374912,
2.3672381796161));
#51206=CARTESIAN_POINT('Ctrl Pts',(-63.4406566114878,-3.60662012532815,
-1.23370697617605));
#51207=CARTESIAN_POINT('Ctrl Pts',(-63.2417830797903,-0.911841610381489,
-3.70111962912095));
#51208=CARTESIAN_POINT('Ctrl Pts',(-63.0429095480929,2.62073884844303,-2.7679359674221));
#51209=CARTESIAN_POINT('Ctrl Pts',(-62.8440360163953,3.74537907222691,0.708432944471117));
#51210=CARTESIAN_POINT('Ctrl Pts',(-62.6451624846981,1.42875731416466,3.53389221237837));
#51211=CARTESIAN_POINT('Ctrl Pts',(-62.4462889530004,-2.20060959778032,
3.11240405950844));
#51212=CARTESIAN_POINT('Ctrl Pts',(-62.2474154213031,-3.80805189283341,
-0.168767333851733));
#51213=CARTESIAN_POINT('Ctrl Pts',(-62.0485418896055,-1.91664828978265,
-3.29487495434361));
#51214=CARTESIAN_POINT('Ctrl Pts',(-61.8496683579083,1.73577569732174,-3.39364470150818));
#51215=CARTESIAN_POINT('Ctrl Pts',(-61.6507948262106,3.79336540970629,-0.374326728849534));
#51216=CARTESIAN_POINT('Ctrl Pts',(-61.4519212945133,2.36560319483962,2.9889234108709));
#51217=CARTESIAN_POINT('Ctrl Pts',(-61.2530477628157,-1.23568009267388,
3.6059445836087));
#51218=CARTESIAN_POINT('Ctrl Pts',(-61.0541742311184,-3.70161797385057,
0.909816468939726));
#51219=CARTESIAN_POINT('Ctrl Pts',(-60.8553006994208,-2.76650166022269,
-2.62225288549229));
#51220=CARTESIAN_POINT('Ctrl Pts',(-60.6564271677235,0.71048205919978,-3.74499090453405));
#51221=CARTESIAN_POINT('Ctrl Pts',(-60.4575536360259,3.53467340381617,-1.42682359100281));
#51222=CARTESIAN_POINT('Ctrl Pts',(-60.2586801043286,3.1111995673583,2.20231216759956));
#51223=CARTESIAN_POINT('Ctrl Pts',(-60.059806572631,-0.170850819729117,
3.80795898466428));
#51224=CARTESIAN_POINT('Ctrl Pts',(-59.8609330409336,-3.29592312284612,
1.91484526784171));
#51225=CARTESIAN_POINT('Ctrl Pts',(-59.6620595092362,-3.39269449326354,
-1.73763221277302));
#51226=CARTESIAN_POINT('Ctrl Pts',(-59.4631859775387,-0.372251197144022,
-3.79356964845936));
#51227=CARTESIAN_POINT('Ctrl Pts',(-59.2643124458413,2.99021726324463,-2.36396750190888));
#51228=CARTESIAN_POINT('Ctrl Pts',(-59.0654389141438,3.60526796243309,1.23765283926516));
#51229=CARTESIAN_POINT('Ctrl Pts',(-58.8665653824463,0.90779105514019,3.70211521048372));
#51230=CARTESIAN_POINT('Ctrl Pts',(-58.6676918507489,-2.62376613755799,
2.76506652485823));
#51231=CARTESIAN_POINT('Ctrl Pts',(-58.4688183190513,-3.74460161576084,
-0.712530961242275));
#51232=CARTESIAN_POINT('Ctrl Pts',(-58.2699447873541,-1.42488944071483,
-3.53545353713309));
#51233=CARTESIAN_POINT('Ctrl Pts',(-58.0710712556564,2.20401407814638,-3.10999414385624));
#51234=CARTESIAN_POINT('Ctrl Pts',(-57.8721977239591,3.80786493656502,0.172934254461413));
#51235=CARTESIAN_POINT('Ctrl Pts',(-57.6733241922616,1.9130416726831,3.29697030469875));
#51236=CARTESIAN_POINT('Ctrl Pts',(-57.4744506605642,-1.73948820805607,
3.39174326940018));
#51237=CARTESIAN_POINT('Ctrl Pts',(-57.2755771288667,-3.79377275158988,
0.37017555400328));
#51238=CARTESIAN_POINT('Ctrl Pts',(-57.0767035971692,-2.3623311013134,-2.99151022048307));
#51239=CARTESIAN_POINT('Ctrl Pts',(-56.8778300654718,1.23962521535938,-3.60459026200378));
#51240=CARTESIAN_POINT('Ctrl Pts',(-56.6789565337743,3.70261133887159,-0.905765369589214));
#51241=CARTESIAN_POINT('Ctrl Pts',(-56.4800830020769,2.76363056175831,2.62527860418717));
#51242=CARTESIAN_POINT('Ctrl Pts',(-56.2812094703794,-0.714579649985331,
3.74421120602382));
#51243=CARTESIAN_POINT('Ctrl Pts',(-56.082335938682,-3.53623261209566,1.4229548638796));
#51244=CARTESIAN_POINT('Ctrl Pts',(-55.8834624069845,-3.10878778936306,
-2.20571532891139));
#51245=CARTESIAN_POINT('Ctrl Pts',(-55.6845888752871,0.175017637425035,
-3.80776974856381));
#51246=CARTESIAN_POINT('Ctrl Pts',(-55.4857153435897,3.29801649958808,-1.9112375048466));
#51247=CARTESIAN_POINT('Ctrl Pts',(-55.2868418118921,3.39079103020278,1.74134368261521));
#51248=CARTESIAN_POINT('Ctrl Pts',(-55.0879682801948,0.368099800048924,
3.79397471903694));
#51249=CARTESIAN_POINT('Ctrl Pts',(-54.8890947484972,-2.99280228219903,
2.36069399354332));
#51250=CARTESIAN_POINT('Ctrl Pts',(-54.6902212167998,-3.60391148252377,
-1.24159722036601));
#51251=CARTESIAN_POINT('Ctrl Pts',(-54.4913476851023,-0.90373941289318,
-3.70310635886562));
#51252=CARTESIAN_POINT('Ctrl Pts',(-54.2924741534049,2.62679028492706,-2.76219377135282));
#51253=CARTESIAN_POINT('Ctrl Pts',(-54.0936006217074,3.74381967543987,0.71662812481567));
#51254=CARTESIAN_POINT('Ctrl Pts',(-53.89472709001,1.42101986107626,3.53701062847065));
#51255=CARTESIAN_POINT('Ctrl Pts',(-53.6958535583125,-2.20741591938532,
3.10758050423988));
#51256=CARTESIAN_POINT('Ctrl Pts',(-53.4969800266151,-3.80767342068911,
-0.177100967996319));
#51257=CARTESIAN_POINT('Ctrl Pts',(-53.2981064949176,-1.90943276487233,
-3.29906170720093));
#51258=CARTESIAN_POINT('Ctrl Pts',(-53.0992329632202,1.74319863589507,-3.38983777595641));
#51259=CARTESIAN_POINT('Ctrl Pts',(-52.9003594315227,3.79417555074013,-0.366023935902194));
#51260=CARTESIAN_POINT('Ctrl Pts',(-52.7014858998253,2.35905617908858,2.99409344800579));
#51261=CARTESIAN_POINT('Ctrl Pts',(-52.5026123681278,-1.24356885369478,
3.60323162419618));
#51262=CARTESIAN_POINT('Ctrl Pts',(-52.3037388364304,-3.70360027031765,
0.901713185658582));
#51263=CARTESIAN_POINT('Ctrl Pts',(-52.1048653047329,-2.76075615407185,
-2.62830117932514));
#51264=CARTESIAN_POINT('Ctrl Pts',(-51.9059917730355,0.718676385120064,
-3.74342702412619));
#51265=CARTESIAN_POINT('Ctrl Pts',(-51.707118241338,3.53778758602515,-1.41908443288405));
#51266=CARTESIAN_POINT('Ctrl Pts',(-51.5082447096405,3.10637228884811,2.2091158490591));
#51267=CARTESIAN_POINT('Ctrl Pts',(-51.3093711779431,-0.179184245551611,
3.80757595296977));
#51268=CARTESIAN_POINT('Ctrl Pts',(-51.1104976462456,-3.3001059272244,1.90762745330053));
#51269=CARTESIAN_POINT('Ctrl Pts',(-50.9116241145482,-3.38888350694643,
-1.74505306734036));
#51270=CARTESIAN_POINT('Ctrl Pts',(-50.7127505828507,-0.363947962184506,
-3.79437524663933));
#51271=CARTESIAN_POINT('Ctrl Pts',(-50.5138770511533,2.99538371751683,-2.35741765843947));
#51272=CARTESIAN_POINT('Ctrl Pts',(-50.3150035194558,3.60255068722456,1.24554011475546));
#51273=CARTESIAN_POINT('Ctrl Pts',(-50.1161299877584,0.899686688491969,
3.70409307307982));
#51274=CARTESIAN_POINT('Ctrl Pts',(-49.9172564560609,-2.62981128692911,
2.75931771034576));
#51275=CARTESIAN_POINT('Ctrl Pts',(-49.7183829243635,-3.74303325220033,
-0.720724430285355));
#51276=CARTESIAN_POINT('Ctrl Pts',(-49.519509392666,-1.41714857988236,-3.53856348452659));
#51277=CARTESIAN_POINT('Ctrl Pts',(-49.3206358609686,2.21081511742383,-3.10516314354943));
#51278=CARTESIAN_POINT('Ctrl Pts',(-49.1217623292711,3.80747734543496,0.181267469467265));
#51279=CARTESIAN_POINT('Ctrl Pts',(-48.9228887975737,1.90582157067163,3.30114915934591));
#51280=CARTESIAN_POINT('Ctrl Pts',(-48.7240152658761,-1.74690697639595,
3.3879282234585));
#51281=CARTESIAN_POINT('Ctrl Pts',(-48.5251417341788,-3.79457380667476,
0.361871879517312));
#51282=CARTESIAN_POINT('Ctrl Pts',(-48.3262682024813,-2.35577843208649,
-2.99667309034592));
#51283=CARTESIAN_POINT('Ctrl Pts',(-48.1273946707838,1.24751100295795,-3.60186867181274));
#51284=CARTESIAN_POINT('Ctrl Pts',(-47.9285211390864,3.7045847670046,-0.897659921999986));
#51285=CARTESIAN_POINT('Ctrl Pts',(-47.7296476073888,2.75787844060516,2.63132060728692));
#51286=CARTESIAN_POINT('Ctrl Pts',(-47.5307740756916,-0.722772259698463,
3.74263835978015));
#51287=CARTESIAN_POINT('Ctrl Pts',(-47.3319005439939,-3.53933832374268,
1.41521230265069));
#51288=CARTESIAN_POINT('Ctrl Pts',(-47.1330270122967,-3.10395306870581,
-2.21251372397084));
#51289=CARTESIAN_POINT('Ctrl Pts',(-46.934153480599,0.183350639119669,-3.80737759811421));
#51290=CARTESIAN_POINT('Ctrl Pts',(-46.7352799489018,3.30219140325315,-1.90401511752624));
#51291=CARTESIAN_POINT('Ctrl Pts',(-46.5364064172041,3.3869719257786,1.74876036250685));
#51292=CARTESIAN_POINT('Ctrl Pts',(-46.3375328855069,0.3597956885221,3.79477123078697));
#51293=CARTESIAN_POINT('Ctrl Pts',(-46.1386593538092,-2.99796156610706,
2.35413850052034));
#51294=CARTESIAN_POINT('Ctrl Pts',(-45.9397858221119,-3.60118557816487,
-1.24948151771226));
#51295=CARTESIAN_POINT('Ctrl Pts',(-45.7409122904144,-0.895632886789359,
-3.7050753519448));
#51296=CARTESIAN_POINT('Ctrl Pts',(-45.5420387587169,2.63282913994673,-2.7564383452809));
#51297=CARTESIAN_POINT('Ctrl Pts',(-45.3431652270195,3.74224234698389,0.724819872746352));
#51298=CARTESIAN_POINT('Ctrl Pts',(-45.144291695322,1.41327560176868,3.54011210344149));
#51299=CARTESIAN_POINT('Ctrl Pts',(-44.9454181636246,-2.21421166819163,
3.10274206467949));
#51300=CARTESIAN_POINT('Ctrl Pts',(-44.7465446319271,-3.80727671103737,
-0.185433753885211));
#51301=CARTESIAN_POINT('Ctrl Pts',(-44.5476711002297,-1.90220809440512,
-3.30323265863413));
#51302=CARTESIAN_POINT('Ctrl Pts',(-44.3487975685321,1.75061322511827,-3.386014614193));
#51303=CARTESIAN_POINT('Ctrl Pts',(-44.1499240368348,3.79496751891687,-0.357719389820383));
#51304=CARTESIAN_POINT('Ctrl Pts',(-43.9510505051372,2.35249786423195,2.99924914441454));
#51305=CARTESIAN_POINT('Ctrl Pts',(-43.7521769734399,-1.2514516584285,3.60050140648546));
#51306=CARTESIAN_POINT('Ctrl Pts',(-43.5533034417424,-3.70556482775357,
0.893605583466879));
#51307=CARTESIAN_POINT('Ctrl Pts',(-43.3544299100449,-2.75499742480407,
-2.63433688445697));
#51308=CARTESIAN_POINT('Ctrl Pts',(-43.1555563783475,0.726867268816058,
-3.74184521393008));
#51309=CARTESIAN_POINT('Ctrl Pts',(-42.95668284665,3.54088482339137,-1.41133847781607));
#51310=CARTESIAN_POINT('Ctrl Pts',(-42.7578093149525,3.10153013183299,2.21590894957792));
#51311=CARTESIAN_POINT('Ctrl Pts',(-42.5589357832551,-0.187516813140302,
3.80717468423465));
#51312=CARTESIAN_POINT('Ctrl Pts',(-42.3600622515577,-3.30427292517715,
1.90040050184921));
#51313=CARTESIAN_POINT('Ctrl Pts',(-42.1611887198602,-3.38505628898826,
-1.75246556367551));
#51314=CARTESIAN_POINT('Ctrl Pts',(-41.9623151881627,-0.355642984033713,
-3.7951626710057));
#51315=CARTESIAN_POINT('Ctrl Pts',(-41.7634416564653,3.00053582488292,-2.35085652371245));
#51316=CARTESIAN_POINT('Ctrl Pts',(-41.5645681247678,3.59981615697931,1.2534214245169));
#51317=CARTESIAN_POINT('Ctrl Pts',(-41.3656945930704,0.891578012639441,
3.70605319428438));
#51318=CARTESIAN_POINT('Ctrl Pts',(-41.1668210613729,-2.63584384036628,
2.75355567960603));
#51319=CARTESIAN_POINT('Ctrl Pts',(-40.9679475296755,-3.7414469607376,-0.72891444729469));
#51320=CARTESIAN_POINT('Ctrl Pts',(-40.7690739979781,-1.40940093137277,
-3.54165648336101));
#51321=CARTESIAN_POINT('Ctrl Pts',(-40.5702004662805,2.21760556762163,-3.10031727052911));
#51322=CARTESIAN_POINT('Ctrl Pts',(-40.3713269345832,3.80707151773659,0.189599816261364));
#51323=CARTESIAN_POINT('Ctrl Pts',(-40.1724534028856,1.89859234039963,3.30531220257079));
#51324=CARTESIAN_POINT('Ctrl Pts',(-39.9735798711882,-1.75431737762409,
3.38409695045128));
#51325=CARTESIAN_POINT('Ctrl Pts',(-39.7747063394907,-3.79535668699504,
0.353566471783673));
#51326=CARTESIAN_POINT('Ctrl Pts',(-39.5758328077933,-2.34921447945318,
-3.00182160712704));
#51327=CARTESIAN_POINT('Ctrl Pts',(-39.3769592760958,1.25539081538779,-3.59912982985154));
#51328=CARTESIAN_POINT('Ctrl Pts',(-39.1780857443985,3.70654045139103,-0.889550174914005));
#51329=CARTESIAN_POINT('Ctrl Pts',(-38.9792122127009,2.75211311011837,2.63735000722356));
#51330=CARTESIAN_POINT('Ctrl Pts',(-38.7803386810035,-0.73096140756941,
3.74104758752567));
#51331=CARTESIAN_POINT('Ctrl Pts',(-38.581465149306,-3.54242708311941,1.40746296301879));
#51332=CARTESIAN_POINT('Ctrl Pts',(-38.3825916176086,-3.09910348113092,
-2.21930152181486));
#51333=CARTESIAN_POINT('Ctrl Pts',(-38.1837180859111,0.191682762624847,
-3.80696721157406));
#51334=CARTESIAN_POINT('Ctrl Pts',(-37.9848445542137,3.30635049050394,-1.89678361059766));
#51335=CARTESIAN_POINT('Ctrl Pts',(-37.7859710225162,3.38313659886923,1.75616866640966));
#51336=CARTESIAN_POINT('Ctrl Pts',(-37.5870974908188,0.351489853691939,
3.79554956682676));
#51337=CARTESIAN_POINT('Ctrl Pts',(-37.3882239591213,-3.00310649076192,
2.34757173194576));
#51338=CARTESIAN_POINT('Ctrl Pts',(-37.1893504274238,-3.59844242530768,
-1.2573598304516));
#51339=CARTESIAN_POINT('Ctrl Pts',(-36.9904768957264,-0.887522070897608,
-3.70702659892766));
#51340=CARTESIAN_POINT('Ctrl Pts',(-36.7916033640289,2.63885538457792,-2.75066971677293));
#51341=CARTESIAN_POINT('Ctrl Pts',(-36.5927298323315,3.74064709441386,0.733008149027457));
#51342=CARTESIAN_POINT('Ctrl Pts',(-36.393856300634,1.40552457333426,3.54319662243588));
#51343=CARTESIAN_POINT('Ctrl Pts',(-36.1949827689366,-2.22099681164992,
3.09788876400177));
#51344=CARTESIAN_POINT('Ctrl Pts',(-35.9961092372391,-3.80686176577831,
-0.19376565160721));
#51345=CARTESIAN_POINT('Ctrl Pts',(-35.7972357055417,-1.89497431298474,
-3.30738778866578));
#51346=CARTESIAN_POINT('Ctrl Pts',(-35.5983621738442,1.75801942947801,-3.3821752345296));
#51347=CARTESIAN_POINT('Ctrl Pts',(-35.3994886421468,3.79574131044322,-0.34941313038003));
#51348=CARTESIAN_POINT('Ctrl Pts',(-35.2006151104493,2.34592828168183,3.00439047540306));
#51349=CARTESIAN_POINT('Ctrl Pts',(-35.0017415787519,-1.25932846911898,
3.59775394355339));
#51350=CARTESIAN_POINT('Ctrl Pts',(-34.8028680470544,-3.70751163674873,
0.885493701197379));
#51351=CARTESIAN_POINT('Ctrl Pts',(-34.603994515357,-2.74922550000179,-2.64035997197872));
#51352=CARTESIAN_POINT('Ctrl Pts',(-34.4051209836595,0.735054671056124,
-3.74024548152205));
#51353=CARTESIAN_POINT('Ctrl Pts',(-34.206247451962,3.54396510108007,-1.40358576289945));
#51354=CARTESIAN_POINT('Ctrl Pts',(-34.0073739202646,3.09667311950531,2.22269143661931));
#51355=CARTESIAN_POINT('Ctrl Pts',(-33.8085003885672,-0.195848482584929,
3.80675518038088));
#51356=CARTESIAN_POINT('Ctrl Pts',(-33.6096268568697,-3.30842409674581,
1.8931644481025));
#51357=CARTESIAN_POINT('Ctrl Pts',(-33.4107533251723,-3.38121285772017,
-1.75986966627512));
#51358=CARTESIAN_POINT('Ctrl Pts',(-33.2118797934747,-0.347336302469681,
-3.79593191778697));
#51359=CARTESIAN_POINT('Ctrl Pts',(-33.0130062617774,3.005673560666,-2.34428412915341));
#51360=CARTESIAN_POINT('Ctrl Pts',(-32.8141327300798,3.59706438479482,1.26129673080056));
#51361=CARTESIAN_POINT('Ctrl Pts',(-32.6152591983825,0.883465066420513,
3.70799556470907));
#51362=CARTESIAN_POINT('Ctrl Pts',(-32.4163856666849,-2.64186376897555,
2.74778046023728));
#51363=CARTESIAN_POINT('Ctrl Pts',(-32.2175121349875,-3.73984274897046,
-0.737100973042777));
#51364=CARTESIAN_POINT('Ctrl Pts',(-32.0186386032901,-1.40164653229475,
-3.54473251882192));
#51365=CARTESIAN_POINT('Ctrl Pts',(-31.8197650715926,2.22438539621574,-3.09545654800542));
#51366=CARTESIAN_POINT('Ctrl Pts',(-31.6208915398952,3.8066474554137,0.1979312549345));
#51367=CARTESIAN_POINT('Ctrl Pts',(-31.4220180081977,1.89135401649272,3.30945941443378));
#51368=CARTESIAN_POINT('Ctrl Pts',(-31.2231444765003,-1.7617193762471,3.38024946872905));
#51369=CARTESIAN_POINT('Ctrl Pts',(-31.0242709448028,-3.79612138880096,
0.345259370582608));
#51370=CARTESIAN_POINT('Ctrl Pts',(-30.8253974131054,-2.34263927485271,
-3.00695574616668));
#51371=CARTESIAN_POINT('Ctrl Pts',(-30.6265238814079,1.26326461490713,-3.59637374923839));
#51372=CARTESIAN_POINT('Ctrl Pts',(-30.4276503497104,3.70847838266379,-0.881436167174301));
#51373=CARTESIAN_POINT('Ctrl Pts',(-30.228776818013,2.74633459791199,2.64336677511825));
#51374=CARTESIAN_POINT('Ctrl Pts',(-30.0299032863155,-0.739147054374844,
3.73943889687965));
#51375=CARTESIAN_POINT('Ctrl Pts',(-29.8310297546182,-3.5454988754317,1.39970688210069));
#51376=CARTESIAN_POINT('Ctrl Pts',(-29.6321562229205,-3.09423904986631,
-2.22607868993213));
#51377=CARTESIAN_POINT('Ctrl Pts',(-29.4332826912232,0.200013968032432,
-3.80653859090899));
#51378=CARTESIAN_POINT('Ctrl Pts',(-29.2344091595257,3.31049374141978,-1.88954301869738));
#51379=CARTESIAN_POINT('Ctrl Pts',(-29.0355356278283,3.37928506784462,1.76356855884025));
#51380=CARTESIAN_POINT('Ctrl Pts',(-28.8366620961308,0.343182335340544,
3.79630972342846));
#51381=CARTESIAN_POINT('Ctrl Pts',(-28.6377885644334,-3.00823703152125,
2.3409937192721));
#51382=CARTESIAN_POINT('Ctrl Pts',(-28.4389150327359,-3.59568203709087,
-1.2652321208496));
#51383=CARTESIAN_POINT('Ctrl Pts',(-28.2400415010384,-0.879407004066094,
-3.70896009046836));
#51384=CARTESIAN_POINT('Ctrl Pts',(-28.041167969341,2.64486898995689,-2.74488791345875));
#51385=CARTESIAN_POINT('Ctrl Pts',(-27.8422944376435,3.73903392537052,0.741192914439823));
#51386=CARTESIAN_POINT('Ctrl Pts',(-27.6434209059461,1.3977668128979,3.54626417068001));
#51387=CARTESIAN_POINT('Ctrl Pts',(-27.4445473742486,-2.22777131726157,
3.09302062545243));
#51388=CARTESIAN_POINT('Ctrl Pts',(-27.2456738425512,-3.80642858689937,
-0.202096621255259));
#51389=CARTESIAN_POINT('Ctrl Pts',(-27.0468003108537,-1.88773145525861,
-3.31152707739417));
#51390=CARTESIAN_POINT('Ctrl Pts',(-26.8479267791563,1.765417213501,-3.37831965535559));
#51391=CARTESIAN_POINT('Ctrl Pts',(-26.6490532474588,3.79649692161308,-0.341105197365262));
#51392=CARTESIAN_POINT('Ctrl Pts',(-26.4501797157614,2.33934746290421,3.00951741634616));
#51393=CARTESIAN_POINT('Ctrl Pts',(-26.2513061840639,-1.26719924803898,
3.5949892485593));
#51394=CARTESIAN_POINT('Ctrl Pts',(-26.0524326523664,-3.70944068797857,
0.877377577703335));
#51395=CARTESIAN_POINT('Ctrl Pts',(-25.853559120669,-2.74344040731062,-2.64637041304177));
#51396=CARTESIAN_POINT('Ctrl Pts',(-25.6546855889715,0.74323855262528,-3.73862783456431));
#51397=CARTESIAN_POINT('Ctrl Pts',(-25.4558120572741,3.54702840433774,-1.39582632526716));
#51398=CARTESIAN_POINT('Ctrl Pts',(-25.2569385255766,3.09180127512853,2.22946327769737));
#51399=CARTESIAN_POINT('Ctrl Pts',(-25.0580649938792,-0.204179213979529,
3.80631744341775));
#51400=CARTESIAN_POINT('Ctrl Pts',(-24.8591914621818,-3.31255942204762,
1.88591932671869));
#51401=CARTESIAN_POINT('Ctrl Pts',(-24.6603179304842,-3.37735323155094,
-1.76726533967594));
#51402=CARTESIAN_POINT('Ctrl Pts',(-24.4614443987868,-0.339027957278562,
-3.79668298329881));
#51403=CARTESIAN_POINT('Ctrl Pts',(-24.2625708670894,3.01079690025812,-2.33770050624184));
#51404=CARTESIAN_POINT('Ctrl Pts',(-24.0636973353919,3.59429538385108,1.26916599588641));
#51405=CARTESIAN_POINT('Ctrl Pts',(-23.8648238036945,0.87534788869354,3.70992017505057));
#51406=CARTESIAN_POINT('Ctrl Pts',(-23.665950271997,-2.64787104392343,2.74199207990092));
#51407=CARTESIAN_POINT('Ctrl Pts',(-23.4670767402996,-3.73822062458257,
-0.745283968318842));
#51408=CARTESIAN_POINT('Ctrl Pts',(-23.2682032086021,-1.39388541978934,
-3.54779157617611));
#51409=CARTESIAN_POINT('Ctrl Pts',(-23.0693296769047,2.23115457073302,-3.09058099925963));
#51410=CARTESIAN_POINT('Ctrl Pts',(-22.8704561452071,3.8062051604974,0.206261745581809));
#51411=CARTESIAN_POINT('Ctrl Pts',(-22.6715826135097,1.8841066336201,3.31359077507109));
#51412=CARTESIAN_POINT('Ctrl Pts',(-22.4727090818123,-1.76911293681183,
3.37638579672));
#51413=CARTESIAN_POINT('Ctrl Pts',(-22.2738355501148,-3.79686790842993,
0.336950615702276));
#51414=CARTESIAN_POINT('Ctrl Pts',(-22.0749620184174,-2.33605284977801,
-3.01207548287411));
#51415=CARTESIAN_POINT('Ctrl Pts',(-21.8760884867199,1.27113236380313,-3.59360044317391));
#51416=CARTESIAN_POINT('Ctrl Pts',(-21.6772149550225,3.71039855154082,-0.873317937644316));
#51417=CARTESIAN_POINT('Ctrl Pts',(-21.478341423325,2.74054293166321,2.64937088215266));
#51418=CARTESIAN_POINT('Ctrl Pts',(-21.2794678916276,-0.747329160908197,
3.73781229554719));
#51419=CARTESIAN_POINT('Ctrl Pts',(-21.0805943599301,-3.54855368596668,
1.39194409704549));
#51420=CARTESIAN_POINT('Ctrl Pts',(-20.8817208282327,-3.08935979821102,
-2.23284519586224));
#51421=CARTESIAN_POINT('Ctrl Pts',(-20.6828472965351,0.20834421543868,-3.80609173817195));
#51422=CARTESIAN_POINT('Ctrl Pts',(-20.4839737648378,3.31462113615585,-1.88229337650549));
#51423=CARTESIAN_POINT('Ctrl Pts',(-20.2851002331403,3.37541735115235,1.77096000435559));
#51424=CARTESIAN_POINT('Ctrl Pts',(-20.0862267014428,0.334873173258265,
3.79705169695109));
#51425=CARTESIAN_POINT('Ctrl Pts',(-19.8873531697454,-3.01335316381137,
2.33440449400597));
#51426=CARTESIAN_POINT('Ctrl Pts',(-19.6884796380479,-3.59290442673585,
-1.27309835120051));
#51427=CARTESIAN_POINT('Ctrl Pts',(-19.4896061063505,-0.871287725163321,
-3.71087581730611));
#51428=CARTESIAN_POINT('Ctrl Pts',(-19.290732574653,2.65086992728046,-2.7390929630313));
#51429=CARTESIAN_POINT('Ctrl Pts',(-19.0918590429556,3.73740284758043,0.749374129781112));
#51430=CARTESIAN_POINT('Ctrl Pts',(-18.8929855112581,1.39000235761673,3.5493147334813));
#51431=CARTESIAN_POINT('Ctrl Pts',(-18.6941119795607,-2.23453515257893,
3.08813767234826));
#51432=CARTESIAN_POINT('Ctrl Pts',(-18.4952384478632,-3.80597717647534,
-0.210426622926742));
#51433=CARTESIAN_POINT('Ctrl Pts',(-18.2963649161657,-1.88047955591764,
-3.31565050499345));
#51434=CARTESIAN_POINT('Ctrl Pts',(-18.0974913844683,1.7728065417542,-3.37444789513792));
#51435=CARTESIAN_POINT('Ctrl Pts',(-17.8986178527708,3.79723434880727,-0.332795630568509));
#51436=CARTESIAN_POINT('Ctrl Pts',(-17.6997443210734,2.33275543941922,3.01462994268742));
#51437=CARTESIAN_POINT('Ctrl Pts',(-17.5008707893759,-1.27506395749001,
3.59220733474523));
#51438=CARTESIAN_POINT('Ctrl Pts',(-17.3019972576785,-3.71135197220356,
0.869257251858322));
#51439=CARTESIAN_POINT('Ctrl Pts',(-17.103123725981,-2.73764217443926,-2.65236817885809));
#51440=CARTESIAN_POINT('Ctrl Pts',(-16.9042501942836,0.75141887432542,-3.73699228080485));
#51441=CARTESIAN_POINT('Ctrl Pts',(-16.7053766625861,3.55007471849215,-1.38806020208435));
#51442=CARTESIAN_POINT('Ctrl Pts',(-16.5065031308886,3.08691462203722,2.23622444037719));
#51443=CARTESIAN_POINT('Ctrl Pts',(-16.3076295991912,-0.212508967422626,
3.80586147544186));
#51444=CARTESIAN_POINT('Ctrl Pts',(-16.1087560674937,-3.31667888127574,
1.87866517239955));
#51445=CARTESIAN_POINT('Ctrl Pts',(-15.9098825357963,-3.37347742896691,
-1.77465254845506));
#51446=CARTESIAN_POINT('Ctrl Pts',(-15.7110090040988,-0.330717988254753,
-3.79741586394379));
#51447=CARTESIAN_POINT('Ctrl Pts',(-15.5121354724014,3.01590581912008,-2.33110568651127));
#51448=CARTESIAN_POINT('Ctrl Pts',(-15.3132619407039,3.59150916741074,1.27702918208321));
#51449=CARTESIAN_POINT('Ctrl Pts',(-15.1143884090065,0.867226518337144,
3.71182701609064));
#51450=CARTESIAN_POINT('Ctrl Pts',(-14.915514877309,-2.65386563643705,2.73619056632137));
#51451=CARTESIAN_POINT('Ctrl Pts',(-14.7166413456116,-3.73658059534335,
-0.753463393929017));
#51452=CARTESIAN_POINT('Ctrl Pts',(-14.5177678139141,-1.38611763102972,
-3.55083364077171));
#51453=CARTESIAN_POINT('Ctrl Pts',(-14.3188942822166,2.23791305875133,-3.08569064764402));
#51454=CARTESIAN_POINT('Ctrl Pts',(-14.1200207505192,3.80574463510616,0.214591248302973));
#51455=CARTESIAN_POINT('Ctrl Pts',(-13.9211472188217,1.87685022649435,3.31770626469487));
#51456=CARTESIAN_POINT('Ctrl Pts',(-13.7222736871243,-1.77649802390547,
3.37250595292984));
#51457=CARTESIAN_POINT('Ctrl Pts',(-13.5234001554268,-3.79759624230632,
0.328640246939039));
#51458=CARTESIAN_POINT('Ctrl Pts',(-13.3245266237294,-2.32945523577606,
-3.01718079272738));
#51459=CARTESIAN_POINT('Ctrl Pts',(-13.125653092032,1.27899402439183,-3.59080992494138));
#51460=CARTESIAN_POINT('Ctrl Pts',(-12.9267795603345,3.71230094882514,-0.865195525207697));
#51461=CARTESIAN_POINT('Ctrl Pts',(-12.727906028637,2.7347381391122,2.65536229956906));
#51462=CARTESIAN_POINT('Ctrl Pts',(-12.5290324969396,-0.755507687979863,
3.73616779131918));
#51463=CARTESIAN_POINT('Ctrl Pts',(-12.3301589652421,-3.5515915000928,1.38417464503438));
#51464=CARTESIAN_POINT('Ctrl Pts',(-12.1312854335447,-3.08446574953506,
-2.23960100719584));
#51465=CARTESIAN_POINT('Ctrl Pts',(-11.9324119018472,0.216673464944433,
-3.80562665550321));
#51466=CARTESIAN_POINT('Ctrl Pts',(-11.7335383701498,3.31873265494329,-1.87503471874537));
#51467=CARTESIAN_POINT('Ctrl Pts',(-11.5346648384523,3.37153346731751,1.77834296755299));
#51468=CARTESIAN_POINT('Ctrl Pts',(-11.3357913067549,0.326562407243348,
3.79777548384086));
#51469=CARTESIAN_POINT('Ctrl Pts',(-11.1369177750574,-3.01845486312766,
2.32780408770765));
#51470=CARTESIAN_POINT('Ctrl Pts',(-10.93804424336,-3.59010960754647,-1.28095848382767));
#51471=CARTESIAN_POINT('Ctrl Pts',(-10.7391707116625,-0.863164273077971,
-3.7127737702652));
#51472=CARTESIAN_POINT('Ctrl Pts',(-10.540297179965,2.65685816780609,-2.73328489324651));
#51473=CARTESIAN_POINT('Ctrl Pts',(-10.3414236482676,3.73575386885591,0.757551755865984));
#51474=CARTESIAN_POINT('Ctrl Pts',(-10.1425501165701,1.38223124467995,3.55234829622857));
#51475=CARTESIAN_POINT('Ctrl Pts',(-9.94367658487268,-2.24128828520545,
3.08323992807701));
#51476=CARTESIAN_POINT('Ctrl Pts',(-9.74480305317522,-3.80550753666828,
-0.218755616723621));
#51477=CARTESIAN_POINT('Ctrl Pts',(-9.54592952147778,-1.87321864969616,
-3.31975805171371));
#51478=CARTESIAN_POINT('Ctrl Pts',(-9.34705598978035,1.78018737884529,-3.37055997242112));
#51479=CARTESIAN_POINT('Ctrl Pts',(-9.14818245808286,3.79795358849371,-0.324484469789755));
#51480=CARTESIAN_POINT('Ctrl Pts',(-8.94930892638544,2.32615224280039,3.01972802993948));
#51481=CARTESIAN_POINT('Ctrl Pts',(-8.75043539468796,-1.28292255980254,
3.58940821543569));
#51482=CARTESIAN_POINT('Ctrl Pts',(-8.55156186299052,-3.71324548026926,
0.861132762556118));
#51483=CARTESIAN_POINT('Ctrl Pts',(-8.35268833129305,-2.73183082915942,
-2.65835324070026));
#51484=CARTESIAN_POINT('Ctrl Pts',(-8.1538147995956,0.759595596975361,-3.73533882807744));
#51485=CARTESIAN_POINT('Ctrl Pts',(-7.95494126789815,3.55310402895249,-1.38028743054838));
#51486=CARTESIAN_POINT('Ctrl Pts',(-7.7560677362007,3.08201318363674,2.24297489227504));
#51487=CARTESIAN_POINT('Ctrl Pts',(-7.55719420450326,-0.220837703017022,
3.80538727863702));
#51488=CARTESIAN_POINT('Ctrl Pts',(-7.35832067280577,-3.32078245469979,
1.87140201989046));
#51489=CARTESIAN_POINT('Ctrl Pts',(-7.15944714110835,-3.36958546853095,
-1.78203125723078));
#51490=CARTESIAN_POINT('Ctrl Pts',(-6.96057360941086,-0.322406435201958,
-3.79813055621078));
#51491=CARTESIAN_POINT('Ctrl Pts',(-6.76170007771344,3.02100029278552,-2.32449970155028));
#51492=CARTESIAN_POINT('Ctrl Pts',(-6.56282654601595,3.58870574881201,1.28488625173232));
#51493=CARTESIAN_POINT('Ctrl Pts',(-6.36395301431852,0.85910099426281,3.71371607868986));
#51494=CARTESIAN_POINT('Ctrl Pts',(-6.16507948262105,-2.65984751782854,
2.73037594729784));
#51495=CARTESIAN_POINT('Ctrl Pts',(-5.96620595092362,-3.73492266906212,
-0.761639210718873));
#51496=CARTESIAN_POINT('Ctrl Pts',(-5.76733241922618,-1.3783432033079,-3.55385869799583));
#51497=CARTESIAN_POINT('Ctrl Pts',(-5.5684588875287,2.24466082806341,-3.08078551666176));
#51498=CARTESIAN_POINT('Ctrl Pts',(-5.36958535583126,3.80526588113653,0.222919723353213));
#51499=CARTESIAN_POINT('Ctrl Pts',(-5.17071182413379,1.86958483045521,3.32180586330821));
#51500=CARTESIAN_POINT('Ctrl Pts',(-4.97183829243635,-1.78387460325836,
3.36860995647996));
#51501=CARTESIAN_POINT('Ctrl Pts',(-4.77296476073887,-3.79830638486021,
0.320328303080476));
#51502=CARTESIAN_POINT('Ctrl Pts',(-4.57409122904144,-2.32284646837729,
-3.02227164935517));
#51503=CARTESIAN_POINT('Ctrl Pts',(-4.37521769734396,1.28684956643968,-3.58800221152922));
#51504=CARTESIAN_POINT('Ctrl Pts',(-4.17634416564651,3.71418555139234,-0.857068961927461));
#51505=CARTESIAN_POINT('Ctrl Pts',(-3.97747063394909,2.72892027452058,2.66134098575405));
#51506=CARTESIAN_POINT('Ctrl Pts',(-3.77859710225162,-0.76368264637654,
3.73450541646114));
#51507=CARTESIAN_POINT('Ctrl Pts',(-3.57972357055418,-3.55461220892666,
1.37639851722947));
#51508=CARTESIAN_POINT('Ctrl Pts',(-3.3808500388567,-3.07955710539971,-2.24634600462084));
#51509=CARTESIAN_POINT('Ctrl Pts',(-3.18197650715927,0.225002012982617,
-3.80514350931703));
#51510=CARTESIAN_POINT('Ctrl Pts',(-2.98310297546179,3.32282764303465,-1.86776677016589));
#51511=CARTESIAN_POINT('Ctrl Pts',(-2.78422944376435,3.36763463405492,1.78571682769388));
#51512=CARTESIAN_POINT('Ctrl Pts',(-2.58535591206688,0.318247812933675,
3.79848218594141));
#51513=CARTESIAN_POINT('Ctrl Pts',(-2.38648238036943,-3.02353782982558,
2.32119044494005));
#51514=CARTESIAN_POINT('Ctrl Pts',(-2.18760884867199,-3.58730566537358,
-1.28880854030746));
#51515=CARTESIAN_POINT('Ctrl Pts',(-1.98873531697452,-0.855021444261629,
-3.71466138124353));
#51516=CARTESIAN_POINT('Ctrl Pts',(-1.78986178527709,2.66280490197648,-2.72744968181255));
#51517=CARTESIAN_POINT('Ctrl Pts',(-1.59098825357962,3.73414134137891,0.765699223969745));
#51518=CARTESIAN_POINT('Ctrl Pts',(-1.39211472188218,1.37435089712346,3.55541493832914));
#51519=CARTESIAN_POINT('Ctrl Pts',(-1.19324119018471,-2.24783691714511,
3.07823282251273));
#51520=CARTESIAN_POINT('Ctrl Pts',(-0.994367658487268,-3.80538561390127,
-0.226904901415462));
#51521=CARTESIAN_POINT('Ctrl Pts',(-0.795494126789802,-1.86525717936383,
-3.32418745080932));
#51522=CARTESIAN_POINT('Ctrl Pts',(-0.596620595092344,1.78624879507146,
-3.36601485692819));
#51523=CARTESIAN_POINT('Ctrl Pts',(-0.397747063394925,3.80117096935424,
-0.317409156202402));
#51524=CARTESIAN_POINT('Ctrl Pts',(-0.198873531697423,2.31445171887122,
3.02736545452069));
#51525=CARTESIAN_POINT('Ctrl Pts',(-0.0662911772324812,-0.0808825703380203,
3.39599395944883));
#51526=CARTESIAN_POINT('Ctrl Pts',(0.,-1.09131022003071,3.03235215074973));
#51527=CARTESIAN_POINT('Ctrl Pts',(-109.840375352461,-1.53816642191745,
3.09873914818361));
#51528=CARTESIAN_POINT('Ctrl Pts',(-109.774084175229,-2.57071526811129,
2.586197792408));
#51529=CARTESIAN_POINT('Ctrl Pts',(-109.641501820764,-4.0651012769763,0.456647939553593));
#51530=CARTESIAN_POINT('Ctrl Pts',(-109.442628289066,-2.57873220422192,
-3.18056678679282));
#51531=CARTESIAN_POINT('Ctrl Pts',(-109.243754757369,1.28024521157691,-3.88503862978065));
#51532=CARTESIAN_POINT('Ctrl Pts',(-109.044881225672,3.96125087796401,-1.02519763748056));
#51533=CARTESIAN_POINT('Ctrl Pts',(-108.846007693974,3.00353488488411,2.77935581684627));
#51534=CARTESIAN_POINT('Ctrl Pts',(-108.647134162277,-0.71430246575407,
4.02877424317354));
#51535=CARTESIAN_POINT('Ctrl Pts',(-108.448260630579,-3.77558982751309,
1.57731788801589));
#51536=CARTESIAN_POINT('Ctrl Pts',(-108.249387098882,-3.36798852559464,
-2.32378978877478));
#51537=CARTESIAN_POINT('Ctrl Pts',(-108.050513567184,0.134196937583717,
-4.08957834911196));
#51538=CARTESIAN_POINT('Ctrl Pts',(-107.851640035487,3.51304523067848,-2.09796847093758));
#51539=CARTESIAN_POINT('Ctrl Pts',(-107.652766503789,3.66411981460646,1.82131980977203));
#51540=CARTESIAN_POINT('Ctrl Pts',(-107.453892972092,0.448583282276703,
4.0671435818543));
#51541=CARTESIAN_POINT('Ctrl Pts',(-107.255019440394,-3.17910703215976,
2.57608449495303));
#51542=CARTESIAN_POINT('Ctrl Pts',(-107.056145908697,-3.88583016883055,
-1.28189532651468));
#51543=CARTESIAN_POINT('Ctrl Pts',(-106.857272377,-1.0222430366496,-3.96206231753294));
#51544=CARTESIAN_POINT('Ctrl Pts',(-106.658398845302,2.7805822856922,-3.00188084347272));
#51545=CARTESIAN_POINT('Ctrl Pts',(-106.459525313605,4.02860332407945,0.716436251805123));
#51546=CARTESIAN_POINT('Ctrl Pts',(-106.260651781907,1.57513512905252,3.77648953898132));
#51547=CARTESIAN_POINT('Ctrl Pts',(-106.06177825021,-2.32557033628216,3.36669685901759));
#51548=CARTESIAN_POINT('Ctrl Pts',(-105.862904718512,-4.08953706540046,
-0.13642400659151));
#51549=CARTESIAN_POINT('Ctrl Pts',(-105.664031186815,-2.09602870811142,
-3.51419810952553));
#51550=CARTESIAN_POINT('Ctrl Pts',(-105.465157655117,1.82331511201696,-3.66311982958988));
#51551=CARTESIAN_POINT('Ctrl Pts',(-105.26628412342,4.06739327293676,-0.446359499308134));
#51552=CARTESIAN_POINT('Ctrl Pts',(-105.067410591722,2.57434213819699,3.18051683979354));
#51553=CARTESIAN_POINT('Ctrl Pts',(-104.868537060025,-1.28401983628658,
3.88512778430906));
#51554=CARTESIAN_POINT('Ctrl Pts',(-104.669663528328,-3.96262175015484,
1.02007533898783));
#51555=CARTESIAN_POINT('Ctrl Pts',(-104.47078999663,-3.00035866289289,-2.7822244199646));
#51556=CARTESIAN_POINT('Ctrl Pts',(-104.271916464933,0.718640123994403,
-4.02821067041903));
#51557=CARTESIAN_POINT('Ctrl Pts',(-104.073042933235,3.77735088960066,-1.57306868522629));
#51558=CARTESIAN_POINT('Ctrl Pts',(-103.874169401538,3.36542390180016,2.327412037546));
#51559=CARTESIAN_POINT('Ctrl Pts',(-103.67529586984,-0.138661477048271,
4.08946180159252));
#51560=CARTESIAN_POINT('Ctrl Pts',(-103.476422338143,-3.51534440610599,
2.09410566545931));
#51561=CARTESIAN_POINT('Ctrl Pts',(-103.277548806445,-3.66212167685685,
-1.82531905581637));
#51562=CARTESIAN_POINT('Ctrl Pts',(-103.078675274748,-0.444134031586379,
-4.06763688075757));
#51563=CARTESIAN_POINT('Ctrl Pts',(-102.87980174305,3.18192487383849,-2.57260158767713));
#51564=CARTESIAN_POINT('Ctrl Pts',(-102.680928211353,3.88442467181907,1.28614532640571));
#51565=CARTESIAN_POINT('Ctrl Pts',(-102.482054679656,1.01790710555096,3.9631792737841));
#51566=CARTESIAN_POINT('Ctrl Pts',(-102.283181147958,-2.78386559933878,
2.99883596692024));
#51567=CARTESIAN_POINT('Ctrl Pts',(-102.084307616261,-4.02781687552084,
-0.720843983776407));
#51568=CARTESIAN_POINT('Ctrl Pts',(-101.885434084563,-1.57100173626865,
-3.77821100209074));
#51569=CARTESIAN_POINT('Ctrl Pts',(-101.686560552866,2.32925302396205,-3.36414999398676));
#51570=CARTESIAN_POINT('Ctrl Pts',(-101.487687021168,4.08938532318502,0.140898936108952));
#51571=CARTESIAN_POINT('Ctrl Pts',(-101.288813489471,2.09218199084294,3.51648963440394));
#51572=CARTESIAN_POINT('Ctrl Pts',(-101.089939957773,-1.82732245050554,
3.66112243629685));
#51573=CARTESIAN_POINT('Ctrl Pts',(-100.891066426076,-4.06787927233846,
0.441908426437971));
#51574=CARTESIAN_POINT('Ctrl Pts',(-100.692192894378,-2.5708602662819,-3.18333195299057));
#51575=CARTESIAN_POINT('Ctrl Pts',(-100.493319362681,1.28827043111132,-3.8837203977632));
#51576=CARTESIAN_POINT('Ctrl Pts',(-100.294445830984,3.96373561122914,-1.01573856673447));
#51577=CARTESIAN_POINT('Ctrl Pts',(-100.095572299286,2.99731237312002,2.78550594499804));
#51578=CARTESIAN_POINT('Ctrl Pts',(-99.8966987675887,-0.723047627711036,
4.0274218750634));
#51579=CARTESIAN_POINT('Ctrl Pts',(-99.6978252358912,-3.77906998358733,
1.56893431692567));
#51580=CARTESIAN_POINT('Ctrl Pts',(-99.4989517041938,-3.36287507908286,
-2.33109331305317));
#51581=CARTESIAN_POINT('Ctrl Pts',(-99.3000781724963,0.143136352982075,
-4.08930762062879));
#51582=CARTESIAN_POINT('Ctrl Pts',(-99.1012046407988,3.51763381002914,-2.09025768990755));
#51583=CARTESIAN_POINT('Ctrl Pts',(-98.9023311091013,3.66012209976044,1.82932529816953));
#51584=CARTESIAN_POINT('Ctrl Pts',(-98.703457577404,0.439682689003533,4.068120446185));
#51585=CARTESIAN_POINT('Ctrl Pts',(-98.5045840457065,-3.18473807919821,
2.56911817528557));
#51586=CARTESIAN_POINT('Ctrl Pts',(-98.3057105140089,-3.88301496109731,
-1.2903951501661));
#51587=CARTESIAN_POINT('Ctrl Pts',(-98.1068369823117,-1.01356972385213,
-3.96429076211219));
#51588=CARTESIAN_POINT('Ctrl Pts',(-97.907963450614,2.7871454568033,-2.99578788206015));
#51589=CARTESIAN_POINT('Ctrl Pts',(-97.7090899189167,4.02702566897857,0.725251055197827));
#51590=CARTESIAN_POINT('Ctrl Pts',(-97.5102163872191,1.56686642791497,3.77992783380196));
#51591=CARTESIAN_POINT('Ctrl Pts',(-97.3113428555218,-2.33293290432075,
3.3615991574867));
#51592=CARTESIAN_POINT('Ctrl Pts',(-97.1124693238244,-4.08922869391941,
-0.145373727006639));
#51593=CARTESIAN_POINT('Ctrl Pts',(-96.9135957921267,-2.08833276324387,
-3.5187769326344));
#51594=CARTESIAN_POINT('Ctrl Pts',(-96.7147222604295,1.83132759821652,-3.65912066754955));
#51595=CARTESIAN_POINT('Ctrl Pts',(-96.5158487287319,4.06836040222087,-0.437456819948072));
#51596=CARTESIAN_POINT('Ctrl Pts',(-96.3169751970346,2.56737531521184,3.1861432520398));
#51597=CARTESIAN_POINT('Ctrl Pts',(-96.1181016653369,-1.29251948293511,
3.88230836203293));
#51598=CARTESIAN_POINT('Ctrl Pts',(-95.9192281336396,-3.96484472626648,
1.01140057755301));
#51599=CARTESIAN_POINT('Ctrl Pts',(-95.7203546019421,-2.99426249419735,
-2.78878413426369));
#51600=CARTESIAN_POINT('Ctrl Pts',(-95.5214810702447,0.727454265577372,
-4.02662825738497));
#51601=CARTESIAN_POINT('Ctrl Pts',(-95.3226075385471,3.78078455247771,-1.56479806985557));
#51602=CARTESIAN_POINT('Ctrl Pts',(-95.1237340068498,3.3603222295803,2.33477179721405));
#51603=CARTESIAN_POINT('Ctrl Pts',(-94.9248604751522,-0.147611057512885,
4.08914854308052));
#51604=CARTESIAN_POINT('Ctrl Pts',(-94.725986943455,-3.51991900187753,2.08640721142814));
#51605=CARTESIAN_POINT('Ctrl Pts',(-94.5271134117573,-3.65811813996398,
-1.83332935004715));
#51606=CARTESIAN_POINT('Ctrl Pts',(-94.32823988006,-0.435230819937879,-4.06859914037424));
#51607=CARTESIAN_POINT('Ctrl Pts',(-94.1293663483624,3.18754747109466,-2.56563168658245));
#51608=CARTESIAN_POINT('Ctrl Pts',(-93.9304928166651,3.8816006007816,1.29464342878244));
#51609=CARTESIAN_POINT('Ctrl Pts',(-93.7316192849675,1.00923112848644,3.96539750352618));
#51610=CARTESIAN_POINT('Ctrl Pts',(-93.5327457532702,-2.79042197688866,
2.99273620998821));
#51611=CARTESIAN_POINT('Ctrl Pts',(-93.3338722215725,-4.02622964040159,
-0.729657258190121));
#51612=CARTESIAN_POINT('Ctrl Pts',(-93.1349986898753,-1.56272924336663,
-3.78164013935813));
#51613=CARTESIAN_POINT('Ctrl Pts',(-92.9361251581777,2.33660999118264,-3.35904429574591));
#51614=CARTESIAN_POINT('Ctrl Pts',(-92.7372516264803,4.08906716813612,0.149848343831102));
#51615=CARTESIAN_POINT('Ctrl Pts',(-92.5383780947828,2.08448103503674,3.52106001741663));
#51616=CARTESIAN_POINT('Ctrl Pts',(-92.3395045630855,-1.83533055306216,
3.65711451730382));
#51617=CARTESIAN_POINT('Ctrl Pts',(-92.1406310313879,-4.06883666057366,
0.433004689639325));
#51618=CARTESIAN_POINT('Ctrl Pts',(-91.9417574996906,-2.56388728991935,
-3.18895073594244));
#51619=CARTESIAN_POINT('Ctrl Pts',(-91.7428839679929,1.29676698707227,-3.88089167755519));
#51620=CARTESIAN_POINT('Ctrl Pts',(-91.5440104362956,3.9659490937258,-1.00706137730188));
#51621=CARTESIAN_POINT('Ctrl Pts',(-91.3451369045981,2.99120902988965,2.79205898418792));
#51622=CARTESIAN_POINT('Ctrl Pts',(-91.1462633729006,-0.731860032376595,
4.02582981814775));
#51623=CARTESIAN_POINT('Ctrl Pts',(-90.9473898412033,-3.78249459418708,
1.56065994906748));
#51624=CARTESIAN_POINT('Ctrl Pts',(-90.7485163095056,-3.35776535636607,
-2.33844748567623));
#51625=CARTESIAN_POINT('Ctrl Pts',(-90.5496427778085,0.152085585291523,
-4.08898456911055));
#51626=CARTESIAN_POINT('Ctrl Pts',(-90.3507692461107,3.52219997891014,-2.08255423464631));
#51627=CARTESIAN_POINT('Ctrl Pts',(-90.1518957144135,3.65610979986952,1.83733120666248));
#51628=CARTESIAN_POINT('Ctrl Pts',(-89.9530221827158,0.430778429718823,
4.069072962748));
#51629=CARTESIAN_POINT('Ctrl Pts',(-89.7541486510186,-3.19035304616309,
2.56214212574474));
#51630=CARTESIAN_POINT('Ctrl Pts',(-89.5552751193211,-3.88018159256591,
-1.29889015716891));
#51631=CARTESIAN_POINT('Ctrl Pts',(-89.3564015876235,-1.00489132464883,
-3.96649949670023));
#51632=CARTESIAN_POINT('Ctrl Pts',(-89.1575280559263,2.79369515567141,-2.98968095435883));
#51633=CARTESIAN_POINT('Ctrl Pts',(-88.9586545242286,4.02542879074315,0.734062587477381));
#51634=CARTESIAN_POINT('Ctrl Pts',(-88.7597809925313,1.55859018757754,3.7833479167088));
#51635=CARTESIAN_POINT('Ctrl Pts',(-88.5609074608337,-2.34028428014475,
3.35648541182365));
#51636=CARTESIAN_POINT('Ctrl Pts',(-88.3620339291363,-4.08890074602855,
-0.154322781224421));
#51637=CARTESIAN_POINT('Ctrl Pts',(-88.1631603974389,-2.08062681083363,
-3.5233388860168));
#51638=CARTESIAN_POINT('Ctrl Pts',(-87.9642868657414,1.83933131024921,-3.65510398796186));
#51639=CARTESIAN_POINT('Ctrl Pts',(-87.7654133340439,4.06930804682655,-0.4285520408428));
#51640=CARTESIAN_POINT('Ctrl Pts',(-87.5665398023466,2.56039619458104,3.19175440133679));
#51641=CARTESIAN_POINT('Ctrl Pts',(-87.367666270649,-1.30101293843677,3.87947034602635));
#51642=CARTESIAN_POINT('Ctrl Pts',(-87.1687927389516,-3.9670487122847,1.00272097117692));
#51643=CARTESIAN_POINT('Ctrl Pts',(-86.9699192072541,-2.9881519838532,-2.79533049084934));
#51644=CARTESIAN_POINT('Ctrl Pts',(-86.7710456755567,0.736264922833142,
-4.02502655830782));
#51645=CARTESIAN_POINT('Ctrl Pts',(-86.5721721438591,3.78420010666783,-1.55651995951644));
#51646=CARTESIAN_POINT('Ctrl Pts',(-86.3732986121619,3.35520446250181,2.34212037403835));
#51647=CARTESIAN_POINT('Ctrl Pts',(-86.1744250804642,-0.156559930960084,
4.08881569891521));
#51648=CARTESIAN_POINT('Ctrl Pts',(-85.975551548767,-3.52447673839568,2.07869876417571));
#51649=CARTESIAN_POINT('Ctrl Pts',(-85.7766780170693,-3.65409708188192,
-1.84133086322361));
#51650=CARTESIAN_POINT('Ctrl Pts',(-85.577804485372,-0.426325523677742,
-4.06954191273892));
#51651=CARTESIAN_POINT('Ctrl Pts',(-85.3789309536745,3.19315480104402,-2.55864949695091));
#51652=CARTESIAN_POINT('Ctrl Pts',(-85.180057421977,3.8787579381494,1.30313533024036));
#51653=CARTESIAN_POINT('Ctrl Pts',(-84.9811838902796,1.00055031753589,3.9675967403148));
#51654=CARTESIAN_POINT('Ctrl Pts',(-84.7823103585822,-2.79696498923216,
2.98662211883046));
#51655=CARTESIAN_POINT('Ctrl Pts',(-84.5834368268846,-4.02462312096219,
-0.738467037784595));
#51656=CARTESIAN_POINT('Ctrl Pts',(-84.3845632951873,-1.55444926550391,
-3.78505116380902));
#51657=CARTESIAN_POINT('Ctrl Pts',(-84.1856897634898,2.34395576680736,-3.35392250878403));
#51658=CARTESIAN_POINT('Ctrl Pts',(-83.9868162317923,4.088729427796,0.158797033828775));
#51659=CARTESIAN_POINT('Ctrl Pts',(-83.7879427000949,2.07677009524969,3.52561353570614));
#51660=CARTESIAN_POINT('Ctrl Pts',(-83.5890691683974,-1.84332986498711,
3.65308908193113));
#51661=CARTESIAN_POINT('Ctrl Pts',(-83.3901956367,-4.06977456041508,0.424098878890195));
#51662=CARTESIAN_POINT('Ctrl Pts',(-83.1913221050024,-2.55690203337726,
-3.19455424486561));
#51663=CARTESIAN_POINT('Ctrl Pts',(-82.9924485733052,1.30525733194437,-3.87804436914836));
#51664=CARTESIAN_POINT('Ctrl Pts',(-82.7935750416075,3.96814358062647,-0.99837936437545));
#51665=CARTESIAN_POINT('Ctrl Pts',(-82.5947015099103,2.98509135974858,2.79859865033059));
#51666=CARTESIAN_POINT('Ctrl Pts',(-82.3958279782126,-0.740668931672492,
4.02421847882701));
#51667=CARTESIAN_POINT('Ctrl Pts',(-82.1969544465152,-3.78590108787766,
1.55237810615983));
#51668=CARTESIAN_POINT('Ctrl Pts',(-81.9980809148179,-3.35263955105406,
-2.34579045790239));
#51669=CARTESIAN_POINT('Ctrl Pts',(-81.7992073831203,0.161034089160873,
-4.08864193269671));
#51670=CARTESIAN_POINT('Ctrl Pts',(-81.6003338514228,3.52674927760791,-2.07484080463296));
#51671=CARTESIAN_POINT('Ctrl Pts',(-81.4014603197255,3.65207998841123,1.84532831494129));
#51672=CARTESIAN_POINT('Ctrl Pts',(-81.2025867880279,0.421872107146664,
4.07000598978543));
#51673=CARTESIAN_POINT('Ctrl Pts',(-81.0037132563306,-3.19595273238265,
2.55515380438312));
#51674=CARTESIAN_POINT('Ctrl Pts',(-80.804839724633,-3.87732963923677,-1.3073789429136));
#51675=CARTESIAN_POINT('Ctrl Pts',(-80.6059661929356,-0.996208112345541,
-3.96868923305602));
#51676=CARTESIAN_POINT('Ctrl Pts',(-80.4070926612381,2.80023147365557,-2.98355970706581));
#51677=CARTESIAN_POINT('Ctrl Pts',(-80.2082191295408,4.02381263202344,0.742870603837753));
#51678=CARTESIAN_POINT('Ctrl Pts',(-80.0093455978432,1.55030648210414,3.78674987861933));
#51679=CARTESIAN_POINT('Ctrl Pts',(-79.8104720661458,-2.34762444677422,
3.35135558969589));
#51680=CARTESIAN_POINT('Ctrl Pts',(-79.6115985344483,-4.08855321364357,
-0.163271096286671));
#51681=CARTESIAN_POINT('Ctrl Pts',(-79.412725002751,-2.07291089290303,-3.52788396376096));
#51682=CARTESIAN_POINT('Ctrl Pts',(-79.2138514710534,1.8473262124879,-3.6510698016243));
#51683=CARTESIAN_POINT('Ctrl Pts',(-79.014977939356,4.07023620078068,-0.419645209113765));
#51684=CARTESIAN_POINT('Ctrl Pts',(-78.8161044076585,2.55340481049188,3.19735026317646));
#51685=CARTESIAN_POINT('Ctrl Pts',(-78.6172308759612,-1.3095001625129,3.87661374862863));
#51686=CARTESIAN_POINT('Ctrl Pts',(-78.4183573442636,-3.96923369744009,
0.994036562096127));
#51687=CARTESIAN_POINT('Ctrl Pts',(-78.2194838125662,-2.98202716124064,
-2.80186345871831));
#51688=CARTESIAN_POINT('Ctrl Pts',(-78.0206102808687,0.745072053621266,
-4.02340558067295));
#51689=CARTESIAN_POINT('Ctrl Pts',(-77.8217367491712,3.78759753577992,-1.54823439395703));
#51690=CARTESIAN_POINT('Ctrl Pts',(-77.6228632174739,3.35007062509393,2.34945773287382));
#51691=CARTESIAN_POINT('Ctrl Pts',(-77.4239896857763,-0.165508054536509,
4.08846327066312));
#51692=CARTESIAN_POINT('Ctrl Pts',(-77.2251161540789,-3.52901759382565,
2.07098036063764));
#51693=CARTESIAN_POINT('Ctrl Pts',(-77.0262426223815,-3.65005852187275,
-1.84932355702888));
#51694=CARTESIAN_POINT('Ctrl Pts',(-76.827369090684,-0.417418185458136,
-4.0704651933319));
#51695=CARTESIAN_POINT('Ctrl Pts',(-76.6284955589865,3.19874683682869,-2.5516550522271));
#51696=CARTESIAN_POINT('Ctrl Pts',(-76.4296220272891,3.87589669753825,1.31162099010726));
#51697=CARTESIAN_POINT('Ctrl Pts',(-76.2307484955916,0.991864714277272,
3.96977697361571));
#51698=CARTESIAN_POINT('Ctrl Pts',(-76.0318749638942,-2.80349460503027,
2.98049372273185));
#51699=CARTESIAN_POINT('Ctrl Pts',(-75.8330014321968,-4.0229973248974,-0.747273280364011));
#51700=CARTESIAN_POINT('Ctrl Pts',(-75.6341279004993,-1.54616184233881,
-3.78844405910568));
#51701=CARTESIAN_POINT('Ctrl Pts',(-75.4352543688018,2.35129031565238,-3.34878465763285));
#51702=CARTESIAN_POINT('Ctrl Pts',(-75.2363808371043,4.08837210378228,0.167744963240746));
#51703=CARTESIAN_POINT('Ctrl Pts',(-75.0375073054069,2.06904920841471,3.53015016746261));
#51704=CARTESIAN_POINT('Ctrl Pts',(-74.8386337737095,-1.8513203479663,3.64904614945931));
#51705=CARTESIAN_POINT('Ctrl Pts',(-74.639760242012,-4.07069296737055,0.415191036846439));
#51706=CARTESIAN_POINT('Ctrl Pts',(-74.4408867103145,-2.54990453011259,
-3.20014245292127));
#51707=CARTESIAN_POINT('Ctrl Pts',(-74.2420131786171,1.31374142506182,-3.87517848618026));
#51708=CARTESIAN_POINT('Ctrl Pts',(-74.0431396469197,3.97031906142024,-0.989692569539129));
#51709=CARTESIAN_POINT('Ctrl Pts',(-73.8442661152222,2.97895939199849,2.80512491210317));
#51710=CARTESIAN_POINT('Ctrl Pts',(-73.6453925835248,-0.749474283407049,
4.02258786481901));
#51711=CARTESIAN_POINT('Ctrl Pts',(-73.4465190518271,-3.78928944834319,
1.54408882786989));
#51712=CARTESIAN_POINT('Ctrl Pts',(-73.24764552013,-3.34749768769759,-2.35312219456132));
#51713=CARTESIAN_POINT('Ctrl Pts',(-73.0487719884322,0.169981821729752,
-4.08827971302836));
#51714=CARTESIAN_POINT('Ctrl Pts',(-72.8498984567351,3.53128168433279,-2.06711743681233));
#51715=CARTESIAN_POINT('Ctrl Pts',(-72.6510249250373,3.64803268468702,1.85331658470237));
#51716=CARTESIAN_POINT('Ctrl Pts',(-72.4521513933401,0.412963763945437,
4.07091952282843));
#51717=CARTESIAN_POINT('Ctrl Pts',(-72.2532778616425,-3.2015371110364,2.54815324467241));
#51718=CARTESIAN_POINT('Ctrl Pts',(-72.0544043299451,-3.87445911476969,
-1.31586146674182));
#51719=CARTESIAN_POINT('Ctrl Pts',(-71.8555307982476,-0.987520128531938,
-3.97085996069139));
#51720=CARTESIAN_POINT('Ctrl Pts',(-71.6566572665502,2.80675437944895,-2.97742416949987));
#51721=CARTESIAN_POINT('Ctrl Pts',(-71.4577837348527,4.02217720056034,0.751675062091496));
#51722=CARTESIAN_POINT('Ctrl Pts',(-71.2589102031553,1.54201535117083,3.79013370323939));
#51723=CARTESIAN_POINT('Ctrl Pts',(-71.0600366714579,-2.35495336905225,
3.34620971567343));
#51724=CARTESIAN_POINT('Ctrl Pts',(-70.8611631397604,-4.08818609842901,
-0.172218629333917));
#51725=CARTESIAN_POINT('Ctrl Pts',(-70.6622896080629,-2.06518504640879,
-3.53241214409748));
#51726=CARTESIAN_POINT('Ctrl Pts',(-70.4634160763654,1.85531226663959,-3.64701812785929));
#51727=CARTESIAN_POINT('Ctrl Pts',(-70.264542544668,4.07114485963774,-0.410736367421776));
#51728=CARTESIAN_POINT('Ctrl Pts',(-70.0656690129706,2.54640119643073,3.20293081075661));
#51729=CARTESIAN_POINT('Ctrl Pts',(-69.8667954812731,-1.3179811145126,3.87373858352186));
#51730=CARTESIAN_POINT('Ctrl Pts',(-69.6679219495757,-3.97139967126727,
0.985347391906037));
#51731=CARTESIAN_POINT('Ctrl Pts',(-69.4690484178782,-2.97588805569555,
-2.80838300657983));
#51732=CARTESIAN_POINT('Ctrl Pts',(-69.2701748861808,0.753875615758535,
-4.02176533224433));
#51733=CARTESIAN_POINT('Ctrl Pts',(-69.0713013544833,3.79097682354154,-1.53994141286236));
#51734=CARTESIAN_POINT('Ctrl Pts',(-68.8724278227859,3.34492074194592,2.356783838577));
#51735=CARTESIAN_POINT('Ctrl Pts',(-68.6735542910884,-0.174455385383641,
4.08809126001224));
#51736=CARTESIAN_POINT('Ctrl Pts',(-68.4746807593909,-3.53354154641825,
2.06325203778256));
#51737=CARTESIAN_POINT('Ctrl Pts',(-68.2758072276935,-3.64600247927983,
-1.85730739318052));
#51738=CARTESIAN_POINT('Ctrl Pts',(-68.076933695996,-0.408508847942281,
-4.07136897773102));
#51739=CARTESIAN_POINT('Ctrl Pts',(-67.8780601642986,3.20432355166466,-2.54464838591208));
#51740=CARTESIAN_POINT('Ctrl Pts',(-67.6791866326011,3.87301689265249,1.32010036773963));
#51741=CARTESIAN_POINT('Ctrl Pts',(-67.4803131009036,0.983174360311834,
3.9719381929863));
#51742=CARTESIAN_POINT('Ctrl Pts',(-67.2814395692062,-2.81001079300828,
2.97435105104539));
#51743=CARTESIAN_POINT('Ctrl Pts',(-67.0825660375088,-4.02135225999428,
-0.756075943749426));
#51744=CARTESIAN_POINT('Ctrl Pts',(-66.8836925058113,-1.53786701356531,
-3.79181880899725));
#51745=CARTESIAN_POINT('Ctrl Pts',(-66.6848189741139,2.35861360258762,-3.34363076690093));
#51746=CARTESIAN_POINT('Ctrl Pts',(-66.4859454424164,4.08799519780646,0.176692089209336));
#51747=CARTESIAN_POINT('Ctrl Pts',(-66.287071910719,2.0613184115123,3.53466989095704));
#51748=CARTESIAN_POINT('Ctrl Pts',(-66.0881983790215,-1.85930196372788,
3.64498573925267));
#51749=CARTESIAN_POINT('Ctrl Pts',(-65.8893248473241,-4.07159187704117,
0.406281206173773));
#51750=CARTESIAN_POINT('Ctrl Pts',(-65.6904513156265,-2.54289481364118,
-3.20571533334365));
#51751=CARTESIAN_POINT('Ctrl Pts',(-65.4915777839292,1.32221922578853,-3.87229404237759));
#51752=CARTESIAN_POINT('Ctrl Pts',(-65.2927042522315,3.97247552568726,-0.981001034399843));
#51753=CARTESIAN_POINT('Ctrl Pts',(-65.0938307205343,2.97281315600949,2.81163773824701));
#51754=CARTESIAN_POINT('Ctrl Pts',(-64.8949571888367,-0.758276045405488,
4.02093798393383));
#51755=CARTESIAN_POINT('Ctrl Pts',(-64.6960836571393,-3.79265965935448,
1.53579215390065));
#51756=CARTESIAN_POINT('Ctrl Pts',(-64.4972101254419,-3.3423397909246,-2.36044266053635));
#51757=CARTESIAN_POINT('Ctrl Pts',(-64.2983365937444,0.178928740141437,
-4.08789791184041));
#51758=CARTESIAN_POINT('Ctrl Pts',(-64.099463062047,3.53579717737605,-2.05938416817684));
#51759=CARTESIAN_POINT('Ctrl Pts',(-63.9005895303494,3.64396790808217,1.86129597768461));
#51760=CARTESIAN_POINT('Ctrl Pts',(-63.7017159986521,0.404053442783113,
4.07181355750147));
#51761=CARTESIAN_POINT('Ctrl Pts',(-63.5028424669546,-3.20710615537694,
2.54114048014296));
#51762=CARTESIAN_POINT('Ctrl Pts',(-63.3039689352571,-3.87157003291358,
-1.32433768802498));
#51763=CARTESIAN_POINT('Ctrl Pts',(-63.1050954035597,-0.978827414820659,
-3.97301166920931));
#51764=CARTESIAN_POINT('Ctrl Pts',(-62.9062218718622,2.81326384180894,-2.97127437104824));
#51765=CARTESIAN_POINT('Ctrl Pts',(-62.7073483401648,4.02052250418702,0.76047592006806));
#51766=CARTESIAN_POINT('Ctrl Pts',(-62.5084748084674,1.53371683448956,3.79349937436151));
#51767=CARTESIAN_POINT('Ctrl Pts',(-62.3096012767698,-2.36227101187565,
3.34104781440341));
#51768=CARTESIAN_POINT('Ctrl Pts',(-62.1107277450724,-4.08779940214323,
-0.181165337510387));
#51769=CARTESIAN_POINT('Ctrl Pts',(-61.911854213375,-2.0574493083552,-3.53692340533783));
#51770=CARTESIAN_POINT('Ctrl Pts',(-61.7129806816776,1.86328943445378,-3.64294898607303));
#51771=CARTESIAN_POINT('Ctrl Pts',(-61.51410714998,4.07203401904556,-0.401825558437184));
#51772=CARTESIAN_POINT('Ctrl Pts',(-61.3152336182825,2.53938538594258,3.20849601734817));
#51773=CARTESIAN_POINT('Ctrl Pts',(-61.1163600865852,-1.32645575381482,
3.87084486447718));
#51774=CARTESIAN_POINT('Ctrl Pts',(-60.9174865548877,-3.97354662339195,
0.976653502224961));
#51775=CARTESIAN_POINT('Ctrl Pts',(-60.7186130231902,-2.96973469662225,
-2.81488910320741));
#51776=CARTESIAN_POINT('Ctrl Pts',(-60.5197394914928,0.762675567078782,
-4.02010582087821));
#51777=CARTESIAN_POINT('Ctrl Pts',(-60.3208659597953,3.794337953767,-1.53164105595309));
#51778=CARTESIAN_POINT('Ctrl Pts',(-60.1219924280979,3.33975483772404,2.36409865605831));
#51779=CARTESIAN_POINT('Ctrl Pts',(-59.9231188964004,-0.183401880646781,
4.0876996687444));
#51780=CARTESIAN_POINT('Ctrl Pts',(-59.724245364703,-3.53804857450529,2.05551383262651));
#51781=CARTESIAN_POINT('Ctrl Pts',(-59.5253718330054,-3.64192897353023,
-1.86528233343871));
#51782=CARTESIAN_POINT('Ctrl Pts',(-59.3264983013081,-0.399597553802876,
-4.07225326160742));
#51783=CARTESIAN_POINT('Ctrl Pts',(-59.1276247696106,3.20988491884128,-2.53762953156546));
#51784=CARTESIAN_POINT('Ctrl Pts',(-58.9287512379131,3.87011853728548,1.32857342252401));
#51785=CARTESIAN_POINT('Ctrl Pts',(-58.7298777062157,0.974479297263519,
3.97408038807503));
#51786=CARTESIAN_POINT('Ctrl Pts',(-58.5310041745182,-2.81651352195577,
2.96819413319245));
#51787=CARTESIAN_POINT('Ctrl Pts',(-58.3321306428208,-4.01968793413213,
-0.764874985778962));
#51788=CARTESIAN_POINT('Ctrl Pts',(-58.1332571111233,-1.52956481891289,
-3.79517539731984));
#51789=CARTESIAN_POINT('Ctrl Pts',(-57.9343835794259,2.365925592537,-3.33846086127369));
#51790=CARTESIAN_POINT('Ctrl Pts',(-57.7355100477284,4.08759871167377,0.185638368880856));
#51791=CARTESIAN_POINT('Ctrl Pts',(-57.536636516031,2.05357774157035,3.5391726845415));
#51792=CARTESIAN_POINT('Ctrl Pts',(-57.3377629843335,-1.86727467404277,
3.6409078707592));
#51793=CARTESIAN_POINT('Ctrl Pts',(-57.138889452636,-4.07247128512151,0.397369429547074));
#51794=CARTESIAN_POINT('Ctrl Pts',(-56.9400159209386,-2.53587291753704,
-3.21127285944058));
#51795=CARTESIAN_POINT('Ctrl Pts',(-56.7411423892411,1.33069069351864,-3.86939105155583));
#51796=CARTESIAN_POINT('Ctrl Pts',(-56.5422688575438,3.97461296309879,-0.972304800587201));
#51797=CARTESIAN_POINT('Ctrl Pts',(-56.3433953258462,2.96665268122003,2.8181370975678));
#51798=CARTESIAN_POINT('Ctrl Pts',(-56.1445217941488,-0.767074175510283,
4.01926884407389));
#51799=CARTESIAN_POINT('Ctrl Pts',(-55.9456482624513,-3.79601170476937,
1.5274881239904));
#51800=CARTESIAN_POINT('Ctrl Pts',(-55.7467747307539,-3.33716588543964,
-2.36775182076493));
#51801=CARTESIAN_POINT('Ctrl Pts',(-55.5479011990564,0.187874801543228,
-4.08749653096158));
#51802=CARTESIAN_POINT('Ctrl Pts',(-55.349027667359,3.54029573511,-2.05164103576619));
#51803=CARTESIAN_POINT('Ctrl Pts',(-55.1501541356615,3.63988567806557,1.86926645566944));
#51804=CARTESIAN_POINT('Ctrl Pts',(-54.9512806039641,0.395141186337052,
4.07268808952245));
#51805=CARTESIAN_POINT('Ctrl Pts',(-54.7524070722666,-3.21265983873043,
2.53411554438349));
#51806=CARTESIAN_POINT('Ctrl Pts',(-54.5535335405691,-3.86866240750616,
-1.33280756616482));
#51807=CARTESIAN_POINT('Ctrl Pts',(-54.3546600088718,-0.97013001284694,
-3.97514434830377));
#51808=CARTESIAN_POINT('Ctrl Pts',(-54.1557864771742,2.81975982955745,-2.9651103411664));
#51809=CARTESIAN_POINT('Ctrl Pts',(-53.9569129454769,4.01884855082893,0.769273135614399));
#51810=CARTESIAN_POINT('Ctrl Pts',(-53.7580394137793,1.52541097180728,3.79684687586526));
#51811=CARTESIAN_POINT('Ctrl Pts',(-53.5591658820819,-2.36957734019541,
3.33586991060956));
#51812=CARTESIAN_POINT('Ctrl Pts',(-53.3602923503844,-4.0873931266384,-0.190111177964406));
#51813=CARTESIAN_POINT('Ctrl Pts',(-53.161418818687,-2.04970371579381,-3.5414177258746));
#51814=CARTESIAN_POINT('Ctrl Pts',(-52.9625452869895,1.87125767772255,-3.63886239575533));
#51815=CARTESIAN_POINT('Ctrl Pts',(-52.7636717552921,4.07290367474537,-0.392912824839691));
#51816=CARTESIAN_POINT('Ctrl Pts',(-52.5647982235946,2.53235741263075,3.2140458562957));
#51817=CARTESIAN_POINT('Ctrl Pts',(-52.3659246918972,-1.33492403982889,
3.8679326053545));
#51818=CARTESIAN_POINT('Ctrl Pts',(-52.1670511601997,-3.97567454353092,
0.967954934693781));
#51819=CARTESIAN_POINT('Ctrl Pts',(-51.9681776285023,-2.96356711349329,
-2.82138171743897));
#51820=CARTESIAN_POINT('Ctrl Pts',(-51.7693040968048,0.771471865433048,
-4.01842705452308));
#51821=CARTESIAN_POINT('Ctrl Pts',(-51.5704305651073,3.79768091035748,-1.52333336298533));
#51822=CARTESIAN_POINT('Ctrl Pts',(-51.37155703341,3.3345729371714,2.37140215028196));
#51823=CARTESIAN_POINT('Ctrl Pts',(-51.1726835017124,-0.192347497474924,
4.08728849873519));
#51824=CARTESIAN_POINT('Ctrl Pts',(-50.9738099700151,-3.54253865649944,
2.04776578223315));
#51825=CARTESIAN_POINT('Ctrl Pts',(-50.7749364383174,-3.63783802413481,
-1.87324833960604));
#51826=CARTESIAN_POINT('Ctrl Pts',(-50.5760629066202,-0.390684345722062,
-4.07311804072575));
#51827=CARTESIAN_POINT('Ctrl Pts',(-50.3771893749225,3.21543091172149,-2.53059852280511));
#51828=CARTESIAN_POINT('Ctrl Pts',(-50.1783158432253,3.86720164531933,1.33704011387727));
#51829=CARTESIAN_POINT('Ctrl Pts',(-49.9794423115276,0.965779566778829,
3.97620354862152));
#51830=CARTESIAN_POINT('Ctrl Pts',(-49.7805687798304,-2.82300276072682,
2.96202299866266));
#51831=CARTESIAN_POINT('Ctrl Pts',(-49.5816952481327,-4.01800435528252,
-0.773670364308027));
#51832=CARTESIAN_POINT('Ctrl Pts',(-49.3828217164354,-1.52125529814649,
-3.79851380799636));
#51833=CARTESIAN_POINT('Ctrl Pts',(-49.1839481847379,2.37322625047831,-3.33327496551342));
#51834=CARTESIAN_POINT('Ctrl Pts',(-48.9850746530405,4.08718264728328,0.194583759405334));
#51835=CARTESIAN_POINT('Ctrl Pts',(-48.786201121343,2.04582723566432,3.54365852664896));
#51836=CARTESIAN_POINT('Ctrl Pts',(-48.5873275896455,-1.87523844072396,
3.63681256351067));
#51837=CARTESIAN_POINT('Ctrl Pts',(-48.3884540579481,-4.07333118739941,
0.388455749651265));
#51838=CARTESIAN_POINT('Ctrl Pts',(-48.1895805262506,-2.5288388754331,-3.21681500459317));
#51839=CARTESIAN_POINT('Ctrl Pts',(-47.9907069945532,1.33915578767652,-3.86646952761948));
#51840=CARTESIAN_POINT('Ctrl Pts',(-47.7918334628557,3.97673136341719,-0.963603909753304));
#51841=CARTESIAN_POINT('Ctrl Pts',(-47.5929599311583,2.96047799713676,2.82462295893575));
#51842=CARTESIAN_POINT('Ctrl Pts',(-47.3940863994608,-0.775868631581208,
4.01758045323378));
#51843=CARTESIAN_POINT('Ctrl Pts',(-47.1952128677634,-3.79934556853258,
1.51917677791285));
#51844=CARTESIAN_POINT('Ctrl Pts',(-46.9963393360659,-3.33197599602417,
-2.37504964023841));
#51845=CARTESIAN_POINT('Ctrl Pts',(-46.7974658043685,0.196819963086194,
-4.08707557231434));
#51846=CARTESIAN_POINT('Ctrl Pts',(-46.598592272671,3.54477733598791,-2.04388807666766));
#51847=CARTESIAN_POINT('Ctrl Pts',(-46.3997187409736,3.63578601418986,1.87722798048059));
#51848=CARTESIAN_POINT('Ctrl Pts',(-46.2008452092761,0.386227037294444,
4.07354311470255));
#51849=CARTESIAN_POINT('Ctrl Pts',(-46.0019716775787,-3.2181981344964,2.52707847104148));
#51850=CARTESIAN_POINT('Ctrl Pts',(-45.8030981458811,-3.8657362524741,-1.34127106059329));
#51851=CARTESIAN_POINT('Ctrl Pts',(-45.6042246141838,-0.961427964268491,
-3.97725798775995));
#51852=CARTESIAN_POINT('Ctrl Pts',(-45.4053510824863,2.82624231158073,-2.95893210937808));
#51853=CARTESIAN_POINT('Ctrl Pts',(-45.2064775507888,4.01715534850376,0.778066666594522));
#51854=CARTESIAN_POINT('Ctrl Pts',(-45.0076040190914,1.51709780290662,3.80017619171714));
#51855=CARTESIAN_POINT('Ctrl Pts',(-44.8087304873939,-2.37687231901642,
3.33067602909248));
#51856=CARTESIAN_POINT('Ctrl Pts',(-44.6098569556966,-4.08696727386044,
-0.199056107848081));
#51857=CARTESIAN_POINT('Ctrl Pts',(-44.4109834239989,-2.04194830582366,
-3.54589508418139));
#51858=CARTESIAN_POINT('Ctrl Pts',(-44.2121098923016,1.87921695828035,-3.6347583764797));
#51859=CARTESIAN_POINT('Ctrl Pts',(-44.013236360604,4.07375382257173,-0.383998209318782));
#51860=CARTESIAN_POINT('Ctrl Pts',(-43.8143628289067,2.52531731015724,3.21958030101716));
#51861=CARTESIAN_POINT('Ctrl Pts',(-43.6154892972092,-1.34338593199437,
3.86500182010269));
#51862=CARTESIAN_POINT('Ctrl Pts',(-43.4166157655118,-3.97778342149215,
0.959251730975778));
#51863=CARTESIAN_POINT('Ctrl Pts',(-43.2177422338142,-2.95738533584939,
-2.82786081817702));
#51864=CARTESIAN_POINT('Ctrl Pts',(-43.0188687021169,0.780264468689989,
-4.0167290412197));
#51865=CARTESIAN_POINT('Ctrl Pts',(-42.8199951704193,3.80100567730137,-1.51501837375015));
#51866=CARTESIAN_POINT('Ctrl Pts',(-42.621121638722,3.32937506510755,2.37869428626672));
#51867=CARTESIAN_POINT('Ctrl Pts',(-42.4222481070244,-0.201292193021611,
4.08685775195398));
#51868=CARTESIAN_POINT('Ctrl Pts',(-42.223374575327,-3.54701177089477,2.04000792371299));
#51869=CARTESIAN_POINT('Ctrl Pts',(-42.0245010436295,-3.63372965068782,
-1.88120537352782));
#51870=CARTESIAN_POINT('Ctrl Pts',(-41.8256275119322,-0.381769266391471,
-4.07396331094387));
#51871=CARTESIAN_POINT('Ctrl Pts',(-41.6267539802346,3.22096150374165,-2.52355539330758));
#51872=CARTESIAN_POINT('Ctrl Pts',(-41.4278804485373,3.86426623072513,1.34550040124665));
#51873=CARTESIAN_POINT('Ctrl Pts',(-41.2290069168397,0.957075210526619,
3.97830766445649));
#51874=CARTESIAN_POINT('Ctrl Pts',(-41.0301333851423,-2.82947847824009,
2.95583767701373));
#51875=CARTESIAN_POINT('Ctrl Pts',(-40.8312598534449,-4.01630153150924,
-0.782462037209674));
#51876=CARTESIAN_POINT('Ctrl Pts',(-40.6323863217473,-1.51293849106592,
-3.801834025037));
#51877=CARTESIAN_POINT('Ctrl Pts',(-40.43351279005,2.38051554144388,-3.32807310445879));
#51878=CARTESIAN_POINT('Ctrl Pts',(-40.2346392583525,4.08674700662777,0.203528217937388));
#51879=CARTESIAN_POINT('Ctrl Pts',(-40.0357657266551,2.03806693091652,3.54812739579378));
#51880=CARTESIAN_POINT('Ctrl Pts',(-39.8368921949575,-1.88319322562777,
3.63269983712218));
#51881=CARTESIAN_POINT('Ctrl Pts',(-39.6380186632601,-4.07417157975626,
0.379540209179764));
#51882=CARTESIAN_POINT('Ctrl Pts',(-39.4391451315626,-2.52179272101996,
-3.22234174225643));
#51883=CARTESIAN_POINT('Ctrl Pts',(-39.2402715998652,1.34761446771718,-3.86352948456161));
#51884=CARTESIAN_POINT('Ctrl Pts',(-39.0413980681678,3.97883071649604,-0.954898403572573));
#51885=CARTESIAN_POINT('Ctrl Pts',(-38.8425245364703,2.9542891333344,2.8310952912857));
#51886=CARTESIAN_POINT('Ctrl Pts',(-38.6436510047728,-0.784659371495732,
4.01587281950036));
#51887=CARTESIAN_POINT('Ctrl Pts',(-38.4447774730754,-3.80266123467603,
1.51085815547656));
#51888=CARTESIAN_POINT('Ctrl Pts',(-38.2459039413779,-3.32677014753596,
-2.38233608400271));
#51889=CARTESIAN_POINT('Ctrl Pts',(-38.0470304096805,0.205764181926051,
-4.08663503791495));
#51890=CARTESIAN_POINT('Ctrl Pts',(-37.848156877983,3.54924195854446,-2.03612532801529));
#51891=CARTESIAN_POINT('Ctrl Pts',(-37.6492833462856,3.63166893609104,1.88518051398512));
#51892=CARTESIAN_POINT('Ctrl Pts',(-37.4504098145881,0.377311038351019,
4.0743786289465));
#51893=CARTESIAN_POINT('Ctrl Pts',(-37.2515362828907,-3.22372101614827,
2.5200292938221));
#51894=CARTESIAN_POINT('Ctrl Pts',(-37.0526627511932,-3.86279158183273,
-1.34972813077302));
#51895=CARTESIAN_POINT('Ctrl Pts',(-36.8537892194958,-0.952721310765272,
-3.97935257745422));
#51896=CARTESIAN_POINT('Ctrl Pts',(-36.6549156877983,2.83271125682985,-2.95273970527496));
#51897=CARTESIAN_POINT('Ctrl Pts',(-36.4560421561009,4.01544290532138,0.786856470890383));
#51898=CARTESIAN_POINT('Ctrl Pts',(-36.2571686244033,1.50877736760482,3.80348730597083));
#51899=CARTESIAN_POINT('Ctrl Pts',(-36.058295092706,-2.38415591339822,3.32546619472911));
#51900=CARTESIAN_POINT('Ctrl Pts',(-35.8594215610084,-4.08652184584904,
-0.208000084318258));
#51901=CARTESIAN_POINT('Ctrl Pts',(-35.6605480293111,-2.03418311559052,
-3.55035545881314));
#51902=CARTESIAN_POINT('Ctrl Pts',(-35.4616744976136,1.88716723800497,-3.63063694790301));
#51903=CARTESIAN_POINT('Ctrl Pts',(-35.2628009659162,4.07458445845272,-0.375081754572397));
#51904=CARTESIAN_POINT('Ctrl Pts',(-35.0639274342186,2.51826511224174,3.22509932500437));
#51905=CARTESIAN_POINT('Ctrl Pts',(-34.8650539025213,-1.35184138978157,
3.86205252275927));
#51906=CARTESIAN_POINT('Ctrl Pts',(-34.6661803708237,-3.97987324717481,
0.950543932756447));
#51907=CARTESIAN_POINT('Ctrl Pts',(-34.4673068391263,-2.95118939329924,
-2.83432637438878));
#51908=CARTESIAN_POINT('Ctrl Pts',(-34.2684333074289,0.789053334735911,
-4.015011789101));
#51909=CARTESIAN_POINT('Ctrl Pts',(-34.0695597757314,3.80431223867413,-1.50669612807361));
#51910=CARTESIAN_POINT('Ctrl Pts',(-33.870686244034,3.32416124642858,2.38597502908564));
#51911=CARTESIAN_POINT('Ctrl Pts',(-33.6718127123365,-0.210235924444678,
4.08640743046392));
#51912=CARTESIAN_POINT('Ctrl Pts',(-33.4729391806391,-3.5514678962665,2.03224029422364));
#51913=CARTESIAN_POINT('Ctrl Pts',(-33.2740656489416,-3.62960387286703,
-1.88915339709258));
#51914=CARTESIAN_POINT('Ctrl Pts',(-33.0751921172442,-0.372852358511318,
-4.07478906821323));
#51915=CARTESIAN_POINT('Ctrl Pts',(-32.8763185855467,3.22647666841207,-2.51650017680708));
#51916=CARTESIAN_POINT('Ctrl Pts',(-32.6774450538492,3.86131230756254,1.35395424411015));
#51917=CARTESIAN_POINT('Ctrl Pts',(-32.4785715221518,0.9483662701979,3.98039272550194));
#51918=CARTESIAN_POINT('Ctrl Pts',(-32.2796979904543,-2.83594064347902,
2.94963819787132));
#51919=CARTESIAN_POINT('Ctrl Pts',(-32.0808244587569,-4.01457947096827,
-0.791249962374674));
#51920=CARTESIAN_POINT('Ctrl Pts',(-31.8819509270594,-1.50461443750595,
-3.80513603253898));
#51921=CARTESIAN_POINT('Ctrl Pts',(-31.683077395362,2.3877934305204,-3.32285530302501));
#51922=CARTESIAN_POINT('Ctrl Pts',(-31.4842038636645,4.08629179179384,0.212471701636003));
#51923=CARTESIAN_POINT('Ctrl Pts',(-31.285330331967,2.03029686449623,3.55257927057153));
#51924=CARTESIAN_POINT('Ctrl Pts',(-31.0864568002696,-1.89113899065338,
3.62856971129236));
#51925=CARTESIAN_POINT('Ctrl Pts',(-30.8875832685721,-4.07499245816681,
0.370622850835159));
#51926=CARTESIAN_POINT('Ctrl Pts',(-30.6887097368747,-2.51473448804646,
-3.22785304595907));
#51927=CARTESIAN_POINT('Ctrl Pts',(-30.4898362051772,1.35606669312626,-3.86057093646411));
#51928=CARTESIAN_POINT('Ctrl Pts',(-30.2909626734798,3.98091101228011,-0.946188323741529));
#51929=CARTESIAN_POINT('Ctrl Pts',(-30.0920891417823,2.94808611945558,2.83755406361732));
#51930=CARTESIAN_POINT('Ctrl Pts',(-29.8932156100849,-0.793446353149102,
4.01414595105263));
#51931=CARTESIAN_POINT('Ctrl Pts',(-29.6943420783874,-3.80595868731876,
1.50253229652499));
#51932=CARTESIAN_POINT('Ctrl Pts',(-29.49546854669,-3.32154836490935,-2.38961111715816));
#51933=CARTESIAN_POINT('Ctrl Pts',(-29.2965950149925,0.214707415222938,
-4.08617492987343));
#51934=CARTESIAN_POINT('Ctrl Pts',(-29.0977214832951,3.55368958139554,-2.02835282699007));
#51935=CARTESIAN_POINT('Ctrl Pts',(-28.8988479515976,3.62753446348856,1.89312401809299));
#51936=CARTESIAN_POINT('Ctrl Pts',(-28.6999744199002,0.368393232211336,
4.07519462825255));
#51937=CARTESIAN_POINT('Ctrl Pts',(-28.5011008882027,-3.22922845723333,
2.51296804648844));
#51938=CARTESIAN_POINT('Ctrl Pts',(-28.3022273565053,-3.85982840968593,
-1.35817873619754));
#51939=CARTESIAN_POINT('Ctrl Pts',(-28.1033538248078,-0.944010094039302,
-3.98142810735417));
#51940=CARTESIAN_POINT('Ctrl Pts',(-27.9044802931104,2.83916663432068,-2.94653315851663));
#51941=CARTESIAN_POINT('Ctrl Pts',(-27.7056067614129,4.01371122948384,0.795642506401697));
#51942=CARTESIAN_POINT('Ctrl Pts',(-27.5067332297155,1.50044970575405,3.80678020276722));
#51943=CARTESIAN_POINT('Ctrl Pts',(-27.307859698018,-2.39142808845478,3.32024043247283));
#51944=CARTESIAN_POINT('Ctrl Pts',(-27.1089861663205,-4.08605684473766,
-0.216943064536219));
#51945=CARTESIAN_POINT('Ctrl Pts',(-26.9101126346231,-2.02640818228711,
-3.55479882840614));
#51946=CARTESIAN_POINT('Ctrl Pts',(-26.7112391029256,1.89510847881717,-3.62649812976556));
#51947=CARTESIAN_POINT('Ctrl Pts',(-26.5123655712282,4.07539557840993,-0.366163503307297));
#51948=CARTESIAN_POINT('Ctrl Pts',(-26.3134920395307,2.51120085266183,3.23060290182313));
#51949=CARTESIAN_POINT('Ctrl Pts',(-26.1146185078333,-1.36029037269174,
3.85908472745028));
#51950=CARTESIAN_POINT('Ctrl Pts',(-25.9157449761358,-3.9819440105693,0.941831581743292));
#51951=CARTESIAN_POINT('Ctrl Pts',(-25.7168714444383,-2.94497931551936,
-2.84077835510638));
#51952=CARTESIAN_POINT('Ctrl Pts',(-25.5179979127409,0.797838421475032,
-4.01327530639203));
#51953=CARTESIAN_POINT('Ctrl Pts',(-25.3191243810434,3.80760057863841,-1.49836666581655));
#51954=CARTESIAN_POINT('Ctrl Pts',(-25.120250849346,3.31893150610698,2.39324434386635));
#51955=CARTESIAN_POINT('Ctrl Pts',(-24.9213773176485,-0.219178648906594,
4.08593753642188));
#51956=CARTESIAN_POINT('Ctrl Pts',(-24.7225037859511,-3.55590701127126,
2.0244629309695));
#51957=CARTESIAN_POINT('Ctrl Pts',(-24.5236302542536,-3.62546071043357,
-1.89709237223187));
#51958=CARTESIAN_POINT('Ctrl Pts',(-24.3247567225562,-0.363933664790518,
-4.07559530857881));
#51959=CARTESIAN_POINT('Ctrl Pts',(-24.1258831908587,3.23197637931701,-2.50943290709563));
#51960=CARTESIAN_POINT('Ctrl Pts',(-23.9270096591613,3.85833988997977,1.36240160197672));
#51961=CARTESIAN_POINT('Ctrl Pts',(-23.7281361274638,0.939652787505642,
3.9824587217711));
#51962=CARTESIAN_POINT('Ctrl Pts',(-23.5292625957663,-2.84238922549196,
2.94342459092891));
#51963=CARTESIAN_POINT('Ctrl Pts',(-23.3303890640689,-4.01283818190772,
-0.800034097711746));
#51964=CARTESIAN_POINT('Ctrl Pts',(-23.1315155323714,-1.49628317733607,
-3.80841981468678));
#51965=CARTESIAN_POINT('Ctrl Pts',(-22.932642000674,2.39505988284916,-3.31762158620365));
#51966=CARTESIAN_POINT('Ctrl Pts',(-22.7337684689765,4.08581700496182,0.221414167664817));
#51967=CARTESIAN_POINT('Ctrl Pts',(-22.5348949372791,2.02251707361955,3.55701412965921));
#51968=CARTESIAN_POINT('Ctrl Pts',(-22.3360214055816,-1.8990756977432,3.62442220580315));
#51969=CARTESIAN_POINT('Ctrl Pts',(-22.1371478738842,-4.0757938186994,0.361703717328525));
#51970=CARTESIAN_POINT('Ctrl Pts',(-21.9382743421867,-2.50766421031908,
-3.23334888930383));
#51971=CARTESIAN_POINT('Ctrl Pts',(-21.7394008104893,1.36451242342049,-3.85759389749737));
#51972=CARTESIAN_POINT('Ctrl Pts',(-21.5405272787918,3.98297224080547,-0.937473711978594));
#51973=CARTESIAN_POINT('Ctrl Pts',(-21.3416537470944,2.9418689852107,2.84399924499518));
#51974=CARTESIAN_POINT('Ctrl Pts',(-21.1427802153969,-0.80222953445455,
4.01239985616173));
#51975=CARTESIAN_POINT('Ctrl Pts',(-20.9439066836995,-3.80923791066707,
1.4941992409363));
#51976=CARTESIAN_POINT('Ctrl Pts',(-20.745033152002,-3.31631067315495,-2.39687470485972));
#51977=CARTESIAN_POINT('Ctrl Pts',(-20.5461596203046,0.22364962014169,-4.08569525039353));
#51978=CARTESIAN_POINT('Ctrl Pts',(-20.3472860886071,3.55812018323851,-2.02057061081977));
#51979=CARTESIAN_POINT('Ctrl Pts',(-20.1484125569097,3.6233826161852,1.90105845475743));
#51980=CARTESIAN_POINT('Ctrl Pts',(-19.9495390252122,0.359473661588844,
4.07599110871226));
#51981=CARTESIAN_POINT('Ctrl Pts',(-19.7506654935147,-3.2347204313727,2.50589476286167));
#51982=CARTESIAN_POINT('Ctrl Pts',(-19.5517919618173,-3.85684675022641,
-1.36662283639115));
#51983=CARTESIAN_POINT('Ctrl Pts',(-19.3529184301198,-0.935294355814451,
-3.98348456751868));
#51984=CARTESIAN_POINT('Ctrl Pts',(-19.1540448984224,2.84560841313408,-2.94031249883042));
#51985=CARTESIAN_POINT('Ctrl Pts',(-18.9551713667249,4.0119603292853,0.804424731046237));
#51986=CARTESIAN_POINT('Ctrl Pts',(-18.7562978350274,1.49211485724107,3.81005486633438));
#51987=CARTESIAN_POINT('Ctrl Pts',(-18.55742430333,-2.39868880935476,3.31499876735332));
#51988=CARTESIAN_POINT('Ctrl Pts',(-18.3585507716326,-4.0855722727535,-0.225885005668014));
#51989=CARTESIAN_POINT('Ctrl Pts',(-18.1596772399351,-2.01862354315282,
-3.5592251716781));
#51990=CARTESIAN_POINT('Ctrl Pts',(-17.9608037082376,1.90304064268095,-3.6223419418909));
#51991=CARTESIAN_POINT('Ctrl Pts',(-17.7619301765402,4.07618717855833,-0.357243498239154));
#51992=CARTESIAN_POINT('Ctrl Pts',(-17.5630566448428,2.50412456525315,3.23609100511305));
#51993=CARTESIAN_POINT('Ctrl Pts',(-17.3641831131453,-1.36873284025696,
3.85609844839054));
#51994=CARTESIAN_POINT('Ctrl Pts',(-17.1653095814478,-3.98399570175737,
0.933114719665619));
#51995=CARTESIAN_POINT('Ctrl Pts',(-16.9664360497504,-2.93875513225399,
-2.84721672942694));
#51996=CARTESIAN_POINT('Ctrl Pts',(-16.7675625180529,0.806619686829663,
-4.01151960141));
#51997=CARTESIAN_POINT('Ctrl Pts',(-16.5686889863555,3.81087068144415,-1.49003002687437));
#51998=CARTESIAN_POINT('Ctrl Pts',(-16.369815454658,3.31368586919149,2.40050219579121));
#51999=CARTESIAN_POINT('Ctrl Pts',(-16.1709419229606,-0.22812032357462,
4.08544807207852));
#52000=CARTESIAN_POINT('Ctrl Pts',(-15.9720683912631,-3.56032909464717,
2.01667587120158));
#52001=CARTESIAN_POINT('Ctrl Pts',(-15.7731948595656,-3.6213001832318,-1.90502226092053));
#52002=CARTESIAN_POINT('Ctrl Pts',(-15.5743213278682,-0.355013227946878,
-4.07638202817894));
#52003=CARTESIAN_POINT('Ctrl Pts',(-15.3754477961708,3.2374606101146,-2.50235361802328));
#52004=CARTESIAN_POINT('Ctrl Pts',(-15.1765742644733,3.85534899221378,1.37084243438626));
#52005=CARTESIAN_POINT('Ctrl Pts',(-14.9777007327758,0.93093480418458,3.98450564336853));
#52006=CARTESIAN_POINT('Ctrl Pts',(-14.7788272010784,-2.84882419339231,
2.93719688594763));
#52007=CARTESIAN_POINT('Ctrl Pts',(-14.5799536693809,-4.01107767266776,
-0.808814401147756));
#52008=CARTESIAN_POINT('Ctrl Pts',(-14.3810801376835,-1.48794475046029,
-3.81168535575216));
#52009=CARTESIAN_POINT('Ctrl Pts',(-14.182206605986,2.40231486362624,-3.31237197906248));
#52010=CARTESIAN_POINT('Ctrl Pts',(-13.9833330742886,4.08532264840576,0.230355573192351));
#52011=CARTESIAN_POINT('Ctrl Pts',(-13.7844595425911,2.01472759554911,3.56143195181527));
#52012=CARTESIAN_POINT('Ctrl Pts',(-13.5855860108937,-1.90700330888289,
3.62025734051975));
#52013=CARTESIAN_POINT('Ctrl Pts',(-13.3867124791962,-4.07657565751574,
0.352782851379752));
#52014=CARTESIAN_POINT('Ctrl Pts',(-13.1878389474988,-2.50058192170229,
-3.23882924596736));
#52015=CARTESIAN_POINT('Ctrl Pts',(-12.9889654158013,1.37295161814754,-3.85459838192047));
#52016=CARTESIAN_POINT('Ctrl Pts',(-12.7900918841038,3.9850143921995,-0.928754610023908));
#52017=CARTESIAN_POINT('Ctrl Pts',(-12.5912183524064,2.9356377603778,2.85043080454899));
#52018=CARTESIAN_POINT('Ctrl Pts',(-12.3923448207089,-0.811008873343517,
4.01063454319088));
#52019=CARTESIAN_POINT('Ctrl Pts',(-12.1934712890115,-3.81249888901455,
1.48585902862307));
#52020=CARTESIAN_POINT('Ctrl Pts',(-11.994597757314,-3.31105709735959,-2.4041268123172));
#52021=CARTESIAN_POINT('Ctrl Pts',(-11.7957242256166,0.23259075385208,-4.08519600177279));
#52022=CARTESIAN_POINT('Ctrl Pts',(-11.5968506939191,3.56253374285225,-2.01277871677862));
#52023=CARTESIAN_POINT('Ctrl Pts',(-11.3979771622217,3.61921341406693,1.908983785975));
#52024=CARTESIAN_POINT('Ctrl Pts',(-11.1991036305242,0.350552369205444,
4.07676806651077));
#52025=CARTESIAN_POINT('Ctrl Pts',(-11.0002300988268,-3.24019691226161,
2.49880947682055));
#52026=CARTESIAN_POINT('Ctrl Pts',(-10.8013565671293,-3.85384661773532,
-1.3750603909094));
#52027=CARTESIAN_POINT('Ctrl Pts',(-10.6024830354319,-0.926574137836242,
-3.985521948098));
#52028=CARTESIAN_POINT('Ctrl Pts',(-10.4036095037344,2.85203656241603,-2.93407775601124));
#52029=CARTESIAN_POINT('Ctrl Pts',(-10.204735972037,4.010190213112,0.813203102760025));
#52030=CARTESIAN_POINT('Ctrl Pts',(-10.0058624403395,1.48377286198708,3.81331128098776));
#52031=CARTESIAN_POINT('Ctrl Pts',(-9.80698890864205,-2.40593804132169,
3.30974122447646));
#52032=CARTESIAN_POINT('Ctrl Pts',(-9.60811537694457,-4.08506813221747,
-0.234825864884617));
#52033=CARTESIAN_POINT('Ctrl Pts',(-9.40924184524715,-2.01082923547359,
-3.56363446742823));
#52034=CARTESIAN_POINT('Ctrl Pts',(-9.21036831354969,1.91096369160394,-3.61816840418592));
#52035=CARTESIAN_POINT('Ctrl Pts',(-9.01149478185224,4.07695925510639,-0.348321782091731));
#52036=CARTESIAN_POINT('Ctrl Pts',(-8.81262125015477,2.4970362839087,3.24156360858787));
#52037=CARTESIAN_POINT('Ctrl Pts',(-8.61374771845734,-1.37716875204044,
3.85309369988341));
#52038=CARTESIAN_POINT('Ctrl Pts',(-8.41487418675986,-3.98602831091206,
0.924393388274425));
#52039=CARTESIAN_POINT('Ctrl Pts',(-8.21600065506242,-2.93251687331501,
-2.85364146651265));
#52040=CARTESIAN_POINT('Ctrl Pts',(-8.01712712336496,0.81539708874029,-4.00974468256414));
#52041=CARTESIAN_POINT('Ctrl Pts',(-7.8182535916675,3.81412253142865,-1.481686251177));
#52042=CARTESIAN_POINT('Ctrl Pts',(-7.61938005997007,3.30842436080689,2.40774855009751));
#52043=CARTESIAN_POINT('Ctrl Pts',(-7.4205065282726,-0.237060905620641,
4.08493903977805));
#52044=CARTESIAN_POINT('Ctrl Pts',(-7.22163299657515,-3.56473412521439,
2.00887915221773));
#52045=CARTESIAN_POINT('Ctrl Pts',(-7.0227594648777,-3.61712231118831,-1.91294302517764));
#52046=CARTESIAN_POINT('Ctrl Pts',(-6.82388593318022,-0.346091090708137,
-4.07714922324453));
#52047=CARTESIAN_POINT('Ctrl Pts',(-6.6250124014828,3.24292933454114,-2.49526234349918));
#52048=CARTESIAN_POINT('Ctrl Pts',(-6.42613886978531,3.85233962858262,1.37927670091363));
#52049=CARTESIAN_POINT('Ctrl Pts',(-6.22726533808788,0.92221236200472,3.98653348048341));
#52050=CARTESIAN_POINT('Ctrl Pts',(-6.0283918063904,-2.85524551638475,2.93095511276885));
#52051=CARTESIAN_POINT('Ctrl Pts',(-5.82951827469298,-4.0092979516314,-0.81759083065191));
#52052=CARTESIAN_POINT('Ctrl Pts',(-5.63064474299553,-1.47959919691017,
-3.81493264004876));
#52053=CARTESIAN_POINT('Ctrl Pts',(-5.43177121129806,2.40955833827837,-3.30710650683126));
#52054=CARTESIAN_POINT('Ctrl Pts',(-5.23289767960062,4.08480872416158,0.239295875554097));
#52055=CARTESIAN_POINT('Ctrl Pts',(-5.03402414790315,2.00692846822076,3.56583271557382));
#52056=CARTESIAN_POINT('Ctrl Pts',(-4.83515061620571,-1.91492178728529,
3.61607513596826));
#52057=CARTESIAN_POINT('Ctrl Pts',(-4.63627708450823,-4.07733796863674,
0.343860294625829));
#52058=CARTESIAN_POINT('Ctrl Pts',(-4.43740355281079,-2.49348766033667,
-3.24429408764104));
#52059=CARTESIAN_POINT('Ctrl Pts',(-4.23853002111333,1.38138424485284,-3.85158440796985));
#52060=CARTESIAN_POINT('Ctrl Pts',(-4.03965648941587,3.98703744163902,-0.920031052295885));
#52061=CARTESIAN_POINT('Ctrl Pts',(-3.84078295771845,2.92939250320468,2.85684869760832));
#52062=CARTESIAN_POINT('Ctrl Pts',(-3.64190942602098,-0.819784381395129,
4.00885004677589));
#52063=CARTESIAN_POINT('Ctrl Pts',(-3.44303589432354,-3.81574150547896,
1.47751165009818));
#52064=CARTESIAN_POINT('Ctrl Pts',(-3.24416236262606,-3.30578785389167,
-2.41136731145358));
#52065=CARTESIAN_POINT('Ctrl Pts',(-3.04528883092862,0.241531134563617,
-4.08467736265059));
#52066=CARTESIAN_POINT('Ctrl Pts',(-2.84641529923116,3.56692955739015,-2.00497684939494));
#52067=CARTESIAN_POINT('Ctrl Pts',(-2.6475417675337,3.61502816430448,1.91689934540635));
#52068=CARTESIAN_POINT('Ctrl Pts',(-2.44866823583624,0.341626967292691,
4.07752668443549));
#52069=CARTESIAN_POINT('Ctrl Pts',(-2.24979470413878,-3.24565328439454,
2.49170998193123));
#52070=CARTESIAN_POINT('Ctrl Pts',(-2.05092117244136,-3.85083669206714,
-1.38348712906526));
#52071=CARTESIAN_POINT('Ctrl Pts',(-1.85204764074388,-0.917833119671589,
-3.98754822695286));
#52072=CARTESIAN_POINT('Ctrl Pts',(-1.65317410904645,2.85842015619851,-2.92781387766021));
#52073=CARTESIAN_POINT('Ctrl Pts',(-1.45430057734898,4.00845922597162,0.82194910102392));
#52074=CARTESIAN_POINT('Ctrl Pts',(-1.25542704565154,1.47531360750824,3.81660320507337));
#52075=CARTESIAN_POINT('Ctrl Pts',(-1.05655351395407,-2.41296774955078,
3.30436628639575));
#52076=CARTESIAN_POINT('Ctrl Pts',(-0.857679982256626,-4.08493725274729,
-0.243573813186974));
#52077=CARTESIAN_POINT('Ctrl Pts',(-0.658806450559161,-2.00228289876901,
-3.56838925950682));
#52078=CARTESIAN_POINT('Ctrl Pts',(-0.459932918861702,1.91747039222746,
-3.61328939493983));
#52079=CARTESIAN_POINT('Ctrl Pts',(-0.261059387164285,4.08041299153864,
-0.340726701072281));
#52080=CARTESIAN_POINT('Ctrl Pts',(-0.0621858554667818,2.48447621485804,
3.24976209445823));
#52081=CARTESIAN_POINT('Ctrl Pts',(0.0703964989981598,-0.0868243742411749,
3.6454708254482));
#52082=CARTESIAN_POINT('Ctrl Pts',(0.136687676230641,-1.17148016637885,
3.25511512389055));
#52083=CARTESIAN_POINT('Ctrl Pts',(-109.703687676231,-1.64343044862366,
3.31080057131755));
#52084=CARTESIAN_POINT('Ctrl Pts',(-109.637396498998,-2.74664151170901,
2.7631835786059));
#52085=CARTESIAN_POINT('Ctrl Pts',(-109.504814144533,-4.34329544588056,
0.487898524808049));
#52086=CARTESIAN_POINT('Ctrl Pts',(-109.305940612836,-2.75520708479667,
-3.39822806350164));
#52087=CARTESIAN_POINT('Ctrl Pts',(-109.107067081138,1.36785846604787,-4.15091025735692));
#52088=CARTESIAN_POINT('Ctrl Pts',(-108.908193549441,4.23233807130361,-1.09535677627866));
#52089=CARTESIAN_POINT('Ctrl Pts',(-108.709320017743,3.20908102854513,2.96956032317362));
#52090=CARTESIAN_POINT('Ctrl Pts',(-108.510446486046,-0.763185572783635,
4.30448238078623));
#52091=CARTESIAN_POINT('Ctrl Pts',(-108.311572954348,-4.03397135422629,
1.68526123531646));
#52092=CARTESIAN_POINT('Ctrl Pts',(-108.112699422651,-3.59847596118754,
-2.48281775018356));
#52093=CARTESIAN_POINT('Ctrl Pts',(-107.913825890954,0.143380670774777,
-4.3694476002038));
#52094=CARTESIAN_POINT('Ctrl Pts',(-107.714952359256,3.75345958488109,-2.24154240806525));
#52095=CARTESIAN_POINT('Ctrl Pts',(-107.516078827559,3.91487291942144,1.9459613663452));
#52096=CARTESIAN_POINT('Ctrl Pts',(-107.317205295861,0.479281964767665,
4.34547751537191));
#52097=CARTESIAN_POINT('Ctrl Pts',(-107.118331764164,-3.39666841093264,
2.75237818021938));
#52098=CARTESIAN_POINT('Ctrl Pts',(-106.919458232466,-4.15175596517978,
-1.36962150618047));
#52099=CARTESIAN_POINT('Ctrl Pts',(-106.720584700769,-1.09219997809354,
-4.23320504153245));
#52100=CARTESIAN_POINT('Ctrl Pts',(-106.521711169071,2.97087072510216,-3.20731379323168));
#52101=CARTESIAN_POINT('Ctrl Pts',(-106.322837637374,4.30429976488753,0.765465383938776));
#52102=CARTESIAN_POINT('Ctrl Pts',(-106.123964105677,1.68292909980025,4.03493263721933));
#52103=CARTESIAN_POINT('Ctrl Pts',(-105.925090573979,-2.4847201490054,3.59709589973779));
#52104=CARTESIAN_POINT('Ctrl Pts',(-105.726217042282,-4.36940349125203,
-0.145760148682));
#52105=CARTESIAN_POINT('Ctrl Pts',(-105.527343510584,-2.2394698980649,-3.75469136069795));
#52106=CARTESIAN_POINT('Ctrl Pts',(-105.328469978887,1.94809321659027,-3.91380450068533));
#52107=CARTESIAN_POINT('Ctrl Pts',(-105.129596447189,4.34574429399991,-0.476905997778922));
#52108=CARTESIAN_POINT('Ctrl Pts',(-104.930722915492,2.7505165857232,3.39817469839221));
#52109=CARTESIAN_POINT('Ctrl Pts',(-104.731849383794,-1.37189140623665,
4.15100551315273));
#52110=CARTESIAN_POINT('Ctrl Pts',(-104.532975852097,-4.23380275878313,
1.08988393459526));
#52111=CARTESIAN_POINT('Ctrl Pts',(-104.334102320399,-3.20568744261217,
-2.97262523841459));
#52112=CARTESIAN_POINT('Ctrl Pts',(-104.135228788702,0.767820077559129,
-4.30388024007402));
#52113=CARTESIAN_POINT('Ctrl Pts',(-103.936355257005,4.03585293414859,-1.68072123941791));
#52114=CARTESIAN_POINT('Ctrl Pts',(-103.737481725307,3.59573582801791,2.48668788662542));
#52115=CARTESIAN_POINT('Ctrl Pts',(-103.53860819361,-0.148150739858707,
4.3693230767846));
#52116=CARTESIAN_POINT('Ctrl Pts',(-103.339734661912,-3.75591610379247,
2.23741525247945));
#52117=CARTESIAN_POINT('Ctrl Pts',(-103.140861130215,-3.91273803962465,
-1.9502342997724));
#52118=CARTESIAN_POINT('Ctrl Pts',(-102.941987598517,-0.474528230741329,
-4.34600457305979));
#52119=CARTESIAN_POINT('Ctrl Pts',(-102.74311406682,3.39967909088784,-2.74865692107253));
#52120=CARTESIAN_POINT('Ctrl Pts',(-102.544240535122,4.15025428333885,1.37416235372989));
#52121=CARTESIAN_POINT('Ctrl Pts',(-102.345367003425,1.08756731865623,4.23439843639973));
#52122=CARTESIAN_POINT('Ctrl Pts',(-102.146493471728,-2.97437873148058,
3.20406054132907));
#52123=CARTESIAN_POINT('Ctrl Pts',(-101.94761994003,-4.30345949592243,-0.77017475792313));
#52124=CARTESIAN_POINT('Ctrl Pts',(-101.748746408333,-1.67851283933561,
-4.03677190821751));
#52125=CARTESIAN_POINT('Ctrl Pts',(-101.549872876635,2.48865486047723,-3.59437474064827));
#52126=CARTESIAN_POINT('Ctrl Pts',(-101.350999344938,4.36924136459678,0.150541318859443));
#52127=CARTESIAN_POINT('Ctrl Pts',(-101.15212581324,2.23535993168143,3.75713970549685));
#52128=CARTESIAN_POINT('Ctrl Pts',(-100.953252281543,-1.95237479626607,
3.91167041629182));
#52129=CARTESIAN_POINT('Ctrl Pts',(-100.754378749845,-4.34626355264668,
0.472150316872331));
#52130=CARTESIAN_POINT('Ctrl Pts',(-100.555505218148,-2.74679643279182,
-3.40118246314275));
#52131=CARTESIAN_POINT('Ctrl Pts',(-100.356631686451,1.37643288943393,-4.14950181246763));
#52132=CARTESIAN_POINT('Ctrl Pts',(-100.157758154753,4.23499284665589,-1.08525037643902));
#52133=CARTESIAN_POINT('Ctrl Pts',(-99.9588846230556,3.20243268077579,2.97613133377659));
#52134=CARTESIAN_POINT('Ctrl Pts',(-99.7600110913579,-0.772529207668281,
4.30303746370945));
#52135=CARTESIAN_POINT('Ctrl Pts',(-99.5611375596606,-4.0376896738937,1.67630393667729));
#52136=CARTESIAN_POINT('Ctrl Pts',(-99.362264027963,-3.59301257726815,-2.49062108928285));
#52137=CARTESIAN_POINT('Ctrl Pts',(-99.1633904962658,0.152931852785523,
-4.36915834448594));
#52138=CARTESIAN_POINT('Ctrl Pts',(-98.9645169645681,3.75836218248909,-2.2333039417024));
#52139=CARTESIAN_POINT('Ctrl Pts',(-98.7656434328708,3.91060162197971,1.95451470829903));
#52140=CARTESIAN_POINT('Ctrl Pts',(-98.5667699011732,0.469772261664343,
4.34652123116388));
#52141=CARTESIAN_POINT('Ctrl Pts',(-98.367896369476,-3.40268481723872,2.74493512224255));
#52142=CARTESIAN_POINT('Ctrl Pts',(-98.1690228377782,-4.14874809942346,
-1.37870301309521));
#52143=CARTESIAN_POINT('Ctrl Pts',(-97.970149306081,-1.08293310934729,-4.23558598914802));
#52144=CARTESIAN_POINT('Ctrl Pts',(-97.7712757743834,2.97788304515402,-3.20080386155913));
#52145=CARTESIAN_POINT('Ctrl Pts',(-97.5724022426862,4.30261414336226,0.774883426153052));
#52146=CARTESIAN_POINT('Ctrl Pts',(-97.3735287109885,1.67409453220965,4.03860623086893));
#52147=CARTESIAN_POINT('Ctrl Pts',(-97.1746551792912,-2.49258657250956,
3.59164933830304));
#52148=CARTESIAN_POINT('Ctrl Pts',(-96.9757816475936,-4.36907401644734,
-0.155322340930722));
#52149=CARTESIAN_POINT('Ctrl Pts',(-96.7769081158962,-2.23124728317354,
-3.75958353439823));
#52150=CARTESIAN_POINT('Ctrl Pts',(-96.5780345841988,1.95665403523896,-3.90953165701095));
#52151=CARTESIAN_POINT('Ctrl Pts',(-96.3791610525013,4.34677760852986,-0.467394065827876));
#52152=CARTESIAN_POINT('Ctrl Pts',(-96.1802875208038,2.74307298998427,3.40418615272527));
#52153=CARTESIAN_POINT('Ctrl Pts',(-95.9814139891064,-1.38097272403537,
4.14799314443235));
#52154=CARTESIAN_POINT('Ctrl Pts',(-95.7825404574089,-4.23617786369789,
1.08061551807453));
#52155=CARTESIAN_POINT('Ctrl Pts',(-95.5836669257115,-3.19917408416705,
-2.97963386508839));
#52156=CARTESIAN_POINT('Ctrl Pts',(-95.384793394014,0.77723741267289,-4.30218953500764));
#52157=CARTESIAN_POINT('Ctrl Pts',(-95.1859198623165,4.03952157886872,-1.67188462659408));
#52158=CARTESIAN_POINT('Ctrl Pts',(-94.9870463306192,3.5902850241611,2.49455130956892));
#52159=CARTESIAN_POINT('Ctrl Pts',(-94.7881727989216,-0.157712782579426,
4.36898838050624));
#52160=CARTESIAN_POINT('Ctrl Pts',(-94.5892992672242,-3.76080376085868,
2.22918995671049));
#52161=CARTESIAN_POINT('Ctrl Pts',(-94.3904257355267,-3.90846052170578,
-1.95879277644548));
#52162=CARTESIAN_POINT('Ctrl Pts',(-94.1915522038293,-0.465015730074829,
-4.34703268466786));
#52163=CARTESIAN_POINT('Ctrl Pts',(-93.9926786721319,3.40568646915293,-2.74121003657442));
#52164=CARTESIAN_POINT('Ctrl Pts',(-93.7938051404342,4.14723694772034,1.38324202157495));
#52165=CARTESIAN_POINT('Ctrl Pts',(-93.5949316087372,1.07829760331451,4.23676847012835));
#52166=CARTESIAN_POINT('Ctrl Pts',(-93.3960580770393,-2.9813837930556,3.1975433490874));
#52167=CARTESIAN_POINT('Ctrl Pts',(-93.1971845453423,-4.30176363877268,
-0.779591166523121));
#52168=CARTESIAN_POINT('Ctrl Pts',(-92.9983110136444,-1.66967422049213,
-4.04043571761904));
#52169=CARTESIAN_POINT('Ctrl Pts',(-92.7994374819473,2.49651529987284,-3.58891963525074));
#52170=CARTESIAN_POINT('Ctrl Pts',(-92.6005639502496,4.36890143668827,0.16010317701611));
#52171=CARTESIAN_POINT('Ctrl Pts',(-92.4016904185522,2.2271319629291,3.76202286150513));
#52172=CARTESIAN_POINT('Ctrl Pts',(-92.2028168868548,-1.96093093127833,
3.9073882163849));
#52173=CARTESIAN_POINT('Ctrl Pts',(-92.0039433551572,-4.34728645950153,
0.462637255117168));
#52174=CARTESIAN_POINT('Ctrl Pts',(-91.8050698234599,-2.73934626257066,
-3.40718576607261));
#52175=CARTESIAN_POINT('Ctrl Pts',(-91.6061962917623,1.38551090503464,-4.14647950951377));
#52176=CARTESIAN_POINT('Ctrl Pts',(-91.4073227600651,4.23735780826257,-1.07597936576111));
#52177=CARTESIAN_POINT('Ctrl Pts',(-91.2084492283674,3.19591165680837,2.98313282853178));
#52178=CARTESIAN_POINT('Ctrl Pts',(-91.0095756966701,-0.781944686999132,
4.3013364547849));
#52179=CARTESIAN_POINT('Ctrl Pts',(-90.8107021649725,-4.04134864684625,
1.66746331456547));
#52180=CARTESIAN_POINT('Ctrl Pts',(-90.6118286332753,-3.5875531719807,-2.49847854283336));
#52181=CARTESIAN_POINT('Ctrl Pts',(-90.4129551015775,0.162493523525171,
-4.36881318501945));
#52182=CARTESIAN_POINT('Ctrl Pts',(-90.2140815698803,3.76324083597265,-2.22507330244547));
#52183=CARTESIAN_POINT('Ctrl Pts',(-90.0152080381827,3.90631474136929,1.96306849909743));
#52184=CARTESIAN_POINT('Ctrl Pts',(-89.8163345064852,0.460258641666905,
4.34753893295489));
#52185=CARTESIAN_POINT('Ctrl Pts',(-89.617460974788,-3.40868404303548,2.73748166853095));
#52186=CARTESIAN_POINT('Ctrl Pts',(-89.4185874430904,-4.1457208300394,-1.38777937373523));
#52187=CARTESIAN_POINT('Ctrl Pts',(-89.2197139113929,-1.07366080610832,
-4.23794587792415));
#52188=CARTESIAN_POINT('Ctrl Pts',(-89.0208403796957,2.98488097099337,-3.19427900781841));
#52189=CARTESIAN_POINT('Ctrl Pts',(-88.8219668479979,4.30090798317216,0.78429797339638));
#52190=CARTESIAN_POINT('Ctrl Pts',(-88.6230933163007,1.66525190947596,4.04226036627706));
#52191=CARTESIAN_POINT('Ctrl Pts',(-88.4242197846031,-2.50044103786279,
3.58618563476002));
#52192=CARTESIAN_POINT('Ctrl Pts',(-88.2253462529058,-4.36872362552622,
-0.164883821391037));
#52193=CARTESIAN_POINT('Ctrl Pts',(-88.0264727212081,-2.22301397587585,
-3.76445768389663));
#52194=CARTESIAN_POINT('Ctrl Pts',(-87.8275991895109,1.96520547926291,-3.9052400969803));
#52195=CARTESIAN_POINT('Ctrl Pts',(-87.6287256578132,4.34779010495238,-0.457879890436096));
#52196=CARTESIAN_POINT('Ctrl Pts',(-87.4298521261159,2.73561625501344,3.41018129959302));
#52197=CARTESIAN_POINT('Ctrl Pts',(-87.2309785944184,-1.39004742699766,
4.14496090952432));
#52198=CARTESIAN_POINT('Ctrl Pts',(-87.0321050627209,-4.23853267893703,
1.07134192505021));
#52199=CARTESIAN_POINT('Ctrl Pts',(-86.8332315310236,-3.19264540260626,
-2.98662821991703));
#52200=CARTESIAN_POINT('Ctrl Pts',(-86.634357999326,0.786651025010412,-4.30047822406273));
#52201=CARTESIAN_POINT('Ctrl Pts',(-86.4354844676287,4.04317087563854,-1.66304000588559));
#52202=CARTESIAN_POINT('Ctrl Pts',(-86.2366109359312,3.58481702399811,2.50240278437361));
#52203=CARTESIAN_POINT('Ctrl Pts',(-86.0377374042336,-0.16727406989818,
4.36863275823537));
#52204=CARTESIAN_POINT('Ctrl Pts',(-85.8388638725364,-3.76567340491278,
2.22095398383672));
#52205=CARTESIAN_POINT('Ctrl Pts',(-85.6399903408387,-3.90416428353964,
-1.96734187113503));
#52206=CARTESIAN_POINT('Ctrl Pts',(-85.4411168091414,-0.455501002136817,
-4.34803997541882));
#52207=CARTESIAN_POINT('Ctrl Pts',(-85.2422432774438,3.41167753529698,-2.73375002257656));
#52208=CARTESIAN_POINT('Ctrl Pts',(-85.0433697457464,4.14419974819605,1.3923150641429));
#52209=CARTESIAN_POINT('Ctrl Pts',(-84.844496214049,1.06902272328098,4.23911821112559));
#52210=CARTESIAN_POINT('Ctrl Pts',(-84.6456226823515,-2.98837457477973,
3.19101084166095));
#52211=CARTESIAN_POINT('Ctrl Pts',(-84.4467491506541,-4.30004717758527,
-0.789003841136819));
#52212=CARTESIAN_POINT('Ctrl Pts',(-84.2478756189566,-1.66082760445654,
-4.04408017465809));
#52213=CARTESIAN_POINT('Ctrl Pts',(-84.0490020872592,2.50436378177857,-3.58344734010467));
#52214=CARTESIAN_POINT('Ctrl Pts',(-83.8501285555617,4.36854058317413,0.169664268331013));
#52215=CARTESIAN_POINT('Ctrl Pts',(-83.6512550238642,2.21889332694475,3.76688799865721));
#52216=CARTESIAN_POINT('Ctrl Pts',(-83.4523814921669,-1.96947767407428,
3.90308730136935));
#52217=CARTESIAN_POINT('Ctrl Pts',(-83.2535079604693,-4.34828854427934,
0.453121977481246));
#52218=CARTESIAN_POINT('Ctrl Pts',(-83.0546344287718,-2.73188297177902,
-3.41317274969951));
#52219=CARTESIAN_POINT('Ctrl Pts',(-82.8557608970745,1.39458228449222,-4.14343734628245));
#52220=CARTESIAN_POINT('Ctrl Pts',(-82.6568873653769,4.23970247431449,-1.06670320149481));
#52221=CARTESIAN_POINT('Ctrl Pts',(-82.4580138336795,3.18937532547179,2.99012003505869));
#52222=CARTESIAN_POINT('Ctrl Pts',(-82.2591403019821,-0.791356421071236,
4.29961484386878));
#52223=CARTESIAN_POINT('Ctrl Pts',(-82.0602667702846,-4.04498826306357,
1.65861470585109));
#52224=CARTESIAN_POINT('Ctrl Pts',(-81.8613932385872,-3.58207658348971,
-2.50632402949067));
#52225=CARTESIAN_POINT('Ctrl Pts',(-81.6625197068897,0.172054415974101,
-4.36844710037005));
#52226=CARTESIAN_POINT('Ctrl Pts',(-81.4636461751922,3.76810146476629,-2.21683200581681));
#52227=CARTESIAN_POINT('Ctrl Pts',(-81.2647726434949,3.90200915079183,1.97161288744128));
#52228=CARTESIAN_POINT('Ctrl Pts',(-81.0658991117974,0.450742817181481,
4.34853581145962));
#52229=CARTESIAN_POINT('Ctrl Pts',(-80.8670255800998,-3.41466694235303,
2.73001510317963));
#52230=CARTESIAN_POINT('Ctrl Pts',(-80.6681520484026,-4.14267370401169,
-1.39684908736692));
#52231=CARTESIAN_POINT('Ctrl Pts',(-80.4692785167048,-1.0643833603861,-4.24028546832885));
#52232=CARTESIAN_POINT('Ctrl Pts',(-80.2704049850077,2.99186460023139,-3.18773885452838));
#52233=CARTESIAN_POINT('Ctrl Pts',(-80.07153145331,4.29918122304274,0.793708764109494));
#52234=CARTESIAN_POINT('Ctrl Pts',(-79.8726579216127,1.65640131073161,4.04589514058312));
#52235=CARTESIAN_POINT('Ctrl Pts',(-79.6737843899151,-2.5082835269231,3.58070475456353));
#52236=CARTESIAN_POINT('Ctrl Pts',(-79.4749108582177,-4.36835230985113,
-0.174444512111902));
#52237=CARTESIAN_POINT('Ctrl Pts',(-79.2760373265202,-2.21477002106995,
-3.76931380287679));
#52238=CARTESIAN_POINT('Ctrl Pts',(-79.0771637948228,1.97374751059685,-3.90092983212983));
#52239=CARTESIAN_POINT('Ctrl Pts',(-78.8782902631254,4.3487817768856,-0.448363521949776));
#52240=CARTESIAN_POINT('Ctrl Pts',(-78.6794167314278,2.7281464173376,3.41616011281022));
#52241=CARTESIAN_POINT('Ctrl Pts',(-78.4805431997305,-1.39911547208838,
4.14190882161239));
#52242=CARTESIAN_POINT('Ctrl Pts',(-78.2816696680329,-4.24086719299416,
1.06206320064932));
#52243=CARTESIAN_POINT('Ctrl Pts',(-78.0827961363356,-3.18610142932061,
-2.9936082697756));
#52244=CARTESIAN_POINT('Ctrl Pts',(-77.883922604638,0.796060869547362,-4.29874631523692));
#52245=CARTESIAN_POINT('Ctrl Pts',(-77.6850490729406,4.04680080694526,-1.65418741976074));
#52246=CARTESIAN_POINT('Ctrl Pts',(-77.4861755412432,3.57933185373683,2.51024227348926));
#52247=CARTESIAN_POINT('Ctrl Pts',(-77.2873020095457,-0.176834556028938,
4.36825621164575));
#52248=CARTESIAN_POINT('Ctrl Pts',(-77.0884284778483,-3.77052501262576,
2.21270737332146));
#52249=CARTESIAN_POINT('Ctrl Pts',(-76.8895549461508,-3.89984934570645,
-1.97588154290197));
#52250=CARTESIAN_POINT('Ctrl Pts',(-76.6906814144534,-0.445984092498367,
-4.34902644048364));
#52251=CARTESIAN_POINT('Ctrl Pts',(-76.4918078827558,3.41765226062408,-2.72627691481233));
#52252=CARTESIAN_POINT('Ctrl Pts',(-76.2929343510585,4.14114269931356,1.40138143797816));
#52253=CARTESIAN_POINT('Ctrl Pts',(-76.094060819361,1.05974272297901,4.24144764813627));
#52254=CARTESIAN_POINT('Ctrl Pts',(-75.8951872876635,-2.99535104316932,
3.18446305033865));
#52255=CARTESIAN_POINT('Ctrl Pts',(-75.6963137559662,-4.29831012058151,
-0.79841273668073));
#52256=CARTESIAN_POINT('Ctrl Pts',(-75.4974402242686,-1.65197303360122,
-4.04770526187887));
#52257=CARTESIAN_POINT('Ctrl Pts',(-75.2985666925712,2.5122002686028,-3.57795788142059));
#52258=CARTESIAN_POINT('Ctrl Pts',(-75.0996931608737,4.36815880578268,0.179224547009723));
#52259=CARTESIAN_POINT('Ctrl Pts',(-74.9008196291763,2.21064406318877,3.77173509365066));
#52260=CARTESIAN_POINT('Ctrl Pts',(-74.7019460974789,-1.97801498371782,
3.89876769184514));
#52261=CARTESIAN_POINT('Ctrl Pts',(-74.5030725657813,-4.34926980218053,
0.443604529539567));
#52262=CARTESIAN_POINT('Ctrl Pts',(-74.3041990340839,-2.72440659616345,
-3.41914338534794));
#52263=CARTESIAN_POINT('Ctrl Pts',(-74.1053255023865,1.40364698435792,-4.1403753373445));
#52264=CARTESIAN_POINT('Ctrl Pts',(-73.9064519706889,4.24202683358142,-1.05742192806981));
#52265=CARTESIAN_POINT('Ctrl Pts',(-73.7075784389916,3.18282371807295,2.99709291989086));
#52266=CARTESIAN_POINT('Ctrl Pts',(-73.508704907294,-0.800764364805553,
4.29787263920711));
#52267=CARTESIAN_POINT('Ctrl Pts',(-73.3098313755967,-4.04860850511319,
1.64975815291593));
#52268=CARTESIAN_POINT('Ctrl Pts',(-73.1109578438992,-3.57658283802612,
-2.51415751167756));
#52269=CARTESIAN_POINT('Ctrl Pts',(-72.9120843122017,0.181614484338818,
-4.36806009229109));
#52270=CARTESIAN_POINT('Ctrl Pts',(-72.7132107805044,3.7729440455892,-2.20858009128957));
#52271=CARTESIAN_POINT('Ctrl Pts',(-72.5143372488068,3.8976848708697,1.98014783240569));
#52272=CARTESIAN_POINT('Ctrl Pts',(-72.3154637171094,0.441224833785749,
4.34951186190338));
#52273=CARTESIAN_POINT('Ctrl Pts',(-72.1165901854119,-3.42063348653541,
2.72253546195091));
#52274=CARTESIAN_POINT('Ctrl Pts',(-71.9177166537145,-4.13960673593495,
-1.40591211054947));
#52275=CARTESIAN_POINT('Ctrl Pts',(-71.718843122017,-1.05510081661648,-4.24260474915622));
#52276=CARTESIAN_POINT('Ctrl Pts',(-71.5199695903195,2.99883389941879,-3.18118343301426));
#52277=CARTESIAN_POINT('Ctrl Pts',(-71.3210960586221,4.29743387124465,0.803115753217863));
#52278=CARTESIAN_POINT('Ctrl Pts',(-71.1222225269246,1.64754277836791,4.04951053637785));
#52279=CARTESIAN_POINT('Ctrl Pts',(-70.9233489952272,-2.51611400212766,
3.57520672396504));
#52280=CARTESIAN_POINT('Ctrl Pts',(-70.7244754635297,-4.36796007120051,
-0.184004367300773));
#52281=CARTESIAN_POINT('Ctrl Pts',(-70.5256019318323,-2.20651545824171,
-3.77415186807951));
#52282=CARTESIAN_POINT('Ctrl Pts',(-70.3267284001348,1.9822800883272,-3.89660088310427));
#52283=CARTESIAN_POINT('Ctrl Pts',(-70.1278548684374,4.34975261957975,-0.438845005949189));
#52284=CARTESIAN_POINT('Ctrl Pts',(-69.92898133674,2.72066351273476,3.42212256374044));
#52285=CARTESIAN_POINT('Ctrl Pts',(-69.7301078050424,-1.40817681587473,
4.13883689531498));
#52286=CARTESIAN_POINT('Ctrl Pts',(-69.5312342733451,-4.24318139468768,
1.05277938931384));
#52287=CARTESIAN_POINT('Ctrl Pts',(-69.3323607416474,-3.1795421956536,-3.00057398123192));
#52288=CARTESIAN_POINT('Ctrl Pts',(-69.1334872099503,0.805466901213757,
-4.2969938168255));
#52289=CARTESIAN_POINT('Ctrl Pts',(-68.9346136782525,4.0504113554028,-1.64532691062035));
#52290=CARTESIAN_POINT('Ctrl Pts',(-68.7357401465554,3.5738295396493,2.5180697393674));
#52291=CARTESIAN_POINT('Ctrl Pts',(-68.5368666148576,-0.186394195180171,
4.36785874254088));
#52292=CARTESIAN_POINT('Ctrl Pts',(-68.3379930831604,-3.77535856076001,
2.20445016466324));
#52293=CARTESIAN_POINT('Ctrl Pts',(-68.1391195514628,-3.89551572887335,
-1.98441175084401));
#52294=CARTESIAN_POINT('Ctrl Pts',(-67.9402460197655,-0.436465046742345,
-4.34999207513758));
#52295=CARTESIAN_POINT('Ctrl Pts',(-67.7413724880679,3.42361061651726,-2.7187907490754));
#52296=CARTESIAN_POINT('Ctrl Pts',(-67.5424989563705,4.13806581571506,1.41044109965575));
#52297=CARTESIAN_POINT('Ctrl Pts',(-67.343625424673,1.05045764685681,4.24375677000317));
#52298=CARTESIAN_POINT('Ctrl Pts',(-67.1447518929755,-3.00231316480936,
3.17790000648228));
#52299=CARTESIAN_POINT('Ctrl Pts',(-66.9458783612782,-4.29655247608139,
-0.807817808089409));
#52300=CARTESIAN_POINT('Ctrl Pts',(-66.7470048295806,-1.64311055033657,
-4.0513109619184));
#52301=CARTESIAN_POINT('Ctrl Pts',(-66.5481312978833,2.52002472281131,-3.57245128549116));
#52302=CARTESIAN_POINT('Ctrl Pts',(-66.3492577661856,4.36775610634255,0.188783967261603));
#52303=CARTESIAN_POINT('Ctrl Pts',(-66.1503842344884,2.20238421117243,3.77656412326947));
#52304=CARTESIAN_POINT('Ctrl Pts',(-65.9515107027907,-1.98654281931798,
3.89442940850179));
#52305=CARTESIAN_POINT('Ctrl Pts',(-65.7526371710935,-4.35023022850515,
0.434084956877671));
#52306=CARTESIAN_POINT('Ctrl Pts',(-65.5537636393959,-2.71691717153346,
-3.42509764442042));
#52307=CARTESIAN_POINT('Ctrl Pts',(-65.3548901076986,1.41270496121471,-4.137293497366));
#52308=CARTESIAN_POINT('Ctrl Pts',(-65.156016576001,4.24433087493045,-1.04813558994043));
#52309=CARTESIAN_POINT('Ctrl Pts',(-64.9571430443036,3.17625686599191,3.00405144963047));
#52310=CARTESIAN_POINT('Ctrl Pts',(-64.7582695126061,-0.810168473141068,
4.29610984914443));
#52311=CARTESIAN_POINT('Ctrl Pts',(-64.5593959809086,-4.05220935565532,
1.64089369818005));
#52312=CARTESIAN_POINT('Ctrl Pts',(-64.3605224492113,-3.57107196190321,
-2.52197895187418));
#52313=CARTESIAN_POINT('Ctrl Pts',(-64.1616489175137,0.191173682829687,
-4.36765216263623));
#52314=CARTESIAN_POINT('Ctrl Pts',(-63.9627753858163,3.777768555247,-2.20031759838772));
#52315=CARTESIAN_POINT('Ctrl Pts',(-63.7639018541189,3.89334192231479,1.98867329311118));
#52316=CARTESIAN_POINT('Ctrl Pts',(-63.5650283224214,0.431704737067659,
4.3504670796112));
#52317=CARTESIAN_POINT('Ctrl Pts',(-63.3661547907239,-3.42658364700476,
2.71504278066981));
#52318=CARTESIAN_POINT('Ctrl Pts',(-63.1672812590265,-4.13651994049901,
-1.4149683998739));
#52319=CARTESIAN_POINT('Ctrl Pts',(-62.968407727329,-1.04581321925983,-4.24490370929767));
#52320=CARTESIAN_POINT('Ctrl Pts',(-62.7695341956316,3.00578883517485,-3.17461277467437));
#52321=CARTESIAN_POINT('Ctrl Pts',(-62.5706606639341,4.29566593614713,0.812518895664999));
#52322=CARTESIAN_POINT('Ctrl Pts',(-62.3717871322366,1.63867635481445,4.05310653634465));
#52323=CARTESIAN_POINT('Ctrl Pts',(-62.1729136005392,-2.52393242597099,
3.56969156929837));
#52324=CARTESIAN_POINT('Ctrl Pts',(-61.9740400688417,-4.36754691145306,
-0.193563341169043));
#52325=CARTESIAN_POINT('Ctrl Pts',(-61.7751665371444,-2.19825032692777,
-3.77897185633205));
#52326=CARTESIAN_POINT('Ctrl Pts',(-61.5762930054469,1.99080317158582,-3.89225327063788));
#52327=CARTESIAN_POINT('Ctrl Pts',(-61.3774194737493,4.35070262838482,-0.429324388024834));
#52328=CARTESIAN_POINT('Ctrl Pts',(-61.178545942052,2.71316757704555,3.42806862382544));
#52329=CARTESIAN_POINT('Ctrl Pts',(-60.9796724103545,-1.41723141495577,
4.13574514534565));
#52330=CARTESIAN_POINT('Ctrl Pts',(-60.780798878657,-4.24547527293333,1.0434905355102));
#52331=CARTESIAN_POINT('Ctrl Pts',(-60.5819253469596,-3.1729677330218,-3.00752532092253));
#52332=CARTESIAN_POINT('Ctrl Pts',(-60.3830518152621,0.814869074957788,
-4.29522073722237));
#52333=CARTESIAN_POINT('Ctrl Pts',(-60.1841782835647,4.05400250371783,-1.63645852090336));
#52334=CARTESIAN_POINT('Ctrl Pts',(-59.9853047518672,3.56831010808978,2.52588514451706));
#52335=CARTESIAN_POINT('Ctrl Pts',(-59.7864312201697,-0.195952941564444,
4.36744035282451));
#52336=CARTESIAN_POINT('Ctrl Pts',(-59.5875576884724,-3.78017402616446,
2.1961823974113));
#52337=CARTESIAN_POINT('Ctrl Pts',(-59.3886841567748,-3.8911634537969,-1.99293245410441));
#52338=CARTESIAN_POINT('Ctrl Pts',(-59.1898106250775,-0.426943910461734,
-4.35093687475548));
#52339=CARTESIAN_POINT('Ctrl Pts',(-58.9909370933799,3.42955257443794,-2.71129156122203));
#52340=CARTESIAN_POINT('Ctrl Pts',(-58.7920635616825,4.13496911213787,1.41949400578286));
#52341=CARTESIAN_POINT('Ctrl Pts',(-58.5931900299851,1.04116753938684,4.24604556566634));
#52342=CARTESIAN_POINT('Ctrl Pts',(-58.3943164982875,-3.00926090635356,
3.17132174152668));
#52343=CARTESIAN_POINT('Ctrl Pts',(-58.1954429665903,-4.29477425250343,
-0.81721901031565));
#52344=CARTESIAN_POINT('Ctrl Pts',(-57.9965694348925,-1.63424019711096,
-4.05489725750658));
#52345=CARTESIAN_POINT('Ctrl Pts',(-57.7976959031953,2.52783710692763,-3.56692757869113));
#52346=CARTESIAN_POINT('Ctrl Pts',(-57.5988223714977,4.36733248678251,0.198342483300303));
#52347=CARTESIAN_POINT('Ctrl Pts',(-57.3999488398004,2.1941138104576,3.78137506438423));
#52348=CARTESIAN_POINT('Ctrl Pts',(-57.2010753081028,-1.99506114002947,
3.89007247211823));
#52349=CARTESIAN_POINT('Ctrl Pts',(-57.0022017764055,-4.35116981865314,
0.424563305090861));
#52350=CARTESIAN_POINT('Ctrl Pts',(-56.8033282447079,-2.70941473376068,
-3.43103549839809));
#52351=CARTESIAN_POINT('Ctrl Pts',(-56.6044547130105,1.42175617167791,-4.1341918411079));
#52352=CARTESIAN_POINT('Ctrl Pts',(-56.4055811813131,4.24661458732599,-1.03884423158519));
#52353=CARTESIAN_POINT('Ctrl Pts',(-56.2067076496156,3.16967480068174,3.01099559094843));
#52354=CARTESIAN_POINT('Ctrl Pts',(-56.0078341179182,-0.819568701035232,
4.29432648212395));
#52355=CARTESIAN_POINT('Ctrl Pts',(-55.8089605862207,-4.05579079744309,
1.6320213841012));
#52356=CARTESIAN_POINT('Ctrl Pts',(-55.6100870545232,-3.56554398151623,
-2.52978831261849));
#52357=CARTESIAN_POINT('Ctrl Pts',(-55.4112135228258,0.200731965661421,
-4.36722331335934));
#52358=CARTESIAN_POINT('Ctrl Pts',(-55.2123399911283,3.78257497063191,-2.19204456668579));
#52359=CARTESIAN_POINT('Ctrl Pts',(-55.0134664594309,3.88898032592836,1.99718922872367));
#52360=CARTESIAN_POINT('Ctrl Pts',(-54.8145929277334,0.422182572625175,
4.35140146000794));
#52361=CARTESIAN_POINT('Ctrl Pts',(-54.6157193960359,-3.43251739526182,
2.70753709522368));
#52362=CARTESIAN_POINT('Ctrl Pts',(-54.4168458643385,-4.13341333248855,
-1.42401791196362));
#52363=CARTESIAN_POINT('Ctrl Pts',(-54.2179723326411,-1.0365206128007,-4.24718233774192));
#52364=CARTESIAN_POINT('Ctrl Pts',(-54.0190988009436,3.01272937418784,-3.16802691097999));
#52365=CARTESIAN_POINT('Ctrl Pts',(-53.8202252692461,4.293877426218,0.821918146413134));
#52366=CARTESIAN_POINT('Ctrl Pts',(-53.6213517375487,1.62980208253829,4.05668312325988));
#52367=CARTESIAN_POINT('Ctrl Pts',(-53.4224782058512,-2.53173876100551,
3.56415931697925));
#52368=CARTESIAN_POINT('Ctrl Pts',(-53.2236046741539,-4.36711283258768,
-0.203121387932494));
#52369=CARTESIAN_POINT('Ctrl Pts',(-53.0247311424563,-2.18997466671529,
-3.78377374454828));
#52370=CARTESIAN_POINT('Ctrl Pts',(-52.825857610759,1.99931671955004,-3.88788701555426));
#52371=CARTESIAN_POINT('Ctrl Pts',(-52.6269840790614,4.3516317987506,-0.419801713777189));
#52372=CARTESIAN_POINT('Ctrl Pts',(-52.4281105473641,2.70565864617292,3.43399826458561));
#52373=CARTESIAN_POINT('Ctrl Pts',(-52.2292370156665,-1.42627922596299,
4.13263358651281));
#52374=CARTESIAN_POINT('Ctrl Pts',(-52.0303634839691,-4.24774881674419,
1.03419668372898));
#52375=CARTESIAN_POINT('Ctrl Pts',(-51.8314899522716,-3.16637807291474,
-3.0144622555528));
#52376=CARTESIAN_POINT('Ctrl Pts',(-51.6326164205741,0.824267345746038,
-4.29342708491998));
#52377=CARTESIAN_POINT('Ctrl Pts',(-51.4337428888768,4.05757423468981,-1.6275822930866));
#52378=CARTESIAN_POINT('Ctrl Pts',(-51.2348693571792,3.5627735854947,2.53368845150483));
#52379=CARTESIAN_POINT('Ctrl Pts',(-51.0359958254819,-0.205510749398244,
4.36700104450061));
#52380=CARTESIAN_POINT('Ctrl Pts',(-50.8371222937843,-3.78497138577449,
2.18790411116576));
#52381=CARTESIAN_POINT('Ctrl Pts',(-50.6382487620869,-3.8867925413232,-2.00144361187171));
#52382=CARTESIAN_POINT('Ctrl Pts',(-50.4393752303894,-0.417420729259616,
-4.35186083481216));
#52383=CARTESIAN_POINT('Ctrl Pts',(-50.240501698692,3.43547810592614,-2.70377938717074));
#52384=CARTESIAN_POINT('Ctrl Pts',(-50.0416281669945,4.1318526034141,1.42854011299908));
#52385=CARTESIAN_POINT('Ctrl Pts',(-49.8427546352971,1.03187244506569,4.24831402416321));
#52386=CARTESIAN_POINT('Ctrl Pts',(-49.6438811035996,-3.01619423452454,
3.16472828697957));
#52387=CARTESIAN_POINT('Ctrl Pts',(-49.4450075719022,-4.29297545836471,
-0.826616298330698));
#52388=CARTESIAN_POINT('Ctrl Pts',(-49.2461340402047,-1.62536201641063,
-4.05846413146615));
#52389=CARTESIAN_POINT('Ctrl Pts',(-49.0472605085073,2.5356373835328,-3.5613867874774));
#52390=CARTESIAN_POINT('Ctrl Pts',(-48.8483869768098,4.36688794913159,0.207900049343396));
#52391=CARTESIAN_POINT('Ctrl Pts',(-48.6495134451124,2.18583290065701,3.78616789395201));
#52392=CARTESIAN_POINT('Ctrl Pts',(-48.4506399134149,-2.00356990505197,
3.88569690356282));
#52393=CARTESIAN_POINT('Ctrl Pts',(-48.2517663817174,-4.35208856812407,
0.415039619785222));
#52394=CARTESIAN_POINT('Ctrl Pts',(-48.05289285002,-2.7018993187797,-3.43695691884043));
#52395=CARTESIAN_POINT('Ctrl Pts',(-47.8540193183225,1.43080057239508,-4.13107038342622));
#52396=CARTESIAN_POINT('Ctrl Pts',(-47.655145786625,4.24887795982979,-1.02954789750662));
#52397=CARTESIAN_POINT('Ctrl Pts',(-47.4562722549277,3.16307755366836,3.01792531058458));
#52398=CARTESIAN_POINT('Ctrl Pts',(-47.2573987232301,-0.828965003463952,
4.2925225466874));
#52399=CARTESIAN_POINT('Ctrl Pts',(-47.0585251915328,-4.05935281332248,
1.62314125317501));
#52400=CARTESIAN_POINT('Ctrl Pts',(-46.8596516598352,-3.55999892334251,
-2.53758555650599));
#52401=CARTESIAN_POINT('Ctrl Pts',(-46.6607781281379,0.210289287052714,
-4.36677354651447));
#52402=CARTESIAN_POINT('Ctrl Pts',(-46.4619045964403,3.78736326872267,-2.18376103580909));
#52403=CARTESIAN_POINT('Ctrl Pts',(-46.2630310647429,3.88460010260112,2.00569559845433));
#52404=CARTESIAN_POINT('Ctrl Pts',(-46.0641575330454,0.412658386066791,
4.35231499861814));
#52405=CARTESIAN_POINT('Ctrl Pts',(-45.865284001348,-3.43843470288575,2.70001844156262));
#52406=CARTESIAN_POINT('Ctrl Pts',(-45.6664104696505,-4.13028692678332,
-1.43306060347432));
#52407=CARTESIAN_POINT('Ctrl Pts',(-45.4675369379531,-1.02722304174763,
-4.24944062357511));
#52408=CARTESIAN_POINT('Ctrl Pts',(-45.2686634062556,3.01965548321474,-3.16142587347527));
#52409=CARTESIAN_POINT('Ctrl Pts',(-45.0697898745582,4.29206835002362,0.831313460442701));
#52410=CARTESIAN_POINT('Ctrl Pts',(-44.8709163428607,1.62092000404456,4.06024027999278));
#52411=CARTESIAN_POINT('Ctrl Pts',(-44.6720428111633,-2.53953296984122,
3.55860999350548));
#52412=CARTESIAN_POINT('Ctrl Pts',(-44.4731692794658,-4.3666578366835,-0.212678461810957));
#52413=CARTESIAN_POINT('Ctrl Pts',(-44.2742957477684,-2.18168851724219,
-3.78855750972863));
#52414=CARTESIAN_POINT('Ctrl Pts',(-44.0754222160709,2.00782069144243,-3.88350213876641));
#52415=CARTESIAN_POINT('Ctrl Pts',(-43.8765486843735,4.3525401262266,-0.410277028817174));
#52416=CARTESIAN_POINT('Ctrl Pts',(-43.677675152676,2.69813675608252,3.43991145761977));
#52417=CARTESIAN_POINT('Ctrl Pts',(-43.4788016209786,-1.43532020556023,
4.12950223371992));
#52418=CARTESIAN_POINT('Ctrl Pts',(-43.2799280892811,-4.25000201523073,
1.02489787848468));
#52419=CARTESIAN_POINT('Ctrl Pts',(-43.0810545575836,-3.15977324689472,
-3.02138475189707));
#52420=CARTESIAN_POINT('Ctrl Pts',(-42.8821810258862,0.83366166856392,-4.29161286850933));
#52421=CARTESIAN_POINT('Ctrl Pts',(-42.6833074941888,4.06112653121138,-1.61869826968422));
#52422=CARTESIAN_POINT('Ctrl Pts',(-42.4844339624912,3.55721999838211,2.54147962295552));
#52423=CARTESIAN_POINT('Ctrl Pts',(-42.2855604307939,-0.215067572902925,
4.36654081967332));
#52424=CARTESIAN_POINT('Ctrl Pts',(-42.0866868990963,-3.78975061661238,
2.17961534557676));
#52425=CARTESIAN_POINT('Ctrl Pts',(-41.887813367399,-3.88240301238739,-2.00994518338014));
#52426=CARTESIAN_POINT('Ctrl Pts',(-41.6889398357014,-0.407895548749227,
-4.35276395088204));
#52427=CARTESIAN_POINT('Ctrl Pts',(-41.4900663040041,3.44138718260039,-2.69625426290272));
#52428=CARTESIAN_POINT('Ctrl Pts',(-41.2911927723065,4.12871630447095,1.43757937797641));
#52429=CARTESIAN_POINT('Ctrl Pts',(-41.0923192406092,1.0225724084138,4.25056213462861));
#52430=CARTESIAN_POINT('Ctrl Pts',(-40.8934457089116,-3.02311311611391,
3.15811967442143));
#52431=CARTESIAN_POINT('Ctrl Pts',(-40.6945721772142,-4.29115610228089,
-0.83600962712466));
#52432=CARTESIAN_POINT('Ctrl Pts',(-40.4956986455168,-1.61647605075906,
-4.06201156671298));
#52433=CARTESIAN_POINT('Ctrl Pts',(-40.2968251138193,2.54342551526614,-3.55582893838847));
#52434=CARTESIAN_POINT('Ctrl Pts',(-40.0979515821218,4.36642249551896,0.217456619613414));
#52435=CARTESIAN_POINT('Ctrl Pts',(-39.8990780504244,2.1775415214334,3.79094258901677));
#52436=CARTESIAN_POINT('Ctrl Pts',(-39.7002045187269,-2.01206907363145,
3.88130272379308));
#52437=CARTESIAN_POINT('Ctrl Pts',(-39.5013309870295,-4.35298647251748,
0.40551394657586));
#52438=CARTESIAN_POINT('Ctrl Pts',(-39.302457455332,-2.69437096258673,-3.44286187738583));
#52439=CARTESIAN_POINT('Ctrl Pts',(-39.1035839236346,1.43983812004655,-4.12792913927167));
#52440=CARTESIAN_POINT('Ctrl Pts',(-38.9047103919372,4.25112098160105,-1.02024663223114));
#52441=CARTESIAN_POINT('Ctrl Pts',(-38.7058368602396,3.15646515655044,3.02484057534785));
#52442=CARTESIAN_POINT('Ctrl Pts',(-38.5069633285422,-0.83835733542206,
4.29069805147503));
#52443=CARTESIAN_POINT('Ctrl Pts',(-38.3080897968448,-4.06289538623264,
1.61425334793433));
#52444=CARTESIAN_POINT('Ctrl Pts',(-38.1092162651473,-3.55443681394101,
-2.54537064619057));
#52445=CARTESIAN_POINT('Ctrl Pts',(-37.9103427334499,0.219845601227261,
-4.36630286425583));
#52446=CARTESIAN_POINT('Ctrl Pts',(-37.7114692017524,3.79213342658497,-2.17546704543292));
#52447=CARTESIAN_POINT('Ctrl Pts',(-37.5125956700549,3.88020127331285,2.01419236156059));
#52448=CARTESIAN_POINT('Ctrl Pts',(-37.3137221383575,0.403132223010095,
4.35320769106624));
#52449=CARTESIAN_POINT('Ctrl Pts',(-37.11484860666,-3.44433554153461,2.69248685569843));
#52450=CARTESIAN_POINT('Ctrl Pts',(-36.9159750749626,-4.12714073835777,
-1.44209643109444));
#52451=CARTESIAN_POINT('Ctrl Pts',(-36.7171015432651,-1.01792055063294,
-4.25167855598078));
#52452=CARTESIAN_POINT('Ctrl Pts',(-36.5182280115677,3.02656712908178,-3.15480969377699));
#52453=CARTESIAN_POINT('Ctrl Pts',(-36.3193544798703,4.29023871622889,0.840704792753313));
#52454=CARTESIAN_POINT('Ctrl Pts',(-36.1204809481727,1.61203016187539,4.06377798950578));
#52455=CARTESIAN_POINT('Ctrl Pts',(-35.9216074164753,-2.54731501514653,
3.55304362545645));
#52456=CARTESIAN_POINT('Ctrl Pts',(-35.7227338847778,-4.36618192591977,
-0.222234517029311));
#52457=CARTESIAN_POINT('Ctrl Pts',(-35.5238603530804,-2.17339191819631,
-3.79332312896049));
#52458=CARTESIAN_POINT('Ctrl Pts',(-35.3249868213829,2.01631504653193,-3.87909866127643));
#52459=CARTESIAN_POINT('Ctrl Pts',(-35.1261132896855,4.3534276064622,-0.400750378764763));
#52460=CARTESIAN_POINT('Ctrl Pts',(-34.9272397579881,2.69060194280166,3.44580817460567));
#52461=CARTESIAN_POINT('Ctrl Pts',(-34.7283662262906,-1.44435431044416,
4.12635110196515));
#52462=CARTESIAN_POINT('Ctrl Pts',(-34.5294926945932,-4.25223485760088,
1.01559416431552));
#52463=CARTESIAN_POINT('Ctrl Pts',(-34.3306191628957,-3.15315328659669,
-3.02829277679886));
#52464=CARTESIAN_POINT('Ctrl Pts',(-34.1317456311983,0.843051998415699,
-4.28977809667994));
#52465=CARTESIAN_POINT('Ctrl Pts',(-33.9328720995008,4.0646593762682,-1.60980649324777));
#52466=CARTESIAN_POINT('Ctrl Pts',(-33.7339985678033,3.55164937335186,2.54925862155197));
#52467=CARTESIAN_POINT('Ctrl Pts',(-33.5351250361059,-0.224623366304428,
4.36605968054695));
#52468=CARTESIAN_POINT('Ctrl Pts',(-33.3362515044084,-3.7945116957872,2.17131614034479));
#52469=CARTESIAN_POINT('Ctrl Pts',(-33.1373779727109,-3.8779948880139,-2.01843712791005));
#52470=CARTESIAN_POINT('Ctrl Pts',(-32.9385044410135,-0.398368414552949,
-4.35364621863948));
#52471=CARTESIAN_POINT('Ctrl Pts',(-32.7396309093161,3.44727977615813,-2.68871622446075));
#52472=CARTESIAN_POINT('Ctrl Pts',(-32.5407573776186,4.12556023033026,1.44661175741973));
#52473=CARTESIAN_POINT('Ctrl Pts',(-32.3418838459212,1.01326747397528,4.25278988629482));
#52474=CARTESIAN_POINT('Ctrl Pts',(-32.1430103142237,-3.03001751798249,
3.15149593550537));
#52475=CARTESIAN_POINT('Ctrl Pts',(-31.9441367825262,-4.28931619296609,
-0.845398951706575));
#52476=CARTESIAN_POINT('Ctrl Pts',(-31.7452632508288,-1.60758234271713,
-4.06553954625603));
#52477=CARTESIAN_POINT('Ctrl Pts',(-31.5463897191313,2.55120146482505,-3.55025405804461));
#52478=CARTESIAN_POINT('Ctrl Pts',(-31.3475161874339,4.36593612817399,0.227012148337509));
#52479=CARTESIAN_POINT('Ctrl Pts',(-31.1486426557364,2.16923971249975,3.79569912670929));
#52480=CARTESIAN_POINT('Ctrl Pts',(-30.949769124039,-2.02055860505967,3.87688995385567));
#52481=CARTESIAN_POINT('Ctrl Pts',(-30.7508955923414,-4.35386352753264,
0.395986331087709));
#52482=CARTESIAN_POINT('Ctrl Pts',(-30.5520220606441,-2.68682970124021,
-3.44875034575145));
#52483=CARTESIAN_POINT('Ctrl Pts',(-30.3531485289466,1.44886877134539,-4.12476812368983));
#52484=CARTESIAN_POINT('Ctrl Pts',(-30.1542749972492,4.25334364189643,-1.01094048030875));
#52485=CARTESIAN_POINT('Ctrl Pts',(-29.9554014655517,3.14983764099918,3.03174135211637));
#52486=CARTESIAN_POINT('Ctrl Pts',(-29.7565279338542,-0.847745651923367,
4.28885300522561));
#52487=CARTESIAN_POINT('Ctrl Pts',(-29.5576544021568,-4.06641849920581,
1.60535771094929));
#52488=CARTESIAN_POINT('Ctrl Pts',(-29.3587808704593,-3.54885767995239,
-2.55314354438418));
#52489=CARTESIAN_POINT('Ctrl Pts',(-29.1599073387619,0.229400862413447,
-4.36581126883786));
#52490=CARTESIAN_POINT('Ctrl Pts',(-28.9610338070644,3.7968854213713,-2.16716263528277));
#52491=CARTESIAN_POINT('Ctrl Pts',(-28.762160275367,3.8757838591325,2.02267947734574));
#52492=CARTESIAN_POINT('Ctrl Pts',(-28.5632867436695,0.393604129082132,
4.35407953307663));
#52493=CARTESIAN_POINT('Ctrl Pts',(-28.3644132119721,-3.45021988294541,
2.68494237370479));
#52494=CARTESIAN_POINT('Ctrl Pts',(-28.1655396802746,-4.123974782281,-1.45112535154548));
#52495=CARTESIAN_POINT('Ctrl Pts',(-27.9666661485772,-1.00861318401251,
-4.25389612423997));
#52496=CARTESIAN_POINT('Ctrl Pts',(-27.7677926168797,3.03346427868447,-3.14817840357452));
#52497=CARTESIAN_POINT('Ctrl Pts',(-27.5689190851823,4.28838853359714,0.850092098363576));
#52498=CARTESIAN_POINT('Ctrl Pts',(-27.3700455534848,1.60313259861021,4.06729623485442));
#52499=CARTESIAN_POINT('Ctrl Pts',(-27.1711720217873,-2.55508485964799,
3.54746023949322));
#52500=CARTESIAN_POINT('Ctrl Pts',(-26.9722984900899,-4.36568510257594,
-0.231789507817176));
#52501=CARTESIAN_POINT('Ctrl Pts',(-26.7734249583924,-2.16508490931564,
-3.79807057941811));
#52502=CARTESIAN_POINT('Ctrl Pts',(-26.574551426695,2.02479974413336,-3.87467660417552));
#52503=CARTESIAN_POINT('Ctrl Pts',(-26.3756778949975,4.35429423520678,-0.391221809249338));
#52504=CARTESIAN_POINT('Ctrl Pts',(-26.1768043633001,2.68305424241945,3.45168838730009));
#52505=CARTESIAN_POINT('Ctrl Pts',(-25.9779308316026,-1.45338149734449,
4.12318020634126));
#52506=CARTESIAN_POINT('Ctrl Pts',(-25.7790572999052,-4.25444733316004,
1.00628558578325));
#52507=CARTESIAN_POINT('Ctrl Pts',(-25.5801837682078,-3.1465182237281,-3.035186297171));
#52508=CARTESIAN_POINT('Ctrl Pts',(-25.3813102365102,0.852438290324783,
-4.28792277821976));
#52509=CARTESIAN_POINT('Ctrl Pts',(-25.1824367048128,4.06817275293909,-1.60090700636595));
#52510=CARTESIAN_POINT('Ctrl Pts',(-24.9835631731153,3.54606173708543,2.55702541003533));
#52511=CARTESIAN_POINT('Ctrl Pts',(-24.7846896414179,-0.23417808383365,
4.36555762942601));
#52512=CARTESIAN_POINT('Ctrl Pts',(-24.5858161097204,-3.79925460049492,
2.16300653522032));
#52513=CARTESIAN_POINT('Ctrl Pts',(-24.386942578023,-3.87356818931619,-2.0269194047878));
#52514=CARTESIAN_POINT('Ctrl Pts',(-24.1880690463255,-0.388839372302486,
-4.35450763385882));
#52515=CARTESIAN_POINT('Ctrl Pts',(-23.9891955146281,3.4531558583759,-2.68116530794941));
#52516=CARTESIAN_POINT('Ctrl Pts',(-23.7903219829307,4.12238439610845,1.45563720806703));
#52517=CARTESIAN_POINT('Ctrl Pts',(-23.5914484512331,1.00395768631775,4.25499726849163));
#52518=CARTESIAN_POINT('Ctrl Pts',(-23.3925749195357,-3.03690740706049,
3.14485710195691));
#52519=CARTESIAN_POINT('Ctrl Pts',(-23.1937013878383,-4.28745573923285,
-0.854784227104649));
#52520=CARTESIAN_POINT('Ctrl Pts',(-22.9948278561408,-1.5986809348828,-4.06904805319745));
#52521=CARTESIAN_POINT('Ctrl Pts',(-22.7959543244434,2.5589651949653,-3.54466217314766));
#52522=CARTESIAN_POINT('Ctrl Pts',(-22.5970807927458,4.36542884942622,0.23656658974783));
#52523=CARTESIAN_POINT('Ctrl Pts',(-22.3982072610485,2.16092751361901,3.80043748424731));
#52524=CARTESIAN_POINT('Ctrl Pts',(-22.199333729351,-2.02903845867456,3.87245861488632));
#52525=CARTESIAN_POINT('Ctrl Pts',(-22.0004601976535,-4.35471972896887,
0.386456818954767));
#52526=CARTESIAN_POINT('Ctrl Pts',(-21.8015866659561,-2.67927557086015,
-3.45462229573354));
#52527=CARTESIAN_POINT('Ctrl Pts',(-21.6027131342586,1.45789248303785,-4.12158735182083));
#52528=CARTESIAN_POINT('Ctrl Pts',(-21.4038396025612,4.25554593007011,-1.00162948631287));
#52529=CARTESIAN_POINT('Ctrl Pts',(-21.2049660708637,3.14319503875821,3.0386276078377));
#52530=CARTESIAN_POINT('Ctrl Pts',(-21.0060925391664,-0.857129908000908,
4.28698741677627));
#52531=CARTESIAN_POINT('Ctrl Pts',(-20.8072190074687,-4.06992213536745,
1.5964543848271));
#52532=CARTESIAN_POINT('Ctrl Pts',(-20.6083454757714,-3.54326154809888,
-2.5609042138572));
#52533=CARTESIAN_POINT('Ctrl Pts',(-20.4094719440739,0.238955024844702,
-4.36529876261513));
#52534=CARTESIAN_POINT('Ctrl Pts',(-20.2105984123765,3.80161923032118,-2.15884784513404));
#52535=CARTESIAN_POINT('Ctrl Pts',(-20.011724880679,3.87134788121805,2.03115690515927));
#52536=CARTESIAN_POINT('Ctrl Pts',(-19.8128513489816,0.384074149919422,
4.35493052047343));
#52537=CARTESIAN_POINT('Ctrl Pts',(-19.6139778172841,-3.45608769893403,
2.67738503171736));
#52538=CARTESIAN_POINT('Ctrl Pts',(-19.4151042855866,-4.12078907371697,
-1.4601473215818));
#52539=CARTESIAN_POINT('Ctrl Pts',(-19.2162307538892,-0.999300986465579,
-4.25609331773125));
#52540=CARTESIAN_POINT('Ctrl Pts',(-19.0173572221917,3.04034689898769,-3.14153203462953));
#52541=CARTESIAN_POINT('Ctrl Pts',(-18.8184836904943,4.28651781099017,0.859475332311362));
#52542=CARTESIAN_POINT('Ctrl Pts',(-18.6196101587968,1.59422735686541,4.07079499918746));
#52543=CARTESIAN_POINT('Ctrl Pts',(-18.4207366270994,-2.56284246613059,
3.54185986235838));
#52544=CARTESIAN_POINT('Ctrl Pts',(-18.2218630954019,-4.36516736903167,
-0.241343388409285));
#52545=CARTESIAN_POINT('Ctrl Pts',(-18.0229895637045,-2.156767530388,-3.80279983836275));
#52546=CARTESIAN_POINT('Ctrl Pts',(-17.824116032007,2.03327474360769,-3.87023598864389));
#52547=CARTESIAN_POINT('Ctrl Pts',(-17.6252425003096,4.35514000830941,-0.381691365909796));
#52548=CARTESIAN_POINT('Ctrl Pts',(-17.4263689686121,2.67549369108707,3.45755206753867));
#52549=CARTESIAN_POINT('Ctrl Pts',(-17.2274954369147,-1.46240172302391,
4.11998956203585));
#52550=CARTESIAN_POINT('Ctrl Pts',(-17.0286219052172,-4.25663943131118,
0.996972187472916));
#52551=CARTESIAN_POINT('Ctrl Pts',(-16.8297483735197,-3.13986809006872,
-3.04206527999579));
#52552=CARTESIAN_POINT('Ctrl Pts',(-16.6308748418223,0.861820499333901,
-4.28604692201515));
#52553=CARTESIAN_POINT('Ctrl Pts',(-16.4320013101249,4.07166664439615,-1.59199985166439));
#52554=CARTESIAN_POINT('Ctrl Pts',(-16.2331277784274,3.54045711634576,2.56477995120524));
#52555=CARTESIAN_POINT('Ctrl Pts',(-16.0342542467299,-0.243731679726614,
4.36503466871517));
#52556=CARTESIAN_POINT('Ctrl Pts',(-15.8353807150324,-3.8039793080186,2.15468657000362));
#52557=CARTESIAN_POINT('Ctrl Pts',(-15.636507183335,-3.8691229374967,-2.035391973386));
#52558=CARTESIAN_POINT('Ctrl Pts',(-15.4376336516376,-0.379308467639,-4.35534819241408));
#52559=CARTESIAN_POINT('Ctrl Pts',(-15.2387601199401,3.45901540110913,-2.6736015495353));
#52560=CARTESIAN_POINT('Ctrl Pts',(-15.0398865882427,4.11918881701681,1.46465568668931));
#52561=CARTESIAN_POINT('Ctrl Pts',(-14.8410130565452,0.994643090032016,
4.25718427064641));
#52562=CARTESIAN_POINT('Ctrl Pts',(-14.6421395248478,-3.04378275034757,
3.13820320557389));
#52563=CARTESIAN_POINT('Ctrl Pts',(-14.4432659931503,-4.28557474999217,
-0.864165408366494));
#52564=CARTESIAN_POINT('Ctrl Pts',(-14.2443924614529,-1.58977186989086,
-4.07253707073262));
#52565=CARTESIAN_POINT('Ctrl Pts',(-14.0455189297554,2.56671666850115,-3.53905331048093));
#52566=CARTESIAN_POINT('Ctrl Pts',(-13.8466453980579,4.36490066170536,0.246119898081736));
#52567=CARTESIAN_POINT('Ctrl Pts',(-13.6477718663605,2.15260496460386,3.80515763893567));
#52568=CARTESIAN_POINT('Ctrl Pts',(-13.448898334663,-2.03750859386031,3.86800872810968));
#52569=CARTESIAN_POINT('Ctrl Pts',(-13.2500248029656,-4.35555507272516,
0.376925455820456));
#52570=CARTESIAN_POINT('Ctrl Pts',(-13.0511512712682,-2.67170860762853,
-3.46047769920734));
#52571=CARTESIAN_POINT('Ctrl Pts',(-12.8522777395706,1.46690921190324,-4.11838683889956));
#52572=CARTESIAN_POINT('Ctrl Pts',(-12.6534042078732,4.25772783557386,-0.992313694840112));
#52573=CARTESIAN_POINT('Ctrl Pts',(-12.4545306761757,3.13653738164341,3.04549930952892));
#52574=CARTESIAN_POINT('Ctrl Pts',(-12.2556571444783,-0.866510058707176,
4.28510129506258));
#52575=CARTESIAN_POINT('Ctrl Pts',(-12.0567836127808,-4.07340627793628,
1.58754341221176));
#52576=CARTESIAN_POINT('Ctrl Pts',(-11.8579100810834,-3.53764844518413,
-2.56865261743856));
#52577=CARTESIAN_POINT('Ctrl Pts',(-11.6590365493859,0.248508042759728,
-4.36476534804237));
#52578=CARTESIAN_POINT('Ctrl Pts',(-11.4601630176885,3.8063348307612,-2.15052271481186));
#52579=CARTESIAN_POINT('Ctrl Pts',(-11.261289485991,3.86689336081636,2.03962460439701));
#52580=CARTESIAN_POINT('Ctrl Pts',(-11.0624159542936,0.374542331167539,
4.35576064918068));
#52581=CARTESIAN_POINT('Ctrl Pts',(-10.8635424225961,-3.46193896139555,
2.66981486593344));
#52582=CARTESIAN_POINT('Ctrl Pts',(-10.6646688908987,-4.11758362792416,
-1.46916229799113));
#52583=CARTESIAN_POINT('Ctrl Pts',(-10.4657953592012,-0.989984002594516,
-4.25827012593079));
#52584=CARTESIAN_POINT('Ctrl Pts',(-10.2669218275038,3.04721495702597,-3.13487061877597));
#52585=CARTESIAN_POINT('Ctrl Pts',(-10.0680482958063,4.2846265573681,0.868854449654062));
#52586=CARTESIAN_POINT('Ctrl Pts',(-9.86917476410884,1.58531447929421,4.07427426574695));
#52587=CARTESIAN_POINT('Ctrl Pts',(-9.67030123241142,-2.57058779743794,
3.53624252087591));
#52588=CARTESIAN_POINT('Ctrl Pts',(-9.47142770071392,-4.36462872776664,
-0.250896113045607));
#52589=CARTESIAN_POINT('Ctrl Pts',(-9.27255416901652,-2.14843982125103,
-3.80751088314276));
#52590=CARTESIAN_POINT('Ctrl Pts',(-9.07368063731904,2.04174000436261,-3.86577683595071));
#52591=CARTESIAN_POINT('Ctrl Pts',(-8.87480710562161,4.35596492171907,-0.37215909439371));
#52592=CARTESIAN_POINT('Ctrl Pts',(-8.67593357392413,2.667920325017,3.46339918723626));
#52593=CARTESIAN_POINT('Ctrl Pts',(-8.4770600422267,-1.47141494427834,4.11677918433113));
#52594=CARTESIAN_POINT('Ctrl Pts',(-8.27818651052922,-4.25881114155487,
0.987654013992727));
#52595=CARTESIAN_POINT('Ctrl Pts',(-8.07931297883178,-3.1332029174706,-3.04892969232504));
#52596=CARTESIAN_POINT('Ctrl Pts',(-7.88043944713431,0.871198580505213,
-4.28415053705085));
#52597=CARTESIAN_POINT('Ctrl Pts',(-7.68156591543687,4.07514103390481,-1.58308507180563));
#52598=CARTESIAN_POINT('Ctrl Pts',(-7.48269238373942,3.53483553797703,2.57252220791998));
#52599=CARTESIAN_POINT('Ctrl Pts',(-7.28381885204197,-0.253284108224254,
4.36449080091907));
#52600=CARTESIAN_POINT('Ctrl Pts',(-7.0849453203445,-3.808685795729,2.14635628454501));
#52601=CARTESIAN_POINT('Ctrl Pts',(-6.88607178864706,-3.86465915384566,
-2.0438547931245));
#52602=CARTESIAN_POINT('Ctrl Pts',(-6.68719825694959,-0.36977574621432,
-4.35616789027829));
#52603=CARTESIAN_POINT('Ctrl Pts',(-6.48832472525215,3.46485837629675,-2.66602498544807));
#52604=CARTESIAN_POINT('Ctrl Pts',(-6.28945119355468,4.11597350835323,1.47366715009494));
#52605=CARTESIAN_POINT('Ctrl Pts',(-6.09057766185723,0.985323729746626,
4.25935088227696));
#52606=CARTESIAN_POINT('Ctrl Pts',(-5.89170413015977,-3.05064351494095,
3.13153427823985));
#52607=CARTESIAN_POINT('Ctrl Pts',(-5.69283059846234,-4.28367323420068,
-0.873542450584943));
#52608=CARTESIAN_POINT('Ctrl Pts',(-5.49395706676489,-1.58085519051244,
-4.07600658210169));
#52609=CARTESIAN_POINT('Ctrl Pts',(-5.29508353506742,2.57445584849332,-3.53342749700076));
#52610=CARTESIAN_POINT('Ctrl Pts',(-5.09621000336997,4.36435156718664,0.255672027754977));
#52611=CARTESIAN_POINT('Ctrl Pts',(-4.89733647167251,2.14427210598631,3.80985956783942));
#52612=CARTESIAN_POINT('Ctrl Pts',(-4.69846293997507,-2.04596897131221,
3.86354031545655));
#52613=CARTESIAN_POINT('Ctrl Pts',(-4.49958940827759,-4.35636955241326,
0.367392286171182));
#52614=CARTESIAN_POINT('Ctrl Pts',(-4.30071587658015,-2.66412885229606,
-3.46631652592691));
#52615=CARTESIAN_POINT('Ctrl Pts',(-4.10184234488268,1.47591892326601,-4.11516660441047));
#52616=CARTESIAN_POINT('Ctrl Pts',(-3.90296881318523,4.25988933188569,-0.982993142664311));
#52617=CARTESIAN_POINT('Ctrl Pts',(-3.70409528148781,3.12986473188877,3.0523564094626));
#52618=CARTESIAN_POINT('Ctrl Pts',(-3.50522174979033,-0.875886116413711,
4.28319467709064));
#52619=CARTESIAN_POINT('Ctrl Pts',(-3.3063482180929,-4.07687080203127,1.57862478296689));
#52620=CARTESIAN_POINT('Ctrl Pts',(-3.10747468639542,-3.53201860238364,
-2.57638861828632));
#52621=CARTESIAN_POINT('Ctrl Pts',(-2.90860115469799,0.258060256144617,
-4.36421121598415));
#52622=CARTESIAN_POINT('Ctrl Pts',(-2.70972762300051,3.81103147174565,-2.14218692862399));
#52623=CARTESIAN_POINT('Ctrl Pts',(-2.51085409130307,3.86242169455405,2.04808186311882));
#52624=CARTESIAN_POINT('Ctrl Pts',(-2.3119805596056,0.365006121651707,4.35657118292956));
#52625=CARTESIAN_POINT('Ctrl Pts',(-2.11310702790815,-3.46776873896351,
2.66222951892241));
#52626=CARTESIAN_POINT('Ctrl Pts',(-1.91423349621071,-4.11436771876071,
-1.47816571782307));
#52627=CARTESIAN_POINT('Ctrl Pts',(-1.71535996451324,-0.980644795081548,
-4.2604350726622));
#52628=CARTESIAN_POINT('Ctrl Pts',(-1.51648643281581,3.05403541042053,-3.12817807350787));
#52629=CARTESIAN_POINT('Ctrl Pts',(-1.31761290111834,4.28277711056433,0.878198978078091));
#52630=CARTESIAN_POINT('Ctrl Pts',(-1.1187393694209,1.57627631789302,4.0777914718176));
#52631=CARTESIAN_POINT('Ctrl Pts',(-0.919865837723429,-2.57809858195644,
3.53049975027877));
#52632=CARTESIAN_POINT('Ctrl Pts',(-0.720992306025984,-4.36448889159331,
-0.260242724958486));
#52633=CARTESIAN_POINT('Ctrl Pts',(-0.522118774328522,-2.13930861817419,
-3.81259106820431));
#52634=CARTESIAN_POINT('Ctrl Pts',(-0.323245242631061,2.04869198938347,
-3.86056393295148));
#52635=CARTESIAN_POINT('Ctrl Pts',(-0.124371710933644,4.35965501372303,
-0.364044245942155));
#52636=CARTESIAN_POINT('Ctrl Pts',(0.0745018207638594,2.65450071084487,
3.47215873439577));
#52637=CARTESIAN_POINT('Ctrl Pts',(0.207084175228801,-0.0927661781443274,
3.89494769144758));
#52638=CARTESIAN_POINT('Ctrl Pts',(0.273375352461282,-1.251650112727,3.47787809703136));
#52639=CARTESIAN_POINT('Ctrl Pts',(-109.567,-1.74869447532986,3.5228619944515));
#52640=CARTESIAN_POINT('Ctrl Pts',(-109.500708822768,-2.92256775530673,
2.9401693648038));
#52641=CARTESIAN_POINT('Ctrl Pts',(-109.368126468303,-4.62148961478483,
0.519149110062505));
#52642=CARTESIAN_POINT('Ctrl Pts',(-109.169252936605,-2.93168196537142,
-3.61588934021046));
#52643=CARTESIAN_POINT('Ctrl Pts',(-108.970379404908,1.45547172051883,-4.41678188493319));
#52644=CARTESIAN_POINT('Ctrl Pts',(-108.77150587321,4.50342526464322,-1.16551591507676));
#52645=CARTESIAN_POINT('Ctrl Pts',(-108.572632341513,3.41462717220614,3.15976482950097));
#52646=CARTESIAN_POINT('Ctrl Pts',(-108.373758809815,-0.812068679813194,
4.58019051839891));
#52647=CARTESIAN_POINT('Ctrl Pts',(-108.174885278118,-4.2923528809395,1.79320458261704));
#52648=CARTESIAN_POINT('Ctrl Pts',(-107.976011746421,-3.82896339678044,
-2.64184571159234));
#52649=CARTESIAN_POINT('Ctrl Pts',(-107.777138214723,0.152564403965833,
-4.64931685129564));
#52650=CARTESIAN_POINT('Ctrl Pts',(-107.578264683026,3.99387393908369,-2.38511634519291));
#52651=CARTESIAN_POINT('Ctrl Pts',(-107.379391151328,4.16562602423641,2.07060292291838));
#52652=CARTESIAN_POINT('Ctrl Pts',(-107.180517619631,0.509980647258628,
4.62381144888953));
#52653=CARTESIAN_POINT('Ctrl Pts',(-106.981644087933,-3.61422978970552,
2.92867186548573));
#52654=CARTESIAN_POINT('Ctrl Pts',(-106.782770556236,-4.41768176152901,
-1.45734768584626));
#52655=CARTESIAN_POINT('Ctrl Pts',(-106.583897024538,-1.16215691953748,
-4.50434776553196));
#52656=CARTESIAN_POINT('Ctrl Pts',(-106.385023492841,3.16115916451212,-3.41274674299064));
#52657=CARTESIAN_POINT('Ctrl Pts',(-106.186149961143,4.5799962056956,0.814494516072427));
#52658=CARTESIAN_POINT('Ctrl Pts',(-105.987276429446,1.79072307054798,4.29337573545735));
#52659=CARTESIAN_POINT('Ctrl Pts',(-105.788402897749,-2.64386996172864,
3.82749494045799));
#52660=CARTESIAN_POINT('Ctrl Pts',(-105.589529366051,-4.64926991710361,
-0.155096290772498));
#52661=CARTESIAN_POINT('Ctrl Pts',(-105.390655834354,-2.38291108801837,
-3.99518461187035));
#52662=CARTESIAN_POINT('Ctrl Pts',(-105.191782302656,2.07287132116358,-4.16448917178079));
#52663=CARTESIAN_POINT('Ctrl Pts',(-104.992908770959,4.62409531506305,-0.507452496249705));
#52664=CARTESIAN_POINT('Ctrl Pts',(-104.794035239261,2.92669103324941,3.61583255699087));
#52665=CARTESIAN_POINT('Ctrl Pts',(-104.595161707564,-1.45976297618673,
4.41688324199641));
#52666=CARTESIAN_POINT('Ctrl Pts',(-104.396288175866,-4.50498376741142,
1.15969253020268));
#52667=CARTESIAN_POINT('Ctrl Pts',(-104.197414644169,-3.41101622233145,
-3.16302605686458));
#52668=CARTESIAN_POINT('Ctrl Pts',(-103.998541112471,0.817000031123855,
-4.57954980972901));
#52669=CARTESIAN_POINT('Ctrl Pts',(-103.799667580774,4.29435497869652,-1.78837379360953));
#52670=CARTESIAN_POINT('Ctrl Pts',(-103.600794049077,3.82604775423565,2.64596373570485));
#52671=CARTESIAN_POINT('Ctrl Pts',(-103.401920517379,-0.157640002669139,
4.64918435197667));
#52672=CARTESIAN_POINT('Ctrl Pts',(-103.203046985682,-3.99648780147895,
2.38072483949959));
#52673=CARTESIAN_POINT('Ctrl Pts',(-103.004173453984,-4.16335440239243,
-2.07514954372844));
#52674=CARTESIAN_POINT('Ctrl Pts',(-102.805299922287,-0.504922429896287,
-4.62437226536201));
#52675=CARTESIAN_POINT('Ctrl Pts',(-102.606426390589,3.6174333079372,-2.92471225446792));
#52676=CARTESIAN_POINT('Ctrl Pts',(-102.407552858892,4.41608389485863,1.46217938105407));
#52677=CARTESIAN_POINT('Ctrl Pts',(-102.208679327194,1.15722753176151,4.50561759901536));
#52678=CARTESIAN_POINT('Ctrl Pts',(-102.009805795497,-3.16489186362239,
3.4092851157379));
#52679=CARTESIAN_POINT('Ctrl Pts',(-101.810932263799,-4.57910211632402,
-0.819505532069846));
#52680=CARTESIAN_POINT('Ctrl Pts',(-101.612058732102,-1.78602394240258,
-4.29533281434428));
#52681=CARTESIAN_POINT('Ctrl Pts',(-101.413185200404,2.64805669699241,-3.82459948730979));
#52682=CARTESIAN_POINT('Ctrl Pts',(-101.214311668707,4.64909740600855,0.160183701609936));
#52683=CARTESIAN_POINT('Ctrl Pts',(-101.015438137009,2.37853787251991,3.99778977658976));
#52684=CARTESIAN_POINT('Ctrl Pts',(-100.816564605312,-2.0774271420266,4.16221839628679));
#52685=CARTESIAN_POINT('Ctrl Pts',(-100.617691073615,-4.6246478329549,0.50239220730669));
#52686=CARTESIAN_POINT('Ctrl Pts',(-100.418817541917,-2.92273259930173,
-3.61903297329493));
#52687=CARTESIAN_POINT('Ctrl Pts',(-100.21994401022,1.46459534775654,-4.41528322717206));
#52688=CARTESIAN_POINT('Ctrl Pts',(-100.021070478522,4.50625008208266,-1.15476218614357));
#52689=CARTESIAN_POINT('Ctrl Pts',(-99.8221969468247,3.40755298843155,3.16675672255514));
#52690=CARTESIAN_POINT('Ctrl Pts',(-99.6233234151276,-0.822010787625527,
4.57865305235549));
#52691=CARTESIAN_POINT('Ctrl Pts',(-99.4244498834296,-4.29630936420008,
1.78367355642891));
#52692=CARTESIAN_POINT('Ctrl Pts',(-99.2255763517326,-3.82315007545343,
-2.65014886551254));
#52693=CARTESIAN_POINT('Ctrl Pts',(-99.0267028200349,0.162727352588974,
-4.64900906834309));
#52694=CARTESIAN_POINT('Ctrl Pts',(-98.8278292883376,3.99909055494903,-2.37635019349726));
#52695=CARTESIAN_POINT('Ctrl Pts',(-98.62895575664,4.161081144199,2.07970411842853));
#52696=CARTESIAN_POINT('Ctrl Pts',(-98.4300822249428,0.499861834325147,
4.62492201614277));
#52697=CARTESIAN_POINT('Ctrl Pts',(-98.2312086932451,-3.62063155527922,
2.92075206919953));
#52698=CARTESIAN_POINT('Ctrl Pts',(-98.0323351615478,-4.41448123774961,
-1.46701087602433));
#52699=CARTESIAN_POINT('Ctrl Pts',(-97.8334616298503,-1.15229649484245,
-4.50688121618384));
#52700=CARTESIAN_POINT('Ctrl Pts',(-97.6345880981527,3.16862063350473,-3.4058198410581));
#52701=CARTESIAN_POINT('Ctrl Pts',(-97.4357145664554,4.57820261774596,0.824515797108271));
#52702=CARTESIAN_POINT('Ctrl Pts',(-97.236841034758,1.78132263650433,4.29728462793591));
#52703=CARTESIAN_POINT('Ctrl Pts',(-97.0379675030604,-2.65224024069837,
3.82169951911937));
#52704=CARTESIAN_POINT('Ctrl Pts',(-96.8390939713631,-4.64891933897527,
-0.165270954854797));
#52705=CARTESIAN_POINT('Ctrl Pts',(-96.6402204396655,-2.3741618031032,-4.00039013616206));
#52706=CARTESIAN_POINT('Ctrl Pts',(-96.4413469079682,2.08198047226141,-4.15994264647233));
#52707=CARTESIAN_POINT('Ctrl Pts',(-96.2424733762706,4.62519481483885,-0.49733131170768));
#52708=CARTESIAN_POINT('Ctrl Pts',(-96.0435998445732,2.9187706647567,3.62222905341074));
#52709=CARTESIAN_POINT('Ctrl Pts',(-95.8447263128757,-1.46942596513563,
4.41367792683178));
#52710=CARTESIAN_POINT('Ctrl Pts',(-95.6458527811783,-4.50751100112929,
1.14983045859604));
#52711=CARTESIAN_POINT('Ctrl Pts',(-95.4469792494808,-3.40408567413676,
-3.17048359591309));
#52712=CARTESIAN_POINT('Ctrl Pts',(-95.2481057177833,0.827020559768415,
-4.5777508126303));
#52713=CARTESIAN_POINT('Ctrl Pts',(-95.049232186086,4.29825860525972,-1.7789711833326));
#52714=CARTESIAN_POINT('Ctrl Pts',(-94.8503586543885,3.8202478187419,2.6543308219238));
#52715=CARTESIAN_POINT('Ctrl Pts',(-94.6514851226909,-0.167814507645974,
4.64882821793195));
#52716=CARTESIAN_POINT('Ctrl Pts',(-94.4526115909937,-4.00168851983982,
2.37197270199285));
#52717=CARTESIAN_POINT('Ctrl Pts',(-94.2537380592959,-4.1588029034476,-2.08425620284382));
#52718=CARTESIAN_POINT('Ctrl Pts',(-94.0548645275989,-0.494800640211771,
-4.62546622896147));
#52719=CARTESIAN_POINT('Ctrl Pts',(-93.8559909959011,3.62382546721121,-2.91678838656638));
#52720=CARTESIAN_POINT('Ctrl Pts',(-93.6571174642038,4.41287329465908,1.47184061436746));
#52721=CARTESIAN_POINT('Ctrl Pts',(-93.4582439325062,1.14736407814257,4.50813943673051));
#52722=CARTESIAN_POINT('Ctrl Pts',(-93.2593704008089,-3.17234560922253,
3.4023504881866));
#52723=CARTESIAN_POINT('Ctrl Pts',(-93.0604968691113,-4.57729763714377,
-0.829525074856124));
#52724=CARTESIAN_POINT('Ctrl Pts',(-92.8616233374139,-1.77661919761762,
-4.29923129587995));
#52725=CARTESIAN_POINT('Ctrl Pts',(-92.6627498057165,2.65642060856304,-3.81879497475558));
#52726=CARTESIAN_POINT('Ctrl Pts',(-92.4638762740189,4.64873570524042,0.170358010201121));
#52727=CARTESIAN_POINT('Ctrl Pts',(-92.2650027423217,2.36978289082147,4.00298570559363));
#52728=CARTESIAN_POINT('Ctrl Pts',(-92.0661292106241,-2.0865313094945,4.15766191546598));
#52729=CARTESIAN_POINT('Ctrl Pts',(-91.8672556789266,-4.6257362584294,0.492269820595009));
#52730=CARTESIAN_POINT('Ctrl Pts',(-91.6683821472293,-2.91480523522198,
-3.62542079620279));
#52731=CARTESIAN_POINT('Ctrl Pts',(-91.4695086155317,1.47425482299701,-4.41206734147235));
#52732=CARTESIAN_POINT('Ctrl Pts',(-91.2706350838344,4.50876652279934,-1.14489735422035));
#52733=CARTESIAN_POINT('Ctrl Pts',(-91.0717615521368,3.4006142837271,3.17420667287565));
#52734=CARTESIAN_POINT('Ctrl Pts',(-90.8728880204394,-0.83202934162167,
4.57684309142205));
#52735=CARTESIAN_POINT('Ctrl Pts',(-90.6740144887419,-4.30020269950541,
1.77426668006346));
#52736=CARTESIAN_POINT('Ctrl Pts',(-90.4751409570445,-3.81734098759532,
-2.65850959999049));
#52737=CARTESIAN_POINT('Ctrl Pts',(-90.276267425347,0.172901461758815,-4.64864180092837));
#52738=CARTESIAN_POINT('Ctrl Pts',(-90.0773938936496,4.00428169303516,-2.36759237024463));
#52739=CARTESIAN_POINT('Ctrl Pts',(-89.8785203619521,4.15651968286905,2.08880579153238));
#52740=CARTESIAN_POINT('Ctrl Pts',(-89.6796468302546,0.489738853614996,
4.62600490316179));
#52741=CARTESIAN_POINT('Ctrl Pts',(-89.4807732985572,-3.62701503990788,
2.91282121131715));
#52742=CARTESIAN_POINT('Ctrl Pts',(-89.2818997668597,-4.41126006751287,
-1.47666859030155));
#52743=CARTESIAN_POINT('Ctrl Pts',(-89.0830262351625,-1.14243028756782,
-4.50939225914807));
#52744=CARTESIAN_POINT('Ctrl Pts',(-88.8841527034647,3.17606678631533,-3.39887706127799));
#52745=CARTESIAN_POINT('Ctrl Pts',(-88.6852791717675,4.57638717560117,0.834533359315383));
#52746=CARTESIAN_POINT('Ctrl Pts',(-88.4864056400698,1.77191363137438,4.30117281584531));
#52747=CARTESIAN_POINT('Ctrl Pts',(-88.2875321083726,-2.66059779558081,
3.8158858576964));
#52748=CARTESIAN_POINT('Ctrl Pts',(-88.088658576675,-4.64854650502389,-0.175444861557656));
#52749=CARTESIAN_POINT('Ctrl Pts',(-87.8897850449775,-2.36540114091807,
-4.00557648177645));
#52750=CARTESIAN_POINT('Ctrl Pts',(-87.6909115132801,2.0910796482766,-4.15537620599874));
#52751=CARTESIAN_POINT('Ctrl Pts',(-87.4920379815827,4.62627216307823,-0.487207740029394));
#52752=CARTESIAN_POINT('Ctrl Pts',(-87.2931644498852,2.91083631544583,3.62860819784926));
#52753=CARTESIAN_POINT('Ctrl Pts',(-87.0942909181878,-1.47908191555853,
4.4104514730223));
#52754=CARTESIAN_POINT('Ctrl Pts',(-86.8954173864902,-4.51001664558938,
1.1399628789235));
#52755=CARTESIAN_POINT('Ctrl Pts',(-86.696543854793,-3.39713882135932,-3.17792594898473));
#52756=CARTESIAN_POINT('Ctrl Pts',(-86.4976703230953,0.837037127187677,
-4.57592988981764));
#52757=CARTESIAN_POINT('Ctrl Pts',(-86.298796791398,4.30214164460925,-1.76956005225475));
#52758=CARTESIAN_POINT('Ctrl Pts',(-86.0999232597005,3.8144295854944,2.66268519470887));
#52759=CARTESIAN_POINT('Ctrl Pts',(-85.901049728003,-0.177988208836268,
4.64844981755554));
#52760=CARTESIAN_POINT('Ctrl Pts',(-85.7021761963055,-4.0068700714299,2.36320920349774));
#52761=CARTESIAN_POINT('Ctrl Pts',(-85.5033026646083,-4.15423148519735,
-2.09335287904645));
#52762=CARTESIAN_POINT('Ctrl Pts',(-85.3044291329106,-0.484676480595899,
-4.62653803809871));
#52763=CARTESIAN_POINT('Ctrl Pts',(-85.1055556012133,3.63020026954995,-2.90885054820222));
#52764=CARTESIAN_POINT('Ctrl Pts',(-84.9066820695158,4.4096415582427,1.48149479804545));
#52765=CARTESIAN_POINT('Ctrl Pts',(-84.7078085378183,1.13749512902607,4.51063968193637));
#52766=CARTESIAN_POINT('Ctrl Pts',(-84.5089350061209,-3.17978416032731,
3.39539956449144));
#52767=CARTESIAN_POINT('Ctrl Pts',(-84.3100614744233,-4.57547123420834,
-0.839540644489037));
#52768=CARTESIAN_POINT('Ctrl Pts',(-84.1111879427261,-1.76720594340918,
-4.30310918550717));
#52769=CARTESIAN_POINT('Ctrl Pts',(-83.9123144110284,2.66477179674978,-3.81297217142531));
#52770=CARTESIAN_POINT('Ctrl Pts',(-83.7134408793312,4.64835173855226,0.180531502833249));
#52771=CARTESIAN_POINT('Ctrl Pts',(-83.5145673476335,2.36101655863981,4.00816246160827));
#52772=CARTESIAN_POINT('Ctrl Pts',(-83.3156938159363,-2.09562548316145,
4.15308552080756));
#52773=CARTESIAN_POINT('Ctrl Pts',(-83.1168202842386,-4.62680252814361,
0.482145076072292));
#52774=CARTESIAN_POINT('Ctrl Pts',(-82.9179467525412,-2.90686391018077,
-3.63179125453341));
#52775=CARTESIAN_POINT('Ctrl Pts',(-82.7190732208439,1.48390723704007,-4.40883032341654));
#52776=CARTESIAN_POINT('Ctrl Pts',(-82.5201996891462,4.5112613680025,-1.13502703861416));
#52777=CARTESIAN_POINT('Ctrl Pts',(-82.321326157449,3.393659291195,3.1816414197868));
#52778=CARTESIAN_POINT('Ctrl Pts',(-82.1224526257514,-0.842043910469987,
4.57501120891056));
#52779=CARTESIAN_POINT('Ctrl Pts',(-81.923579094054,-4.30407543824946,1.76485130554235));
#52780=CARTESIAN_POINT('Ctrl Pts',(-81.7247055623566,-3.81151361592538,
-2.66685760107894));
#52781=CARTESIAN_POINT('Ctrl Pts',(-81.525832030659,0.18307474278733,-4.64825226804338));
#52782=CARTESIAN_POINT('Ctrl Pts',(-81.3269584989616,4.00945365192469,-2.35882320700066));
#52783=CARTESIAN_POINT('Ctrl Pts',(-81.1280849672642,4.15193831317242,2.09789745994127));
#52784=CARTESIAN_POINT('Ctrl Pts',(-80.9292114355667,0.479613527216301,
4.62706563313381));
#52785=CARTESIAN_POINT('Ctrl Pts',(-80.7303379038692,-3.63338115232342,
2.90487640197613));
#52786=CARTESIAN_POINT('Ctrl Pts',(-80.5314643721718,-4.4080177687866,-1.48631923182023));
#52787=CARTESIAN_POINT('Ctrl Pts',(-80.3325908404743,-1.13255860842666,
-4.51188170360169));
#52788=CARTESIAN_POINT('Ctrl Pts',(-80.1337173087769,3.18349772680722,-3.39191800199096));
#52789=CARTESIAN_POINT('Ctrl Pts',(-79.9348437770794,4.57454981406204,0.844546924381235));
#52790=CARTESIAN_POINT('Ctrl Pts',(-79.7359702453821,1.76249613935908,4.3050404025469));
#52791=CARTESIAN_POINT('Ctrl Pts',(-79.5370967136844,-2.66894260707198,
3.81005391943118));
#52792=CARTESIAN_POINT('Ctrl Pts',(-79.3382231819871,-4.64815140605869,
-0.185617927937138));
#52793=CARTESIAN_POINT('Ctrl Pts',(-79.1393496502896,-2.35662914923688,
-4.0107436419926));
#52794=CARTESIAN_POINT('Ctrl Pts',(-78.9404761185922,2.10016880870579,-4.15078986263536));
#52795=CARTESIAN_POINT('Ctrl Pts',(-78.7416025868947,4.62732735299052,-0.477081834785776));
#52796=CARTESIAN_POINT('Ctrl Pts',(-78.5427290551972,2.90288802418331,3.63496996244397));
#52797=CARTESIAN_POINT('Ctrl Pts',(-78.3438555234999,-1.48873078166386,
4.40720389459616));
#52798=CARTESIAN_POINT('Ctrl Pts',(-78.1449819918022,-4.51250068854823,
1.13008983920251));
#52799=CARTESIAN_POINT('Ctrl Pts',(-77.9461084601051,-3.39017569740059,
-3.18535308083288));
#52800=CARTESIAN_POINT('Ctrl Pts',(-77.7472349284073,0.847049685473463,
-4.57408704980088));
#52801=CARTESIAN_POINT('Ctrl Pts',(-77.5483613967101,4.30600407811059,-1.76014044556444));
#52802=CARTESIAN_POINT('Ctrl Pts',(-77.3494878650125,3.80859308237973,2.67102681410471));
#52803=CARTESIAN_POINT('Ctrl Pts',(-77.1506143333151,-0.188161057521362,
4.64804915262839));
#52804=CARTESIAN_POINT('Ctrl Pts',(-76.9517408016176,-4.01203243142588,
2.35443438600527));
#52805=CARTESIAN_POINT('Ctrl Pts',(-76.7528672699202,-4.14964016954015,
-2.10243952877506));
#52806=CARTESIAN_POINT('Ctrl Pts',(-76.5539937382226,-0.474549999538605,
-4.6275876876354));
#52807=CARTESIAN_POINT('Ctrl Pts',(-76.3551202065254,3.63655768441947,-2.90089877739755));
#52808=CARTESIAN_POINT('Ctrl Pts',(-76.1562466748277,4.40638870108887,1.49114188584904));
#52809=CARTESIAN_POINT('Ctrl Pts',(-75.9573731431305,1.12762073168075,4.51311832265683));
#52810=CARTESIAN_POINT('Ctrl Pts',(-75.7584996114328,-3.18720748130837,
3.38843237794545));
#52811=CARTESIAN_POINT('Ctrl Pts',(-75.5596260797356,-4.57362291626562,
-0.849552192997447));
#52812=CARTESIAN_POINT('Ctrl Pts',(-75.3607525480378,-1.75778422486363,
-4.30696646465206));
#52813=CARTESIAN_POINT('Ctrl Pts',(-75.1618790163406,2.67311022155321,-3.80713110520833));
#52814=CARTESIAN_POINT('Ctrl Pts',(-74.963005484643,4.64794550778309,0.190704130778702));
#52815=CARTESIAN_POINT('Ctrl Pts',(-74.7641319529456,2.35223891796283,4.0133200198387));
#52816=CARTESIAN_POINT('Ctrl Pts',(-74.5652584212482,-2.10470961946934,
4.14848923423098));
#52817=CARTESIAN_POINT('Ctrl Pts',(-74.3663848895507,-4.6278466369905,0.472018022232693));
#52818=CARTESIAN_POINT('Ctrl Pts',(-74.1675113578532,-2.89890866221432,
-3.6381443177746));
#52819=CARTESIAN_POINT('Ctrl Pts',(-73.9686378261559,1.49355254365402,-4.40557218850874));
#52820=CARTESIAN_POINT('Ctrl Pts',(-73.7697642944583,4.5137346057426,-1.1251512866005));
#52821=CARTESIAN_POINT('Ctrl Pts',(-73.570890762761,3.38668804414742,3.18906092767856));
#52822=CARTESIAN_POINT('Ctrl Pts',(-73.3720172310633,-0.852054446204056,
4.5731574135952));
#52823=CARTESIAN_POINT('Ctrl Pts',(-73.1731436993661,-4.3079275618832,1.75542747796197));
#52824=CARTESIAN_POINT('Ctrl Pts',(-72.9742701676685,-3.80566798835464,
-2.6751928287938));
#52825=CARTESIAN_POINT('Ctrl Pts',(-72.7753966359711,0.193247146947877,
-4.64784047155381));
#52826=CARTESIAN_POINT('Ctrl Pts',(-72.5765231042737,4.01460640684562,-2.3500427457668));
#52827=CARTESIAN_POINT('Ctrl Pts',(-72.3776495725761,4.14733705705237,2.10697908010902));
#52828=CARTESIAN_POINT('Ctrl Pts',(-72.1787760408788,0.469485903626064,
4.62810420097833));
#52829=CARTESIAN_POINT('Ctrl Pts',(-71.9799025091812,-3.63972986203442,
2.89691767922942));
#52830=CARTESIAN_POINT('Ctrl Pts',(-71.7810289774839,-4.40475435710021,
-1.49596275435712));
#52831=CARTESIAN_POINT('Ctrl Pts',(-71.5821554457863,-1.12268150470101,
-4.51434953762105));
#52832=CARTESIAN_POINT('Ctrl Pts',(-71.3832819140889,3.19091341938862,-3.38494269652865));
#52833=CARTESIAN_POINT('Ctrl Pts',(-71.1844083823914,4.57269054192897,0.854556444344225));
#52834=CARTESIAN_POINT('Ctrl Pts',(-70.985534850694,1.75307020556499,4.30888736951631));
#52835=CARTESIAN_POINT('Ctrl Pts',(-70.7866613189966,-2.67727463520306,
3.80420373225664));
#52836=CARTESIAN_POINT('Ctrl Pts',(-70.587787787299,-4.64773404397201,-0.195790105267626));
#52837=CARTESIAN_POINT('Ctrl Pts',(-70.3889142556017,-2.34784587007461,
-4.01589159206155));
#52838=CARTESIAN_POINT('Ctrl Pts',(-70.1900407239042,2.10924791001481,-4.14618363834924));
#52839=CARTESIAN_POINT('Ctrl Pts',(-69.9911671922067,4.62836037952177,-0.466953644476603));
#52840=CARTESIAN_POINT('Ctrl Pts',(-69.7922936605093,2.89492582903878,3.64131431672428));
#52841=CARTESIAN_POINT('Ctrl Pts',(-69.5934201288119,-1.49837251723686,
4.4039352071081));
#52842=CARTESIAN_POINT('Ctrl Pts',(-69.3945465971143,-4.51496311810808,
1.12021138672163));
#52843=CARTESIAN_POINT('Ctrl Pts',(-69.195673065417,-3.38319633561165,-3.19276495588401));
#52844=CARTESIAN_POINT('Ctrl Pts',(-68.9967995337194,0.857058186668978,
-4.57222230140667));
#52845=CARTESIAN_POINT('Ctrl Pts',(-68.797926002022,4.30984588726406,-1.75071240837834));
#52846=CARTESIAN_POINT('Ctrl Pts',(-68.5990524703246,3.80273833735267,2.67935564015779));
#52847=CARTESIAN_POINT('Ctrl Pts',(-68.4001789386271,-0.198333004976704,
4.64762622506952));
#52848=CARTESIAN_POINT('Ctrl Pts',(-68.2013054069296,-4.01717557510177,
2.34564829154392));
#52849=CARTESIAN_POINT('Ctrl Pts',(-68.0024318752322,-4.14502897846688,
-2.1115161085075));
#52850=CARTESIAN_POINT('Ctrl Pts',(-67.8035583435347,-0.464421245542407,
-4.62861517254413));
#52851=CARTESIAN_POINT('Ctrl Pts',(-67.6046848118373,3.64289768136986,-2.89293311223871));
#52852=CARTESIAN_POINT('Ctrl Pts',(-67.4058112801398,4.40311473877763,1.50078183157187));
#52853=CARTESIAN_POINT('Ctrl Pts',(-67.2069377484423,1.11774093340179,4.51557534702004));
#52854=CARTESIAN_POINT('Ctrl Pts',(-67.008064216745,-3.19461553661043,3.38144896191918));
#52855=CARTESIAN_POINT('Ctrl Pts',(-66.8091906850474,-4.5717526921685,-0.859559672429393));
#52856=CARTESIAN_POINT('Ctrl Pts',(-66.6103171533501,-1.74835408710783,
-4.31080311483954));
#52857=CARTESIAN_POINT('Ctrl Pts',(-66.4114436216526,2.68143584303501,-3.80127180408139));
#52858=CARTESIAN_POINT('Ctrl Pts',(-66.212570089955,4.64751701487864,0.200875845313876));
#52859=CARTESIAN_POINT('Ctrl Pts',(-66.0136965582578,2.34345001083256,4.0184583555819));
#52860=CARTESIAN_POINT('Ctrl Pts',(-65.81482302656,-2.11378367490808,4.14387307775092));
#52861=CARTESIAN_POINT('Ctrl Pts',(-65.6159494948629,-4.62886857996913,
0.461888707581565));
#52862=CARTESIAN_POINT('Ctrl Pts',(-65.4170759631652,-2.89093952942574,
-3.64447995549718));
#52863=CARTESIAN_POINT('Ctrl Pts',(-65.2182024314679,1.50319069664089,-4.40229295235441));
#52864=CARTESIAN_POINT('Ctrl Pts',(-65.0193288997703,4.51618622417364,-1.11527014548103));
#52865=CARTESIAN_POINT('Ctrl Pts',(-64.820455368073,3.37970057597434,3.19646516101393));
#52866=CARTESIAN_POINT('Ctrl Pts',(-64.6215818363755,-0.862060900876653,
4.57128171435502));
#52867=CARTESIAN_POINT('Ctrl Pts',(-64.422708304678,-4.31175905195616,1.74599524245944));
#52868=CARTESIAN_POINT('Ctrl Pts',(-64.2238347729806,-3.79980413288183,
-2.68351524321201));
#52869=CARTESIAN_POINT('Ctrl Pts',(-64.0249612412831,0.203418625517942,
-4.64740641343205));
#52870=CARTESIAN_POINT('Ctrl Pts',(-63.8260877095857,4.01973993311795,-2.3412510285986));
#52871=CARTESIAN_POINT('Ctrl Pts',(-63.6272141778882,4.14271593654741,2.11605060853774));
#52872=CARTESIAN_POINT('Ctrl Pts',(-63.4283406461908,0.459356031352204,
4.62912060172093));
#52873=CARTESIAN_POINT('Ctrl Pts',(-63.2294671144932,-3.64606113863258,
2.88894508119666));
#52874=CARTESIAN_POINT('Ctrl Pts',(-63.0305935827959,-4.40146984808443,
-1.50559911172283));
#52875=CARTESIAN_POINT('Ctrl Pts',(-62.8317200510983,-1.112799023699,-4.51679574938602));
#52876=CARTESIAN_POINT('Ctrl Pts',(-62.632846519401,3.19831382854077,-3.37795117830051));
#52877=CARTESIAN_POINT('Ctrl Pts',(-62.4339729877035,4.57080936810724,0.864561871261937));
#52878=CARTESIAN_POINT('Ctrl Pts',(-62.235099456006,1.74363587513935,4.31271369832778));
#52879=CARTESIAN_POINT('Ctrl Pts',(-62.0362259243087,-2.68559384006632,
3.79833532419333));
#52880=CARTESIAN_POINT('Ctrl Pts',(-61.837352392611,-4.64729442076289,-0.205961344827695));
#52881=CARTESIAN_POINT('Ctrl Pts',(-61.6384788609138,-2.33905134550033,
-4.02102030732626));
#52882=CARTESIAN_POINT('Ctrl Pts',(-61.4396053292161,2.11831690871786,-4.14155755520273));
#52883=CARTESIAN_POINT('Ctrl Pts',(-61.2407317975188,4.62937123772409,-0.456823217612489));
#52884=CARTESIAN_POINT('Ctrl Pts',(-61.0418582658213,2.88694976814851,3.64764123030272));
#52885=CARTESIAN_POINT('Ctrl Pts',(-60.8429847341239,-1.50800707609672,
4.40064542621412));
#52886=CARTESIAN_POINT('Ctrl Pts',(-60.6441112024264,-4.51740392247471,
1.11032756879543));
#52887=CARTESIAN_POINT('Ctrl Pts',(-60.445237670729,-3.37620076942136,-3.20016153863765));
#52888=CARTESIAN_POINT('Ctrl Pts',(-60.2463641390314,0.867062582836786,
-4.57033565356654));
#52889=CARTESIAN_POINT('Ctrl Pts',(-60.0474906073341,4.31366705366866,-1.74127598585364));
#52890=CARTESIAN_POINT('Ctrl Pts',(-59.8486170756365,3.79686537845552,2.68767163297581));
#52891=CARTESIAN_POINT('Ctrl Pts',(-59.6497435439392,-0.208504002482106,
4.64718103690463));
#52892=CARTESIAN_POINT('Ctrl Pts',(-59.4508700122417,-4.02229947782363,
2.3368509621961));
#52893=CARTESIAN_POINT('Ctrl Pts',(-59.2519964805442,-4.14039793406358,
-2.12058257477011));
#52894=CARTESIAN_POINT('Ctrl Pts',(-59.0531229488468,-0.45429026712059,
-4.62962048790353));
#52895=CARTESIAN_POINT('Ctrl Pts',(-58.8542494171492,3.64922023003459,-2.88495359087861));
#52896=CARTESIAN_POINT('Ctrl Pts',(-58.655375885452,4.39981968699025,1.51041458904172));
#52897=CARTESIAN_POINT('Ctrl Pts',(-58.4565023537543,1.10785578151018,4.51801074325765));
#52898=CARTESIAN_POINT('Ctrl Pts',(-58.2576288220571,-3.20200829075135,
3.37444934986091));
#52899=CARTESIAN_POINT('Ctrl Pts',(-58.0587552903594,-4.56986057087472,
-0.869563034852338));
#52900=CARTESIAN_POINT('Ctrl Pts',(-57.8598817586621,-1.73891557530902,
-4.31461911769333));
#52901=CARTESIAN_POINT('Ctrl Pts',(-57.6610082269646,2.68974862131826,-3.79539429610858));
#52902=CARTESIAN_POINT('Ctrl Pts',(-57.4621346952672,4.64706626189126,0.211046597719749));
#52903=CARTESIAN_POINT('Ctrl Pts',(-57.2632611635697,2.33464987934486,4.02357744422698));
#52904=CARTESIAN_POINT('Ctrl Pts',(-57.0643876318722,-2.12284760601617,
4.13923707347725));
#52905=CARTESIAN_POINT('Ctrl Pts',(-56.8655141001748,-4.62986835218477,
0.451757180634654));
#52906=CARTESIAN_POINT('Ctrl Pts',(-56.6666405684773,-2.88295654998432,
-3.6507981373556));
#52907=CARTESIAN_POINT('Ctrl Pts',(-56.4677670367799,1.51282164983718,-4.39899263065995));
#52908=CARTESIAN_POINT('Ctrl Pts',(-56.2688935050824,4.51861621155319,-1.10538366258318));
#52909=CARTESIAN_POINT('Ctrl Pts',(-56.070019973385,3.37269692014345,3.20385408432906));
#52910=CARTESIAN_POINT('Ctrl Pts',(-55.8711464416876,-0.872063226560181,
4.56938412017402));
#52911=CARTESIAN_POINT('Ctrl Pts',(-55.67227290999,-4.31556989011681,1.736554644212));
#52912=CARTESIAN_POINT('Ctrl Pts',(-55.4733993782926,-3.79392207759281,
-2.69182480447203));
#52913=CARTESIAN_POINT('Ctrl Pts',(-55.2745258465952,0.213589129779611,
-4.64695009575711));
#52914=CARTESIAN_POINT('Ctrl Pts',(-55.0756523148977,4.02485420615382,-2.33244809760538));
#52915=CARTESIAN_POINT('Ctrl Pts',(-54.8767787832003,4.13807497379115,2.1251120017779));
#52916=CARTESIAN_POINT('Ctrl Pts',(-54.6779052515027,0.449223958913303,
4.63011483049344));
#52917=CARTESIAN_POINT('Ctrl Pts',(-54.4790317198054,-3.65237495179322,
2.88095864606385));
#52918=CARTESIAN_POINT('Ctrl Pts',(-54.2801581881078,-4.39816425747094,
-1.51522825776243));
#52919=CARTESIAN_POINT('Ctrl Pts',(-54.0812846564105,-1.10291121275446,
-4.51922032718007));
#52920=CARTESIAN_POINT('Ctrl Pts',(-53.8824111247129,3.20569891881823,-3.37094348079357));
#52921=CARTESIAN_POINT('Ctrl Pts',(-53.6835375930156,4.56890630160706,0.874563157211865));
#52922=CARTESIAN_POINT('Ctrl Pts',(-53.4846640613179,1.73419319326931,4.31651937065449));
#52923=CARTESIAN_POINT('Ctrl Pts',(-53.2857905296208,-2.6939001818156,3.79244872334894));
#52924=CARTESIAN_POINT('Ctrl Pts',(-53.086916997923,-4.64683253853698,-0.216131597900584));
#52925=CARTESIAN_POINT('Ctrl Pts',(-52.8880434662258,-2.33024561763677,
-4.02612976322195));
#52926=CARTESIAN_POINT('Ctrl Pts',(-52.6891699345282,2.12737576137752,-4.13691163535318));
#52927=CARTESIAN_POINT('Ctrl Pts',(-52.4902964028309,4.63035992275584,-0.446690602714689));
#52928=CARTESIAN_POINT('Ctrl Pts',(-52.2914228711333,2.87895987971509,3.65395067287553));
#52929=CARTESIAN_POINT('Ctrl Pts',(-52.0925493394359,-1.5176344120971,4.39733456767112));
#52930=CARTESIAN_POINT('Ctrl Pts',(-51.8936758077385,-4.51982308995746,
1.10043843276417));
#52931=CARTESIAN_POINT('Ctrl Pts',(-51.6948022760409,-3.36918903233618,
-3.20754279366662));
#52932=CARTESIAN_POINT('Ctrl Pts',(-51.4959287443436,0.877062826059023,
-4.56842711531687));
#52933=CARTESIAN_POINT('Ctrl Pts',(-51.2970552126461,4.31746755902214,-1.73183122318787));
#52934=CARTESIAN_POINT('Ctrl Pts',(-51.0981816809486,3.790974233818,2.69597475272769));
#52935=CARTESIAN_POINT('Ctrl Pts',(-50.8993081492512,-0.21867400132156,
4.64671359026604));
#52936=CARTESIAN_POINT('Ctrl Pts',(-50.7004346175536,-4.02740411504953,
2.32804244009837));
#52937=CARTESIAN_POINT('Ctrl Pts',(-50.5015610858563,-4.13574705851158,
-2.12963888413737));
#52938=CARTESIAN_POINT('Ctrl Pts',(-50.3026875541588,-0.444157112797176,
-4.63060362889859));
#52939=CARTESIAN_POINT('Ctrl Pts',(-50.1038140224614,3.6555253001308,-2.87696025153637));
#52940=CARTESIAN_POINT('Ctrl Pts',(-49.9049404907639,4.39650356150887,1.52004011212088));
#52941=CARTESIAN_POINT('Ctrl Pts',(-49.7060669590665,1.09796532335256,4.52042449970491));
#52942=CARTESIAN_POINT('Ctrl Pts',(-49.507193427369,-3.20938570832225,3.36743357529647));
#52943=CARTESIAN_POINT('Ctrl Pts',(-49.3083198956715,-4.56794656144691,
-0.879562232353367));
#52944=CARTESIAN_POINT('Ctrl Pts',(-49.1094463639741,-1.72946873467476,
-4.31841445493593));
#52945=CARTESIAN_POINT('Ctrl Pts',(-48.9105728322766,2.69804851658728,-3.78949860944139));
#52946=CARTESIAN_POINT('Ctrl Pts',(-48.7116993005792,4.6465932509799,0.221216339281466));
#52947=CARTESIAN_POINT('Ctrl Pts',(-48.5128257688817,2.3258385656497,4.02867726125506));
#52948=CARTESIAN_POINT('Ctrl Pts',(-48.3139522371842,-2.13190136937999,
4.13458124361499));
#52949=CARTESIAN_POINT('Ctrl Pts',(-48.1150787054868,-4.63084594884872,
0.441623489919174));
#52950=CARTESIAN_POINT('Ctrl Pts',(-47.9162051737893,-2.87495976212631,
-3.65709883308768));
#52951=CARTESIAN_POINT('Ctrl Pts',(-47.7173316420919,1.52244535711364,-4.39567123923295));
#52952=CARTESIAN_POINT('Ctrl Pts',(-47.5184581103945,4.52102455624239,-1.09549188525994));
#52953=CARTESIAN_POINT('Ctrl Pts',(-47.319584578697,3.36567711019996,3.21122766223342));
#52954=CARTESIAN_POINT('Ctrl Pts',(-47.1207110469995,-0.882061375346694,
4.56746464014102));
#52955=CARTESIAN_POINT('Ctrl Pts',(-46.9218375153021,-4.31936005811238,
1.72710572843718));
#52956=CARTESIAN_POINT('Ctrl Pts',(-46.7229639836046,-3.78802185066086,
-2.70012147277357));
#52957=CARTESIAN_POINT('Ctrl Pts',(-46.5240904519073,0.223758611019232,
-4.6464715207146));
#52958=CARTESIAN_POINT('Ctrl Pts',(-46.3252169202096,4.02994920145744,-2.3236339949505));
#52959=CARTESIAN_POINT('Ctrl Pts',(-46.1263433885124,4.13341419101237,2.13416321642806));
#52960=CARTESIAN_POINT('Ctrl Pts',(-45.9274698568147,0.439089734839147,
4.63108688253373));
#52961=CARTESIAN_POINT('Ctrl Pts',(-45.7285963251174,-3.65867127127512,
2.87295841208375));
#52962=CARTESIAN_POINT('Ctrl Pts',(-45.5297227934199,-4.39483760109253,
-1.52485014635534));
#52963=CARTESIAN_POINT('Ctrl Pts',(-45.3308492617225,-1.09301811922677,
-4.52162325939027));
#52964=CARTESIAN_POINT('Ctrl Pts',(-45.131975730025,3.21306865484875,-3.36391963757244));
#52965=CARTESIAN_POINT('Ctrl Pts',(-44.9331021983275,4.56698135154348,0.88456025429087));
#52966=CARTESIAN_POINT('Ctrl Pts',(-44.7342286666301,1.72474220518251,4.32030436826842));
#52967=CARTESIAN_POINT('Ctrl Pts',(-44.5353551349326,-2.70219362066602,
3.78654395791848));
#52968=CARTESIAN_POINT('Ctrl Pts',(-44.3364816032352,-4.64634839950656,
-0.22630081577383));
#52969=CARTESIAN_POINT('Ctrl Pts',(-44.1376080715377,-2.32142872866073,
-4.03121993527588));
#52970=CARTESIAN_POINT('Ctrl Pts',(-43.9387345398403,2.13642442460452,-4.13224590105312));
#52971=CARTESIAN_POINT('Ctrl Pts',(-43.7398610081428,4.63132642988146,-0.43655584831557));
#52972=CARTESIAN_POINT('Ctrl Pts',(-43.5409874764454,2.8709562020078,3.66024261422239));
#52973=CARTESIAN_POINT('Ctrl Pts',(-43.3421139447479,-1.52725447912609,
4.39400264733715));
#52974=CARTESIAN_POINT('Ctrl Pts',(-43.1432404130505,-4.52222060896932,
1.09054402599357));
#52975=CARTESIAN_POINT('Ctrl Pts',(-42.944366881353,-3.36216115794003,-3.21490868561712));
#52976=CARTESIAN_POINT('Ctrl Pts',(-42.7454933496555,0.887058868437845,
-4.56649669579896));
#52977=CARTESIAN_POINT('Ctrl Pts',(-42.5466198179581,4.32124738512139,-1.72237816561829));
#52978=CARTESIAN_POINT('Ctrl Pts',(-42.3477462862606,3.78506493165666,2.70426495964431));
#52979=CARTESIAN_POINT('Ctrl Pts',(-42.1488727545632,-0.228842952784232,
4.64622388739265));
#52980=CARTESIAN_POINT('Ctrl Pts',(-41.9499992228657,-4.03248946233,2.31922276744054));
#52981=CARTESIAN_POINT('Ctrl Pts',(-41.7511256911683,-4.13107637408695,
-2.13868499323244));
#52982=CARTESIAN_POINT('Ctrl Pts',(-41.5522521594709,-0.434021831106983,
-4.63156459082021));
#52983=CARTESIAN_POINT('Ctrl Pts',(-41.3533786277734,3.66181286145911,-2.86895313249785));
#52984=CARTESIAN_POINT('Ctrl Pts',(-41.1545050960759,4.39316637821677,1.52965835470616));
#52985=CARTESIAN_POINT('Ctrl Pts',(-40.9556315643785,1.08806960630097,4.52281660480072));
#52986=CARTESIAN_POINT('Ctrl Pts',(-40.756758032681,-3.21674775398771,3.36040167182914));
#52987=CARTESIAN_POINT('Ctrl Pts',(-40.5578845009836,-4.56601067305254,
-0.889557217039647));
#52988=CARTESIAN_POINT('Ctrl Pts',(-40.3590109692861,-1.72001361045221,
-4.32218910838897));
#52989=CARTESIAN_POINT('Ctrl Pts',(-40.1601374375886,2.70633548908839,-3.78358477231815));
#52990=CARTESIAN_POINT('Ctrl Pts',(-39.9612639058912,4.64609798441014,0.231385021289438));
#52991=CARTESIAN_POINT('Ctrl Pts',(-39.7623903741937,2.31701611195028,4.03375778223976));
#52992=CARTESIAN_POINT('Ctrl Pts',(-39.5635168424963,-2.14094492163513,
4.12990561046398));
#52993=CARTESIAN_POINT('Ctrl Pts',(-39.3646433107988,-4.6318013652787,0.431487683971952));
#52994=CARTESIAN_POINT('Ctrl Pts',(-39.1657697791014,-2.86694920415351,
-3.66338201251523));
#52995=CARTESIAN_POINT('Ctrl Pts',(-38.9668962474039,1.53206177237593,-4.39232879398173));
#52996=CARTESIAN_POINT('Ctrl Pts',(-38.7680227157065,4.52341124670607,-1.08559486088971));
#52997=CARTESIAN_POINT('Ctrl Pts',(-38.569149184009,3.35864117976647,3.21858585941));
#52998=CARTESIAN_POINT('Ctrl Pts',(-38.3702756523116,-0.892055299348385,
4.56552328344972));
#52999=CARTESIAN_POINT('Ctrl Pts',(-38.1714021206141,-4.32312953778925,
1.7176485403921));
#53000=CARTESIAN_POINT('Ctrl Pts',(-37.9725285889166,-3.78210348034605,
-2.70840520837842));
#53001=CARTESIAN_POINT('Ctrl Pts',(-37.7736550572192,0.233927020528463,
-4.64597069059672));
#53002=CARTESIAN_POINT('Ctrl Pts',(-37.5747815255217,4.03502489462548,-2.31480876285055));
#53003=CARTESIAN_POINT('Ctrl Pts',(-37.3759079938243,4.12873361053465,2.14320420913606));
#53004=CARTESIAN_POINT('Ctrl Pts',(-37.1770344621268,0.428953407669176,
4.63203675318597));
#53005=CARTESIAN_POINT('Ctrl Pts',(-36.9781609304295,-3.66495006692095,
2.86494441757476));
#53006=CARTESIAN_POINT('Ctrl Pts',(-36.7792873987319,-4.39148989488282,
-1.53446473141587));
#53007=CARTESIAN_POINT('Ctrl Pts',(-36.5804138670346,-1.0831197905006,-4.52400453450735));
#53008=CARTESIAN_POINT('Ctrl Pts',(-36.381540335337,3.22042300133372,-3.35687968227903));
#53009=CARTESIAN_POINT('Ctrl Pts',(-36.1826668036397,4.5650345271364,0.894553114616239));
#53010=CARTESIAN_POINT('Ctrl Pts',(-35.983793271942,1.71528295614595,4.32406867304074));
#53011=CARTESIAN_POINT('Ctrl Pts',(-35.7849197402448,-2.71047411689484,
3.78062105618378));
#53012=CARTESIAN_POINT('Ctrl Pts',(-35.5860462085471,-4.64584200599049,
-0.236468949740354));
#53013=CARTESIAN_POINT('Ctrl Pts',(-35.3871726768498,-2.3126007208021,-4.03629079910785));
#53014=CARTESIAN_POINT('Ctrl Pts',(-35.1882991451523,2.1454628550589,-4.12756037464984));
#53015=CARTESIAN_POINT('Ctrl Pts',(-34.9894256134549,4.63227075447169,-0.426419002957134));
#53016=CARTESIAN_POINT('Ctrl Pts',(-34.7905520817573,2.86293877336157,3.66651702420699));
#53017=CARTESIAN_POINT('Ctrl Pts',(-34.59167855006,-1.53686723110675,4.39064968117103));
#53018=CARTESIAN_POINT('Ctrl Pts',(-34.3928050183625,-4.52459646802695,
1.08064439587459));
#53019=CARTESIAN_POINT('Ctrl Pts',(-34.1939314866651,-3.35511717989414,
-3.22225917920893));
#53020=CARTESIAN_POINT('Ctrl Pts',(-33.9950579549676,0.897050662095486,
-4.56454440425889));
#53021=CARTESIAN_POINT('Ctrl Pts',(-33.7961844232701,4.32500651386226,-1.71291685842193));
#53022=CARTESIAN_POINT('Ctrl Pts',(-33.5973108915727,3.77913750027513,2.7125422140183));
#53023=CARTESIAN_POINT('Ctrl Pts',(-33.3984373598752,-0.239010808164181,
4.64571193062998));
#53024=CARTESIAN_POINT('Ctrl Pts',(-33.1995638281778,-4.0375554953079,2.31039198646595));
#53025=CARTESIAN_POINT('Ctrl Pts',(-33.0006902964803,-4.12638590316076,
-2.14772085872751));
#53026=CARTESIAN_POINT('Ctrl Pts',(-32.8018167647829,-0.423884470594582,
-4.63250336906573));
#53027=CARTESIAN_POINT('Ctrl Pts',(-32.6029432330854,3.66808288390419,-2.86093227211442));
#53028=CARTESIAN_POINT('Ctrl Pts',(-32.4040697013879,4.38980815309797,1.53926927072932));
#53029=CARTESIAN_POINT('Ctrl Pts',(-32.2051961696905,1.07816867775268,4.52518704708768));
#53030=CARTESIAN_POINT('Ctrl Pts',(-32.006322637993,-3.22409439248597,3.35335367313942));
#53031=CARTESIAN_POINT('Ctrl Pts',(-31.8074491062956,-4.56405291496391,
-0.899547941038473));
#53032=CARTESIAN_POINT('Ctrl Pts',(-31.6085755745981,-1.71055024792833,
-4.3259430599731));
#53033=CARTESIAN_POINT('Ctrl Pts',(-31.4097020429007,2.71460949912971,-3.7776528130642));
#53034=CARTESIAN_POINT('Ctrl Pts',(-31.2108285112032,4.64558046455413,0.241552595039009));
#53035=CARTESIAN_POINT('Ctrl Pts',(-31.0119549795058,2.30818256050327,4.03881898284705));
#53036=CARTESIAN_POINT('Ctrl Pts',(-30.8130814478083,-2.14997821946597,
4.12521019641897));
#53037=CARTESIAN_POINT('Ctrl Pts',(-30.6142079161108,-4.63273459689848,
0.421349811340259));
#53038=CARTESIAN_POINT('Ctrl Pts',(-30.4153343844134,-2.85892491443397,
-3.66964764554383));
#53039=CARTESIAN_POINT('Ctrl Pts',(-30.216460852716,1.54167084956452,-4.38896531091555));
#53040=CARTESIAN_POINT('Ctrl Pts',(-30.0175873210185,4.52577627151276,-1.07569263687598));
#53041=CARTESIAN_POINT('Ctrl Pts',(-29.818713789321,3.35158916254276,3.22592864061543));
#53042=CARTESIAN_POINT('Ctrl Pts',(-29.6198402576236,-0.902044950697624,
4.56356005939858));
#53043=CARTESIAN_POINT('Ctrl Pts',(-29.4209667259261,-4.32687831109287,
1.70818312537359));
#53044=CARTESIAN_POINT('Ctrl Pts',(-29.2220931942287,-3.77616699499543,
-2.71667597161021));
#53045=CARTESIAN_POINT('Ctrl Pts',(-29.0232196625312,0.244094309603952,
-4.64544760780229));
#53046=CARTESIAN_POINT('Ctrl Pts',(-28.8243461308338,4.04008126134707,-2.30597244357546));
#53047=CARTESIAN_POINT('Ctrl Pts',(-28.6254725991363,4.12403325477644,2.15223493659848));
#53048=CARTESIAN_POINT('Ctrl Pts',(-28.4265990674389,0.418815025952924,
4.63296443790072));
#53049=CARTESIAN_POINT('Ctrl Pts',(-28.2277255357414,-3.67121130865748,
2.85691670092113));
#53050=CARTESIAN_POINT('Ctrl Pts',(-28.0288520040439,-4.38812115487607,
-1.54407196689343));
#53051=CARTESIAN_POINT('Ctrl Pts',(-27.8299784723465,-1.07321627398572,
-4.52636414112578));
#53052=CARTESIAN_POINT('Ctrl Pts',(-27.6311049406491,3.22776192304825,-3.3498236486324));
#53053=CARTESIAN_POINT('Ctrl Pts',(-27.4322314089516,4.56306583771046,0.904541690325447));
#53054=CARTESIAN_POINT('Ctrl Pts',(-27.2333578772542,1.70581549146635,4.32781226694163));
#53055=CARTESIAN_POINT('Ctrl Pts',(-27.0344843455567,-2.7187416308412,3.77468004651361));
#53056=CARTESIAN_POINT('Ctrl Pts',(-26.8356108138592,-4.64531336041423,
-0.246635951098138));
#53057=CARTESIAN_POINT('Ctrl Pts',(-26.6367372821618,-2.30376163634415,
-4.04134233043008));
#53058=CARTESIAN_POINT('Ctrl Pts',(-26.4378637504643,2.15449100944954,-4.12285507858549));
#53059=CARTESIAN_POINT('Ctrl Pts',(-26.2389902187669,4.63319289200362,-0.416280115191373));
#53060=CARTESIAN_POINT('Ctrl Pts',(-26.0401166870694,2.85490763217707,3.67277387277706));
#53061=CARTESIAN_POINT('Ctrl Pts',(-25.841243155372,-1.54647262199725,4.38727568523224));
#53062=CARTESIAN_POINT('Ctrl Pts',(-25.6423696236745,-4.52695065575077,
1.07073958982321));
#53063=CARTESIAN_POINT('Ctrl Pts',(-25.4434960919771,-3.34805713193684,
-3.22959423923561));
#53064=CARTESIAN_POINT('Ctrl Pts',(-25.2446225602796,0.907038159174535,
-4.56257025004749));
#53065=CARTESIAN_POINT('Ctrl Pts',(-25.0457490285821,4.32874492723977,-1.70344734691535));
#53066=CARTESIAN_POINT('Ctrl Pts',(-24.8468754968847,3.77319196806387,2.72080647620431));
#53067=CARTESIAN_POINT('Ctrl Pts',(-24.6480019651872,-0.249177518760706,
4.64517772243015));
#53068=CARTESIAN_POINT('Ctrl Pts',(-24.4491284334898,-4.04260218971858,
2.30155013947114));
#53069=CARTESIAN_POINT('Ctrl Pts',(-24.2502549017923,-4.12167566819881,
-2.15674643734374));
#53070=CARTESIAN_POINT('Ctrl Pts',(-24.0513813700949,-0.41374507981445,
-4.63341995913882));
#53071=CARTESIAN_POINT('Ctrl Pts',(-23.8525078383975,3.6743353374348,-2.8528977088032));
#53072=CARTESIAN_POINT('Ctrl Pts',(-23.6536343067,4.38642890223714,1.54887281415735));
#53073=CARTESIAN_POINT('Ctrl Pts',(-23.4547607750026,1.06826258512985,4.52753581521215));
#53074=CARTESIAN_POINT('Ctrl Pts',(-23.255887243305,-3.23142558862902,3.34628961298491));
#53075=CARTESIAN_POINT('Ctrl Pts',(-23.0570137116077,-4.56207329655801,
-0.909534356497557));
#53076=CARTESIAN_POINT('Ctrl Pts',(-22.8581401799101,-1.70107869242952,
-4.32967629170811));
#53077=CARTESIAN_POINT('Ctrl Pts',(-22.6592666482128,2.72287050708144,-3.77170276009168));
#53078=CARTESIAN_POINT('Ctrl Pts',(-22.4603931165152,4.64504069389063,0.251719011830838));
#53079=CARTESIAN_POINT('Ctrl Pts',(-22.2615195848178,2.29933795361846,4.04386083883543));
#53080=CARTESIAN_POINT('Ctrl Pts',(-22.0626460531203,-2.15900121960593,
4.12049502396947));
#53081=CARTESIAN_POINT('Ctrl Pts',(-21.8637725214229,-4.63364563923833,
0.411209920581015));
#53082=CARTESIAN_POINT('Ctrl Pts',(-21.6648989897254,-2.85088693140123,
-3.67589570216326));
#53083=CARTESIAN_POINT('Ctrl Pts',(-21.466025458028,1.5512725426552,-4.38558080614428));
#53084=CARTESIAN_POINT('Ctrl Pts',(-21.2671519263305,4.52811961933476,-1.06578526064715));
#53085=CARTESIAN_POINT('Ctrl Pts',(-21.0682783946331,3.3445210923057,3.23325597068022));
#53086=CARTESIAN_POINT('Ctrl Pts',(-20.8694048629356,-0.912030281547263,
4.5615749773908));
#53087=CARTESIAN_POINT('Ctrl Pts',(-20.6705313312382,-4.33060636006784,
1.69870952871791));
#53088=CARTESIAN_POINT('Ctrl Pts',(-20.4716577995407,-3.77021242304282,
-2.72493372285468));
#53089=CARTESIAN_POINT('Ctrl Pts',(-20.2727842678433,0.254260429547719,
-4.64490227483671));
#53090=CARTESIAN_POINT('Ctrl Pts',(-20.0739107361458,4.04511827740384,-2.29712507944832));
#53091=CARTESIAN_POINT('Ctrl Pts',(-19.8750372044484,4.1193131462509,2.16125535556112));
#53092=CARTESIAN_POINT('Ctrl Pts',(-19.6761636727509,0.408674638249995,
4.6338699322346));
#53093=CARTESIAN_POINT('Ctrl Pts',(-19.4772901410535,-3.67745496649536,
2.84887530057306));
#53094=CARTESIAN_POINT('Ctrl Pts',(-19.278416609356,-4.38473139720753,-1.55367180677245));
#53095=CARTESIAN_POINT('Ctrl Pts',(-19.0795430776586,-1.0633076171167,-4.52870206794382));
#53096=CARTESIAN_POINT('Ctrl Pts',(-18.8806695459611,3.23508538484131,-3.34275157042865));
#53097=CARTESIAN_POINT('Ctrl Pts',(-18.6817960142637,4.56107529269504,0.914525933576483));
#53098=CARTESIAN_POINT('Ctrl Pts',(-18.4829224825662,1.69633985648975,4.33153513204054));
#53099=CARTESIAN_POINT('Ctrl Pts',(-18.2840489508687,-2.72699612290642,
3.76872095736344));
#53100=CARTESIAN_POINT('Ctrl Pts',(-18.0851754191713,-4.64476246530983,
-0.256801771150557));
#53101=CARTESIAN_POINT('Ctrl Pts',(-17.8863018874738,-2.29491151762317,
-4.0463745050474));
#53102=CARTESIAN_POINT('Ctrl Pts',(-17.6874283557763,2.16350884453443,-4.11813003539688));
#53103=CARTESIAN_POINT('Ctrl Pts',(-17.4885548240789,4.63409283806047,-0.406139233580442));
#53104=CARTESIAN_POINT('Ctrl Pts',(-17.2896812923815,2.846862816921,3.6790131299643));
#53105=CARTESIAN_POINT('Ctrl Pts',(-17.090807760684,-1.55607060579087,4.38388067568116));
#53106=CARTESIAN_POINT('Ctrl Pts',(-16.8919342289866,-4.52928316086499,
1.06082965528021));
#53107=CARTESIAN_POINT('Ctrl Pts',(-16.6930606972891,-3.34098104788346,
-3.23691383056463));
#53108=CARTESIAN_POINT('Ctrl Pts',(-16.4941871655917,0.917021311838145,
-4.5605742426203));
#53109=CARTESIAN_POINT('Ctrl Pts',(-16.2953136338942,4.33246260734816,-1.69396967645442));
#53110=CARTESIAN_POINT('Ctrl Pts',(-16.0964401021967,3.76722836350003,2.72905770661926));
#53111=CARTESIAN_POINT('Ctrl Pts',(-15.8975665704993,-0.259343035878605,
4.64462126535182));
#53112=CARTESIAN_POINT('Ctrl Pts',(-15.6986930388018,-4.04762952139003,
2.29269726880566));
#53113=CARTESIAN_POINT('Ctrl Pts',(-15.4998195071044,-4.11694569176161,
-2.16576168585147));
#53114=CARTESIAN_POINT('Ctrl Pts',(-15.3009459754069,-0.40360370733112,
-4.63431435664923));
#53115=CARTESIAN_POINT('Ctrl Pts',(-15.1020724437095,3.68057019210366,-2.84484948104731));
#53116=CARTESIAN_POINT('Ctrl Pts',(-14.903198912012,4.38302864181985,1.55846893899236));
#53117=CARTESIAN_POINT('Ctrl Pts',(-14.7043253803146,1.05835137587945,4.5298628979243));
#53118=CARTESIAN_POINT('Ctrl Pts',(-14.5054518486171,-3.23874130730283,
3.33920952520015));
#53119=CARTESIAN_POINT('Ctrl Pts',(-14.3065783169196,-4.56007182731658,
-0.919516415585235));
#53120=CARTESIAN_POINT('Ctrl Pts',(-14.1077047852222,-1.69159898932142,
-4.33338878571307));
#53121=CARTESIAN_POINT('Ctrl Pts',(-13.9088312535247,2.73111847337605,-3.76573464189939));
#53122=CARTESIAN_POINT('Ctrl Pts',(-13.7099577218273,4.64447867500497,0.261884222971118));
#53123=CARTESIAN_POINT('Ctrl Pts',(-13.5110841901299,2.29048233365862,4.04888332605607));
#53124=CARTESIAN_POINT('Ctrl Pts',(-13.3122106584324,-2.16801387883773,
4.1157601156996));
#53125=CARTESIAN_POINT('Ctrl Pts',(-13.1133371267349,-4.63453448793457,
0.401068060261169));
#53126=CARTESIAN_POINT('Ctrl Pts',(-12.9144635950375,-2.84283529355476,
-3.68212615244732));
#53127=CARTESIAN_POINT('Ctrl Pts',(-12.7155900633401,1.56086680565895,-4.38217529587864));
#53128=CARTESIAN_POINT('Ctrl Pts',(-12.5167165316425,4.53044127894822,-1.05587277965632));
#53129=CARTESIAN_POINT('Ctrl Pts',(-12.3178429999451,3.33743700290902,3.24056781450885));
#53130=CARTESIAN_POINT('Ctrl Pts',(-12.1189694682477,-0.922011244070831,
4.55956804693427));
#53131=CARTESIAN_POINT('Ctrl Pts',(-11.9200959365502,-4.33431366685802,
1.68922779580046));
#53132=CARTESIAN_POINT('Ctrl Pts',(-11.7212224048528,-3.76423979300867,
-2.73317842255992));
#53133=CARTESIAN_POINT('Ctrl Pts',(-11.5223488731553,0.264425331667373,
-4.64433469431195));
#53134=CARTESIAN_POINT('Ctrl Pts',(-11.3234753414579,4.05013591867016,-2.2882667128451));
#53135=CARTESIAN_POINT('Ctrl Pts',(-11.1246018097604,4.11457330756578,2.17026542281901));
#53136=CARTESIAN_POINT('Ctrl Pts',(-10.925728278063,0.398532293129632,4.63475323185059));
#53137=CARTESIAN_POINT('Ctrl Pts',(-10.7268547463655,-3.68368101052949,
2.84082025504633));
#53138=CARTESIAN_POINT('Ctrl Pts',(-10.5279812146681,-4.38132063811301,
-1.56326420507285));
#53139=CARTESIAN_POINT('Ctrl Pts',(-10.3291076829706,-1.05339386735279,
-4.53101830376359));
#53140=CARTESIAN_POINT('Ctrl Pts',(-10.1302341512731,3.24239335163591,-3.3356634815407));
#53141=CARTESIAN_POINT('Ctrl Pts',(-9.93136061957567,4.55906290162419,0.924505796548103));
#53142=CARTESIAN_POINT('Ctrl Pts',(-9.7324870878782,1.68685609660134,4.33523725050613));
#53143=CARTESIAN_POINT('Ctrl Pts',(-9.53361355618078,-2.73523755355419,
3.76274381727536));
#53144=CARTESIAN_POINT('Ctrl Pts',(-9.33474002448328,-4.64418932331583,
-0.266966361206601));
#53145=CARTESIAN_POINT('Ctrl Pts',(-9.13586649278587,-2.28605040702846,
-4.05138729885728));
#53146=CARTESIAN_POINT('Ctrl Pts',(-8.9369929610884,2.17251631712126,-4.1133852677155));
#53147=CARTESIAN_POINT('Ctrl Pts',(-8.73811942939097,4.63497058833175,-0.395996406695693));
#53148=CARTESIAN_POINT('Ctrl Pts',(-8.53924589769349,2.8388043661253,3.68523476588466));
#53149=CARTESIAN_POINT('Ctrl Pts',(-8.34037236599606,-1.56566113651624,
4.38046466877884));
#53150=CARTESIAN_POINT('Ctrl Pts',(-8.14149883429858,-4.53159397219767,
1.05091463971103));
#53151=CARTESIAN_POINT('Ctrl Pts',(-7.94262530260114,-3.33388896162619,
-3.24421791813743));
#53152=CARTESIAN_POINT('Ctrl Pts',(-7.74375177090367,0.927000072270143,
-4.55855639153756));
#53153=CARTESIAN_POINT('Ctrl Pts',(-7.54487823920623,4.33615953638097,-1.68448389243425));
#53154=CARTESIAN_POINT('Ctrl Pts',(-7.34600470750878,3.76124671514718,2.73729586574244));
#53155=CARTESIAN_POINT('Ctrl Pts',(-7.14713117581134,-0.269507310827875,
4.64404256206009));
#53156=CARTESIAN_POINT('Ctrl Pts',(-6.94825764411386,-4.05263746624359,
2.28383341687229));
#53157=CARTESIAN_POINT('Ctrl Pts',(-6.74938411241643,-4.11219599650301,
-2.17476656107136));
#53158=CARTESIAN_POINT('Ctrl Pts',(-6.55051058071893,-0.393460401720496,
-4.63518655731204));
#53159=CARTESIAN_POINT('Ctrl Pts',(-6.35163704902152,3.68678741805236,-2.83678762739698));
#53160=CARTESIAN_POINT('Ctrl Pts',(-6.15276351732402,4.37960738812384,1.56805759927625));
#53161=CARTESIAN_POINT('Ctrl Pts',(-5.9538899856266,1.04843509748853,4.53216828407051));
#53162=CARTESIAN_POINT('Ctrl Pts',(-5.75501645392912,-3.24604151349715,
3.33211344371086));
#53163=CARTESIAN_POINT('Ctrl Pts',(-5.5561429222317,-4.55804851676996,-0.929494070517982));
#53164=CARTESIAN_POINT('Ctrl Pts',(-5.35726939053425,-1.68211118411471,
-4.33708052415461));
#53165=CARTESIAN_POINT('Ctrl Pts',(-5.15839585883678,2.73935335870827,-3.75974848717027));
#53166=CARTESIAN_POINT('Ctrl Pts',(-4.95952232713934,4.64389441021169,0.272048179955862));
#53167=CARTESIAN_POINT('Ctrl Pts',(-4.76064879544187,2.28161574375186,4.05388642010502));
#53168=CARTESIAN_POINT('Ctrl Pts',(-4.56177526374442,-2.17701615533913,
4.11100549494485));
#53169=CARTESIAN_POINT('Ctrl Pts',(-4.36290173204695,-4.63540113618978,
0.39092427771653));
#53170=CARTESIAN_POINT('Ctrl Pts',(-4.16402820034951,-2.83477004425545,
-3.68833896421277));
#53171=CARTESIAN_POINT('Ctrl Pts',(-3.96515466865204,1.57045360167918,-4.3787488008511));
#53172=CARTESIAN_POINT('Ctrl Pts',(-3.76628113695459,4.53274122213237,-1.04595523303274));
#53173=CARTESIAN_POINT('Ctrl Pts',(-3.56740760525717,3.33033696057287,3.24786412131688));
#53174=CARTESIAN_POINT('Ctrl Pts',(-3.36853407355969,-0.931987851432297,
4.55753930740539));
#53175=CARTESIAN_POINT('Ctrl Pts',(-3.16966054186226,-4.33800009858357,
1.67973791583561));
#53176=CARTESIAN_POINT('Ctrl Pts',(-2.97078701016478,-3.7582493508756,-2.74140992511906));
#53177=CARTESIAN_POINT('Ctrl Pts',(-2.77191347846734,0.274589377725611,
-4.6437450693177));
#53178=CARTESIAN_POINT('Ctrl Pts',(-2.57303994676988,4.05513338610117,-2.27939700785305));
#53179=CARTESIAN_POINT('Ctrl Pts',(-2.37416641507242,4.10981522480361,2.1792643808313));
#53180=CARTESIAN_POINT('Ctrl Pts',(-2.17529288337496,0.388385276010726,
4.63561568142362));
#53181=CARTESIAN_POINT('Ctrl Pts',(-1.9764193516775,-3.68988419353248,2.8327490559136));
#53182=CARTESIAN_POINT('Ctrl Pts',(-1.77754581998008,-4.37789874545427,
-1.57284430658088));
#53183=CARTESIAN_POINT('Ctrl Pts',(-1.57867228828259,-1.04345647049151,
-4.53332191837153));
#53184=CARTESIAN_POINT('Ctrl Pts',(-1.37979875658517,3.24965066464255,-3.32854226935553));
#53185=CARTESIAN_POINT('Ctrl Pts',(-1.1809252248877,4.55709499515704,0.934448855132265));
#53186=CARTESIAN_POINT('Ctrl Pts',(-0.982051693190257,1.6772390282778,4.33897973856184));
#53187=CARTESIAN_POINT('Ctrl Pts',(-0.783178161492788,-2.7432294143621,
3.75663321416178));
#53188=CARTESIAN_POINT('Ctrl Pts',(-0.584304629795343,-4.64404053043935,
-0.276911636729995));
#53189=CARTESIAN_POINT('Ctrl Pts',(-0.385431098097881,-2.27633433757937,
-4.05679287690181));
#53190=CARTESIAN_POINT('Ctrl Pts',(-0.18655756640042,2.17991358653948,-4.10783847096312));
#53191=CARTESIAN_POINT('Ctrl Pts',(0.0123159652969969,4.63889703590742,
-0.38736179081203));
#53192=CARTESIAN_POINT('Ctrl Pts',(0.2111894969945,2.82452520683169,3.6945553743333));
#53193=CARTESIAN_POINT('Ctrl Pts',(0.343771851459442,-0.0987079820474816,
4.14442455744695));
#53194=CARTESIAN_POINT('Ctrl Pts',(0.410063028691923,-1.33182005907514,
3.70064107017218));
#53195=CARTESIAN_POINT('',(0.,3.89175630324273,-0.568086152067144));
#53196=CARTESIAN_POINT('Ctrl Pts',(-8.04911692853238E-15,3.89860680620593,
-0.567889413565848));
#53197=CARTESIAN_POINT('Ctrl Pts',(-1.07269636646957E-14,3.90357565560566,
-0.487072913846011));
#53198=CARTESIAN_POINT('Ctrl Pts',(2.32719976779923E-14,3.9058565072249,
-0.406193250504373));
#53199=CARTESIAN_POINT('Ctrl Pts',(1.50990331349021E-14,3.90537360502758,
-0.32534746124043));
#53200=CARTESIAN_POINT('Ctrl Pts',(2.76112838444297E-15,3.90464797577591,
-0.203865161326043));
#53201=CARTESIAN_POINT('Ctrl Pts',(-6.82244033398785E-15,3.89768417373717,
-0.0824584493220015));
#53202=CARTESIAN_POINT('Ctrl Pts',(-9.2148511043888E-15,3.88471463000325,
0.0384874957482827));
#53203=CARTESIAN_POINT('Ctrl Pts',(-1.06155140461537E-14,3.87712146937028,
0.109296616536635));
#53204=CARTESIAN_POINT('Ctrl Pts',(-8.57920104564936E-15,3.86746876710794,
0.179947588184905));
#53205=CARTESIAN_POINT('Ctrl Pts',(-5.38458166943201E-15,3.85579555749106,
0.250360153300933));
#53206=CARTESIAN_POINT('Ctrl Pts',(-2.93363335536299E-15,3.84683973832737,
0.304381473976933));
#53207=CARTESIAN_POINT('Ctrl Pts',(2.92444448707381E-14,3.83669450630869,
0.358262424434777));
#53208=CARTESIAN_POINT('Ctrl Pts',(3.66373598126302E-14,3.82537548919011,
0.411965518384648));
#53209=CARTESIAN_POINT('Ctrl Pts',(3.95702663936449E-14,3.82088502500127,
0.433270532564362));
#53210=CARTESIAN_POINT('Ctrl Pts',(2.77330594251881E-14,3.81620949621549,
0.454548537547267));
#53211=CARTESIAN_POINT('Ctrl Pts',(2.66453525910038E-14,3.81135385472659,
0.475780514671049));
#53212=CARTESIAN_POINT('Ctrl Pts',(2.04972267428747E-14,3.78390795293671,
0.595791590504276));
#53213=CARTESIAN_POINT('Ctrl Pts',(-4.54776054783641E-15,3.75068649423825,
0.714458464692085));
#53214=CARTESIAN_POINT('Ctrl Pts',(6.77236045021345E-15,3.71192731145421,
0.831378922517886));
#53215=CARTESIAN_POINT('Ctrl Pts',(1.66774663235071E-14,3.67801302651818,
0.933684323115462));
#53216=CARTESIAN_POINT('Ctrl Pts',(2.44821053095673E-14,3.63985784417228,
1.03465273289086));
#53217=CARTESIAN_POINT('Ctrl Pts',(2.1094237467878E-14,3.59759146080822,
1.1339965863823));
#53218=CARTESIAN_POINT('Ctrl Pts',(1.96107288013879E-14,3.57908349386506,
1.17749812614235));
#53219=CARTESIAN_POINT('Ctrl Pts',(-2.10007386744337E-15,3.55978689124514,
1.22068790168118));
#53220=CARTESIAN_POINT('Ctrl Pts',(-7.54951656745106E-15,3.53971110958904,
1.26354040163506));
#53221=CARTESIAN_POINT('Ctrl Pts',(-1.09169839508804E-14,3.52730533827528,
1.29002098026246));
#53222=CARTESIAN_POINT('Ctrl Pts',(5.45879109936265E-15,3.51460201437022,
1.31637274971798));
#53223=CARTESIAN_POINT('Ctrl Pts',(3.88578058618805E-15,3.50160321988813,
1.342589505873));
#53224=CARTESIAN_POINT('Ctrl Pts',(2.67861275308231E-15,3.49162761804916,
1.36270890396579));
#53225=CARTESIAN_POINT('Ctrl Pts',(-2.2629275639963E-14,3.48147646278302,
1.38275156313355));
#53226=CARTESIAN_POINT('Ctrl Pts',(-1.90958360235527E-14,3.47116236725966,
1.40269254368647));
#53227=CARTESIAN_POINT('Ctrl Pts',(-3.81991545211577E-16,3.4165367331714,
1.50830419955852));
#53228=CARTESIAN_POINT('Ctrl Pts',(-2.56312607080658E-15,3.35728334038055,
1.61119239851335));
#53229=CARTESIAN_POINT('Ctrl Pts',(-3.05311331771918E-15,3.2936112110481,
1.71099772625822));
#53230=CARTESIAN_POINT('Ctrl Pts',(-3.53944506258838E-15,3.23041410142351,
1.81005846609429));
#53231=CARTESIAN_POINT('Ctrl Pts',(2.27276944610714E-14,3.16286336209999,
1.90608284429344));
#53232=CARTESIAN_POINT('Ctrl Pts',(2.23154827949656E-14,3.09112535423912,
1.99868541489889));
#53233=CARTESIAN_POINT('Ctrl Pts',(2.19154714197454E-14,3.02151058702234,
2.08854721324816));
#53234=CARTESIAN_POINT('Ctrl Pts',(2.65458674629001E-14,2.94795215192818,
2.17518718759128));
#53235=CARTESIAN_POINT('Ctrl Pts',(2.56183962932255E-14,2.87057487892889,
2.25821308833352));
#53236=CARTESIAN_POINT('Ctrl Pts',(2.49982485680853E-14,2.81883705526706,
2.3137278311703));
#53237=CARTESIAN_POINT('Ctrl Pts',(1.93937339864825E-14,2.76539134747941,
2.36762595258285));
#53238=CARTESIAN_POINT('Ctrl Pts',(2.06779038336435E-14,2.71026985849297,
2.41977831105942));
#53239=CARTESIAN_POINT('Ctrl Pts',(2.12972403643666E-14,2.68368556216127,
2.4449306387202));
#53240=CARTESIAN_POINT('Ctrl Pts',(5.6667007202163E-15,2.65671142532864,
2.46967675127111));
#53241=CARTESIAN_POINT('Ctrl Pts',(7.02216063075412E-15,2.62935077228863,
2.49400127076223));
#53242=CARTESIAN_POINT('Ctrl Pts',(7.56656610583958E-15,2.61836166873706,
2.5037709448683));
#53243=CARTESIAN_POINT('Ctrl Pts',(5.67951698064326E-14,2.60731240461056,
2.51347060811221));
#53244=CARTESIAN_POINT('Ctrl Pts',(5.52891066263328E-14,2.59620959029183,
2.52309397415439));
#53245=CARTESIAN_POINT('Ctrl Pts',(4.38243996477893E-14,2.51169088318614,
2.59635057671843));
#53246=CARTESIAN_POINT('Ctrl Pts',(6.92167992872912E-15,2.42396547938964,
2.66528379542761));
#53247=CARTESIAN_POINT('Ctrl Pts',(7.13318293321663E-15,2.33318085873788,
2.72955162985394));
#53248=CARTESIAN_POINT('Ctrl Pts',(7.25502550614834E-15,2.28088168790746,
2.76657502024136));
#53249=CARTESIAN_POINT('Ctrl Pts',(1.05441232867865E-14,2.22756672536945,
2.80204936230559));
#53250=CARTESIAN_POINT('Ctrl Pts',(1.21846976952611E-14,2.17326041266705,
2.83590230914314));
#53251=CARTESIAN_POINT('Ctrl Pts',(1.50908074605165E-14,2.07718824792624,
2.89579085107679));
#53252=CARTESIAN_POINT('Ctrl Pts',(1.62408507202679E-14,1.97801391730883,
2.95060784545968));
#53253=CARTESIAN_POINT('Ctrl Pts',(2.30648833365876E-14,1.87615319865268,
3.00032665839637));
#53254=CARTESIAN_POINT('Ctrl Pts',(2.99199362602384E-14,1.77382944721587,
3.05027148034329));
#53255=CARTESIAN_POINT('Ctrl Pts',(4.48598975355489E-14,1.66879386290452,
3.09507168092574));
#53256=CARTESIAN_POINT('Ctrl Pts',(5.18474152499948E-14,1.56146419487867,
3.13464824772879));
#53257=CARTESIAN_POINT('Ctrl Pts',(5.3933480596659E-14,1.52942181441002,
3.14646350286254));
#53258=CARTESIAN_POINT('Ctrl Pts',(1.45371142394304E-14,1.49717499764285,
3.15781283903599));
#53259=CARTESIAN_POINT('Ctrl Pts',(1.41830991395864E-14,1.46473499388962,
3.16869325771511));
#53260=CARTESIAN_POINT('Ctrl Pts',(1.39834571560156E-14,1.44644089654973,
3.17482912132131));
#53261=CARTESIAN_POINT('Ctrl Pts',(8.93808405976052E-15,1.42808321458713,
3.18081643667667));
#53262=CARTESIAN_POINT('Ctrl Pts',(9.49240686054509E-15,1.40968594116012,
3.18664793170129));
#53263=CARTESIAN_POINT('Ctrl Pts',(1.26906562468948E-14,1.30354008469316,
3.22029362579435));
#53264=CARTESIAN_POINT('Ctrl Pts',(-3.59846457681172E-15,1.19592044539289,
3.24881064998302));
#53265=CARTESIAN_POINT('Ctrl Pts',(-1.0547118733939E-15,1.0872294197538,
3.27220684178733));
#53266=CARTESIAN_POINT('Ctrl Pts',(1.49132431113259E-15,0.978440824133397,
3.29562403593276));
#53267=CARTESIAN_POINT('Ctrl Pts',(3.55444460830568E-14,0.868577967529425,
3.31391114504953));
#53268=CARTESIAN_POINT('Ctrl Pts',(4.57966997657877E-14,0.758041213997769,
3.32702390602429));
#53269=CARTESIAN_POINT('Ctrl Pts',(5.59225919287158E-14,0.648866852833935,
3.33997504903125));
#53270=CARTESIAN_POINT('Ctrl Pts',(-2.24905070291909E-15,0.539034240310298,
3.34787845352108));
#53271=CARTESIAN_POINT('Ctrl Pts',(4.01068067645838E-15,0.428939545617156,
3.35064237850942));
#53272=CARTESIAN_POINT('Ctrl Pts',(7.73133663615164E-15,0.363501516872001,
3.35228519884096));
#53273=CARTESIAN_POINT('Ctrl Pts',(-4.85704133178524E-15,0.297971159229881,
3.3521113829659));
#53274=CARTESIAN_POINT('Ctrl Pts',(-1.02279296143593E-14,0.232435308205704,
3.35009360870352));
#53275=CARTESIAN_POINT('Ctrl Pts',(-1.28532778767699E-14,0.200400675653365,
3.34910729882796));
#53276=CARTESIAN_POINT('Ctrl Pts',(1.79661326338799E-14,0.168364780635814,
3.34768031034544));
#53277=CARTESIAN_POINT('Ctrl Pts',(1.75137682134618E-14,0.136338088246541,
3.34580893463049));
#53278=CARTESIAN_POINT('Ctrl Pts',(1.72908107034634E-14,0.120553045775695,
3.34488658695936));
#53279=CARTESIAN_POINT('Ctrl Pts',(4.81777123886202E-15,0.104779344373586,
3.34385680185526));
#53280=CARTESIAN_POINT('Ctrl Pts',(5.6621374255883E-15,0.0890209173056848,
3.34271970942635));
#53281=CARTESIAN_POINT('Ctrl Pts',(1.14070011246775E-14,-0.0181956162792568,
3.3349832070414));
#53282=CARTESIAN_POINT('Ctrl Pts',(2.34325705547898E-14,-0.124748133264004,
3.32228092968165));
#53283=CARTESIAN_POINT('Ctrl Pts',(2.26901830657766E-14,-0.230273591897684,
3.30457403911883));
#53284=CARTESIAN_POINT('Ctrl Pts',(2.19582654213507E-14,-0.334310831551059,
3.2871168677324));
#53285=CARTESIAN_POINT('Ctrl Pts',(-1.6042210484668E-14,-0.437350531390714,
3.26479505345607));
#53286=CARTESIAN_POINT('Ctrl Pts',(-1.62231339473351E-14,-0.539027315639043,
3.23752483134509));
#53287=CARTESIAN_POINT('Ctrl Pts',(-1.63984945268408E-14,-0.637577827248858,
3.21109309119302));
#53288=CARTESIAN_POINT('Ctrl Pts',(6.57984010550879E-17,-0.734848489443402,
3.18001228206578));
#53289=CARTESIAN_POINT('Ctrl Pts',(-4.31252256127834E-15,-0.830480771345168,
3.14416574488326));
#53290=CARTESIAN_POINT('Ctrl Pts',(-8.36192191764401E-15,-0.918928672746715,
3.11101218080159));
#53291=CARTESIAN_POINT('Ctrl Pts',(1.49022108953379E-15,-1.00597524039212,
3.07378159410529));
#53292=CARTESIAN_POINT('Ctrl Pts',(0.,-1.0913102200307,3.03235215074973));
#53293=CARTESIAN_POINT('Ctrl Pts',(-0.596163522034903,-3.93901438905508,
-0.00135576060872734));
#53294=CARTESIAN_POINT('Ctrl Pts',(-0.592210557955047,-3.93937169862689,
-0.0791783416986369));
#53295=CARTESIAN_POINT('Ctrl Pts',(-0.58825759387519,-3.93726116271843,
-0.156981519214978));
#53296=CARTESIAN_POINT('Ctrl Pts',(-0.584304629795334,-3.9326209789498,
-0.234634368276791));
#53297=CARTESIAN_POINT('Ctrl Pts',(-0.518013452562853,-3.85480513281932,
-1.53687205012064));
#53298=CARTESIAN_POINT('Ctrl Pts',(-0.45172227533037,-3.06556973519939,
-2.79683246351116));
#53299=CARTESIAN_POINT('Ctrl Pts',(-0.385431098097887,-1.92824404903633,
-3.43532026921666));
#53300=CARTESIAN_POINT('Ctrl Pts',(-0.319139920865397,-0.790918362873148,
-4.07380807492224));
#53301=CARTESIAN_POINT('Ctrl Pts',(-0.252848743632905,0.694497611833248,
-4.09082327294269));
#53302=CARTESIAN_POINT('Ctrl Pts',(-0.186557566400421,1.8470361740811,-3.479251425261));
#53303=CARTESIAN_POINT('Ctrl Pts',(-0.124371710933646,2.92819960251862,
-2.90555338405549));
#53304=CARTESIAN_POINT('Ctrl Pts',(-0.0621858554668791,3.71643826597518,
-1.77871263703401));
#53305=CARTESIAN_POINT('Ctrl Pts',(-9.86016823745217E-14,3.89860680620567,
-0.567889413567609));
#53306=CARTESIAN_POINT('',(-109.567,-1.87158653174005,-2.62360084934985));
#53307=CARTESIAN_POINT('Ctrl Pts',(-109.567,-1.87558868214585,-2.62754025481268));
#53308=CARTESIAN_POINT('Ctrl Pts',(-109.567,-1.93405508168532,-2.59497549554658));
#53309=CARTESIAN_POINT('Ctrl Pts',(-109.567,-1.99134228758153,-2.56051026827204));
#53310=CARTESIAN_POINT('Ctrl Pts',(-109.567,-2.04734666558749,-2.52416324142431));
#53311=CARTESIAN_POINT('Ctrl Pts',(-109.567,-2.13340847164491,-2.46830884420198));
#53312=CARTESIAN_POINT('Ctrl Pts',(-109.567,-2.21644226853764,-2.4080133982524));
#53313=CARTESIAN_POINT('Ctrl Pts',(-109.567,-2.29635488563297,-2.34366975158224));
#53314=CARTESIAN_POINT('Ctrl Pts',(-109.567,-2.34682481961543,-2.30303261920351));
#53315=CARTESIAN_POINT('Ctrl Pts',(-109.567,-2.39604948944602,-2.26077970899706));
#53316=CARTESIAN_POINT('Ctrl Pts',(-109.567,-2.44400132255651,-2.21700032194834));
#53317=CARTESIAN_POINT('Ctrl Pts',(-109.567,-2.47482458050397,-2.18885909663428));
#53318=CARTESIAN_POINT('Ctrl Pts',(-109.567,-2.50512185085323,-2.1600870049542));
#53319=CARTESIAN_POINT('Ctrl Pts',(-109.567,-2.53488497154578,-2.13070632870751));
#53320=CARTESIAN_POINT('Ctrl Pts',(-109.567,-2.54830243821907,-2.11746127122677));
#53321=CARTESIAN_POINT('Ctrl Pts',(-109.567,-2.56161091598415,-2.10409282722601));
#53322=CARTESIAN_POINT('Ctrl Pts',(-109.567,-2.57480027481449,-2.09061288448896));
#53323=CARTESIAN_POINT('Ctrl Pts',(-109.567,-2.64900045473092,-2.01477794897633));
#53324=CARTESIAN_POINT('Ctrl Pts',(-109.567,-2.71951129357198,-1.9353409036445));
#53325=CARTESIAN_POINT('Ctrl Pts',(-109.567,-2.78623172025196,-1.85270968846994));
#53326=CARTESIAN_POINT('Ctrl Pts',(-109.567,-2.84985923039024,-1.77390895617731));
#53327=CARTESIAN_POINT('Ctrl Pts',(-109.567,-2.91003979995533,-1.69220250627302));
#53328=CARTESIAN_POINT('Ctrl Pts',(-109.567,-2.96666467242472,-1.60790763032119));
#53329=CARTESIAN_POINT('Ctrl Pts',(-109.567,-2.99143805413007,-1.57102862209226));
#53330=CARTESIAN_POINT('Ctrl Pts',(-109.567,-3.01553055578497,-1.53365375878569));
#53331=CARTESIAN_POINT('Ctrl Pts',(-109.567,-3.03893156594076,-1.49580784353154));
#53332=CARTESIAN_POINT('Ctrl Pts',(-109.567,-3.04980560210158,-1.47822151506651));
#53333=CARTESIAN_POINT('Ctrl Pts',(-109.567,-3.06053031082592,-1.46053345873251));
#53334=CARTESIAN_POINT('Ctrl Pts',(-109.567,-3.07110455244537,-1.44274609509514));
#53335=CARTESIAN_POINT('Ctrl Pts',(-109.567,-3.08003851032833,-1.42771791971349));
#53336=CARTESIAN_POINT('Ctrl Pts',(-109.567,-3.08886464794213,-1.41261942057115));
#53337=CARTESIAN_POINT('Ctrl Pts',(-109.567,-3.09757568073968,-1.3974639260691));
#53338=CARTESIAN_POINT('Ctrl Pts',(-109.567,-3.15304228551282,-1.3009628746756));
#53339=CARTESIAN_POINT('Ctrl Pts',(-109.567,-3.20391780446871,-1.20203235076329));
#53340=CARTESIAN_POINT('Ctrl Pts',(-109.567,-3.25009311850581,-1.10110149034648));
#53341=CARTESIAN_POINT('Ctrl Pts',(-109.567,-3.29699647665682,-0.998579257561797));
#53342=CARTESIAN_POINT('Ctrl Pts',(-109.567,-3.33905083589063,-0.893992444125954));
#53343=CARTESIAN_POINT('Ctrl Pts',(-109.567,-3.37610808814847,-0.787749106949813));
#53344=CARTESIAN_POINT('Ctrl Pts',(-109.567,-3.41307771922245,-0.681756980168778));
#53345=CARTESIAN_POINT('Ctrl Pts',(-109.567,-3.44507435458282,-0.574115341585501));
#53346=CARTESIAN_POINT('Ctrl Pts',(-109.567,-3.471909492288,-0.465199525320855));
#53347=CARTESIAN_POINT('Ctrl Pts',(-109.567,-3.48930969706608,-0.394577286396749));
#53348=CARTESIAN_POINT('Ctrl Pts',(-109.567,-3.50453895879291,-0.323418758370256));
#53349=CARTESIAN_POINT('Ctrl Pts',(-109.567,-3.51753498407954,-0.251822000732028));
#53350=CARTESIAN_POINT('Ctrl Pts',(-109.567,-3.52185337791623,-0.228031419374075));
#53351=CARTESIAN_POINT('Ctrl Pts',(-109.567,-3.5259251160337,-0.204192432008078));
#53352=CARTESIAN_POINT('Ctrl Pts',(-109.567,-3.52974768103556,-0.18030858771712));
#53353=CARTESIAN_POINT('Ctrl Pts',(-109.567,-3.5322279650709,-0.164811475786041));
#53354=CARTESIAN_POINT('Ctrl Pts',(-109.567,-3.53460305911876,-0.149296894027067));
#53355=CARTESIAN_POINT('Ctrl Pts',(-109.567,-3.53687070026767,-0.133777965353361));
#53356=CARTESIAN_POINT('Ctrl Pts',(-109.567,-3.55362006210883,-0.0191512961964261));
#53357=CARTESIAN_POINT('Ctrl Pts',(-109.567,-3.56453969470775,0.0958883104104314));
#53358=CARTESIAN_POINT('Ctrl Pts',(-109.567,-3.56948236683328,0.210916428015749));
#53359=CARTESIAN_POINT('Ctrl Pts',(-109.567,-3.57215030524466,0.273005906248279));
#53360=CARTESIAN_POINT('Ctrl Pts',(-109.567,-3.57307608943884,0.335092588218926));
#53361=CARTESIAN_POINT('Ctrl Pts',(-109.567,-3.57223104459554,0.397112793171267));
#53362=CARTESIAN_POINT('Ctrl Pts',(-109.567,-3.57071960889364,0.508041287378316));
#53363=CARTESIAN_POINT('Ctrl Pts',(-109.567,-3.5635465120436,0.618756803306876));
#53364=CARTESIAN_POINT('Ctrl Pts',(-109.567,-3.55097661781193,0.728974557829716));
#53365=CARTESIAN_POINT('Ctrl Pts',(-109.567,-3.53816715848062,0.841292912950918));
#53366=CARTESIAN_POINT('Ctrl Pts',(-109.567,-3.5197531319118,0.953095028235097));
#53367=CARTESIAN_POINT('Ctrl Pts',(-109.567,-3.49596074425854,1.0640829788475));
#53368=CARTESIAN_POINT('Ctrl Pts',(-109.567,-3.488522449697,1.09878151694581));
#53369=CARTESIAN_POINT('Ctrl Pts',(-109.567,-3.48055809112876,1.1334004624857));
#53370=CARTESIAN_POINT('Ctrl Pts',(-109.567,-3.47207355089471,1.16793061249935));
#53371=CARTESIAN_POINT('Ctrl Pts',(-109.567,-3.46814577917836,1.18391575050844));
#53372=CARTESIAN_POINT('Ctrl Pts',(-109.567,-3.46410593314054,1.19988411131588));
#53373=CARTESIAN_POINT('Ctrl Pts',(-109.567,-3.4599564744153,1.21582745846855));
#53374=CARTESIAN_POINT('Ctrl Pts',(-109.567,-3.43129298422129,1.32596037098317));
#53375=CARTESIAN_POINT('Ctrl Pts',(-109.567,-3.39747435133908,1.43463252196887));
#53376=CARTESIAN_POINT('Ctrl Pts',(-109.567,-3.35880367683646,1.54155102136754));
#53377=CARTESIAN_POINT('Ctrl Pts',(-109.567,-3.31885844540897,1.65199347568964));
#53378=CARTESIAN_POINT('Ctrl Pts',(-109.567,-3.27373604012402,1.76056546471733));
#53379=CARTESIAN_POINT('Ctrl Pts',(-109.567,-3.22371511386614,1.86694840066266));
#53380=CARTESIAN_POINT('Ctrl Pts',(-109.567,-3.17318630958296,1.97441147565131));
#53381=CARTESIAN_POINT('Ctrl Pts',(-109.567,-3.11765875257899,2.07964161817074));
#53382=CARTESIAN_POINT('Ctrl Pts',(-109.567,-3.05736645015778,2.18230326993847));
#53383=CARTESIAN_POINT('Ctrl Pts',(-109.567,-3.01747154321521,2.25023361725265));
#53384=CARTESIAN_POINT('Ctrl Pts',(-109.567,-2.97548937180041,2.31703922297468));
#53385=CARTESIAN_POINT('Ctrl Pts',(-109.567,-2.93147598465934,2.38261852576162));
#53386=CARTESIAN_POINT('Ctrl Pts',(-109.567,-2.91011659414414,2.41444370507471));
#53387=CARTESIAN_POINT('Ctrl Pts',(-109.567,-2.88827869870454,2.44598001332719));
#53388=CARTESIAN_POINT('Ctrl Pts',(-109.567,-2.8659679668509,2.47721541551838));
#53389=CARTESIAN_POINT('Ctrl Pts',(-109.567,-2.85153128249921,2.49742701794319));
#53390=CARTESIAN_POINT('Ctrl Pts',(-109.567,-2.83689258662859,2.517517866556));
#53391=CARTESIAN_POINT('Ctrl Pts',(-109.567,-2.82207503428789,2.53745591080546));
#53392=CARTESIAN_POINT('Ctrl Pts',(-109.567,-2.7489276911345,2.63588073367702));
#53393=CARTESIAN_POINT('Ctrl Pts',(-109.567,-2.67135364275062,2.73068902811859));
#53394=CARTESIAN_POINT('Ctrl Pts',(-109.567,-2.58964383806861,2.82154575548173));
#53395=CARTESIAN_POINT('Ctrl Pts',(-109.567,-2.50782128256363,2.9125278554464));
#53396=CARTESIAN_POINT('Ctrl Pts',(-109.567,-2.42185116409135,2.99954830547996));
#53397=CARTESIAN_POINT('Ctrl Pts',(-109.567,-2.33197556942183,3.08225487705311));
#53398=CARTESIAN_POINT('Ctrl Pts',(-109.567,-2.2422857465215,3.16479049514126));
#53399=CARTESIAN_POINT('Ctrl Pts',(-109.567,-2.14870616705358,3.24303087993829));
#53400=CARTESIAN_POINT('Ctrl Pts',(-109.567,-2.05143358017556,3.31659784347169));
#53401=CARTESIAN_POINT('Ctrl Pts',(-109.567,-1.95416099329755,3.3901648070051));
#53402=CARTESIAN_POINT('Ctrl Pts',(-109.567,-1.85319500343946,3.45905921673876));
#53403=CARTESIAN_POINT('Ctrl Pts',(-109.567,-1.74869447533098,3.52286199445095));
#53404=CARTESIAN_POINT('Ctrl Pts',(-109.567,-1.8755886821457,-2.62754025481279));
#53405=CARTESIAN_POINT('Ctrl Pts',(-109.504814144533,-1.05624460814695,
-3.20663122225699));
#53406=CARTESIAN_POINT('Ctrl Pts',(-109.376337111834,1.24418819625944,-3.56417172636872));
#53407=CARTESIAN_POINT('Ctrl Pts',(-109.181568901902,3.6901636846244,-0.955038498682453));
#53408=CARTESIAN_POINT('Ctrl Pts',(-108.982695370205,2.7979887412231,2.58915131051891));
#53409=CARTESIAN_POINT('Ctrl Pts',(-108.783821838507,-0.665419358724505,
3.75306610556087));
#53410=CARTESIAN_POINT('Ctrl Pts',(-108.624998898681,-2.94289439362547,
1.92928088442713));
#53411=CARTESIAN_POINT('Ctrl Pts',(-108.532467136088,-3.22041771955432,
0.428199733749597));
#53412=CARTESIAN_POINT('Ctrl Pts',(-108.506226550727,-3.21833411702487,
0.00177219254916029));
#53413=CARTESIAN_POINT('Origin',(-109.567,-5.160062080289E-16,2.1385152528819E-16));
#53414=CARTESIAN_POINT('',(-109.567,-3.93300000000001,-4.81653586104655E-16));
#53415=CARTESIAN_POINT('Origin',(-109.567,0.,0.));
#53416=CARTESIAN_POINT('Origin',(-109.567,0.,0.));
#53417=CARTESIAN_POINT('',(-109.567,1.87158653173898,-2.62360084935061));
#53418=CARTESIAN_POINT('Ctrl Pts',(-109.567,1.75275645914455,3.52838181187388));
#53419=CARTESIAN_POINT('Ctrl Pts',(-109.567,1.82202500014327,3.48645490739411));
#53420=CARTESIAN_POINT('Ctrl Pts',(-109.567,1.88981509185284,3.44228222701039));
#53421=CARTESIAN_POINT('Ctrl Pts',(-109.567,1.95600382845685,3.3958567385041));
#53422=CARTESIAN_POINT('Ctrl Pts',(-109.567,2.05546182159306,3.32609583726757));
#53423=CARTESIAN_POINT('Ctrl Pts',(-109.567,2.15130605150922,3.25124954236935));
#53424=CARTESIAN_POINT('Ctrl Pts',(-109.567,2.24335219247688,3.17172823304734));
#53425=CARTESIAN_POINT('Ctrl Pts',(-109.567,2.29724160807795,3.12517161652716));
#53426=CARTESIAN_POINT('Ctrl Pts',(-109.567,2.34982843551166,3.07701188213643));
#53427=CARTESIAN_POINT('Ctrl Pts',(-109.567,2.40106891848523,3.02732681361603));
#53428=CARTESIAN_POINT('Ctrl Pts',(-109.567,2.44038120004853,2.98920786371907));
#53429=CARTESIAN_POINT('Ctrl Pts',(-109.567,2.47890090599221,2.95019101034076));
#53430=CARTESIAN_POINT('Ctrl Pts',(-109.567,2.51660611613464,2.91031044345441));
#53431=CARTESIAN_POINT('Ctrl Pts',(-109.567,2.53156447098204,2.89448908431736));
#53432=CARTESIAN_POINT('Ctrl Pts',(-109.567,2.54639525737649,2.87853096014503));
#53433=CARTESIAN_POINT('Ctrl Pts',(-109.567,2.56108565929238,2.86245096993407));
#53434=CARTESIAN_POINT('Ctrl Pts',(-109.567,2.64412131549488,2.77156084000153));
#53435=CARTESIAN_POINT('Ctrl Pts',(-109.567,2.72276365995974,2.67668790351876));
#53436=CARTESIAN_POINT('Ctrl Pts',(-109.567,2.79681743724591,2.57825667956293));
#53437=CARTESIAN_POINT('Ctrl Pts',(-109.567,2.86161449237131,2.49212935860158));
#53438=CARTESIAN_POINT('Ctrl Pts',(-109.567,2.92289790212134,2.40327677587802));
#53439=CARTESIAN_POINT('Ctrl Pts',(-109.567,2.98050509863801,2.31196927698884));
#53440=CARTESIAN_POINT('Ctrl Pts',(-109.567,3.00573063331407,2.27198676406189));
#53441=CARTESIAN_POINT('Ctrl Pts',(-109.567,3.03025086583581,2.23153340920802));
#53442=CARTESIAN_POINT('Ctrl Pts',(-109.567,3.05405020721428,2.19063151133595));
#53443=CARTESIAN_POINT('Ctrl Pts',(-109.567,3.06875694113979,2.16535630226663));
#53444=CARTESIAN_POINT('Ctrl Pts',(-109.567,3.08318837281295,2.13990980974904));
#53445=CARTESIAN_POINT('Ctrl Pts',(-109.567,3.09734058716092,2.114297277655));
#53446=CARTESIAN_POINT('Ctrl Pts',(-109.567,3.10820135238902,2.09464157635407));
#53447=CARTESIAN_POINT('Ctrl Pts',(-109.567,3.11889908116918,2.07488524212842));
#53448=CARTESIAN_POINT('Ctrl Pts',(-109.567,3.12942045161792,2.05505284340651));
#53449=CARTESIAN_POINT('Ctrl Pts',(-109.567,3.18514385739147,1.95001626030842));
#53450=CARTESIAN_POINT('Ctrl Pts',(-109.567,3.23599354366025,1.84272574147176));
#53451=CARTESIAN_POINT('Ctrl Pts',(-109.567,3.28179303842333,1.73355775273866));
#53452=CARTESIAN_POINT('Ctrl Pts',(-109.567,3.32725085049152,1.62520420121232));
#53453=CARTESIAN_POINT('Ctrl Pts',(-109.567,3.36773377451,1.51500022479072));
#53454=CARTESIAN_POINT('Ctrl Pts',(-109.567,3.40301964925438,1.40330203831042));
#53455=CARTESIAN_POINT('Ctrl Pts',(-109.567,3.43726116268567,1.29490979976387));
#53456=CARTESIAN_POINT('Ctrl Pts',(-109.567,3.46660872504405,1.18510975826472));
#53457=CARTESIAN_POINT('Ctrl Pts',(-109.567,3.49081093656453,1.07422785924485));
#53458=CARTESIAN_POINT('Ctrl Pts',(-109.567,3.50699359207182,1.00008737946617));
#53459=CARTESIAN_POINT('Ctrl Pts',(-109.567,3.52087485467189,0.925463243069554));
#53460=CARTESIAN_POINT('Ctrl Pts',(-109.567,3.53236683395441,0.85045536704003));
#53461=CARTESIAN_POINT('Ctrl Pts',(-109.567,3.53790924920365,0.81428015425042));
#53462=CARTESIAN_POINT('Ctrl Pts',(-109.567,3.54289576268122,0.778015725169597));
#53463=CARTESIAN_POINT('Ctrl Pts',(-109.567,3.54731562475149,0.741673567948634));
#53464=CARTESIAN_POINT('Ctrl Pts',(-109.567,3.54909081350037,0.727077142181763));
#53465=CARTESIAN_POINT('Ctrl Pts',(-109.567,3.55077419437748,0.712471117916151));
#53466=CARTESIAN_POINT('Ctrl Pts',(-109.567,3.55236436289117,0.697864508620402));
#53467=CARTESIAN_POINT('Ctrl Pts',(-109.567,3.56446931029815,0.586673628033493));
#53468=CARTESIAN_POINT('Ctrl Pts',(-109.567,3.57119429444985,0.475307970362645));
#53469=CARTESIAN_POINT('Ctrl Pts',(-109.567,3.57234212104006,0.364083492885442));
#53470=CARTESIAN_POINT('Ctrl Pts',(-109.567,3.57300336055886,0.300009336917556));
#53471=CARTESIAN_POINT('Ctrl Pts',(-109.567,3.57181279307812,0.235982024622193));
#53472=CARTESIAN_POINT('Ctrl Pts',(-109.567,3.56872485737067,0.172062839259968));
#53473=CARTESIAN_POINT('Ctrl Pts',(-109.567,3.5632620547378,0.0589847420555476));
#53474=CARTESIAN_POINT('Ctrl Pts',(-109.567,3.55186373352207,-0.0537562397880342));
#53475=CARTESIAN_POINT('Ctrl Pts',(-109.567,3.53474471555629,-0.165803129864622));
#53476=CARTESIAN_POINT('Ctrl Pts',(-109.567,3.5175478789259,-0.278359356363241));
#53477=CARTESIAN_POINT('Ctrl Pts',(-109.567,3.49457768041398,-0.390215969444795));
#53478=CARTESIAN_POINT('Ctrl Pts',(-109.567,3.46600700359361,-0.500984551047218));
#53479=CARTESIAN_POINT('Ctrl Pts',(-109.567,3.45747746547809,-0.534053590493489));
#53480=CARTESIAN_POINT('Ctrl Pts',(-109.567,3.44844850025554,-0.567025433035426));
#53481=CARTESIAN_POINT('Ctrl Pts',(-109.567,3.43892404746731,-0.599889123387569));
#53482=CARTESIAN_POINT('Ctrl Pts',(-109.567,3.43355286207557,-0.618422153836961));
#53483=CARTESIAN_POINT('Ctrl Pts',(-109.567,3.4280233534425,-0.636922883471933));
#53484=CARTESIAN_POINT('Ctrl Pts',(-109.567,3.42234320335153,-0.655367447148205));
#53485=CARTESIAN_POINT('Ctrl Pts',(-109.567,3.38957071812405,-0.76178614752175));
#53486=CARTESIAN_POINT('Ctrl Pts',(-109.567,3.35174285235985,-0.866496509973046));
#53487=CARTESIAN_POINT('Ctrl Pts',(-109.567,3.30909514849801,-0.969172184804078));
#53488=CARTESIAN_POINT('Ctrl Pts',(-109.567,3.26640916057173,-1.0719400297122));
#53489=CARTESIAN_POINT('Ctrl Pts',(-109.567,3.2188940912709,-1.17267028238691));
#53490=CARTESIAN_POINT('Ctrl Pts',(-109.567,3.16674149373716,-1.27100860119449));
#53491=CARTESIAN_POINT('Ctrl Pts',(-109.567,3.11523168974658,-1.36813487612768));
#53492=CARTESIAN_POINT('Ctrl Pts',(-109.567,3.05919735145539,-1.4629284384482));
#53493=CARTESIAN_POINT('Ctrl Pts',(-109.567,2.99878861195219,-1.5550113642337));
#53494=CARTESIAN_POINT('Ctrl Pts',(-109.567,2.96288289596785,-1.60974356701515));
#53495=CARTESIAN_POINT('Ctrl Pts',(-109.567,2.9254311493055,-1.66351739572016));
#53496=CARTESIAN_POINT('Ctrl Pts',(-109.567,2.88646034894762,-1.71624590697244));
#53497=CARTESIAN_POINT('Ctrl Pts',(-109.567,2.86741100001697,-1.74202017386495));
#53498=CARTESIAN_POINT('Ctrl Pts',(-109.567,2.84799864852909,-1.76754458402546));
#53499=CARTESIAN_POINT('Ctrl Pts',(-109.567,2.82822620377072,-1.7928084225986));
#53500=CARTESIAN_POINT('Ctrl Pts',(-109.567,2.81848093071187,-1.8052602467619));
#53501=CARTESIAN_POINT('Ctrl Pts',(-109.567,2.80865378977432,-1.81764157929085));
#53502=CARTESIAN_POINT('Ctrl Pts',(-109.567,2.79874712727207,-1.8299492607085));
#53503=CARTESIAN_POINT('Ctrl Pts',(-109.567,2.73134458457393,-1.91368775710731));
#53504=CARTESIAN_POINT('Ctrl Pts',(-109.567,2.6602377061028,-1.99405316358428));
#53505=CARTESIAN_POINT('Ctrl Pts',(-109.567,2.58560125585586,-2.07072490991953));
#53506=CARTESIAN_POINT('Ctrl Pts',(-109.567,2.51201739882552,-2.14631535938401));
#53507=CARTESIAN_POINT('Ctrl Pts',(-109.567,2.43500223422176,-2.21831610629024));
#53508=CARTESIAN_POINT('Ctrl Pts',(-109.567,2.35469492044372,-2.28637908316542));
#53509=CARTESIAN_POINT('Ctrl Pts',(-109.567,2.27685682873383,-2.35234931659522));
#53510=CARTESIAN_POINT('Ctrl Pts',(-109.567,2.19592538297238,-2.41462049371991));
#53511=CARTESIAN_POINT('Ctrl Pts',(-109.567,2.11200880209288,-2.47283144644441));
#53512=CARTESIAN_POINT('Ctrl Pts',(-109.567,2.0343964590955,-2.52666929805499));
#53513=CARTESIAN_POINT('Ctrl Pts',(-109.567,1.95423020934163,-2.5770339076807));
#53514=CARTESIAN_POINT('Ctrl Pts',(-109.567,1.87158653173824,-2.62360084935114));
#53515=CARTESIAN_POINT('Origin',(-109.567,0.,0.));
#53516=CARTESIAN_POINT('Origin',(-111.877773449273,0.,0.));
#53517=CARTESIAN_POINT('Ctrl Pts',(-109.567,1.87158653173818,-2.62360084935118));
#53518=CARTESIAN_POINT('Ctrl Pts',(-109.500708822768,2.74581178927839,-1.99995864473678));
#53519=CARTESIAN_POINT('Ctrl Pts',(-109.368126468303,3.80651295487345,0.179129781420444));
#53520=CARTESIAN_POINT('Ctrl Pts',(-109.169252936605,1.9032035356359,3.30567173395145));
#53521=CARTESIAN_POINT('Ctrl Pts',(-108.970379404908,-1.7502378889635,3.3848793341849));
#53522=CARTESIAN_POINT('Ctrl Pts',(-108.83155290913,-3.17746554677698,1.27272365819482));
#53523=CARTESIAN_POINT('Ctrl Pts',(-108.759017590586,-3.22751915473568,
0.102767056756573));
#53524=CARTESIAN_POINT('Ctrl Pts',(-108.752773449273,-3.22685723674299,
0.00199079345700971));
#53525=CARTESIAN_POINT('Ctrl Pts',(-109.977063028692,2.28405859260862,-3.20180657528383));
#53526=CARTESIAN_POINT('Ctrl Pts',(-109.910771851459,3.35095113404214,-2.44072216267053));
#53527=CARTESIAN_POINT('Ctrl Pts',(-109.778189496995,4.64541632193532,0.21860753404117));
#53528=CARTESIAN_POINT('Ctrl Pts',(-109.579315965297,2.32264355151719,4.03419654941691));
#53529=CARTESIAN_POINT('Ctrl Pts',(-109.3804424336,-2.13596636949734,4.13086042086637));
#53530=CARTESIAN_POINT('Ctrl Pts',(-109.181568901902,-4.63110802863978,
0.438297717986617));
#53531=CARTESIAN_POINT('Ctrl Pts',(-108.982695370205,-2.87167397122528,
-3.66022965207199));
#53532=CARTESIAN_POINT('Ctrl Pts',(-108.783821838507,1.52652252159763,-4.394010664145));
#53533=CARTESIAN_POINT('Ctrl Pts',(-108.58494830681,4.52200798253338,-1.09147594363445));
#53534=CARTESIAN_POINT('Ctrl Pts',(-108.386074775112,3.3627368399975,3.21439114027321));
#53535=CARTESIAN_POINT('Ctrl Pts',(-108.187201243415,-0.886262802760796,
4.56661377013007));
#53536=CARTESIAN_POINT('Ctrl Pts',(-107.988327711717,-4.32094171494865,
1.72315748479787));
#53537=CARTESIAN_POINT('Ctrl Pts',(-107.78945418002,-3.78554144244751,-2.70361103446967));
#53538=CARTESIAN_POINT('Ctrl Pts',(-107.590580648323,0.228027871382542,
-4.64625826502713));
#53539=CARTESIAN_POINT('Ctrl Pts',(-107.391707116625,4.03208164170884,-2.31993394368827));
#53540=CARTESIAN_POINT('Ctrl Pts',(-107.192833584928,4.13145214500505,2.13796108409874));
#53541=CARTESIAN_POINT('Ctrl Pts',(-106.99396005323,0.434835074219217,4.63148744537977));
#53542=CARTESIAN_POINT('Ctrl Pts',(-106.795086521533,-3.66130890000019,
2.86959661519726));
#53543=CARTESIAN_POINT('Ctrl Pts',(-106.596212989835,-4.39343498051869,
-1.52888705693157));
#53544=CARTESIAN_POINT('Ctrl Pts',(-106.397339458138,-1.08886385223194,
-4.52262532524078));
#53545=CARTESIAN_POINT('Ctrl Pts',(-106.19846592644,3.21615755154426,-3.3609666016501));
#53546=CARTESIAN_POINT('Ctrl Pts',(-105.999592394743,4.56616682915475,0.888755371192072));
#53547=CARTESIAN_POINT('Ctrl Pts',(-105.800718863045,1.72077262957113,4.3218869598412));
#53548=CARTESIAN_POINT('Ctrl Pts',(-105.601845331348,-2.70567098522491,
3.78406000159801));
#53549=CARTESIAN_POINT('Ctrl Pts',(-105.402971799651,-4.64613854864029,
-0.230569090679434));
#53550=CARTESIAN_POINT('Ctrl Pts',(-105.204098267953,-2.31772447095656,
-4.03335081055775));
#53551=CARTESIAN_POINT('Ctrl Pts',(-105.005224736256,2.14021960806887,-4.13028153390441));
#53552=CARTESIAN_POINT('Ctrl Pts',(-104.806351204558,4.63172551753725,-0.432301098127802));
#53553=CARTESIAN_POINT('Ctrl Pts',(-104.607477672861,2.86759251087864,3.66287847149825));
#53554=CARTESIAN_POINT('Ctrl Pts',(-104.408604141163,-1.53129038250247,
4.39259778207621));
#53555=CARTESIAN_POINT('Ctrl Pts',(-104.209730609466,-4.52322052840125,
1.08638923051286));
#53556=CARTESIAN_POINT('Ctrl Pts',(-104.010857077768,-3.35920636533815,
-3.21799597629154));
#53557=CARTESIAN_POINT('Ctrl Pts',(-103.811983546071,0.891253503530981,
-4.56567987287217));
#53558=CARTESIAN_POINT('Ctrl Pts',(-103.613110014374,4.32282782338692,-1.71840772755835));
#53559=CARTESIAN_POINT('Ctrl Pts',(-103.414236482676,3.78257906316194,2.707740966135));
#53560=CARTESIAN_POINT('Ctrl Pts',(-103.215362950979,-0.233111106957137,
4.64601170044533));
#53561=CARTESIAN_POINT('Ctrl Pts',(-103.016489419281,-4.03461831336596,
2.31551734484117));
#53562=CARTESIAN_POINT('Ctrl Pts',(-102.817615887584,-4.12910992928167,
-2.1424791015823));
#53563=CARTESIAN_POINT('Ctrl Pts',(-102.618742355886,-0.42976686398599,
-4.63196135038316));
#53564=CARTESIAN_POINT('Ctrl Pts',(-102.419868824189,3.66444687836893,-2.86558799977029));
#53565=CARTESIAN_POINT('Ctrl Pts',(-102.220995292491,4.39175930477002,1.53369348886343));
#53566=CARTESIAN_POINT('Ctrl Pts',(-102.022121760794,1.08391426446963,4.52381425083935));
#53567=CARTESIAN_POINT('Ctrl Pts',(-101.823248229096,-3.21983342759692,
3.35744519052003));
#53568=CARTESIAN_POINT('Ctrl Pts',(-101.624374697399,-4.56519155519177,
-0.893751404598992));
#53569=CARTESIAN_POINT('Ctrl Pts',(-101.425501165701,-1.71604230829386,
-4.32376737405733));
#53570=CARTESIAN_POINT('Ctrl Pts',(-101.226627634004,2.70981013496705,-3.78109700235881));
#53571=CARTESIAN_POINT('Ctrl Pts',(-101.027754102307,4.64588346224142,0.235653058729701));
#53572=CARTESIAN_POINT('Ctrl Pts',(-100.828880570609,2.31330952514332,4.03588460559741));
#53573=CARTESIAN_POINT('Ctrl Pts',(-100.630007038912,-2.14473795351143,
4.12793709007108));
#53574=CARTESIAN_POINT('Ctrl Pts',(-100.431133507214,-4.63219579674829,
0.427232500407485));
#53575=CARTESIAN_POINT('Ctrl Pts',(-100.232259975517,-2.86358263077228,
-3.6660141878553));
#53576=CARTESIAN_POINT('Ctrl Pts',(-100.033386443819,1.53609613607296,-4.39091951299027));
#53577=CARTESIAN_POINT('Ctrl Pts',(-99.8345129121218,4.52440661907031,-1.08143897383521));
#53578=CARTESIAN_POINT('Ctrl Pts',(-99.6356393804243,3.35568301062586,3.22166991496862));
#53579=CARTESIAN_POINT('Ctrl Pts',(-99.4367658487269,-0.896249038113484,
4.56470187093282));
#53580=CARTESIAN_POINT('Ctrl Pts',(-99.2378923170294,-4.3247056303906,1.71367637530684));
#53581=CARTESIAN_POINT('Ctrl Pts',(-99.039018785332,-3.77961380966542,-2.71187849259577));
#53582=CARTESIAN_POINT('Ctrl Pts',(-98.8401452536345,0.238194939957711,
-4.64575383327566));
#53583=CARTESIAN_POINT('Ctrl Pts',(-98.6412717219371,4.03714968966855,-2.31110101294298));
#53584=CARTESIAN_POINT('Ctrl Pts',(-98.4423981902396,4.12676301514323,2.146996163402));
#53585=CARTESIAN_POINT('Ctrl Pts',(-98.2435246585422,0.424698008935038,
4.63242885644492));
#53586=CARTESIAN_POINT('Ctrl Pts',(-98.0446511268446,-3.66758039990343,
2.86157640454717));
#53587=CARTESIAN_POINT('Ctrl Pts',(-97.8457775951473,-4.39007840676843,
-1.53849832344483));
#53588=CARTESIAN_POINT('Ctrl Pts',(-97.6469040634498,-1.07896335946704,
-4.52499763289935));
#53589=CARTESIAN_POINT('Ctrl Pts',(-97.4480305317523,3.22350543791854,-3.35391982619242));
#53590=CARTESIAN_POINT('Ctrl Pts',(-97.249157000055,4.56421082020927,0.898746403331652));
#53591=CARTESIAN_POINT('Ctrl Pts',(-97.0502834683573,1.71130992932287,4.32564259210328));
#53592=CARTESIAN_POINT('Ctrl Pts',(-96.8514099366601,-2.71394603841112,
3.77812948552713));
#53593=CARTESIAN_POINT('Ctrl Pts',(-96.6525364049624,-4.64562281358202,
-0.240736749880956));
#53594=CARTESIAN_POINT('Ctrl Pts',(-96.4536628732651,-2.3088918089039,-4.03841356520025));
#53595=CARTESIAN_POINT('Ctrl Pts',(-96.2547893415676,2.14925373057933,-4.1255877048498));
#53596=CARTESIAN_POINT('Ctrl Pts',(-96.0559158098702,4.63266052940256,-0.422163390327286));
#53597=CARTESIAN_POINT('Ctrl Pts',(-95.8570422781727,2.85956932169593,3.66914551404444));
#53598=CARTESIAN_POINT('Ctrl Pts',(-95.6581687464752,-1.54090005026015,
4.38923598635631));
#53599=CARTESIAN_POINT('Ctrl Pts',(-95.4592952147778,-4.5255872921494,1.07648742210618));
#53600=CARTESIAN_POINT('Ctrl Pts',(-95.2604216830804,-3.35215563774757,
-3.2253399958972));
#53601=CARTESIAN_POINT('Ctrl Pts',(-95.0615481513828,0.901243499505942,
-4.56371840316811));
#53602=CARTESIAN_POINT('Ctrl Pts',(-94.8626746196855,4.32657825891484,-1.70894297105036));
#53603=CARTESIAN_POINT('Ctrl Pts',(-94.6638010879879,3.77664403038834,2.71601277179418));
#53604=CARTESIAN_POINT('Ctrl Pts',(-94.4649275562906,-0.24327848773853,
4.64549040319971));
#53605=CARTESIAN_POINT('Ctrl Pts',(-94.266054024593,-4.0396762318142,2.30668191368736));
#53606=CARTESIAN_POINT('Ctrl Pts',(-94.0671804928956,-4.12441115954261,
-2.15151065436761));
#53607=CARTESIAN_POINT('Ctrl Pts',(-93.8683069611983,-0.419628645342997,
-4.63289081555184));
#53608=CARTESIAN_POINT('Ctrl Pts',(-93.6694334295006,3.67070952980976,-2.85756138281943));
#53609=CARTESIAN_POINT('Ctrl Pts',(-93.4705598978034,4.38839225200612,1.54330131579987));
#53610=CARTESIAN_POINT('Ctrl Pts',(-93.2716863661057,1.07401116249385,4.52617559664399));
#53611=CARTESIAN_POINT('Ctrl Pts',(-93.0728128344084,-3.22717358835541,
3.35039044581944));
#53612=CARTESIAN_POINT('Ctrl Pts',(-92.8739393027109,-4.56322461995675,
-0.903740325888789));
#53613=CARTESIAN_POINT('Ctrl Pts',(-92.6750657710135,-1.70657550119789,
-4.3275126305452));
#53614=CARTESIAN_POINT('Ctrl Pts',(-92.4761922393159,2.71807869212624,-3.7751574446937));
#53615=CARTESIAN_POINT('Ctrl Pts',(-92.2773187076185,4.64535660216838,0.245820152769577));
#53616=CARTESIAN_POINT('Ctrl Pts',(-92.0784451759211,2.30447132795495,4.04093768913237));
#53617=CARTESIAN_POINT('Ctrl Pts',(-91.8795716442236,-2.15376693409124,
4.12323337957387));
#53618=CARTESIAN_POINT('Ctrl Pts',(-91.6806981125262,-4.63311971482384,
0.417093774740931));
#53619=CARTESIAN_POINT('Ctrl Pts',(-91.4818245808287,-2.8555525885187,-3.67227244673119));
#53620=CARTESIAN_POINT('Ctrl Pts',(-91.2829510491312,1.54570211934521,-4.38754720397043));
#53621=CARTESIAN_POINT('Ctrl Pts',(-91.0840775174339,4.52676254620699,-1.07153458137132));
#53622=CARTESIAN_POINT('Ctrl Pts',(-90.8852039857363,3.34862425093643,3.22900621474431));
#53623=CARTESIAN_POINT('Ctrl Pts',(-90.686330454039,-0.9062368817328,4.562729470723));
#53624=CARTESIAN_POINT('Ctrl Pts',(-90.4874569223414,-4.32844570671463,
1.70420752047416));
#53625=CARTESIAN_POINT('Ctrl Pts',(-90.288583390644,-3.77366972888823,-2.72014379878889));
#53626=CARTESIAN_POINT('Ctrl Pts',(-90.0897098589466,0.248361744213206,
-4.64522141052807));
#53627=CARTESIAN_POINT('Ctrl Pts',(-89.8908363272491,4.04219793677718,-2.30226005236837));
#53628=CARTESIAN_POINT('Ctrl Pts',(-89.6919627955516,4.12205436529617,2.15602256907477));
#53629=CARTESIAN_POINT('Ctrl Pts',(-89.4930892638543,0.414558779279898,
4.63334722715004));
#53630=CARTESIAN_POINT('Ctrl Pts',(-89.2942157321566,-3.67383426434092,
2.8535429393951));
#53631=CARTESIAN_POINT('Ctrl Pts',(-89.0953422004594,-4.38670084250218,
-1.54810246017749));
#53632=CARTESIAN_POINT('Ctrl Pts',(-88.8964686687618,-1.06905767947995,
-4.52734814066269));
#53633=CARTESIAN_POINT('Ctrl Pts',(-88.6975951370643,3.23083787451525,-3.34685705362729));
#53634=CARTESIAN_POINT('Ctrl Pts',(-88.498721605367,4.56223295561509,0.908733166290631));
#53635=CARTESIAN_POINT('Ctrl Pts',(-88.2998480736694,1.70183902958803,4.32937748714383));
#53636=CARTESIAN_POINT('Ctrl Pts',(-88.1009745419721,-2.7222080911639,3.77218088341728));
#53637=CARTESIAN_POINT('Ctrl Pts',(-87.9021010102746,-4.64508482831926,
-0.250903261308599));
#53638=CARTESIAN_POINT('Ctrl Pts',(-87.703227478577,-2.30004808758962,-4.04345697437135));
#53639=CARTESIAN_POINT('Ctrl Pts',(-87.5043539468797,2.15827755864299,-4.12087411706242));
#53640=CARTESIAN_POINT('Ctrl Pts',(-87.3054804151822,4.63357335246232,-0.412023659718792));
#53641=CARTESIAN_POINT('Ctrl Pts',(-87.1066068834848,2.85153243605024,3.67539498217135));
#53642=CARTESIAN_POINT('Ctrl Pts',(-86.9077333517873,-1.55050233757813,
4.38585316785479));
#53643=CARTESIAN_POINT('Ctrl Pts',(-86.7088598200898,-4.52793237983578,
1.06658045756125));
#53644=CARTESIAN_POINT('Ctrl Pts',(-86.5099862883923,-3.34508885442102,
-3.2326685671199));
#53645=CARTESIAN_POINT('Ctrl Pts',(-86.311112756695,0.911229178814921,-4.56173507478168));
#53646=CARTESIAN_POINT('Ctrl Pts',(-86.1122392249975,4.33030797155388,-1.69947002924852));
#53647=CARTESIAN_POINT('Ctrl Pts',(-85.9133656933001,3.77069090872654,2.72427156863332));
#53648=CARTESIAN_POINT('Ctrl Pts',(-85.7144921616024,-0.253444703294882,
4.64494685558281));
#53649=CARTESIAN_POINT('Ctrl Pts',(-85.5156186299052,-4.04471480153795,
2.29783543428091));
#53650=CARTESIAN_POINT('Ctrl Pts',(-85.3167450982075,-4.119692635226,-2.16053190212079));
#53651=CARTESIAN_POINT('Ctrl Pts',(-85.1178715665103,-0.409488416816509,
-4.63379809069301));
#53652=CARTESIAN_POINT('Ctrl Pts',(-84.9189980348126,3.67695459975529,-2.84952107908597));
#53653=CARTESIAN_POINT('Ctrl Pts',(-84.7201245031154,4.38500418028194,1.55290175082866));
#53654=CARTESIAN_POINT('Ctrl Pts',(-84.5212509714178,1.0641029163568,4.5285152635514));
#53655=CARTESIAN_POINT('Ctrl Pts',(-84.3223774397204,-3.23449829201034,
3.34331965384694));
#53656=CARTESIAN_POINT('Ctrl Pts',(-84.1235039080229,-4.56123582837174,
-0.913724918558631));
#53657=CARTESIAN_POINT('Ctrl Pts',(-83.9246303763255,-1.69710052016476,
-4.33123715966623));
#53658=CARTESIAN_POINT('Ctrl Pts',(-83.7257568446281,2.72633423057952,-3.76919980526202));
#53659=CARTESIAN_POINT('Ctrl Pts',(-83.5268833129305,4.64480749236006,0.255986069411427));
#53660=CARTESIAN_POINT('Ctrl Pts',(-83.3280097812332,2.29562209310443,4.04597141790051));
#53661=CARTESIAN_POINT('Ctrl Pts',(-83.1291362495355,-2.16278559883345,
4.11850992014049));
#53662=CARTESIAN_POINT('Ctrl Pts',(-82.9302627178384,-4.63402144177481,
0.406953051331925));
#53663=CARTESIAN_POINT('Ctrl Pts',(-82.7313891861407,-2.84750886910435,
-3.67851311662592));
#53664=CARTESIAN_POINT('Ctrl Pts',(-82.5325156544434,1.55530069921097,-4.38415388003783));
#53665=CARTESIAN_POINT('Ctrl Pts',(-82.3336421227458,4.52909679163504,-1.06162505660813));
#53666=CARTESIAN_POINT('Ctrl Pts',(-82.1347685910484,3.34154945243463,3.23632704863876));
#53667=CARTESIAN_POINT('Ctrl Pts',(-81.935895059351,-0.916220384774566,
4.56073521653479));
#53668=CARTESIAN_POINT('Ctrl Pts',(-81.7370215276534,-4.33216505120267,
1.69473050304614));
#53669=CARTESIAN_POINT('Ctrl Pts',(-81.5381479959561,-3.76770757347015,
-2.7283960763849));
#53670=CARTESIAN_POINT('Ctrl Pts',(-81.3392744642586,0.25852735889732,-4.64466673869274));
#53671=CARTESIAN_POINT('Ctrl Pts',(-81.1404009325611,4.04722682308283,-2.29340806472287));
#53672=CARTESIAN_POINT('Ctrl Pts',(-80.9415274008637,4.11732597216001,2.16503864810625));
#53673=CARTESIAN_POINT('Ctrl Pts',(-80.7426538691662,0.404417564024095,
4.63424340564085));
#53674=CARTESIAN_POINT('Ctrl Pts',(-80.5437803374688,-3.6800705323166,2.84549580670783));
#53675=CARTESIAN_POINT('Ctrl Pts',(-80.3449068057713,-4.38330226737701,
-1.5576991820068));
#53676=CARTESIAN_POINT('Ctrl Pts',(-80.1460332740738,-1.05914687905708,
-4.52967696391263));
#53677=CARTESIAN_POINT('Ctrl Pts',(-79.9471597423764,3.23815483645772,-3.33977825071404));
#53678=CARTESIAN_POINT('Ctrl Pts',(-79.7482862106789,4.56023323942065,0.918715576715648));
#53679=CARTESIAN_POINT('Ctrl Pts',(-79.5494126789815,1.69235997860213,4.33309164588549));
#53680=CARTESIAN_POINT('Ctrl Pts',(-79.350539147284,-2.73045710543234,3.7662142137976));
#53681=CARTESIAN_POINT('Ctrl Pts',(-79.1516656155867,-4.64452459462294,
-0.261068570991888));
#53682=CARTESIAN_POINT('Ctrl Pts',(-78.9527920838891,-2.29119334979902,
-4.04848101670905));
#53683=CARTESIAN_POINT('Ctrl Pts',(-78.7539185521917,2.16729104926462,-4.11614079163897));
#53684=CARTESIAN_POINT('Ctrl Pts',(-78.5550450204942,4.63446398222474,-0.401881955652068));
#53685=CARTESIAN_POINT('Ctrl Pts',(-78.3561714887967,2.84348189249898,3.68162684636119));
#53686=CARTESIAN_POINT('Ctrl Pts',(-78.1572979570994,-1.56009719849821,
4.38244934255435));
#53687=CARTESIAN_POINT('Ctrl Pts',(-77.9584244254017,-4.53025578021044,
1.05666838444556));
#53688=CARTESIAN_POINT('Ctrl Pts',(-77.7595508937045,-3.33800604921544,
-3.23998165491997));
#53689=CARTESIAN_POINT('Ctrl Pts',(-77.5606773620069,0.921210493634929,
-4.55972989717965));
#53690=CARTESIAN_POINT('Ctrl Pts',(-77.3618038303096,4.33401694343732,-1.68998894754233));
#53691=CARTESIAN_POINT('Ctrl Pts',(-77.162930298612,3.76471972669138,2.73251731710484));
#53692=CARTESIAN_POINT('Ctrl Pts',(-76.9640567669146,-0.263609704934334,
4.64438106019319));
#53693=CARTESIAN_POINT('Ctrl Pts',(-76.7651832352171,-4.04973399840377,
2.28897794899589));
#53694=CARTESIAN_POINT('Ctrl Pts',(-76.5663097035197,-4.11495437893218,
-2.16954280163448));
#53695=CARTESIAN_POINT('Ctrl Pts',(-76.3674361718222,-0.399346226974714,
-4.63468317146038));
#53696=CARTESIAN_POINT('Ctrl Pts',(-76.1685626401248,3.68318205829376,-2.84146712708065));
#53697=CARTESIAN_POINT('Ctrl Pts',(-75.9696891084273,4.38159510582523,1.56249474796727));
#53698=CARTESIAN_POINT('Ctrl Pts',(-75.7708155767298,1.05418957351549,4.53083324035525));
#53699=CARTESIAN_POINT('Ctrl Pts',(-75.5719420450326,-3.24180750347881,
3.33623284846929));
#53700=CARTESIAN_POINT('Ctrl Pts',(-75.3730685133348,-4.55922518996239,
-0.923705134785675));
#53701=CARTESIAN_POINT('Ctrl Pts',(-75.1741949816376,-1.68761741057648,
-4.33494094358115));
#53702=CARTESIAN_POINT('Ctrl Pts',(-74.97532144994,2.7345767107856,-3.76322411259891));
#53703=CARTESIAN_POINT('Ctrl Pts',(-74.7764479182426,4.64423613544655,0.266150759963972));
#53704=CARTESIAN_POINT('Ctrl Pts',(-74.5775743865452,2.2867618629766,4.05098576779194));
#53705=CARTESIAN_POINT('Ctrl Pts',(-74.3787008548477,-2.17179390454168,
4.11376673439473));
#53706=CARTESIAN_POINT('Ctrl Pts',(-74.1798273231502,-4.63490097328221,
0.396810378751233));
#53707=CARTESIAN_POINT('Ctrl Pts',(-73.9809537914528,-2.839451511056,-3.68473616764873));
#53708=CARTESIAN_POINT('Ctrl Pts',(-73.7820802597553,1.56489182969629,-4.38073955744536));
#53709=CARTESIAN_POINT('Ctrl Pts',(-73.5832067280579,4.53140934417422,-1.0517104470089));
#53710=CARTESIAN_POINT('Ctrl Pts',(-73.3843331963604,3.33445864900637,3.24363238158761));
#53711=CARTESIAN_POINT('Ctrl Pts',(-73.185459664663,-0.926199499420982,
4.55871911791998));
#53712=CARTESIAN_POINT('Ctrl Pts',(-72.9865861329655,-4.33586364604029,
1.68524536841465));
#53713=CARTESIAN_POINT('Ctrl Pts',(-72.7877126012681,-3.76172737196798,
-2.73663528585817));
#53714=CARTESIAN_POINT('Ctrl Pts',(-72.5888390695705,0.268691735320179,
-4.64408982042635));
#53715=CARTESIAN_POINT('Ctrl Pts',(-72.3899655378732,4.05223632449878,-2.28454509240455));
#53716=CARTESIAN_POINT('Ctrl Pts',(-72.1910920061757,4.11257785838219,2.1740443573123));
#53717=CARTESIAN_POINT('Ctrl Pts',(-71.9922184744783,0.394274411740812,
4.63511738762496));
#53718=CARTESIAN_POINT('Ctrl Pts',(-71.7933449427808,-3.68628917396088,
2.8374350450285));
#53719=CARTESIAN_POINT('Ctrl Pts',(-71.5944714110833,-4.37988269767089,
-1.56728844296773));
#53720=CARTESIAN_POINT('Ctrl Pts',(-71.3955978793859,-1.04923100566787,
-4.53198409149484));
#53721=CARTESIAN_POINT('Ctrl Pts',(-71.1967243476885,3.2454562887,-3.33268345135785));
#53722=CARTESIAN_POINT('Ctrl Pts',(-70.9978508159909,4.55821168120396,0.928693586794169));
#53723=CARTESIAN_POINT('Ctrl Pts',(-70.7989772842936,1.68287282176677,4.33678505053868));
#53724=CARTESIAN_POINT('Ctrl Pts',(-70.6001037525961,-2.73869304170636,
3.76022950524648));
#53725=CARTESIAN_POINT('Ctrl Pts',(-70.4012302208986,-4.64394211517639,
-0.271232630242302));
#53726=CARTESIAN_POINT('Ctrl Pts',(-70.2023566892012,-2.28232763794338,
-4.0534856681499));
#53727=CARTESIAN_POINT('Ctrl Pts',(-70.0034831575037,2.17629415927268,-4.11138775125048));
#53728=CARTESIAN_POINT('Ctrl Pts',(-69.8046096258063,4.63533241442395,-0.391738326702473));
#53729=CARTESIAN_POINT('Ctrl Pts',(-69.6057360941088,2.83541772960161,3.68784107676536));
#53730=CARTESIAN_POINT('Ctrl Pts',(-69.4068625624114,-1.56968458706416,
4.37902452675825));
#53731=CARTESIAN_POINT('Ctrl Pts',(-69.2079890307139,-4.53255748214502,
1.04675125023471));
#53732=CARTESIAN_POINT('Ctrl Pts',(-69.0091154990165,-3.33090725605517,
-3.24727922427005));
#53733=CARTESIAN_POINT('Ctrl Pts',(-68.8102419673191,0.931187396158665,
-4.55770287996621));
#53734=CARTESIAN_POINT('Ctrl Pts',(-68.6113684356214,4.33770515680041,-1.6804997713431));
#53735=CARTESIAN_POINT('Ctrl Pts',(-68.4124949039242,3.75873051288291,2.74074997771414));
#53736=CARTESIAN_POINT('Ctrl Pts',(-68.2136213722265,-0.273773443969652,
4.64379301974085));
#53737=CARTESIAN_POINT('Ctrl Pts',(-68.0147478405293,-4.05473379837136,
2.2801095002569));
#53738=CARTESIAN_POINT('Ctrl Pts',(-67.8158743088316,-4.11019641335586,
-2.17854330974936));
#53739=CARTESIAN_POINT('Ctrl Pts',(-67.6170007771344,-0.389202124395414,
-4.63554605361474));
#53740=CARTESIAN_POINT('Ctrl Pts',(-67.4181272454367,3.68939187559753,-2.83339956537932));
#53741=CARTESIAN_POINT('Ctrl Pts',(-67.2192537137394,4.37816504496438,1.57208026126815));
#53742=CARTESIAN_POINT('Ctrl Pts',(-67.0203801820419,1.04427118145181,4.53312951595323));
#53743=CARTESIAN_POINT('Ctrl Pts',(-66.8215066503444,-3.24910118775209,
3.32913006362999));
#53744=CARTESIAN_POINT('Ctrl Pts',(-66.622633118647,-4.55719271435901,-0.933680926767934));
#53745=CARTESIAN_POINT('Ctrl Pts',(-66.4237595869495,-1.67812621785408,
-4.33862396455001));
#53746=CARTESIAN_POINT('Ctrl Pts',(-66.2248860552522,2.74280609326566,-3.757230395326));
#53747=CARTESIAN_POINT('Ctrl Pts',(-66.0260125235546,4.64364253416446,0.276314175741591));
#53748=CARTESIAN_POINT('Ctrl Pts',(-65.8271389918572,2.27789068000911,4.05598071478954));
#53749=CARTESIAN_POINT('Ctrl Pts',(-65.6282654601598,-2.18079180806907,
4.10900384505489));
#53750=CARTESIAN_POINT('Ctrl Pts',(-65.4293919284622,-4.63575830513335,
0.38666580557894));
#53751=CARTESIAN_POINT('Ctrl Pts',(-65.2305183967649,-2.83138055296581,
-3.6909415699932));
#53752=CARTESIAN_POINT('Ctrl Pts',(-65.0316448650673,1.57447546486273,-4.37730425254658));
#53753=CARTESIAN_POINT('Ctrl Pts',(-64.83277133337,4.53370019274813,-1.0417908000614));
#53754=CARTESIAN_POINT('Ctrl Pts',(-64.6338978016724,3.32735187461431,3.25092217860068));
#53755=CARTESIAN_POINT('Ctrl Pts',(-64.435024269975,-0.936174177875471,
4.55668118453508));
#53756=CARTESIAN_POINT('Ctrl Pts',(-64.2361507382776,-4.33954147351247,
1.67575216201024));
#53757=CARTESIAN_POINT('Ctrl Pts',(-64.03727720658,-3.75572915302483,-2.74486138774556));
#53758=CARTESIAN_POINT('Ctrl Pts',(-63.8384036748827,0.27885482479771,-4.64349065849217));
#53759=CARTESIAN_POINT('Ctrl Pts',(-63.6395301431852,4.05722641703115,-2.27567117786416));
#53760=CARTESIAN_POINT('Ctrl Pts',(-63.4406566114878,4.10781004670463,2.18303965355862));
#53761=CARTESIAN_POINT('Ctrl Pts',(-63.2417830797902,0.384129371012292,
4.63596916891631));
#53762=CARTESIAN_POINT('Ctrl Pts',(-63.0429095480929,-3.69249015948847,
2.82936069296544));
#53763=CARTESIAN_POINT('Ctrl Pts',(-62.8440360163953,-4.37644214976249,
-1.57687019713081));
#53764=CARTESIAN_POINT('Ctrl Pts',(-62.645162484698,-1.03931010680609,-4.53426951235894));
#53765=CARTESIAN_POINT('Ctrl Pts',(-62.4462889530004,3.25274219627064,-3.32557268954045));
#53766=CARTESIAN_POINT('Ctrl Pts',(-62.247415421303,4.5561682906476,0.938667148734915));
#53767=CARTESIAN_POINT('Ctrl Pts',(-62.0485418896056,1.67337760452224,4.34045768341317));
#53768=CARTESIAN_POINT('Ctrl Pts',(-61.8496683579081,-2.74691586053853,
3.75422678642872));
#53769=CARTESIAN_POINT('Ctrl Pts',(-61.6507948262107,-4.64333739276948,
-0.2813953903773));
#53770=CARTESIAN_POINT('Ctrl Pts',(-61.4519212945132,-2.2734509944866,-4.0584709047232));
#53771=CARTESIAN_POINT('Ctrl Pts',(-61.2530477628157,2.18528684554512,-4.10661501866251));
#53772=CARTESIAN_POINT('Ctrl Pts',(-61.0541742311184,4.63617864490049,-0.381592821454718));
#53773=CARTESIAN_POINT('Ctrl Pts',(-60.8553006994208,2.82733998598282,3.69403764361975));
#53774=CARTESIAN_POINT('Ctrl Pts',(-60.6564271677235,-1.57926445735542,
4.37557873687019));
#53775=CARTESIAN_POINT('Ctrl Pts',(-60.4575536360258,-4.53483747461512,
1.03682910242867));
#53776=CARTESIAN_POINT('Ctrl Pts',(-60.2586801043286,-3.32379250894121,
-3.25456124021708));
#53777=CARTESIAN_POINT('Ctrl Pts',(-60.059806572631,0.941159838599904,-4.55565403285013));
#53778=CARTESIAN_POINT('Ctrl Pts',(-59.8609330409336,4.34137259397775,-1.67100254610099));
#53779=CARTESIAN_POINT('Ctrl Pts',(-59.6620595092361,3.75272329598755,2.74896951102943));
#53780=CARTESIAN_POINT('Ctrl Pts',(-59.4631859775387,-0.283935871719825,
4.64318273704232));
#53781=CARTESIAN_POINT('Ctrl Pts',(-59.2643124458413,-4.05971417749329,
2.27123013054094));
#53782=CARTESIAN_POINT('Ctrl Pts',(-59.0654389141437,-4.10541876128613,
-2.18753338335589));
#53783=CARTESIAN_POINT('Ctrl Pts',(-58.8665653824463,-0.379056157665712,
-4.63638673302307));
#53784=CARTESIAN_POINT('Ctrl Pts',(-58.6676918507489,3.69558402192361,-2.82531843262312));
#53785=CARTESIAN_POINT('Ctrl Pts',(-58.4688183190514,4.37471401412829,1.58165824481985));
#53786=CARTESIAN_POINT('Ctrl Pts',(-58.269944787354,1.03434778767158,4.53540407934683));
#53787=CARTESIAN_POINT('Ctrl Pts',(-58.0710712556565,-3.25637930989572,
3.32201133334915));
#53788=CARTESIAN_POINT('Ctrl Pts',(-57.872197723959,-4.5551384112965,-0.94365224672451));
#53789=CARTESIAN_POINT('Ctrl Pts',(-57.6733241922616,-1.66862698745729,
-4.34228620493241));
#53790=CARTESIAN_POINT('Ctrl Pts',(-57.4744506605641,2.75102233860371,-3.75121868215123));
#53791=CARTESIAN_POINT('Ctrl Pts',(-57.2755771288667,4.64302669135687,0.286476268064849));
#53792=CARTESIAN_POINT('Ctrl Pts',(-57.0767035971692,2.26900858669214,4.06095623496905));
#53793=CARTESIAN_POINT('Ctrl Pts',(-56.8778300654718,-2.18977926631837,
4.1042212749338));
#53794=CARTESIAN_POINT('Ctrl Pts',(-56.6789565337743,-4.63659343322196,
0.376519380404392));
#53795=CARTESIAN_POINT('Ctrl Pts',(-56.4800830020769,-2.82329603349106,
-3.69712929393748));
#53796=CARTESIAN_POINT('Ctrl Pts',(-56.2812094703794,1.58405155880773,-4.37384798179542));
#53797=CARTESIAN_POINT('Ctrl Pts',(-56.0823359386819,4.53596932638436,-1.03186616327761));
#53798=CARTESIAN_POINT('Ctrl Pts',(-55.8834624069846,3.32022916329763,3.25819640476215));
#53799=CARTESIAN_POINT('Ctrl Pts',(-55.684588875287,-0.946144372362453,
4.55462142614115));
#53800=CARTESIAN_POINT('Ctrl Pts',(-55.4857153435897,-4.34319851600362,
1.66625092930237));
#53801=CARTESIAN_POINT('Ctrl Pts',(-55.286841811892,-3.74971294537027,-2.75307434264664));
#53802=CARTESIAN_POINT('Ctrl Pts',(-55.0879682801948,0.289016578651858,
-4.64286925575996));
#53803=CARTESIAN_POINT('Ctrl Pts',(-54.8890947484972,4.0621970767789,-2.26678636360509));
#53804=CARTESIAN_POINT('Ctrl Pts',(-54.6902212167999,4.10302255996373,2.19202449376046));
#53805=CARTESIAN_POINT('Ctrl Pts',(-54.4913476851023,0.373982490430176,
4.63679874543512));
#53806=CARTESIAN_POINT('Ctrl Pts',(-54.292474153405,-3.69867345919861,2.82127278919229));
#53807=CARTESIAN_POINT('Ctrl Pts',(-54.0936006217074,-4.37298064013094,
-1.58644439860245));
#53808=CARTESIAN_POINT('Ctrl Pts',(-53.89472709001,-1.02938422998975,-4.5365332155585));
#53809=CARTESIAN_POINT('Ctrl Pts',(-53.6958535583125,3.26001252427244,-3.31844599932015));
#53810=CARTESIAN_POINT('Ctrl Pts',(-53.496980026615,4.55410307753876,0.948636214767613));
#53811=CARTESIAN_POINT('Ctrl Pts',(-53.2981064949176,1.66387437234772,4.34410952691816));
#53812=CARTESIAN_POINT('Ctrl Pts',(-53.0992329632202,-2.75512552254401,
3.74820608609554));
#53813=CARTESIAN_POINT('Ctrl Pts',(-52.9003594315228,-4.64271043029872,
-0.291556802720443));
#53814=CARTESIAN_POINT('Ctrl Pts',(-52.7014858998252,-2.26456346194496,
-4.06343670255129));
#53815=CARTESIAN_POINT('Ctrl Pts',(-52.5026123681279,2.19426906500987,-4.10182261673488));
#53816=CARTESIAN_POINT('Ctrl Pts',(-52.3037388364303,4.63700266960115,-0.371445488502572));
#53817=CARTESIAN_POINT('Ctrl Pts',(-52.1048653047329,2.81924870033247,3.70021651724473));
#53818=CARTESIAN_POINT('Ctrl Pts',(-51.9059917730354,-1.58883676348771,
4.37211198939449));
#53819=CARTESIAN_POINT('Ctrl Pts',(-51.707118241338,-4.53709574670044,1.02690198855093));
#53820=CARTESIAN_POINT('Ctrl Pts',(-51.5082447096406,-3.31666184195056,
-3.2618276678828));
#53821=CARTESIAN_POINT('Ctrl Pts',(-51.309371177943,0.951127773194121,-4.55358336564463));
#53822=CARTESIAN_POINT('Ctrl Pts',(-51.1104976462456,4.34501923740356,-1.66149731730449));
#53823=CARTESIAN_POINT('Ctrl Pts',(-50.9116241145482,3.74669810477784,2.75717587768194));
#53824=CARTESIAN_POINT('Ctrl Pts',(-50.7127505828507,-0.294096939510222,
4.64255021502059));
#53825=CARTESIAN_POINT('Ctrl Pts',(-50.5138770511534,-4.06467511191512,
2.2623398823773));
#53826=CARTESIAN_POINT('Ctrl Pts',(-50.3150035194557,-4.10062144560646,
-2.19651297939471));
#53827=CARTESIAN_POINT('Ctrl Pts',(-50.1161299877585,-0.368908375381047,
-4.63720520565898));
#53828=CARTESIAN_POINT('Ctrl Pts',(-49.9172564560607,3.70175846761393,-2.81722376751752));
#53829=CARTESIAN_POINT('Ctrl Pts',(-49.7183829243636,4.37124202984609,1.59122865274734));
#53830=CARTESIAN_POINT('Ctrl Pts',(-49.5195093926659,1.02441943970435,4.53765691964172));
#53831=CARTESIAN_POINT('Ctrl Pts',(-49.3206358609686,-3.26364183505,3.31487669172296));
#53832=CARTESIAN_POINT('Ctrl Pts',(-49.1217623292711,-4.55306229061429,
-0.953619046896171));
#53833=CARTESIAN_POINT('Ctrl Pts',(-48.9228887975736,-1.65911976488428,
-4.34592764718735));
#53834=CARTESIAN_POINT('Ctrl Pts',(-48.7240152658762,2.75922540744653,-3.74518900186874));
#53835=CARTESIAN_POINT('Ctrl Pts',(-48.5251417341786,4.6423886099736,0.296636988260731));
#53836=CARTESIAN_POINT('Ctrl Pts',(-48.3262682024814,2.26011562556773,4.06591230449965));
#53837=CARTESIAN_POINT('Ctrl Pts',(-48.1273946707837,-2.19875623624322,
4.09941904693807));
#53838=CARTESIAN_POINT('Ctrl Pts',(-47.9285211390865,-4.63740635354801,
0.366371151825084));
#53839=CARTESIAN_POINT('Ctrl Pts',(-47.7296476073888,-2.81519799135364,
-3.70329930984454));
#53840=CARTESIAN_POINT('Ctrl Pts',(-47.5307740756915,1.59362006566512,-4.37037076174621));
#53841=CARTESIAN_POINT('Ctrl Pts',(-47.331900543994,4.53821673421451,-1.02193658419319));
#53842=CARTESIAN_POINT('Ctrl Pts',(-47.1330270122966,3.31309054917171,3.26545502523097));
#53843=CARTESIAN_POINT('Ctrl Pts',(-46.934153480599,-0.956110035128021,
4.55253985260366));
#53844=CARTESIAN_POINT('Ctrl Pts',(-46.7352799489017,-4.34683475599761,
1.65674171579889));
#53845=CARTESIAN_POINT('Ctrl Pts',(-46.5364064172041,-3.74367877782001,
-2.76127411122423));
#53846=CARTESIAN_POINT('Ctrl Pts',(-46.3375328855068,0.299176948211582,
-4.64222561520612));
#53847=CARTESIAN_POINT('Ctrl Pts',(-46.1386593538092,4.06714827993455,-2.2578906921821));
#53848=CARTESIAN_POINT('Ctrl Pts',(-45.9397858221119,4.09821542108963,2.20099883488389));
#53849=CARTESIAN_POINT('Ctrl Pts',(-45.7409122904143,0.363833818594308,
4.63760611320794));
#53850=CARTESIAN_POINT('Ctrl Pts',(-45.542038758717,-3.7048390434754,2.81317137244729));
#53851=CARTESIAN_POINT('Ctrl Pts',(-45.3431652270194,-4.36949818535569,
-1.5960110015255));
#53852=CARTESIAN_POINT('Ctrl Pts',(-45.1442916953221,-1.01945342276039,
-4.53877519025113));
#53853=CARTESIAN_POINT('Ctrl Pts',(-44.9454181636245,3.2672672378829,-3.3113034148314));
#53854=CARTESIAN_POINT('Ctrl Pts',(-44.7465446319271,4.55201605176918,0.958600737143906));
#53855=CARTESIAN_POINT('Ctrl Pts',(-44.5476711002296,1.65436317076021,4.34774056356279));
#53856=CARTESIAN_POINT('Ctrl Pts',(-44.3487975685322,-2.76332198840176,
3.74216743308372));
#53857=CARTESIAN_POINT('Ctrl Pts',(-44.1499240368347,-4.64206123076694,
-0.301716818602429));
#53858=CARTESIAN_POINT('Ctrl Pts',(-43.9510505051373,-2.25566508288644,
-4.0683830378498));
#53859=CARTESIAN_POINT('Ctrl Pts',(-43.7521769734398,2.20324077464528,-4.09701056842145));
#53860=CARTESIAN_POINT('Ctrl Pts',(-43.5533034417424,4.6378044845791,-0.361296376448224));
#53861=CARTESIAN_POINT('Ctrl Pts',(-43.3544299100449,2.81114391140508,3.70637766804561));
#53862=CARTESIAN_POINT('Ctrl Pts',(-43.1555563783475,-1.59840145961267,
4.36862430093561));
#53863=CARTESIAN_POINT('Ctrl Pts',(-42.9566828466501,-4.53933228758441,
1.0169699561495));
#53864=CARTESIAN_POINT('Ctrl Pts',(-42.7578093149525,-3.3095152892371,-3.26907847246329));
#53865=CARTESIAN_POINT('Ctrl Pts',(-42.5589357832552,0.961091152198231,
-4.55149088826764));
#53866=CARTESIAN_POINT('Ctrl Pts',(-42.3600622515576,4.34864506961174,-1.65198413048027));
#53867=CARTESIAN_POINT('Ctrl Pts',(-42.1611887198603,3.74065496811231,2.76536903836609));
#53868=CARTESIAN_POINT('Ctrl Pts',(-41.9623151881627,-0.304256598672874,
4.64189545670523));
#53869=CARTESIAN_POINT('Ctrl Pts',(-41.7634416564653,-4.06961657787565,
2.25343879834717));
#53870=CARTESIAN_POINT('Ctrl Pts',(-41.5645681247679,-4.09580448929436,
-2.20548205485632));
#53871=CARTESIAN_POINT('Ctrl Pts',(-41.3656945930703,-0.358758826146377,
-4.63800146760209));
#53872=CARTESIAN_POINT('Ctrl Pts',(-41.166821061373,3.70791518309455,-2.80911560883385));
#53873=CARTESIAN_POINT('Ctrl Pts',(-40.9679475296754,4.36774910874765,1.60079143921098));
#53874=CARTESIAN_POINT('Ctrl Pts',(-40.7690739979781,1.01448618510396,4.53988802604759));
#53875=CARTESIAN_POINT('Ctrl Pts',(-40.5702004662805,-3.27088872842992,
3.30772617292411));
#53876=CARTESIAN_POINT('Ctrl Pts',(-40.3713269345831,-4.55096436225627,
-0.963581279545481));
#53877=CARTESIAN_POINT('Ctrl Pts',(-40.1724534028856,-1.64960459567123,
-4.34954827387366));
#53878=CARTESIAN_POINT('Ctrl Pts',(-39.9735798711882,2.7674152605043,-3.73914138335856));
#53879=CARTESIAN_POINT('Ctrl Pts',(-39.7747063394908,4.6417282930707,0.306796287662675));
#53880=CARTESIAN_POINT('Ctrl Pts',(-39.5758328077933,2.25121183923051,4.0708488996431));
#53881=CARTESIAN_POINT('Ctrl Pts',(-39.3769592760958,-2.20772267484625,
4.09459718406912));
#53882=CARTESIAN_POINT('Ctrl Pts',(-39.1780857443984,-4.63819706221785,
0.356221168448329));
#53883=CARTESIAN_POINT('Ctrl Pts',(-38.979212212701,-2.80708646534088,-3.70945158816194));
#53884=CARTESIAN_POINT('Ctrl Pts',(-38.7803386810035,1.60318093960496,-4.36687260905381));
#53885=CARTESIAN_POINT('Ctrl Pts',(-38.5814651493061,4.5404424054743,-1.01200211036728));
#53886=CARTESIAN_POINT('Ctrl Pts',(-38.3825916176086,3.30593606642799,3.27269800524089));
#53887=CARTESIAN_POINT('Ctrl Pts',(-38.1837180859111,-0.966071118440219,
4.55043647389266));
#53888=CARTESIAN_POINT('Ctrl Pts',(-37.9848445542137,-4.35045017607815,
1.64722456704551));
#53889=CARTESIAN_POINT('Ctrl Pts',(-37.7859710225162,-3.73762667927559,
-2.76946065420398));
#53890=CARTESIAN_POINT('Ctrl Pts',(-37.5870974908188,0.309335884811614,
-4.64155973991339));
#53891=CARTESIAN_POINT('Ctrl Pts',(-37.3882239591213,4.07208000278311,-2.2489842062031));
#53892=CARTESIAN_POINT('Ctrl Pts',(-37.1893504274239,4.0933886531073,2.20996263394419));
#53893=CARTESIAN_POINT('Ctrl Pts',(-36.9904768957264,0.353683404113827,
4.6383912683679));
#53894=CARTESIAN_POINT('Ctrl Pts',(-36.791603364029,-3.71098688278783,2.80505648153359));
#53895=CARTESIAN_POINT('Ctrl Pts',(-36.5927298323315,-4.36599480211647,
-1.60556996007931));
#53896=CARTESIAN_POINT('Ctrl Pts',(-36.393856300634,-1.00951773268308,-4.54099542569859));
#53897=CARTESIAN_POINT('Ctrl Pts',(-36.1949827689366,3.27450630235449,-3.30414497028465));
#53898=CARTESIAN_POINT('Ctrl Pts',(-35.9961092372392,4.54990722333487,0.968560668136903));
#53899=CARTESIAN_POINT('Ctrl Pts',(-35.7972357055417,1.64484404531562,4.35135077595531));
#53900=CARTESIAN_POINT('Ctrl Pts',(-35.5983621738442,-2.77150521885286,
3.73611085631683));
#53901=CARTESIAN_POINT('Ctrl Pts',(-35.3994886421467,-4.64138979728367,
-0.311875389359506));
#53902=CARTESIAN_POINT('Ctrl Pts',(-35.2006151104494,-2.24675589993187,
-4.07330988692714));
#53903=CARTESIAN_POINT('Ctrl Pts',(-35.0017415787518,2.21220193147961,-4.09217889677064));
#53904=CARTESIAN_POINT('Ctrl Pts',(-34.8028680470544,4.63858408599405,-0.351145533902577));
#53905=CARTESIAN_POINT('Ctrl Pts',(-34.6039945153569,2.80302565801969,3.71252106651267));
#53906=CARTESIAN_POINT('Ctrl Pts',(-34.4051209836595,-1.60795849991889,
4.36511568819838));
#53907=CARTESIAN_POINT('Ctrl Pts',(-34.206247451962,-4.54154708655483,1.00703305279517));
#53908=CARTESIAN_POINT('Ctrl Pts',(-34.0073739202647,-3.30235288503029,
-3.27631361922951));
#53909=CARTESIAN_POINT('Ctrl Pts',(-33.8085003885671,0.971049927890603,
-4.54937661074138));
#53910=CARTESIAN_POINT('Ctrl Pts',(-33.6096268568697,4.35225007323551,-1.64246303119386));
#53911=CARTESIAN_POINT('Ctrl Pts',(-33.4107533251722,3.73459391493592,2.77354895383887));
#53912=CARTESIAN_POINT('Ctrl Pts',(-33.2118797934748,-0.314414800546058,
4.64121846523245));
#53913=CARTESIAN_POINT('Ctrl Pts',(-33.0130062617773,-4.07453855170703,
2.24452692108387));
#53914=CARTESIAN_POINT('Ctrl Pts',(-32.8141327300799,-4.09096791542132,
-2.21444056678213));
#53915=CARTESIAN_POINT('Ctrl Pts',(-32.6152591983824,-0.348607558574277,
-4.63877551503864));
#53916=CARTESIAN_POINT('Ctrl Pts',(-32.416385666685,3.71405413887715,-2.80099399540709));
#53917=CARTESIAN_POINT('Ctrl Pts',(-32.2175121349874,4.36423526756273,1.61034655840855));
#53918=CARTESIAN_POINT('Ctrl Pts',(-32.0186386032901,1.00454807144728,4.542097387878));
#53919=CARTESIAN_POINT('Ctrl Pts',(-31.8197650715926,-3.27811995532495,
3.30055981120134));
#53920=CARTESIAN_POINT('Ctrl Pts',(-31.6208915398952,-4.5488446362709,-0.973538896956091));
#53921=CARTESIAN_POINT('Ctrl Pts',(-31.4220180081977,-1.64008152539322,
-4.35314806764954));
#53922=CARTESIAN_POINT('Ctrl Pts',(-31.2231444765002,2.77559185855018,-3.73307585558706));
#53923=CARTESIAN_POINT('Ctrl Pts',(-31.0242709448028,4.64104574381103,0.316954117611085));
#53924=CARTESIAN_POINT('Ctrl Pts',(-30.8253974131053,2.24229727032636,4.07576599675497));
#53925=CARTESIAN_POINT('Ctrl Pts',(-30.6265238814079,-2.21667853918166,
4.08975570942184));
#53926=CARTESIAN_POINT('Ctrl Pts',(-30.4276503497104,-4.63896555544426,
0.346069478888772));
#53927=CARTESIAN_POINT('Ctrl Pts',(-30.228776818013,-2.79896149430411,-3.71558609942221));
#53928=CARTESIAN_POINT('Ctrl Pts',(-30.0299032863155,1.61273413483346,-4.3633535404732));
#53929=CARTESIAN_POINT('Ctrl Pts',(-29.8310297546181,4.54264632950338,-1.00206278938327));
#53930=CARTESIAN_POINT('Ctrl Pts',(-29.6321562229206,3.29876574933446,3.27992531010005));
#53931=CARTESIAN_POINT('Ctrl Pts',(-29.4332826912232,-0.976027574588195,
4.54831130008276));
#53932=CARTESIAN_POINT('Ctrl Pts',(-29.2344091595257,-4.35404475892857,
1.63769952862658));
#53933=CARTESIAN_POINT('Ctrl Pts',(-29.0355356278282,-3.73155667872468,
-2.77763393237523));
#53934=CARTESIAN_POINT('Ctrl Pts',(-28.8366620961308,0.319493339794431,
-4.6408716330711));
#53935=CARTESIAN_POINT('Ctrl Pts',(-28.6377885644333,4.07699222170351,-2.2400669483268));
#53936=CARTESIAN_POINT('Ctrl Pts',(-28.4389150327359,4.08854227913508,2.21891584800811));
#53937=CARTESIAN_POINT('Ctrl Pts',(-28.2400415010384,0.343531295605794,
4.63915420715415));
#53938=CARTESIAN_POINT('Ctrl Pts',(-28.041167969341,-3.71711694768952,2.79692815531905));
#53939=CARTESIAN_POINT('Ctrl Pts',(-27.8422944376435,-4.36247050719351,
-1.61512122847912));
#53940=CARTESIAN_POINT('Ctrl Pts',(-27.6434209059461,-0.999577207347043,
-4.54319391126653));
#53941=CARTESIAN_POINT('Ctrl Pts',(-27.4445473742487,3.28172968301435,-3.29697069996681));
#53942=CARTESIAN_POINT('Ctrl Pts',(-27.2456738425511,4.5477766023366,0.978515960041948));
#53943=CARTESIAN_POINT('Ctrl Pts',(-27.0468003108538,1.63531704160702,4.35494014680417));
#53944=CARTESIAN_POINT('Ctrl Pts',(-26.8479267791562,-2.77967517470273,
3.73003638480356));
#53945=CARTESIAN_POINT('Ctrl Pts',(-26.6490532474588,-4.6406961330648,-0.322032466335979));
#53946=CARTESIAN_POINT('Ctrl Pts',(-26.4501797157613,-2.23783595575289,
-4.0782172261855));
#53947=CARTESIAN_POINT('Ctrl Pts',(-26.2513061840639,2.22115249259184,-4.08732762492435));
#53948=CARTESIAN_POINT('Ctrl Pts',(-26.0524326523664,4.63934147011183,-0.340993009485119));
#53949=CARTESIAN_POINT('Ctrl Pts',(-25.853559120669,2.79489397906051,3.71864668322071));
#53950=CARTESIAN_POINT('Ctrl Pts',(-25.6546855889715,-1.61750783863076,
4.3615861679881));
#53951=CARTESIAN_POINT('Ctrl Pts',(-25.4558120572741,-4.5437401330036,0.997091326082762));
#53952=CARTESIAN_POINT('Ctrl Pts',(-25.2569385255766,-3.29517466363574,
-3.28353307352769));
#53953=CARTESIAN_POINT('Ctrl Pts',(-25.0580649938792,0.981004052572414,
-4.54724054319249));
#53954=CARTESIAN_POINT('Ctrl Pts',(-24.8591914621817,4.35583423100831,-1.63293406504773));
#53955=CARTESIAN_POINT('Ctrl Pts',(-24.6603179304843,3.72851497427881,2.78171558492152));
#53956=CARTESIAN_POINT('Ctrl Pts',(-24.4614443987868,-0.324571496475413,
4.64051924384463));
#53957=CARTESIAN_POINT('Ctrl Pts',(-24.2625708670894,-4.07944100983435,
2.23560429327258));
#53958=CARTESIAN_POINT('Ctrl Pts',(-24.0636973353919,-4.08611174715321,
-2.22338847226336));
#53959=CARTESIAN_POINT('Ctrl Pts',(-23.8648238036945,-0.338454621286521,
-4.63952734426114));
#53960=CARTESIAN_POINT('Ctrl Pts',(-23.665950271997,3.72017530555782,-2.79285896613754));
#53961=CARTESIAN_POINT('Ctrl Pts',(-23.4670767402996,4.3607005231217,1.61989396457395));
#53962=CARTESIAN_POINT('Ctrl Pts',(-23.2682032086021,0.994605146334582,
4.54428499455105));
#53963=CARTESIAN_POINT('Ctrl Pts',(-23.0693296769047,-3.28533548110023,
3.29337764087889));
#53964=CARTESIAN_POINT('Ctrl Pts',(-22.8704561452072,-4.5467031228109,-0.983491851434788));
#53965=CARTESIAN_POINT('Ctrl Pts',(-22.6715826135097,-1.63055059966216,
-4.35672701127326));
#53966=CARTESIAN_POINT('Ctrl Pts',(-22.4727090818123,2.7837551624209,-3.72699244760593));
#53967=CARTESIAN_POINT('Ctrl Pts',(-22.2738355501148,4.64034096546365,0.327110429452991));
#53968=CARTESIAN_POINT('Ctrl Pts',(-22.0749620184174,2.2333719615536,4.08066357228372));
#53969=CARTESIAN_POINT('Ctrl Pts',(-21.8760884867199,-2.2256237863533,4.08489464618556));
#53970=CARTESIAN_POINT('Ctrl Pts',(-21.6772149550225,-4.6397118295465,0.335916131769966));
#53971=CARTESIAN_POINT('Ctrl Pts',(-21.478341423325,-2.79082311715933,-3.72170281424325));
#53972=CARTESIAN_POINT('Ctrl Pts',(-21.2794678916276,1.6222796055944,-4.35981357285946));
#53973=CARTESIAN_POINT('Ctrl Pts',(-21.0805943599301,4.54482849574578,-0.992118668846749));
#53974=CARTESIAN_POINT('Ctrl Pts',(-20.8817208282327,3.29157963223422,3.2871369051924));
#53975=CARTESIAN_POINT('Ctrl Pts',(-20.6828472965352,-0.985979355884234,
4.54616434135269));
#53976=CARTESIAN_POINT('Ctrl Pts',(-20.4839737648377,-4.35761848733187,
1.62816664616376));
#53977=CARTESIAN_POINT('Ctrl Pts',(-20.2851002331403,-3.72546880524065,
-2.78579390659035));
#53978=CARTESIAN_POINT('Ctrl Pts',(-20.0862267014428,0.329649264508629,
-4.6401612979751));
#53979=CARTESIAN_POINT('Ctrl Pts',(-19.8873531697454,4.08188491316758,-2.2311389612644));
#53980=CARTESIAN_POINT('Ctrl Pts',(-19.6884796380479,4.08367632238581,2.22785843419248));
#53981=CARTESIAN_POINT('Ctrl Pts',(-19.4896061063505,0.33337754169537,4.63989492591268));
#53982=CARTESIAN_POINT('Ctrl Pts',(-19.290732574653,-3.72322920881974,2.78878643273532));
#53983=CARTESIAN_POINT('Ctrl Pts',(-19.0918590429556,-4.35892531746685,
-1.62466476097796));
#53984=CARTESIAN_POINT('Ctrl Pts',(-18.8929855112581,-0.989631894363675,
-4.54537063642502));
#53985=CARTESIAN_POINT('Ctrl Pts',(-18.6941119795606,3.28893734526478,-3.28978063824008));
#53986=CARTESIAN_POINT('Ctrl Pts',(-18.4952384478633,4.54562419897928,0.988466565176122));
#53987=CARTESIAN_POINT('Ctrl Pts',(-18.2963649161657,1.62578220526613,4.35850865891729));
#53988=CARTESIAN_POINT('Ctrl Pts',(-18.0974913844683,-2.78783181681954,
3.72394404763897));
#53989=CARTESIAN_POINT('Ctrl Pts',(-17.8986178527708,-4.63998024143282,
-0.332188000882232));
#53990=CARTESIAN_POINT('Ctrl Pts',(-17.6997443210734,-2.22890529307343,
-4.08310503212032));
#53991=CARTESIAN_POINT('Ctrl Pts',(-17.500870789376,2.23009241511192,-4.08245677611868));
#53992=CARTESIAN_POINT('Ctrl Pts',(-17.3019972576785,4.64007663330486,-0.330838851822665));
#53993=CARTESIAN_POINT('Ctrl Pts',(-17.103123725981,2.78674891347519,3.72475448883036));
#53994=CARTESIAN_POINT('Ctrl Pts',(-16.9042501942836,-1.6270494300105,4.35803575720979));
#53995=CARTESIAN_POINT('Ctrl Pts',(-16.7053766625861,-4.54591141642659,
0.987144823629757));
#53996=CARTESIAN_POINT('Ctrl Pts',(-16.5065031308886,-3.28798065943487,
-3.2907368007787));
#53997=CARTESIAN_POINT('Ctrl Pts',(-16.3076295991912,0.990953478566145,
-4.54508269585216));
#53998=CARTESIAN_POINT('Ctrl Pts',(-16.1087560674937,4.35939752576299,-1.623397277683));
#53999=CARTESIAN_POINT('Ctrl Pts',(-15.9098825357963,3.72241817525742,2.78986889249841));
#54000=CARTESIAN_POINT('Ctrl Pts',(-15.7110090040988,-0.334726637813821,
4.63979779589099));
#54001=CARTESIAN_POINT('Ctrl Pts',(-15.5121354724014,-4.0843239287767,2.22667095764937));
#54002=CARTESIAN_POINT('Ctrl Pts',(-15.313261940704,-4.08123600774924,-2.2323257284429));
#54003=CARTESIAN_POINT('Ctrl Pts',(-15.1143884090065,-0.32830006291181,
-4.64025695166864));
#54004=CARTESIAN_POINT('Ctrl Pts',(-14.9155148773091,3.72627865381841,-2.78471055998893));
#54005=CARTESIAN_POINT('Ctrl Pts',(-14.7166413456116,4.35714489235463,1.62943361197828));
#54006=CARTESIAN_POINT('Ctrl Pts',(-14.5177678139142,0.984657457389458,
4.54645083558862));
#54007=CARTESIAN_POINT('Ctrl Pts',(-14.3188942822167,-3.29253527119538,
3.28617969635737));
#54008=CARTESIAN_POINT('Ctrl Pts',(-14.1200207505192,-4.54453983213353,
-0.99344009530966));
#54009=CARTESIAN_POINT('Ctrl Pts',(-13.9211472188218,-1.62101186412838,
-4.36028508760289));
#54010=CARTESIAN_POINT('Ctrl Pts',(-13.7222736871243,2.79190513301711,-3.72089118855278));
#54011=CARTESIAN_POINT('Ctrl Pts',(-13.5234001554269,4.63961396140426,0.337265174543437));
#54012=CARTESIAN_POINT('Ctrl Pts',(-13.3245266237294,2.22443595566105,4.08554160277182));
#54013=CARTESIAN_POINT('Ctrl Pts',(-13.125653092032,-2.23455837351676,4.08001401764292));
#54014=CARTESIAN_POINT('Ctrl Pts',(-12.9267795603345,-4.64043588095,0.32576117572301));
#54015=CARTESIAN_POINT('Ctrl Pts',(-12.7279060286371,-2.78267137288683,
-3.72780170332774));
#54016=CARTESIAN_POINT('Ctrl Pts',(-12.5290324969396,1.63181730616761,-4.35625272316804));
#54017=CARTESIAN_POINT('Ctrl Pts',(-12.3301589652422,4.54698889374953,-0.982169796387303));
#54018=CARTESIAN_POINT('Ctrl Pts',(-12.1312854335447,3.28437774954679,3.29433275597639));
#54019=CARTESIAN_POINT('Ctrl Pts',(-11.9324119018472,-0.995926414662293,
4.54399560798588));
#54020=CARTESIAN_POINT('Ctrl Pts',(-11.7335383701498,-4.36117134417128,
1.61862596531638));
#54021=CARTESIAN_POINT('Ctrl Pts',(-11.5346648384523,-3.71936308798217,
-2.79394053776611));
#54022=CARTESIAN_POINT('Ctrl Pts',(-11.3357913067549,0.339803610311178,
-4.63942873802762));
#54023=CARTESIAN_POINT('Ctrl Pts',(-11.1369177750574,4.0867580537411,-2.22220028777761));
#54024=CARTESIAN_POINT('Ctrl Pts',(-10.93804424336,4.07879080616561,2.23679034966525));
#54025=CARTESIAN_POINT('Ctrl Pts',(-10.7391707116625,0.323222191015989,
4.64061342109551));
#54026=CARTESIAN_POINT('Ctrl Pts',(-10.5402971799651,-3.72932363690246,
2.78063135277903));
#54027=CARTESIAN_POINT('Ctrl Pts',(-10.3414236482676,-4.35535924991699,
-1.63420051186504));
#54028=CARTESIAN_POINT('Ctrl Pts',(-10.1425501165701,-0.979681841367978,
-4.54752559074833));
#54029=CARTESIAN_POINT('Ctrl Pts',(-9.94367658487271,3.29612925458378,-3.28257481954243));
#54030=CARTESIAN_POINT('Ctrl Pts',(-9.74480305317525,4.54345002357212,0.998412435879852));
#54031=CARTESIAN_POINT('Ctrl Pts',(-9.54592952147778,1.61623958196106,4.36205629520292));
#54032=CARTESIAN_POINT('Ctrl Pts',(-9.34705598978034,-2.79597510613618,
3.71783387400295));
#54033=CARTESIAN_POINT('Ctrl Pts',(-9.14818245808287,-4.63924212581646,
-0.342341944357115));
#54034=CARTESIAN_POINT('Ctrl Pts',(-8.94930892638543,-2.21996395466823,
-4.08797328132057));
#54035=CARTESIAN_POINT('Ctrl Pts',(-8.75043539468797,2.23902165622032,-4.07756637368338));
#54036=CARTESIAN_POINT('Ctrl Pts',(-8.55156186299052,4.64078957205195,-0.320683109550672));
#54037=CARTESIAN_POINT('Ctrl Pts',(-8.35268833129305,2.77859050027624,3.73084445408698));
#54038=CARTESIAN_POINT('Ctrl Pts',(-8.15381479959562,-1.63658322835689,
4.35446447286893));
#54039=CARTESIAN_POINT('Ctrl Pts',(-7.95494126789817,-4.54806092642439,
0.977193593076505));
#54040=CARTESIAN_POINT('Ctrl Pts',(-7.75606773620069,-3.28077090688404,
-3.29792476647959));
#54041=CARTESIAN_POINT('Ctrl Pts',(-7.55719420450327,1.00089815821756,-4.5429030790555));
#54042=CARTESIAN_POINT('Ctrl Pts',(-7.35832067280577,4.36293994043349,-1.61385271477731));
#54043=CARTESIAN_POINT('Ctrl Pts',(-7.15944714110836,3.71630354707174,2.79800883751849));
#54044=CARTESIAN_POINT('Ctrl Pts',(-6.96057360941086,-0.344880175919108,
4.63905412482613));
#54045=CARTESIAN_POINT('Ctrl Pts',(-6.76170007771343,-4.08918728515111,
2.21772695700357));
#54046=CARTESIAN_POINT('Ctrl Pts',(-6.56282654601595,-4.07634072055376,
-2.24125229251686));
#54047=CARTESIAN_POINT('Ctrl Pts',(-6.36395301431851,-0.318143932104064,
-4.64096433376144));
#54048=CARTESIAN_POINT('Ctrl Pts',(-6.16507948262108,3.73236415445752,-2.77654881599912));
#54049=CARTESIAN_POINT('Ctrl Pts',(-5.96620595092361,4.35356839223221,1.63896545494819));
#54050=CARTESIAN_POINT('Ctrl Pts',(-5.76733241922618,0.974705052370221,
4.54859490058293));
#54051=CARTESIAN_POINT('Ctrl Pts',(-5.5684588875287,-3.29971929133901,3.27896601217681));
#54052=CARTESIAN_POINT('Ctrl Pts',(-5.36958535583126,-4.54235477419835,
-1.0033835810547));
#54053=CARTESIAN_POINT('Ctrl Pts',(-5.17071182413379,-1.6114653652374,-4.36382227936571));
#54054=CARTESIAN_POINT('Ctrl Pts',(-4.97183829243634,2.80004173273539,-3.71477210808612));
#54055=CARTESIAN_POINT('Ctrl Pts',(-4.77296476073888,4.63886473241052,0.347418305066963));
#54056=CARTESIAN_POINT('Ctrl Pts',(-4.57409122904143,2.21548930055591,4.09040006330192));
#54057=CARTESIAN_POINT('Ctrl Pts',(-4.37521769734399,-2.24348226752039,
4.07511385010318));
#54058=CARTESIAN_POINT('Ctrl Pts',(-4.17634416564654,-4.64113768798076,
0.315604653849238));
#54059=CARTESIAN_POINT('Ctrl Pts',(-3.97747063394909,-2.77450633490745,
-3.73388272700877));
#54060=CARTESIAN_POINT('Ctrl Pts',(-3.77859710225162,1.64134725578213,-4.35267102819626));
#54061=CARTESIAN_POINT('Ctrl Pts',(-3.57972357055418,4.54912739060225,-0.972216182378774));
#54062=CARTESIAN_POINT('Ctrl Pts',(-3.3808500388567,3.27716036719384,3.30151275759948));
#54063=CARTESIAN_POINT('Ctrl Pts',(-3.18197650715927,-1.0058691402618,4.54180524327511));
#54064=CARTESIAN_POINT('Ctrl Pts',(-2.98310297546179,-4.36470248731841,
1.60907728082845));
#54065=CARTESIAN_POINT('Ctrl Pts',(-2.78422944376435,-3.71324111417162,
-2.80207331303322));
#54066=CARTESIAN_POINT('Ctrl Pts',(-2.58535591206692,0.349959270344922,
-4.6386748514615));
#54067=CARTESIAN_POINT('Ctrl Pts',(-2.38648238036945,4.09160606540612,-2.21324928125868));
#54068=CARTESIAN_POINT('Ctrl Pts',(-2.18760884867201,4.07389624223523,2.24570836167469));
#54069=CARTESIAN_POINT('Ctrl Pts',(-1.98873531697453,0.3130454880471,4.64131571257674));
#54070=CARTESIAN_POINT('Ctrl Pts',(-1.7898617852771,-3.73536280844222,2.77245158125543));
#54071=CARTESIAN_POINT('Ctrl Pts',(-1.59098825357963,-4.35184292986101,
-1.64370696036797));
#54072=CARTESIAN_POINT('Ctrl Pts',(-1.39211472188218,-0.969593771807376,
-4.54969931394381));
#54073=CARTESIAN_POINT('Ctrl Pts',(-1.19324119018471,3.30305362104828,-3.27527670617991));
#54074=CARTESIAN_POINT('Ctrl Pts',(-0.99436765848726,4.54172955224769,1.00820889559649));
#54075=CARTESIAN_POINT('Ctrl Pts',(-0.795494126789819,1.60579062235263,
4.36585649554455));
#54076=CARTESIAN_POINT('Ctrl Pts',(-0.596620595092368,-2.80240157693687,
3.71118654204902));
#54077=CARTESIAN_POINT('Ctrl Pts',(-0.397747063394913,-4.64175293605412,
-0.351489043021168));
#54078=CARTESIAN_POINT('Ctrl Pts',(-0.198873531697459,-2.20438994272706,
-4.09491721997484));
#54079=CARTESIAN_POINT('Ctrl Pts',(-0.0662911772324887,0.753200145251245,
-4.0766024725601));
#54080=CARTESIAN_POINT('Ctrl Pts',(0.,1.90056365518826,-3.44330463255539));
#54081=CARTESIAN_POINT('Ctrl Pts',(-109.840375352461,2.1465679056518,-3.00907133330628));
#54082=CARTESIAN_POINT('Ctrl Pts',(-109.774084175229,3.14923801912089,-2.29380099002595));
#54083=CARTESIAN_POINT('Ctrl Pts',(-109.641501820764,4.36578186624803,0.205448283167597));
#54084=CARTESIAN_POINT('Ctrl Pts',(-109.442628289066,2.1828302128901,3.79135494426175));
#54085=CARTESIAN_POINT('Ctrl Pts',(-109.243754757369,-2.00739020931939,
3.88220005863922));
#54086=CARTESIAN_POINT('Ctrl Pts',(-109.044881225672,-4.35233487181785,
0.411914045285927));
#54087=CARTESIAN_POINT('Ctrl Pts',(-108.846007693974,-2.69881131862259,
-3.43989927573611));
#54088=CARTESIAN_POINT('Ctrl Pts',(-108.647134162277,1.43463230878561,-4.12950976794978));
#54089=CARTESIAN_POINT('Ctrl Pts',(-108.448260630579,4.24980218800881,-1.02577369861691));
#54090=CARTESIAN_POINT('Ctrl Pts',(-108.249387098881,3.1603142753221,3.02089836059846));
#54091=CARTESIAN_POINT('Ctrl Pts',(-108.050513567184,-0.832913522680676,
4.29172289545985));
#54092=CARTESIAN_POINT('Ctrl Pts',(-107.851640035487,-4.0608392610929,1.61943067713845));
#54093=CARTESIAN_POINT('Ctrl Pts',(-107.652766503789,-3.55766782523455,
-2.54086506131637));
#54094=CARTESIAN_POINT('Ctrl Pts',(-107.453892972092,0.214301555961404,
-4.3665731279193));
#54095=CARTESIAN_POINT('Ctrl Pts',(-107.255019440394,3.78936734507133,-2.18028371201605));
#54096=CARTESIAN_POINT('Ctrl Pts',(-107.056145908697,3.88275616348223,2.00926485052088));
#54097=CARTESIAN_POINT('Ctrl Pts',(-106.857272376999,0.408659838058558,
4.3526914492715));
#54098=CARTESIAN_POINT('Ctrl Pts',(-106.658398845302,-3.44091355749422,
2.69685901065956));
#54099=CARTESIAN_POINT('Ctrl Pts',(-106.459525313605,-4.12896873804798,
-1.43685450907243));
#54100=CARTESIAN_POINT('Ctrl Pts',(-106.260651781907,-1.023318844092,-4.25038236929084));
#54101=CARTESIAN_POINT('Ctrl Pts',(-106.06177825021,3.02255844136648,-3.15865059785157));
#54102=CARTESIAN_POINT('Ctrl Pts',(-105.862904718512,4.29130285844483,0.835256049012763));
#54103=CARTESIAN_POINT('Ctrl Pts',(-105.664031186815,1.61718938013062,4.06172760623251));
#54104=CARTESIAN_POINT('Ctrl Pts',(-105.465157655117,-2.54280101173057,
3.55627556087148));
#54105=CARTESIAN_POINT('Ctrl Pts',(-105.26628412342,-4.36646061795366,-0.216689804582339));
#54106=CARTESIAN_POINT('Ctrl Pts',(-105.067410591722,-2.17820724021727,
-3.7905601153123));
#54107=CARTESIAN_POINT('Ctrl Pts',(-104.868537060025,2.01138742088055,-3.88165601822906));
#54108=CARTESIAN_POINT('Ctrl Pts',(-104.669663528328,4.35291519048993,-0.406278396632699));
#54109=CARTESIAN_POINT('Ctrl Pts',(-104.47078999663,2.69497554496221,3.44238864741278));
#54110=CARTESIAN_POINT('Ctrl Pts',(-104.271916464933,-1.43911316458767,
4.12818193541817));
#54111=CARTESIAN_POINT('Ctrl Pts',(-104.073042933235,-4.25094174373322,
1.02099318415578));
#54112=CARTESIAN_POINT('Ctrl Pts',(-103.874169401538,-3.15699632033617,
-3.02428620070342));
#54113=CARTESIAN_POINT('Ctrl Pts',(-103.67529586984,0.837603804328724,-4.29084521487517));
#54114=CARTESIAN_POINT('Ctrl Pts',(-103.476422338143,4.06261183376389,-1.61496683523748));
#54115=CARTESIAN_POINT('Ctrl Pts',(-103.277548806445,3.55488376867866,2.54474638852664));
#54116=CARTESIAN_POINT('Ctrl Pts',(-103.078675274748,-0.219078802209198,
4.36634140548465));
#54117=CARTESIAN_POINT('Ctrl Pts',(-102.879801743051,-3.79175131980121,
2.17613297377842));
#54118=CARTESIAN_POINT('Ctrl Pts',(-102.680928211353,-3.88055493925962,
-2.01351090242111));
#54119=CARTESIAN_POINT('Ctrl Pts',(-102.482054679656,-0.40389671268999,
-4.3531368271939));
#54120=CARTESIAN_POINT('Ctrl Pts',(-102.283181147958,3.44386264280962,-2.69309169696215));
#54121=CARTESIAN_POINT('Ctrl Pts',(-102.084307616261,4.12739393090686,1.44137161408848));
#54122=CARTESIAN_POINT('Ctrl Pts',(-101.885434084563,1.01866720062227,4.25149972658647));
#54123=CARTESIAN_POINT('Ctrl Pts',(-101.686560552866,-3.02601304519553,
3.15534116080873));
#54124=CARTESIAN_POINT('Ctrl Pts',(-101.487687021168,-4.29038629185808,
-0.839951342295326));
#54125=CARTESIAN_POINT('Ctrl Pts',(-101.288813489471,-1.61274380422899,
-4.06349482744949));
#54126=CARTESIAN_POINT('Ctrl Pts',(-101.089939957773,2.54669100212833,-3.55349092168056));
#54127=CARTESIAN_POINT('Ctrl Pts',(-100.891066426076,4.36622088667936,0.221467739213865));
#54128=CARTESIAN_POINT('Ctrl Pts',(-100.692192894378,2.17405805550784,3.79294138658497));
#54129=CARTESIAN_POINT('Ctrl Pts',(-100.493319362681,-2.01563378099804,
3.87945270001931));
#54130=CARTESIAN_POINT('Ctrl Pts',(-100.294445830983,-4.35335716087738,
0.401514907102131));
#54131=CARTESIAN_POINT('Ctrl Pts',(-100.095572299286,-2.69120704271377,
-3.44533560688004));
#54132=CARTESIAN_POINT('Ctrl Pts',(-99.8966987675885,1.44362963207685,-4.12660469104774));
#54133=CARTESIAN_POINT('Ctrl Pts',(-99.6978252358912,4.25205643675013,-1.01634091203658));
#54134=CARTESIAN_POINT('Ctrl Pts',(-99.4989517041936,3.15368505670657,3.02773898377871));
#54135=CARTESIAN_POINT('Ctrl Pts',(-99.3000781724963,-0.842298628814002,
4.28992608452472));
#54136=CARTESIAN_POINT('Ctrl Pts',(-99.1012046407987,-4.0643766047116,1.61052029042189));
#54137=CARTESIAN_POINT('Ctrl Pts',(-98.9023311091013,-3.55209701092721,
-2.54863485335771));
#54138=CARTESIAN_POINT('Ctrl Pts',(-98.7034575774039,0.223856609920464,
-4.36609906083021));
#54139=CARTESIAN_POINT('Ctrl Pts',(-98.5045840457063,3.79413031793455,-2.1719824864205));
#54140=CARTESIAN_POINT('Ctrl Pts',(-98.3057105140091,3.87834929944671,2.01775605618441));
#54141=CARTESIAN_POINT('Ctrl Pts',(-98.1068369823113,0.399132981319003,
4.35357619136394));
#54142=CARTESIAN_POINT('Ctrl Pts',(-97.9079634506143,-3.44680753957338,
2.68932158283975));
#54143=CARTESIAN_POINT('Ctrl Pts',(-97.7090899189163,-4.1258142158704,-1.44588721790784));
#54144=CARTESIAN_POINT('Ctrl Pts',(-97.5102163872193,-1.01401431920456,
-4.25261187404115));
#54145=CARTESIAN_POINT('Ctrl Pts',(-97.3113428555217,3.02946401599422,-3.15202800853414));
#54146=CARTESIAN_POINT('Ctrl Pts',(-97.1124693238242,4.28946459298215,0.844645663186656));
#54147=CARTESIAN_POINT('Ctrl Pts',(-96.9135957921268,1.60829629449811,4.06525716528381));
#54148=CARTESIAN_POINT('Ctrl Pts',(-96.7147222604292,-2.55057794164146,
3.55070203683716));
#54149=CARTESIAN_POINT('Ctrl Pts',(-96.5158487287319,-4.36597592796914,
-0.22624541361453));
#54150=CARTESIAN_POINT('Ctrl Pts',(-96.3169751970343,-2.16990626714019,
-3.79531811349369));
#54151=CARTESIAN_POINT('Ctrl Pts',(-96.1181016653371,2.01987772734617,-3.8772447378723));
#54152=CARTESIAN_POINT('Ctrl Pts',(-95.9192281336393,4.35379391858736,-0.396750936053586));
#54153=CARTESIAN_POINT('Ctrl Pts',(-95.7203546019423,2.68743531790485,3.44827844044897));
#54154=CARTESIAN_POINT('Ctrl Pts',(-95.5214810702444,-1.44814437090583,
4.1250225056115));
#54155=CARTESIAN_POINT('Ctrl Pts',(-95.3226075385472,-4.25316603829313,
1.01168742282264));
#54156=CARTESIAN_POINT('Ctrl Pts',(-95.1237340068497,-3.15037001678757,
-3.03118814132569));
#54157=CARTESIAN_POINT('Ctrl Pts',(-94.9248604751521,0.84699244471074,-4.28900181736853));
#54158=CARTESIAN_POINT('Ctrl Pts',(-94.7259869434549,4.06613650890247,-1.60607181712339));
#54159=CARTESIAN_POINT('Ctrl Pts',(-94.5271134117573,3.54930599982806,2.55252026639791));
#54160=CARTESIAN_POINT('Ctrl Pts',(-94.3282398800599,-0.22863414958098,
4.36585148813298));
#54161=CARTESIAN_POINT('Ctrl Pts',(-94.1293663483624,-3.79650477290681,
2.16782939828839));
#54162=CARTESIAN_POINT('Ctrl Pts',(-93.930492816665,-3.87613901562676,-2.02199879384818));
#54163=CARTESIAN_POINT('Ctrl Pts',(-93.7316192849675,-0.394368772018966,
-4.35401034248242));
#54164=CARTESIAN_POINT('Ctrl Pts',(-93.5327457532702,3.44974830906646,-2.68554824847382));
#54165=CARTESIAN_POINT('Ctrl Pts',(-93.3338722215725,4.12422956050804,1.45040109039508));
#54166=CARTESIAN_POINT('Ctrl Pts',(-93.1349986898752,1.00936022358743,4.2537189293402));
#54167=CARTESIAN_POINT('Ctrl Pts',(-92.9361251581777,-3.03291135925695,
3.14871108196318));
#54168=CARTESIAN_POINT('Ctrl Pts',(-92.7372516264802,-4.28853775782238,
-0.849338972683687));
#54169=CARTESIAN_POINT('Ctrl Pts',(-92.5383780947829,-1.60384685896368,
-4.06701463530438));
#54170=CARTESIAN_POINT('Ctrl Pts',(-92.3395045630853,2.55446182704561,-3.54790890031782));
#54171=CARTESIAN_POINT('Ctrl Pts',(-92.140631031388,4.365725741359,0.231022817104761));
#54172=CARTESIAN_POINT('Ctrl Pts',(-91.9417574996904,2.16575188048686,3.79769029581866));
#54173=CARTESIAN_POINT('Ctrl Pts',(-91.742883967993,-2.02411925505553,3.8750321330411));
#54174=CARTESIAN_POINT('Ctrl Pts',(-91.5440104362954,-4.35422546298436,
0.391986489928216));
#54175=CARTESIAN_POINT('Ctrl Pts',(-91.3451369045981,-2.68366037511149,
-3.45121714498581));
#54176=CARTESIAN_POINT('Ctrl Pts',(-91.1462633729005,1.45265737570005,-4.12343538079742));
#54177=CARTESIAN_POINT('Ctrl Pts',(-90.9473898412032,4.25427054701684,-1.00703272219558));
#54178=CARTESIAN_POINT('Ctrl Pts',(-90.7485163095057,3.14705120455755,3.03463366927219));
#54179=CARTESIAN_POINT('Ctrl Pts',(-90.5496427778082,-0.851685246403096,
4.28807241448263));
#54180=CARTESIAN_POINT('Ctrl Pts',(-90.3507692461108,-4.06789154422664,
1.60162142068499));
#54181=CARTESIAN_POINT('Ctrl Pts',(-90.1518957144133,-3.54651073872464,
-2.55640262300335));
#54182=CARTESIAN_POINT('Ctrl Pts',(-89.9530221827159,0.233411415470766,
-4.36559868768483));
#54183=CARTESIAN_POINT('Ctrl Pts',(-89.7541486510185,3.79887468187438,-2.16367371435747));
#54184=CARTESIAN_POINT('Ctrl Pts',(-89.5552751193209,3.87392409044664,2.0262391103334));
#54185=CARTESIAN_POINT('Ctrl Pts',(-89.3564015876237,0.389604090494498,
4.35443928002878));
#54186=CARTESIAN_POINT('Ctrl Pts',(-89.1575280559259,-3.4526849477674,2.681771698383));
#54187=CARTESIAN_POINT('Ctrl Pts',(-88.9586545242288,-4.12263996671732,
-1.45491322614534));
#54188=CARTESIAN_POINT('Ctrl Pts',(-88.759780992531,-1.00470491934382,-4.25482089115792));
#54189=CARTESIAN_POINT('Ctrl Pts',(-88.5609074608338,3.03635507085581,-3.14539038506761));
#54190=CARTESIAN_POINT('Ctrl Pts',(-88.3620339291362,4.28760578748858,0.854031265166599));
#54191=CARTESIAN_POINT('Ctrl Pts',(-88.1631603974388,1.59939550295351,4.06876723540677));
#54192=CARTESIAN_POINT('Ctrl Pts',(-87.9642868657414,-2.55834265369014,
3.54511151546708));
#54193=CARTESIAN_POINT('Ctrl Pts',(-87.7654133340439,-4.36547032714852,
-0.23579994396399));
#54194=CARTESIAN_POINT('Ctrl Pts',(-87.5665398023464,-2.16159490052237,
-3.80005793071938));
#54195=CARTESIAN_POINT('Ctrl Pts',(-87.3676662706491,2.02835835904724,-3.87281488817511));
#54196=CARTESIAN_POINT('Ctrl Pts',(-87.1687927389515,4.35465179355167,-0.387221574430996));
#54197=CARTESIAN_POINT('Ctrl Pts',(-86.9699192072541,2.67988221885378,3.45415171697175));
#54198=CARTESIAN_POINT('Ctrl Pts',(-86.7710456755566,-1.45716864105561,
4.12184331850591));
#54199=CARTESIAN_POINT('Ctrl Pts',(-86.5721721438592,-4.25536996159869,
1.00237681572903));
#54200=CARTESIAN_POINT('Ctrl Pts',(-86.3732986121618,-3.14372862399053,
-3.03807556349247));
#54201=CARTESIAN_POINT('Ctrl Pts',(-86.1744250804642,0.856377028271844,
-4.28713787697993));
#54202=CARTESIAN_POINT('Ctrl Pts',(-85.9755515487668,4.06964170858263,-1.59716910643562));
#54203=CARTESIAN_POINT('Ctrl Pts',(-85.7766780170694,3.54371123096399,2.56028191852522));
#54204=CARTESIAN_POINT('Ctrl Pts',(-85.577804485372,-0.238188401869361,
4.36534065978847));
#54205=CARTESIAN_POINT('Ctrl Pts',(-85.3789309536744,-3.80124004199946,
2.1595154396039));
#54206=CARTESIAN_POINT('Ctrl Pts',(-85.180057421977,-3.87170452655856,-2.03047700056258));
#54207=CARTESIAN_POINT('Ctrl Pts',(-84.9811838902796,-0.384838942450937,
-4.35486300348942));
#54208=CARTESIAN_POINT('Ctrl Pts',(-84.782310358582,3.45561745215982,-2.67799193708943));
#54209=CARTESIAN_POINT('Ctrl Pts',(-84.5834368268847,4.12104543640164,1.45942361975566));
#54210=CARTESIAN_POINT('Ctrl Pts',(-84.3845632951872,1.00004841204814,4.25591775817481));
#54211=CARTESIAN_POINT('Ctrl Pts',(-84.1856897634897,-3.0397951466672,3.14206592182376));
#54212=CARTESIAN_POINT('Ctrl Pts',(-83.9868162317922,-4.28666868309671,
-0.858722535016742));
#54213=CARTESIAN_POINT('Ctrl Pts',(-83.7879427000949,-1.59494223179772,
-4.07051496349243));
#54214=CARTESIAN_POINT('Ctrl Pts',(-83.5890691683973,2.56222041692812,-3.54230988563454));
#54215=CARTESIAN_POINT('Ctrl Pts',(-83.3901956367,4.36520968564351,0.240576788472024));
#54216=CARTESIAN_POINT('Ctrl Pts',(-83.1913221050024,2.15743533222441,3.8024210153608));
#54217=CARTESIAN_POINT('Ctrl Pts',(-82.9924485733051,-2.03259503424531,
3.87059300592932));
#54218=CARTESIAN_POINT('Ctrl Pts',(-82.7935750416076,-4.3550729097788,0.382456195267517));
#54219=CARTESIAN_POINT('Ctrl Pts',(-82.5947015099101,-2.67610085365577,
-3.45708215289286));
#54220=CARTESIAN_POINT('Ctrl Pts',(-82.3958279782126,1.46167816157059,-4.12024632064336));
#54221=CARTESIAN_POINT('Ctrl Pts',(-82.1969544465152,4.25646428072227,-0.997719708998039));
#54222=CARTESIAN_POINT('Ctrl Pts',(-81.9980809148177,3.14040227906498,3.04151381986522));
#54223=CARTESIAN_POINT('Ctrl Pts',(-81.7992073831203,-0.861067784699082,
4.28619820597941));
#54224=CARTESIAN_POINT('Ctrl Pts',(-81.6003338514229,-4.07138699987473,
1.59271487970651));
#54225=CARTESIAN_POINT('Ctrl Pts',(-81.4014603197254,-3.54090747989828,
-2.56415814831845));
#54226=CARTESIAN_POINT('Ctrl Pts',(-81.2025867880279,0.242965103056872,
-4.36507740475289));
#54227=CARTESIAN_POINT('Ctrl Pts',(-81.0037132563305,3.80360085044983,-2.15535457900667));
#54228=CARTESIAN_POINT('Ctrl Pts',(-80.804839724633,3.86948032662017,2.03471245946132));
#54229=CARTESIAN_POINT('Ctrl Pts',(-80.6059661929357,0.380073333594103,
4.35528151235694));
#54230=CARTESIAN_POINT('Ctrl Pts',(-80.407092661238,-3.45854581873234,2.674208969119));
#54231=CARTESIAN_POINT('Ctrl Pts',(-80.2082191295408,-4.11944597147032,
-1.46393226582538));
#54232=CARTESIAN_POINT('Ctrl Pts',(-80.0093455978432,-0.995390707275934,
-4.25700952907747));
#54233=CARTESIAN_POINT('Ctrl Pts',(-79.8104720661457,3.04323158257202,-3.13873769621227));
#54234=CARTESIAN_POINT('Ctrl Pts',(-79.6115985344483,4.28572644576884,0.863412776616762));
#54235=CARTESIAN_POINT('Ctrl Pts',(-79.4127250027508,1.59048705082877,4.07225781746852));
#54236=CARTESIAN_POINT('Ctrl Pts',(-79.2138514710534,-2.56609511211621,
3.53950401417501));
#54237=CARTESIAN_POINT('Ctrl Pts',(-79.014977939356,-4.36494381715614,-0.245353344909039));
#54238=CARTESIAN_POINT('Ctrl Pts',(-78.8161044076585,-2.1532731805736,-3.80477954691332));
#54239=CARTESIAN_POINT('Ctrl Pts',(-78.617230875961,2.03682927557666,-3.86836648896422));
#54240=CARTESIAN_POINT('Ctrl Pts',(-78.4183573442637,4.35548881116147,-0.377690358144029));
#54241=CARTESIAN_POINT('Ctrl Pts',(-78.2194838125661,2.67231628404541,3.46000844924017));
#54242=CARTESIAN_POINT('Ctrl Pts',(-78.0206102808687,-1.46618593184531,
4.11864438912206));
#54243=CARTESIAN_POINT('Ctrl Pts',(-77.8217367491712,-4.25755350307716,
0.99306140757905));
#54244=CARTESIAN_POINT('Ctrl Pts',(-77.6228632174738,-3.13707217376396,
-3.04494843427329));
#54245=CARTESIAN_POINT('Ctrl Pts',(-77.4239896857763,0.865757510067786,
-4.2852534026063));
#54246=CARTESIAN_POINT('Ctrl Pts',(-77.2251161540789,4.07312741601313,-1.58825874583137));
#54247=CARTESIAN_POINT('Ctrl Pts',(-77.0262426223814,3.5380994888848,2.56803130774155));
#54248=CARTESIAN_POINT('Ctrl Pts',(-76.8273690906839,-0.247741513313501,
4.36480892289326));
#54249=CARTESIAN_POINT('Ctrl Pts',(-76.6284955589866,-3.80595710439848,
2.15119113754828));
#54250=CARTESIAN_POINT('Ctrl Pts',(-76.429622027289,-3.86725149329488,-2.03894548195781));
#54251=CARTESIAN_POINT('Ctrl Pts',(-76.2307484955916,-0.375307269630516,
-4.35569480613026));
#54252=CARTESIAN_POINT('Ctrl Pts',(-76.0318749638941,3.46147004397849,-2.67042279900155));
#54253=CARTESIAN_POINT('Ctrl Pts',(-75.8330014321968,4.11784157383855,1.46843915895566));
#54254=CARTESIAN_POINT('Ctrl Pts',(-75.6341279004991,0.990731810604663,
4.25809620255854));
#54255=CARTESIAN_POINT('Ctrl Pts',(-75.4352543688019,-3.04666437445524,
3.13540571221858));
#54256=CARTESIAN_POINT('Ctrl Pts',(-75.2363808371042,-4.28477907663331,
-0.868101984350383));
#54257=CARTESIAN_POINT('Ctrl Pts',(-75.037507305407,-1.58602996538132,-4.07399579524822));
#54258=CARTESIAN_POINT('Ctrl Pts',(-74.8386337737093,2.56996673461481,-3.53669390444816));
#54259=CARTESIAN_POINT('Ctrl Pts',(-74.6397602420121,4.36467272200467,0.250129607555377));
#54260=CARTESIAN_POINT('Ctrl Pts',(-74.4408867103144,2.14910845055393,3.80713352255281));
#54261=CARTESIAN_POINT('Ctrl Pts',(-74.2420131786171,-2.04106107797122,
3.86613533994589));
#54262=CARTESIAN_POINT('Ctrl Pts',(-74.0431396469196,-4.35589949720169,
0.372924068767042));
#54263=CARTESIAN_POINT('Ctrl Pts',(-73.8442661152221,-2.66852851455428,
-3.46293060250971));
#54264=CARTESIAN_POINT('Ctrl Pts',(-73.6453925835248,1.47069194648194,-4.11703752586014));
#54265=CARTESIAN_POINT('Ctrl Pts',(-73.4465190518272,4.25863762735916,-0.988401917050126));
#54266=CARTESIAN_POINT('Ctrl Pts',(-73.2476455201298,3.13373831207497,3.04837940260415));
#54267=CARTESIAN_POINT('Ctrl Pts',(-73.0487719884323,-0.870446198762599,
4.28430346799187));
#54268=CARTESIAN_POINT('Ctrl Pts',(-72.849898456735,-4.07486295491378,1.58380071014596));
#54269=CARTESIAN_POINT('Ctrl Pts',(-72.6510249250373,-3.53528726128592,
-2.57190139215663));
#54270=CARTESIAN_POINT('Ctrl Pts',(-72.4521513933401,0.252517626919826,
-4.36453521453115));
#54271=CARTESIAN_POINT('Ctrl Pts',(-72.2532778616424,3.80830880102412,-2.147025120214));
#54272=CARTESIAN_POINT('Ctrl Pts',(-72.0544043299452,3.86501802925143,2.04317606298353));
#54273=CARTESIAN_POINT('Ctrl Pts',(-71.8555307982476,0.370540756267099,
4.35610288431443));
#54274=CARTESIAN_POINT('Ctrl Pts',(-71.6566572665502,-3.46439012439663,
2.66663343127074));
#54275=CARTESIAN_POINT('Ctrl Pts',(-71.4577837348527,-4.11623224542755,
-1.47294429374982));
#54276=CARTESIAN_POINT('Ctrl Pts',(-71.2589102031553,-0.986071727612851,
-4.25917777731692));
#54277=CARTESIAN_POINT('Ctrl Pts',(-71.0600366714578,3.05009351820653,-3.13206997383232));
#54278=CARTESIAN_POINT('Ctrl Pts',(-70.8611631397603,4.28382657682442,0.872790152602706));
#54279=CARTESIAN_POINT('Ctrl Pts',(-70.6622896080629,1.58157098079249,4.07572889475033));
#54280=CARTESIAN_POINT('Ctrl Pts',(-70.4634160763654,-2.57383527978793,
3.53387955981901));
#54281=CARTESIAN_POINT('Ctrl Pts',(-70.264542544668,-4.36439640051381,-0.254905570691984));
#54282=CARTESIAN_POINT('Ctrl Pts',(-70.0656690129705,-2.14494114715219,
-3.80948293946055));
#54283=CARTESIAN_POINT('Ctrl Pts',(-69.8667954812732,2.04529043636163,-3.86389956154597));
#54284=CARTESIAN_POINT('Ctrl Pts',(-69.6679219495755,4.35630496740768,-0.368157332844027));
#54285=CARTESIAN_POINT('Ctrl Pts',(-69.4690484178782,2.66473754971807,3.4658486092024));
#54286=CARTESIAN_POINT('Ctrl Pts',(-69.2701748861807,-1.47519620008504,
4.11542573278177));
#54287=CARTESIAN_POINT('Ctrl Pts',(-69.0713013544833,-4.25971665227008,
0.983741242990482));
#54288=CARTESIAN_POINT('Ctrl Pts',(-68.8724278227858,-3.13040069799007,
-3.05180672074932));
#54289=CARTESIAN_POINT('Ctrl Pts',(-68.6735542910884,0.875133845169071,
-4.28334840327369));
#54290=CARTESIAN_POINT('Ctrl Pts',(-68.4746807593909,4.07659361449859,-1.5793407779884));
#54291=CARTESIAN_POINT('Ctrl Pts',(-68.2758072276934,3.53247080046894,2.57576839692974));
#54292=CARTESIAN_POINT('Ctrl Pts',(-68.076933695996,-0.257293438156953,
4.3642562799942));
#54293=CARTESIAN_POINT('Ctrl Pts',(-67.8780601642985,-3.81065593751065,
2.14285653199235));
#54294=CARTESIAN_POINT('Ctrl Pts',(-67.6791866326011,-3.86277993716433,
-2.0474041974726));
#54295=CARTESIAN_POINT('Ctrl Pts',(-67.4803131009036,-0.365773799211309,
-4.35650574642089));
#54296=CARTESIAN_POINT('Ctrl Pts',(-67.2814395692062,3.46730605649033,-2.6628408704639));
#54297=CARTESIAN_POINT('Ctrl Pts',(-67.0825660375088,4.11461798816427,1.47744766481337));
#54298=CARTESIAN_POINT('Ctrl Pts',(-66.8836925058112,0.981410463880688,
4.2602542520574));
#54299=CARTESIAN_POINT('Ctrl Pts',(-66.6848189741139,-3.0535190097197,3.12873048504791));
#54300=CARTESIAN_POINT('Ctrl Pts',(-66.4859454424164,-4.28286894748279,
-0.877477275760104));
#54301=CARTESIAN_POINT('Ctrl Pts',(-66.2870719107189,-1.57711010240136,
-4.07745711389967));
#54302=CARTESIAN_POINT('Ctrl Pts',(-66.0881983790215,2.57770074300329,-3.53106098365743));
#54303=CARTESIAN_POINT('Ctrl Pts',(-65.889324847324,4.36411485301436,0.259681228599884));
#54304=CARTESIAN_POINT('Ctrl Pts',(-65.6904513156265,2.1407712753585,3.81182779482331));
#54305=CARTESIAN_POINT('Ctrl Pts',(-65.4915777839291,-2.04951734568369,
3.86165915644162));
#54306=CARTESIAN_POINT('Ctrl Pts',(-65.2927042522317,-4.35670522129393,
0.363390156082553));
#54307=CARTESIAN_POINT('Ctrl Pts',(-65.0938307205342,-2.66094339407605,
-3.46876246582416));
#54308=CARTESIAN_POINT('Ctrl Pts',(-64.8949571888368,1.47969868726097,-4.11380901181689));
#54309=CARTESIAN_POINT('Ctrl Pts',(-64.6960836571392,4.26079057651791,-0.97907939098104));
#54310=CARTESIAN_POINT('Ctrl Pts',(-64.4972101254419,3.12705933550577,3.05523038460505));
#54311=CARTESIAN_POINT('Ctrl Pts',(-64.2983365937443,-0.87982044367422,
4.28238820959525));
#54312=CARTESIAN_POINT('Ctrl Pts',(-64.0994630620469,-4.07831939269513,
1.57487895469916));
#54313=CARTESIAN_POINT('Ctrl Pts',(-63.9005895303495,-3.52965010980649,
-2.57963231743028));
#54314=CARTESIAN_POINT('Ctrl Pts',(-63.7017159986519,0.26206894130613,-4.36397211961652));
#54315=CARTESIAN_POINT('Ctrl Pts',(-63.5028424669547,3.81299851104771,-2.13868537787484));
#54316=CARTESIAN_POINT('Ctrl Pts',(-63.303968935257,3.86053721971338,2.05162988036224));
#54317=CARTESIAN_POINT('Ctrl Pts',(-63.1050954035597,0.361006404171295,
4.35690339196714));
#54318=CARTESIAN_POINT('Ctrl Pts',(-62.9062218718622,-3.47021783676795,
2.65904512112248));
#54319=CARTESIAN_POINT('Ctrl Pts',(-62.7073483401648,-4.11299880398172,
-1.48194926675396));
#54320=CARTESIAN_POINT('Ctrl Pts',(-62.5084748084672,-0.976748024989449,
-4.26132562549107));
#54321=CARTESIAN_POINT('Ctrl Pts',(-62.3096012767699,3.05694084489302,-3.12538724986396));
#54322=CARTESIAN_POINT('Ctrl Pts',(-62.1107277450723,4.28190618975503,0.882163348210001));
#54323=CARTESIAN_POINT('Ctrl Pts',(-61.911854213375,1.57264733554965,4.07918045062685));
#54324=CARTESIAN_POINT('Ctrl Pts',(-61.7129806816774,-2.58156311963242,
3.52823817933844));
#54325=CARTESIAN_POINT('Ctrl Pts',(-61.5141071499801,-4.36382807984344,
-0.264456575560786));
#54326=CARTESIAN_POINT('Ctrl Pts',(-61.3152336182825,-2.13659884016589,
-3.8141680858333));
#54327=CARTESIAN_POINT('Ctrl Pts',(-61.1163600865851,2.05374180087587,-3.85941412731554));
#54328=CARTESIAN_POINT('Ctrl Pts',(-60.9174865548877,4.35710025838121,-0.358622544191085));
#54329=CARTESIAN_POINT('Ctrl Pts',(-60.7186130231903,2.65714605217142,3.47167216888599));
#54330=CARTESIAN_POINT('Ctrl Pts',(-60.5197394914927,-1.48419940261849,
4.11218736490133));
#54331=CARTESIAN_POINT('Ctrl Pts',(-60.3208659597953,-4.26185939881663,
0.974416366603987));
#54332=CARTESIAN_POINT('Ctrl Pts',(-60.1219924280979,-3.1237142286232,-3.05865039007152));
#54333=CARTESIAN_POINT('Ctrl Pts',(-59.9231188964004,0.884505988666006,
-4.28142288810644));
#54334=CARTESIAN_POINT('Ctrl Pts',(-59.724245364703,4.08004028743699,-1.57041524562096));
#54335=CARTESIAN_POINT('Ctrl Pts',(-59.5253718330054,3.52682519267604,2.58349314903161));
#54336=CARTESIAN_POINT('Ctrl Pts',(-59.3264983013081,-0.266844130649094,
4.3636827337383));
#54337=CARTESIAN_POINT('Ctrl Pts',(-59.1276247696105,-3.81533651883011,
2.13451166285616));
#54338=CARTESIAN_POINT('Ctrl Pts',(-58.9287512379131,-3.85828987958418,
-2.05585310659239));
#54339=CARTESIAN_POINT('Ctrl Pts',(-58.7298777062157,-0.356238576855684,
-4.35729582047709));
#54340=CARTESIAN_POINT('Ctrl Pts',(-58.5310041745182,3.47312546174274,-2.65524618779161));
#54341=CARTESIAN_POINT('Ctrl Pts',(-58.3321306428208,4.11137469481877,1.48644909418102));
#54342=CARTESIAN_POINT('Ctrl Pts',(-58.1332571111233,0.972084416522393,
4.26239189633496));
#54343=CARTESIAN_POINT('Ctrl Pts',(-57.9343835794259,-3.06035901962902,
3.12204027228397));
#54344=CARTESIAN_POINT('Ctrl Pts',(-57.7355100477284,-4.28093830479405,
-0.886848364341211));
#54345=CARTESIAN_POINT('Ctrl Pts',(-57.5366365160309,-1.5681826855811,-4.08089890286826));
#54346=CARTESIAN_POINT('Ctrl Pts',(-57.3377629843335,2.58542240505028,-3.52541115024215));
#54347=CARTESIAN_POINT('Ctrl Pts',(-57.138889452636,4.3635360813445,0.269231605856388));
#54348=CARTESIAN_POINT('Ctrl Pts',(-56.9400159209386,2.1324238465706,3.81650380968817));
#54349=CARTESIAN_POINT('Ctrl Pts',(-56.7411423892411,-2.05796379687972,
3.85716447685603));
#54350=CARTESIAN_POINT('Ctrl Pts',(-56.5422688575437,-4.35749007819642,
0.353854502878531));
#54351=CARTESIAN_POINT('Ctrl Pts',(-56.3433953258462,-2.65334552855137,
-3.47457771490351));
#54352=CARTESIAN_POINT('Ctrl Pts',(-56.1445217941488,1.48869834076828,-4.11056079397708));
#54353=CARTESIAN_POINT('Ctrl Pts',(-55.9456482624513,4.26292311788657,-0.969752175442759));
#54354=CARTESIAN_POINT('Ctrl Pts',(-55.7467747307538,3.12036538134755,3.0620667330539));
#54355=CARTESIAN_POINT('Ctrl Pts',(-55.5479011990564,-0.889190474534251,
4.28045243996301));
#54356=CARTESIAN_POINT('Ctrl Pts',(-55.349027667359,-4.08175629666357,1.56594965609849));
#54357=CARTESIAN_POINT('Ctrl Pts',(-55.1501541356615,-3.52399605246015,
-2.58735088711071));
#54358=CARTESIAN_POINT('Ctrl Pts',(-54.9512806039641,0.271619000467934,
-4.36338812270604));
#54359=CARTESIAN_POINT('Ctrl Pts',(-54.7524070722666,3.8176699580583,-2.13033539193406));
#54360=CARTESIAN_POINT('Ctrl Pts',(-54.5535335405692,3.85603791946774,2.06007387110622));
#54361=CARTESIAN_POINT('Ctrl Pts',(-54.3546600088717,0.351470322973323,
4.35768303148091));
#54362=CARTESIAN_POINT('Ctrl Pts',(-54.1557864771742,-3.47602892793337,
2.65144407501989));
#54363=CARTESIAN_POINT('Ctrl Pts',(-53.9569129454769,-4.10974566262001,
-1.49094714170681));
#54364=CARTESIAN_POINT('Ctrl Pts',(-53.7580394137793,-0.967419644063333,
-4.26345306331242));
#54365=CARTESIAN_POINT('Ctrl Pts',(-53.5591658820819,3.06377352983496,-3.11868955631533));
#54366=CARTESIAN_POINT('Ctrl Pts',(-53.3602923503844,4.2799652937587,0.891532318543936));
#54367=CARTESIAN_POINT('Ctrl Pts',(-53.161418818687,1.56371615784177,4.08261246856616));
#54368=CARTESIAN_POINT('Ctrl Pts',(-52.9625452869895,-2.58927859463567,
3.52257989975376));
#54369=CARTESIAN_POINT('Ctrl Pts',(-52.7636717552921,-4.36323885786721,
-0.274006313769111));
#54370=CARTESIAN_POINT('Ctrl Pts',(-52.5647982235946,-2.12824629957168,
-3.81883496359127));
#54371=CARTESIAN_POINT('Ctrl Pts',(-52.3659246918972,2.06218332864007,-3.85491020775668));
#54372=CARTESIAN_POINT('Ctrl Pts',(-52.1670511601997,4.35787468027285,-0.349086037853842));
#54373=CARTESIAN_POINT('Ctrl Pts',(-51.9681776285022,2.64954182776637,3.47747910039789));
#54374=CARTESIAN_POINT('Ctrl Pts',(-51.7693040968048,-1.49319549632342,
4.10892930099158));
#54375=CARTESIAN_POINT('Ctrl Pts',(-51.5704305651073,-4.26398173245389,
0.965086823082352));
#54376=CARTESIAN_POINT('Ctrl Pts',(-51.3715570334099,-3.117012797689,-3.06547940946115));
#54377=CARTESIAN_POINT('Ctrl Pts',(-51.1726835017125,0.893873895669284,
-4.27947686632704));
#54378=CARTESIAN_POINT('Ctrl Pts',(-50.9738099700149,4.08346741831995,-1.56148219147932));
#54379=CARTESIAN_POINT('Ctrl Pts',(-50.7749364383176,3.52116269254666,2.59120552704822));
#54380=CARTESIAN_POINT('Ctrl Pts',(-50.5760629066201,-0.276393545045298,
4.36308828687261));
#54381=CARTESIAN_POINT('Ctrl Pts',(-50.3771893749227,-3.81999882593834,
2.12615657010893));
#54382=CARTESIAN_POINT('Ctrl Pts',(-50.1783158432251,-3.85378134206042,
-2.06429216884982));
#54383=CARTESIAN_POINT('Ctrl Pts',(-49.9794423115277,-0.346701648233845,
-4.35806502451485));
#54384=CARTESIAN_POINT('Ctrl Pts',(-49.7805687798303,3.47892823186297,-2.64763878736025));
#54385=CARTESIAN_POINT('Ctrl Pts',(-49.5816952481328,4.10811170933616,1.49544340394506));
#54386=CARTESIAN_POINT('Ctrl Pts',(-49.3828217164354,0.962753713198245,
4.26450912515266));
#54387=CARTESIAN_POINT('Ctrl Pts',(-49.1839481847379,-3.06718437142193,
3.11533510597052));
#54388=CARTESIAN_POINT('Ctrl Pts',(-48.9850746530405,-4.27898715781424,
-0.896215205209373));
#54389=CARTESIAN_POINT('Ctrl Pts',(-48.786201121343,-1.55924775767987,-4.08432114566889));
#54390=CARTESIAN_POINT('Ctrl Pts',(-48.5873275896455,2.59313168377142,-3.51974443126322));
#54391=CARTESIAN_POINT('Ctrl Pts',(-48.3884540579481,4.36293640976736,0.278780693581792));
#54392=CARTESIAN_POINT('Ctrl Pts',(-48.1895805262506,2.12406620417138,3.82116154475111));
#54393=CARTESIAN_POINT('Ctrl Pts',(-47.9907069945532,-2.06640039110415,
3.8526513227169));
#54394=CARTESIAN_POINT('Ctrl Pts',(-47.7918334628557,-4.35825406414994,
0.344317154827103));
#54395=CARTESIAN_POINT('Ctrl Pts',(-47.5929599311583,-2.64573495437125,
-3.48037632189472));
#54396=CARTESIAN_POINT('Ctrl Pts',(-47.3940863994607,1.49769086389862,-4.10729288789854));
#54397=CARTESIAN_POINT('Ctrl Pts',(-47.1952128677634,4.26503524125097,-0.960420315109474));
#54398=CARTESIAN_POINT('Ctrl Pts',(-46.9963393360659,3.11365648166209,3.06888841520693));
#54399=CARTESIAN_POINT('Ctrl Pts',(-46.7974658043685,-0.898556246463373,
4.2784961683668));
#54400=CARTESIAN_POINT('Ctrl Pts',(-46.5985922726709,-4.08517365035739,
1.5570128571124));
#54401=CARTESIAN_POINT('Ctrl Pts',(-46.3997187409736,-3.51832511632802,
-2.59505706422866));
#54402=CARTESIAN_POINT('Ctrl Pts',(-46.2008452092761,0.281167758664008,
-4.36278322659693));
#54403=CARTESIAN_POINT('Ctrl Pts',(-46.0019716775787,3.8223231196815,-2.12197520238479));
#54404=CARTESIAN_POINT('Ctrl Pts',(-45.8030981458812,3.8515201500644,2.06850799477198));
#54405=CARTESIAN_POINT('Ctrl Pts',(-45.6042246141837,0.341932558347505,
4.35844179912147));
#54406=CARTESIAN_POINT('Ctrl Pts',(-45.4053510824862,-3.48182337005976,
2.64383032936931));
#54407=CARTESIAN_POINT('Ctrl Pts',(-45.2064775507889,-4.10647283692384,
-1.49993787551162));
#54408=CARTESIAN_POINT('Ctrl Pts',(-45.0076040190913,-0.95808662951426,
-4.26556008059126));
#54409=CARTESIAN_POINT('Ctrl Pts',(-44.808730487394,3.07059154030602,-3.11197692526612));
#54410=CARTESIAN_POINT('Ctrl Pts',(-44.6098569556964,4.27800389813174,0.900897018730402));
#54411=CARTESIAN_POINT('Ctrl Pts',(-44.410983423999,1.55477749044593,4.08602493213029));
#54412=CARTESIAN_POINT('Ctrl Pts',(-44.2121098923016,-2.59698166784357,
3.51690474816593));
#54413=CARTESIAN_POINT('Ctrl Pts',(-44.0132363606041,-4.36262873740718,
-0.283554739577348));
#54414=CARTESIAN_POINT('Ctrl Pts',(-43.8143628289067,-2.11988356537511,
-3.82348355038179));
#54415=CARTESIAN_POINT('Ctrl Pts',(-43.6154892972092,2.07061497922229,-3.85038782444153));
#54416=CARTESIAN_POINT('Ctrl Pts',(-43.4166157655118,4.35862822937335,-0.339547859508846));
#54417=CARTESIAN_POINT('Ctrl Pts',(-43.2177422338143,2.64192491292454,3.48326937592491));
#54418=CARTESIAN_POINT('Ctrl Pts',(-43.0188687021169,-1.50218443811134,
4.10565155665745));
#54419=CARTESIAN_POINT('Ctrl Pts',(-42.8199951704193,-4.26608364301641,
0.955752657111389));
#54420=CARTESIAN_POINT('Ctrl Pts',(-42.621121638722,-3.11029643728546,-3.07229374620934));
#54421=CARTESIAN_POINT('Ctrl Pts',(-42.4222481070244,0.903237521309745,
-4.27751034725644));
#54422=CARTESIAN_POINT('Ctrl Pts',(-42.2233745753271,4.08687499073273,-1.55254165834964));
#54423=CARTESIAN_POINT('Ctrl Pts',(-42.0245010436295,3.51548332720214,2.59890549404002));
#54424=CARTESIAN_POINT('Ctrl Pts',(-41.8256275119321,-0.285941635607189,
4.36247294224429));
#54425=CARTESIAN_POINT('Ctrl Pts',(-41.6267539802346,-3.82464283650449,
2.11779129376864));
#54426=CARTESIAN_POINT('Ctrl Pts',(-41.4278804485372,-3.84925434618739,
-2.07272134382439));
#54427=CARTESIAN_POINT('Ctrl Pts',(-41.2290069168397,-0.337163059024936,
-4.35881335484976));
#54428=CARTESIAN_POINT('Ctrl Pts',(-41.0301333851424,3.48471433905729,-2.64001870560726));
#54429=CARTESIAN_POINT('Ctrl Pts',(-40.8312598534448,4.10482904734529,1.50443055102521));
#54430=CARTESIAN_POINT('Ctrl Pts',(-40.6323863217474,0.95341839859954,4.26660592836971));
#54431=CARTESIAN_POINT('Ctrl Pts',(-40.4335127900499,-3.07399503240732,
3.10861501822319));
#54432=CARTESIAN_POINT('Ctrl Pts',(-40.2346392583525,-4.27701551588864,
-0.905577753500761));
#54433=CARTESIAN_POINT('Ctrl Pts',(-40.035765726655,-1.55030536149281,-4.08772382591024));
#54434=CARTESIAN_POINT('Ctrl Pts',(-39.8368921949575,2.600828542242,-3.51406085386219));
#54435=CARTESIAN_POINT('Ctrl Pts',(-39.6380186632601,4.36231584115501,0.288328446039067));
#54436=CARTESIAN_POINT('Ctrl Pts',(-39.4391451315626,2.11569838819149,3.82580097770278));
#54437=CARTESIAN_POINT('Ctrl Pts',(-39.2402715998652,-2.07482708794791,
3.84811971564105));
#54438=CARTESIAN_POINT('Ctrl Pts',(-39.0413980681677,-4.3589971754952,0.334778157609627));
#54439=CARTESIAN_POINT('Ctrl Pts',(-38.8425245364703,-2.63811170798816,
-3.48615825902432));
#54440=CARTESIAN_POINT('Ctrl Pts',(-38.6436510047728,1.50667621358083,-4.10400530923358));
#54441=CARTESIAN_POINT('Ctrl Pts',(-38.4447774730754,4.2671269364948,-0.951083854677481));
#54442=CARTESIAN_POINT('Ctrl Pts',(-38.2459039413779,3.10693266858264,3.07569539839068));
#54443=CARTESIAN_POINT('Ctrl Pts',(-38.0470304096805,-0.907917714602892,
4.27651940417648));
#54444=CARTESIAN_POINT('Ctrl Pts',(-37.848156877983,-4.08857143740867,1.54806860054497));
#54445=CARTESIAN_POINT('Ctrl Pts',(-37.6492833462856,-3.51263732857192,
-2.60275081187394));
#54446=CARTESIAN_POINT('Ctrl Pts',(-37.4504098145881,0.290715170158508,
-4.36215743418637));
#54447=CARTESIAN_POINT('Ctrl Pts',(-37.2515362828907,3.82695797362988,-2.11360484927016));
#54448=CARTESIAN_POINT('Ctrl Pts',(-37.0526627511932,3.84698393314227,2.07693221096233));
#54449=CARTESIAN_POINT('Ctrl Pts',(-36.8537892194957,0.332393155976931,
4.3591796912547));
#54450=CARTESIAN_POINT('Ctrl Pts',(-36.6549156877984,-3.48760113539375,
2.63620392063813));
#54451=CARTESIAN_POINT('Ctrl Pts',(-36.4560421561008,-4.10318034256891,
-1.50892142510596));
#54452=CARTESIAN_POINT('Ctrl Pts',(-36.2571686244034,-0.948749026044068,
-4.26764666723571));
#54453=CARTESIAN_POINT('Ctrl Pts',(-36.0582950927059,3.07739484365031,-3.10524938886745));
#54454=CARTESIAN_POINT('Ctrl Pts',(-35.8594215610085,4.27602201226846,0.910257403915468));
#54455=CARTESIAN_POINT('Ctrl Pts',(-35.660548029311,1.54583137617576,4.08941782497438));
#54456=CARTESIAN_POINT('Ctrl Pts',(-35.4616744976137,-2.60467230236045,
3.51121275175743));
#54457=CARTESIAN_POINT('Ctrl Pts',(-35.2628009659161,-4.36199772138568,
-0.293101807251095));
#54458=CARTESIAN_POINT('Ctrl Pts',(-35.0639274342188,-2.11151067763145,
-3.82811382393941));
#54459=CARTESIAN_POINT('Ctrl Pts',(-34.8650539025212,2.07903671223751,-3.84584699903108));
#54460=CARTESIAN_POINT('Ctrl Pts',(-34.6661803708238,4.35936090207359,-0.330008054840811));
#54461=CARTESIAN_POINT('Ctrl Pts',(-34.4673068391263,2.63429534412827,3.48904296773367));
#54462=CARTESIAN_POINT('Ctrl Pts',(-34.2684333074289,-1.51116618492849,
4.10235414759823));
#54463=CARTESIAN_POINT('Ctrl Pts',(-34.0695597757314,-4.26816512043681,
0.946413913398328));
#54464=CARTESIAN_POINT('Ctrl Pts',(-33.8706862440339,-3.10356517958156,
-3.0790933676776));
#54465=CARTESIAN_POINT('Ctrl Pts',(-33.6718127123365,0.912596820738402,
-4.27552334031354));
#54466=CARTESIAN_POINT('Ctrl Pts',(-33.472939180639,4.09026298835399,-1.5435936890546));
#54467=CARTESIAN_POINT('Ctrl Pts',(-33.2740656489416,3.5097871238451,2.60659301312629));
#54468=CARTESIAN_POINT('Ctrl Pts',(-33.0751921172442,-0.295488356602298,
4.3618367028008));
#54469=CARTESIAN_POINT('Ctrl Pts',(-32.8763185855467,-3.82926852828537,
2.10941587390226));
#54470=CARTESIAN_POINT('Ctrl Pts',(-32.6774450538493,-3.8447089136478,-2.08114059114343));
#54471=CARTESIAN_POINT('Ctrl Pts',(-32.4785715221517,-0.327622854915255,
-4.35954080789764));
#54472=CARTESIAN_POINT('Ctrl Pts',(-32.2796979904543,3.49048375561245,-2.63238597902992));
#54473=CARTESIAN_POINT('Ctrl Pts',(-32.0808244587569,4.10152672456885,1.51341049237635));
#54474=CARTESIAN_POINT('Ctrl Pts',(-31.8819509270594,0.944078517439236,
4.26868229594298));
#54475=CARTESIAN_POINT('Ctrl Pts',(-31.683077395362,-3.08079096996409,3.1018800412291));
#54476=CARTESIAN_POINT('Ctrl Pts',(-31.4842038636645,-4.27502338846088,
-0.914935964371331));
#54477=CARTESIAN_POINT('Ctrl Pts',(-31.2853303319671,-1.54135553985154,
-4.09110692729445));
#54478=CARTESIAN_POINT('Ctrl Pts',(-31.0864568002696,2.60851294359646,-3.50836044526178));
#54479=CARTESIAN_POINT('Ctrl Pts',(-30.8875832685722,4.36167437847994,0.297874817497696));
#54480=CARTESIAN_POINT('Ctrl Pts',(-30.6887097368746,2.10732043870968,3.8304220863221));
#54481=CARTESIAN_POINT('Ctrl Pts',(-30.4898362051773,-2.0832438470503,3.84356967733313));
#54482=CARTESIAN_POINT('Ctrl Pts',(-30.2909626734798,-4.35971940867296,
0.325237556914354));
#54483=CARTESIAN_POINT('Ctrl Pts',(-30.0920891417824,-2.63047582591478,
-3.49192349859863));
#54484=CARTESIAN_POINT('Ctrl Pts',(-29.8932156100849,1.51565434677771,-4.1006980737286));
#54485=CARTESIAN_POINT('Ctrl Pts',(-29.6943420783874,4.26919819359942,-0.941742838865859));
#54486=CARTESIAN_POINT('Ctrl Pts',(-29.49546854669,3.10019397431441,3.08248765000159));
#54487=CARTESIAN_POINT('Ctrl Pts',(-29.2965950149925,-0.917274834113944,
4.27452215686021));
#54488=CARTESIAN_POINT('Ctrl Pts',(-29.0977214832951,-4.09194964154314,
1.53911692923657));
#54489=CARTESIAN_POINT('Ctrl Pts',(-28.8988479515976,-3.50693271643453,
-2.61043209319622));
#54490=CARTESIAN_POINT('Ctrl Pts',(-28.6999744199002,0.300261189222895,
-4.36151074847169));
#54491=CARTESIAN_POINT('Ctrl Pts',(-28.5011008882027,3.83157449770426,-2.10522437268097));
#54492=CARTESIAN_POINT('Ctrl Pts',(-28.3022273565052,3.84242929042812,2.0853464793284));
#54493=CARTESIAN_POINT('Ctrl Pts',(-28.1033538248078,0.322852161552108,
4.35989670434615));
#54494=CARTESIAN_POINT('Ctrl Pts',(-27.9044802931104,-3.4933621962615,2.6285648853545));
#54495=CARTESIAN_POINT('Ctrl Pts',(-27.7056067614129,-4.09986819532533,
-1.5178977474611));
#54496=CARTESIAN_POINT('Ctrl Pts',(-27.5067332297155,-0.939406878377322,
-4.26971281325161));
#54497=CARTESIAN_POINT('Ctrl Pts',(-27.307859698018,3.08418340728215,-3.09850697934234));
#54498=CARTESIAN_POINT('Ctrl Pts',(-27.1089861663205,4.27401964566158,0.919613429266095));
#54499=CARTESIAN_POINT('Ctrl Pts',(-26.9101126346231,1.53687785787983,4.09279113084779));
#54500=CARTESIAN_POINT('Ctrl Pts',(-26.7112391029256,-2.61235046135107,
3.50550393779077));
#54501=CARTESIAN_POINT('Ctrl Pts',(-26.5123655712282,-4.36134581282504,
-0.302647471063524));
#54502=CARTESIAN_POINT('Ctrl Pts',(-26.3134920395307,-2.10312767644367,
-3.83272576208681));
#54503=CARTESIAN_POINT('Ctrl Pts',(-26.1146185078333,2.08744848734839,-3.84128775327418));
#54504=CARTESIAN_POINT('Ctrl Pts',(-25.9157449761358,4.36007269486416,-0.320466669542563));
#54505=CARTESIAN_POINT('Ctrl Pts',(-25.7168714444384,2.62665315792108,3.49479984817026));
#54506=CARTESIAN_POINT('Ctrl Pts',(-25.5179979127409,-1.52014069375477,
4.09903708960756));
#54507=CARTESIAN_POINT('Ctrl Pts',(-25.3191243810434,-4.27022615474555,
0.937070636672996));
#54508=CARTESIAN_POINT('Ctrl Pts',(-25.120250849346,-3.09681905681786,-3.08587824129815));
#54509=CARTESIAN_POINT('Ctrl Pts',(-24.9213773176485,0.921951749127709,
-4.27351585501541));
#54510=CARTESIAN_POINT('Ctrl Pts',(-24.7225037859511,4.0936313949565,-1.53463832645159));
#54511=CARTESIAN_POINT('Ctrl Pts',(-24.5236302542536,3.5040741097582,2.61426804748663));
#54512=CARTESIAN_POINT('Ctrl Pts',(-24.3247567225562,-0.305033662305041,
4.36117957158933));
#54513=CARTESIAN_POINT('Ctrl Pts',(-24.1258831908588,-3.83387587912521,
2.1010303506255));
#54514=CARTESIAN_POINT('Ctrl Pts',(-23.9270096591612,-3.84014506621302,
-2.08954987048108));
#54515=CARTESIAN_POINT('Ctrl Pts',(-23.7281361274639,-0.318081081599751,
-4.3602473801742));
#54516=CARTESIAN_POINT('Ctrl Pts',(-23.5292625957663,3.49623645389453,-2.6247406441869));
#54517=CARTESIAN_POINT('Ctrl Pts',(-23.3303890640689,4.09820475682409,1.5223831849873));
#54518=CARTESIAN_POINT('Ctrl Pts',(-23.1315155323714,0.934734114452248,
4.27073821792754));
#54519=CARTESIAN_POINT('Ctrl Pts',(-22.932642000674,-3.08757215154224,3.09513020724629));
#54520=CARTESIAN_POINT('Ctrl Pts',(-22.7337684689765,-4.27301078507249,
-0.924289792998811));
#54521=CARTESIAN_POINT('Ctrl Pts',(-22.5348949372791,-1.53239833562235,
-4.09447043361766));
#54522=CARTESIAN_POINT('Ctrl Pts',(-22.3360214055817,2.61618485102899,-3.50264323276489));
#54523=CARTESIAN_POINT('Ctrl Pts',(-22.1371478738842,4.36101202481442,0.307419762233428));
#54524=CARTESIAN_POINT('Ctrl Pts',(-21.9382743421868,2.09893239585401,3.8350248484752));
#54525=CARTESIAN_POINT('Ctrl Pts',(-21.7394008104893,-2.09165062809739,
3.8390012295866));
#54526=CARTESIAN_POINT('Ctrl Pts',(-21.5405272787919,-4.36042076022404,
0.315695398437909));
#54527=CARTESIAN_POINT('Ctrl Pts',(-21.3416537470944,-2.62282734472448,
-3.49767201300425));
#54528=CARTESIAN_POINT('Ctrl Pts',(-21.1427802153969,1.52462522048738,-4.09737119722407));
#54529=CARTESIAN_POINT('Ctrl Pts',(-20.9439066836995,4.2712490026443,-0.932397312414519));
#54530=CARTESIAN_POINT('Ctrl Pts',(-20.745033152002,3.09344043113318,3.08926513750733));
#54531=CARTESIAN_POINT('Ctrl Pts',(-20.5461596203046,-0.926627560179405,
4.27250443598403));
#54532=CARTESIAN_POINT('Ctrl Pts',(-20.3472860886071,-4.09530824658019,
1.5301578860626));
#54533=CARTESIAN_POINT('Ctrl Pts',(-20.1484125569097,-3.50121130723917,
-2.61810087140436));
#54534=CARTESIAN_POINT('Ctrl Pts',(-19.9495390252122,0.309805770134372,
-4.36084317255037));
#54535=CARTESIAN_POINT('Ctrl Pts',(-19.7506654935148,3.83617266979276,-2.09683381275741));
#54536=CARTESIAN_POINT('Ctrl Pts',(-19.5517919618172,3.83785624373743,2.09375075956842));
#54537=CARTESIAN_POINT('Ctrl Pts',(-19.3529184301199,0.313309620771175,
4.36059283496176));
#54538=CARTESIAN_POINT('Ctrl Pts',(-19.1540448984224,-3.49910652506968,
2.62091326010657));
#54539=CARTESIAN_POINT('Ctrl Pts',(-18.9551713667249,-4.09653641105705,
-1.52686679958387));
#54540=CARTESIAN_POINT('Ctrl Pts',(-18.7562978350275,-0.930060231259401,
-4.27175850874285));
#54541=CARTESIAN_POINT('Ctrl Pts',(-18.55742430333,3.09095719868646,-3.09174972898448));
#54542=CARTESIAN_POINT('Ctrl Pts',(-18.3585507716326,4.27199680790173,0.928965049969675));
#54543=CARTESIAN_POINT('Ctrl Pts',(-18.1596772399351,1.52791697844301,4.09614483359332));
#54544=CARTESIAN_POINT('Ctrl Pts',(-17.9608037082377,-2.62001610803916,
3.49977833360957));
#54545=CARTESIAN_POINT('Ctrl Pts',(-17.7619301765402,-4.36067301484774,
-0.31219168529352));
#54546=CARTESIAN_POINT('Ctrl Pts',(-17.5630566448428,-2.09473460196391,
-3.8373193427343));
#54547=CARTESIAN_POINT('Ctrl Pts',(-17.3641831131453,2.09585026426548,-3.83671010900824));
#54548=CARTESIAN_POINT('Ctrl Pts',(-17.1653095814479,4.36076360433587,-0.310923749313768));
#54549=CARTESIAN_POINT('Ctrl Pts',(-16.9664360497504,2.61899839090615,3.5005399896614));
#54550=CARTESIAN_POINT('Ctrl Pts',(-16.7675625180529,-1.52910792160562,
4.09570039857291));
#54551=CARTESIAN_POINT('Ctrl Pts',(-16.5686889863555,-4.27226673607081,
0.927722871686493));
#54552=CARTESIAN_POINT('Ctrl Pts',(-16.369815454658,-3.09005810130619,-3.0926483345734));
#54553=CARTESIAN_POINT('Ctrl Pts',(-16.1709419229606,0.931302261670127,
-4.27148790097734));
#54554=CARTESIAN_POINT('Ctrl Pts',(-15.9720683912631,4.09698019440654,-1.52567561343433));
#54555=CARTESIAN_POINT('Ctrl Pts',(-15.7731948595657,3.49834431230515,2.62193056036003));
#54556=CARTESIAN_POINT('Ctrl Pts',(-15.5743213278682,-0.314577506996647,
4.36050155175749));
#54557=CARTESIAN_POINT('Ctrl Pts',(-15.3754477961708,-3.83846486695655,
2.09263476410191));
#54558=CARTESIAN_POINT('Ctrl Pts',(-15.1765742644733,-3.83556282574215,
-2.09794914156006));
#54559=CARTESIAN_POINT('Ctrl Pts',(-14.9777007327758,-0.308537784779887,
-4.36093306829522));
#54560=CARTESIAN_POINT('Ctrl Pts',(-14.7788272010784,3.50197240635021,-2.61708273769649));
#54561=CARTESIAN_POINT('Ctrl Pts',(-14.579953669381,4.09486316002196,1.53134858588184));
#54562=CARTESIAN_POINT('Ctrl Pts',(-14.3810801376835,0.925385234395442,
4.27277368447599));
#54563=CARTESIAN_POINT('Ctrl Pts',(-14.182206605986,-3.09433854466179,3.08836554860464));
#54564=CARTESIAN_POINT('Ctrl Pts',(-13.9833330742886,-4.2709777153633,-0.933639194580945));
#54565=CARTESIAN_POINT('Ctrl Pts',(-13.7844595425911,-1.5234337917076,-4.0978143287698));
#54566=CARTESIAN_POINT('Ctrl Pts',(-13.5855860108937,2.62384422779387,-3.49690924375519));
#54567=CARTESIAN_POINT('Ctrl Pts',(-13.3867124791962,4.36032878333094,0.316963234529536));
#54568=CARTESIAN_POINT('Ctrl Pts',(-13.1878389474988,2.09053429980003,3.83960924211661));
#54569=CARTESIAN_POINT('Ctrl Pts',(-12.9889654158013,-2.1000473908238,3.83441439428258));
#54570=CARTESIAN_POINT('Ctrl Pts',(-12.7900918841039,-4.36110122678905,
0.30615172788398));
#54571=CARTESIAN_POINT('Ctrl Pts',(-12.5912183524064,-2.61516630105115,
-3.5034037747074));
#54572=CARTESIAN_POINT('Ctrl Pts',(-12.3923448207089,1.53358879174183,-4.09402469565482));
#54573=CARTESIAN_POINT('Ctrl Pts',(-12.1934712890115,4.27327935380661,-0.923047320085955));
#54574=CARTESIAN_POINT('Ctrl Pts',(-11.994597757314,3.08667207138658,3.09602782844563));
#54575=CARTESIAN_POINT('Ctrl Pts',(-11.7957242256166,-0.935975848002548,
4.27046625121234));
#54576=CARTESIAN_POINT('Ctrl Pts',(-11.5968506939192,-4.09864723643339,
1.52119151393392));
#54577=CARTESIAN_POINT('Ctrl Pts',(-11.3979771622217,-3.49547312838928,
-2.6257571097678));
#54578=CARTESIAN_POINT('Ctrl Pts',(-11.1991036305242,0.319348867178025,
-4.36015470961981));
#54579=CARTESIAN_POINT('Ctrl Pts',(-11.0002300988268,3.84075246787181,-2.08843320968709));
#54580=CARTESIAN_POINT('Ctrl Pts',(-10.8013565671293,3.8332648149734,2.10214501142864));
#54581=CARTESIAN_POINT('Ctrl Pts',(-10.6024830354319,0.303765579340042,
4.36126807976715));
#54582=CARTESIAN_POINT('Ctrl Pts',(-10.4036095037344,-3.50483409430456,
2.61324908154353));
#54583=CARTESIAN_POINT('Ctrl Pts',(-10.204735972037,-4.09318500572241,-1.53582853851505));
#54584=CARTESIAN_POINT('Ctrl Pts',(-10.0058624403395,-0.920709129457893,
-4.27378374391132));
#54585=CARTESIAN_POINT('Ctrl Pts',(-9.80698890864207,3.09771618541933,-3.08497767015885));
#54586=CARTESIAN_POINT('Ctrl Pts',(-9.60811537694459,4.26995350867754,0.938312221235545));
#54587=CARTESIAN_POINT('Ctrl Pts',(-9.40924184524716,1.51894878078439,4.09947891714805));
#54588=CARTESIAN_POINT('Ctrl Pts',(-9.21036831354968,-2.62766920570929,
3.49403596663726));
#54589=CARTESIAN_POINT('Ctrl Pts',(-9.01149478185225,-4.35997933067613,
-0.321734404227933));
#54590=CARTESIAN_POINT('Ctrl Pts',(-8.81262125015477,-2.08633149439201,
-3.8418945438801));
#54591=CARTESIAN_POINT('Ctrl Pts',(-8.61374771845735,2.10424200274676,-3.83211408815864));
#54592=CARTESIAN_POINT('Ctrl Pts',(-8.41487418675987,4.36143362717948,-0.30137933986224));
#54593=CARTESIAN_POINT('Ctrl Pts',(-8.21600065506241,2.61133107974759,3.50626336471347));
#54594=CARTESIAN_POINT('Ctrl Pts',(-8.01712712336498,-1.53806782553083,
4.09234409047605));
#54595=CARTESIAN_POINT('Ctrl Pts',(-7.81825359166752,-4.27428685463917,
0.91837066321142));
#54596=CARTESIAN_POINT('Ctrl Pts',(-7.61938005997006,-3.08328234542873,
-3.09940361507732));
#54597=CARTESIAN_POINT('Ctrl Pts',(-7.42050652827261,0.940648313580007,
-4.26943948791234));
#54598=CARTESIAN_POINT('Ctrl Pts',(-7.22163299657514,4.10030937066533,-1.51670559293085));
#54599=CARTESIAN_POINT('Ctrl Pts',(-7.0227594648777,3.49259775892826,2.62958051504615));
#54600=CARTESIAN_POINT('Ctrl Pts',(-6.82388593318022,-0.324119844963001,
4.35980264655192));
#54601=CARTESIAN_POINT('Ctrl Pts',(-6.62501240148279,-3.84303546980398,
2.08422915454508));
#54602=CARTESIAN_POINT('Ctrl Pts',(-6.42613886978531,-3.83096221417432,
-2.10633836415309));
#54603=CARTESIAN_POINT('Ctrl Pts',(-6.22726533808787,-0.29899301018082,
-4.36159786897168));
#54604=CARTESIAN_POINT('Ctrl Pts',(-6.02839180639044,3.5076915855359,-2.60941229624663));
#54605=CARTESIAN_POINT('Ctrl Pts',(-5.82951827469298,4.09150195011159,1.54030665213598));
#54606=CARTESIAN_POINT('Ctrl Pts',(-5.63064474299553,0.91603192215228,4.2747886858071));
#54607=CARTESIAN_POINT('Ctrl Pts',(-5.43177121129806,-3.10109011711434,
3.08158609776497));
#54608=CARTESIAN_POINT('Ctrl Pts',(-5.23289767960062,-4.26892418869336,
-0.942984124452568));
#54609=CARTESIAN_POINT('Ctrl Pts',(-5.03402414790315,-1.51446195175697,
-4.10113859651792));
#54610=CARTESIAN_POINT('Ctrl Pts',(-4.83515061620571,2.63149103855122,-3.49115850610583));
#54611=CARTESIAN_POINT('Ctrl Pts',(-4.63627708450823,4.35962465476036,0.326505189448822));
#54612=CARTESIAN_POINT('Ctrl Pts',(-4.43740355281079,2.0821261955711,3.84417524382889));
#54613=CARTESIAN_POINT('Ctrl Pts',(-4.23853002111335,-2.10843410407346,
3.8298091961466));
#54614=CARTESIAN_POINT('Ctrl Pts',(-4.0396564894159,-4.36176078799866,0.296606585759418));
#54615=CARTESIAN_POINT('Ctrl Pts',(-3.84078295771845,-2.60749276389598,
-3.509118746429));
#54616=CARTESIAN_POINT('Ctrl Pts',(-3.64190942602098,1.54254507861259,-4.09065860360309));
#54617=CARTESIAN_POINT('Ctrl Pts',(-3.44303589432354,4.27528912217474,-0.913692871629554));
#54618=CARTESIAN_POINT('Ctrl Pts',(-3.24416236262607,3.0798891449889,3.10277562427561));
#54619=CARTESIAN_POINT('Ctrl Pts',(-3.04528883092862,-0.945320063486189,
4.26840773721229));
#54620=CARTESIAN_POINT('Ctrl Pts',(-2.84641529923116,-4.10196581966695,
1.51221761995006));
#54621=CARTESIAN_POINT('Ctrl Pts',(-2.6475417675337,-3.48971967156313,-2.63340032628982));
#54622=CARTESIAN_POINT('Ctrl Pts',(-2.44866823583628,0.328893199341695,
-4.35944620384304));
#54623=CARTESIAN_POINT('Ctrl Pts',(-2.24979470413881,3.84530864969658,-2.08002101598113));
#54624=CARTESIAN_POINT('Ctrl Pts',(-2.05092117244137,3.82866488313315,2.11052619675534));
#54625=CARTESIAN_POINT('Ctrl Pts',(-1.85204764074389,0.294201470937102,
4.36192809626536));
#54626=CARTESIAN_POINT('Ctrl Pts',(-1.65317410904645,-3.51050973320713,
2.60556169774132));
#54627=CARTESIAN_POINT('Ctrl Pts',(-1.45430057734899,-4.08988035329247,
-1.54476273894195));
#54628=CARTESIAN_POINT('Ctrl Pts',(-1.25542704565154,-0.911228319106154,
-4.27582661814505));
#54629=CARTESIAN_POINT('Ctrl Pts',(-1.05655351395407,3.10422373424832,-3.07811887241764));
#54630=CARTESIAN_POINT('Ctrl Pts',(-0.857679982256619,4.26833660246525,
0.947518975425125));
#54631=CARTESIAN_POINT('Ctrl Pts',(-0.658806450559178,1.5091288044425,4.1030503614686));
#54632=CARTESIAN_POINT('Ctrl Pts',(-0.459932918861728,-2.63370883009196,
3.48778877601057));
#54633=CARTESIAN_POINT('Ctrl Pts',(-0.261059387164271,-4.36233900073485,
-0.330330886159537));
#54634=CARTESIAN_POINT('Ctrl Pts',(-0.0621858554668183,-2.07169497223652,
-3.84842048673565));
#54635=CARTESIAN_POINT('Ctrl Pts',(0.0703964989981522,0.707860675536127,
-3.83120820981452));
#54636=CARTESIAN_POINT('Ctrl Pts',(0.136687676230641,1.78615774484833,-3.23603222682011));
#54637=CARTESIAN_POINT('Ctrl Pts',(-109.703687676231,2.00907721869499,-2.81633609132873));
#54638=CARTESIAN_POINT('Ctrl Pts',(-109.637396498998,2.94752490419964,-2.14687981738136));
#54639=CARTESIAN_POINT('Ctrl Pts',(-109.504814144533,4.08614741056074,0.19228903229402));
#54640=CARTESIAN_POINT('Ctrl Pts',(-109.305940612836,2.043016874263,3.5485133391066));
#54641=CARTESIAN_POINT('Ctrl Pts',(-109.107067081138,-1.87881404914145,
3.63353969641206));
#54642=CARTESIAN_POINT('Ctrl Pts',(-108.908193549441,-4.07356171499593,
0.385530372585237));
#54643=CARTESIAN_POINT('Ctrl Pts',(-108.709320017743,-2.5259486660199,-3.21956889940024));
#54644=CARTESIAN_POINT('Ctrl Pts',(-108.510446486046,1.34274209597358,-3.86500887175455));
#54645=CARTESIAN_POINT('Ctrl Pts',(-108.311572954348,3.97759639348424,-0.960071453599377));
#54646=CARTESIAN_POINT('Ctrl Pts',(-108.112699422651,2.9578917106467,2.82740558092371));
#54647=CARTESIAN_POINT('Ctrl Pts',(-107.913825890954,-0.779564242600549,
4.01683202078962));
#54648=CARTESIAN_POINT('Ctrl Pts',(-107.714952359256,-3.80073680723715,
1.51570386947904));
#54649=CARTESIAN_POINT('Ctrl Pts',(-107.516078827559,-3.32979420802159,
-2.37811908816307));
#54650=CARTESIAN_POINT('Ctrl Pts',(-107.317205295861,0.200575240540261,
-4.08688799081147));
#54651=CARTESIAN_POINT('Ctrl Pts',(-107.118331764164,3.54665304843382,-2.04063348034382));
#54652=CARTESIAN_POINT('Ctrl Pts',(-106.919458232466,3.63406018195941,1.88056861694301));
#54653=CARTESIAN_POINT('Ctrl Pts',(-106.720584700769,0.382484601897899,
4.07389545316324));
#54654=CARTESIAN_POINT('Ctrl Pts',(-106.521711169071,-3.22051821498825,
2.52412140612187));
#54655=CARTESIAN_POINT('Ctrl Pts',(-106.322837637374,-3.86450249557726,
-1.34482196121329));
#54656=CARTESIAN_POINT('Ctrl Pts',(-106.123964105676,-0.957773835952048,
-3.9781394133409));
#54657=CARTESIAN_POINT('Ctrl Pts',(-105.925090573979,2.82895933118871,-2.95633459405304));
#54658=CARTESIAN_POINT('Ctrl Pts',(-105.726217042281,4.01643888773492,0.78175672683345));
#54659=CARTESIAN_POINT('Ctrl Pts',(-105.527343510584,1.5136061306901,3.80156825262383));
#54660=CARTESIAN_POINT('Ctrl Pts',(-105.328469978887,-2.37993103823623,
3.32849112014495));
#54661=CARTESIAN_POINT('Ctrl Pts',(-105.129596447189,-4.08678268726703,
-0.20281051848524));
#54662=CARTESIAN_POINT('Ctrl Pts',(-104.930722915492,-2.03869000947797,
-3.54776942006687));
#54663=CARTESIAN_POINT('Ctrl Pts',(-104.731849383794,1.88255523369223,-3.63303050255371));
#54664=CARTESIAN_POINT('Ctrl Pts',(-104.532975852097,4.07410486344261,-0.380255695137597));
#54665=CARTESIAN_POINT('Ctrl Pts',(-104.334102320399,2.52235857904578,3.22189882332731));
#54666=CARTESIAN_POINT('Ctrl Pts',(-104.135228788702,-1.34693594667287,
3.86376608876015));
#54667=CARTESIAN_POINT('Ctrl Pts',(-103.936355257004,-3.9786629590652,0.955597137798683));
#54668=CARTESIAN_POINT('Ctrl Pts',(-103.737481725307,-2.95478627533421,
-2.83057642511528));
#54669=CARTESIAN_POINT('Ctrl Pts',(-103.538608193609,0.783954105126475,
-4.01601055687818));
#54670=CARTESIAN_POINT('Ctrl Pts',(-103.339734661912,3.80239584414084,-1.51152594291659));
#54671=CARTESIAN_POINT('Ctrl Pts',(-103.140861130215,3.3271884741954,2.38175181091827));
#54672=CARTESIAN_POINT('Ctrl Pts',(-102.941987598517,-0.205046497461266,
4.08667111052397));
#54673=CARTESIAN_POINT('Ctrl Pts',(-102.74311406682,-3.54888432623646,2.03674860271566));
#54674=CARTESIAN_POINT('Ctrl Pts',(-102.544240535122,-3.63199994923757,
-1.88454270325992));
#54675=CARTESIAN_POINT('Ctrl Pts',(-102.345367003425,-0.37802656139399,
-4.07431230400465));
#54676=CARTESIAN_POINT('Ctrl Pts',(-102.146493471727,3.2232784072503,-2.520595394154));
#54677=CARTESIAN_POINT('Ctrl Pts',(-101.94761994003,3.8630285570437,1.34904973931353));
#54678=CARTESIAN_POINT('Ctrl Pts',(-101.748746408332,0.953420136774898,
3.97918520233359));
#54679=CARTESIAN_POINT('Ctrl Pts',(-101.549872876635,-2.83219266279414,
2.95323713109742));
#54680=CARTESIAN_POINT('Ctrl Pts',(-101.350999344938,-4.01558102852441,
-0.786151279991661));
#54681=CARTESIAN_POINT('Ctrl Pts',(-101.15212581324,-1.50944530016411,-3.80322228084165));
#54682=CARTESIAN_POINT('Ctrl Pts',(-100.953252281543,2.38357186928961,-3.32588484100231));
#54683=CARTESIAN_POINT('Ctrl Pts',(-100.754378749845,4.0865583111173,0.20728241969803));
#54684=CARTESIAN_POINT('Ctrl Pts',(-100.555505218148,2.03480658587235,3.54999816757252));
#54685=CARTESIAN_POINT('Ctrl Pts',(-100.35663168645,-1.88652960848464,3.63096830996754));
#54686=CARTESIAN_POINT('Ctrl Pts',(-100.157758154753,-4.07451852500647,
0.375797313796782));
#54687=CARTESIAN_POINT('Ctrl Pts',(-99.9588846230556,-2.51883145465525,
-3.22465702590479));
#54688=CARTESIAN_POINT('Ctrl Pts',(-99.7600110913579,1.35116312808074,-3.86228986910522));
#54689=CARTESIAN_POINT('Ctrl Pts',(-99.5611375596606,3.97970625442996,-0.951242850237956));
#54690=CARTESIAN_POINT('Ctrl Pts',(-99.362264027963,2.95168710278726,2.8338080525888));
#54691=CARTESIAN_POINT('Ctrl Pts',(-99.1633904962657,-0.788348219514519,
4.01515029811662));
#54692=CARTESIAN_POINT('Ctrl Pts',(-98.9645169645681,-3.80404757903259,
1.50736420553696));
#54693=CARTESIAN_POINT('Ctrl Pts',(-98.7656434328706,-3.32458021218899,
-2.38539121411965));
#54694=CARTESIAN_POINT('Ctrl Pts',(-98.5667699011732,0.209518279883212,
-4.08644428838477));
#54695=CARTESIAN_POINT('Ctrl Pts',(-98.3678963694758,3.55111094620056,-2.03286395989802));
#54696=CARTESIAN_POINT('Ctrl Pts',(-98.1690228377782,3.62993558375018,1.88851594896682));
#54697=CARTESIAN_POINT('Ctrl Pts',(-97.970149306081,0.373567953702973,4.07472352628297));
#54698=CARTESIAN_POINT('Ctrl Pts',(-97.7712757743833,-3.22603467924333,
2.51706676113231));
#54699=CARTESIAN_POINT('Ctrl Pts',(-97.5724022426861,-3.86155002497238,
-1.35327611237084));
#54700=CARTESIAN_POINT('Ctrl Pts',(-97.3735287109885,-0.949065278942077,
-3.98022611518296));
#54701=CARTESIAN_POINT('Ctrl Pts',(-97.1746551792911,2.83542259406991,-2.95013619087587));
#54702=CARTESIAN_POINT('Ctrl Pts',(-96.9757816475935,4.01471836575504,0.790544923041662));
#54703=CARTESIAN_POINT('Ctrl Pts',(-96.7769081158962,1.50528265967335,3.80487173846432));
#54704=CARTESIAN_POINT('Ctrl Pts',(-96.5780345841988,-2.3872098448718,3.3232745881472));
#54705=CARTESIAN_POINT('Ctrl Pts',(-96.3791610525012,-4.08632904235626,
-0.211754077348115));
#54706=CARTESIAN_POINT('Ctrl Pts',(-96.1802875208037,-2.03092072537648,
-3.55222266178712));
#54707=CARTESIAN_POINT('Ctrl Pts',(-95.9814139891064,1.89050172411301,-3.62890177089481));
#54708=CARTESIAN_POINT('Ctrl Pts',(-95.7825404574088,4.07492730777215,-0.371338481779884));
#54709=CARTESIAN_POINT('Ctrl Pts',(-95.5836669257115,2.51530131411378,3.22741136685351));
#54710=CARTESIAN_POINT('Ctrl Pts',(-95.3847933940139,-1.35538869155151,
3.86080902486668));
#54711=CARTESIAN_POINT('Ctrl Pts',(-95.1859198623165,-3.98074478443685,
0.946887423539108));
#54712=CARTESIAN_POINT('Ctrl Pts',(-94.9870463306191,-2.94858439582757,
-2.83703628675417));
#54713=CARTESIAN_POINT('Ctrl Pts',(-94.7881727989216,0.792741389915535,
-4.01428523156895));
#54714=CARTESIAN_POINT('Ctrl Pts',(-94.5892992672241,3.8056947588901,-1.50320066319643));
#54715=CARTESIAN_POINT('Ctrl Pts',(-94.3904257355267,3.32196796926779,2.38902776100164));
#54716=CARTESIAN_POINT('Ctrl Pts',(-94.1915522038292,-0.213989811423434,
4.08621257306625));
#54717=CARTESIAN_POINT('Ctrl Pts',(-93.9926786721318,-3.55333331399942,
2.02897688288942));
#54718=CARTESIAN_POINT('Ctrl Pts',(-93.7938051404342,-3.62786687171092,
-1.89248693332876));
#54719=CARTESIAN_POINT('Ctrl Pts',(-93.594931608737,-0.369108898694929,
-4.075129869413));
#54720=CARTESIAN_POINT('Ctrl Pts',(-93.3960580770394,3.22878708832316,-2.5135351141282));
#54721=CARTESIAN_POINT('Ctrl Pts',(-93.197184545342,3.86006686900996,1.35750086499028));
#54722=CARTESIAN_POINT('Ctrl Pts',(-92.9983110136445,0.944709284681018,
3.98126226203641));
#54723=CARTESIAN_POINT('Ctrl Pts',(-92.799437481947,-2.83864913015849,2.94703171810691));
#54724=CARTESIAN_POINT('Ctrl Pts',(-92.6005639502496,-4.01385089568802,
-0.794937619478581));
#54725=CARTESIAN_POINT('Ctrl Pts',(-92.4016904185521,-1.50111821672946,
-3.80651664006356));
#54726=CARTESIAN_POINT('Ctrl Pts',(-92.2028168868548,2.39084496196498,-3.32066035594194));
#54727=CARTESIAN_POINT('Ctrl Pts',(-92.0039433551572,4.08609488054962,0.216225481439941));
#54728=CARTESIAN_POINT('Ctrl Pts',(-91.8050698234598,2.02703243301877,3.55444290250494));
#54729=CARTESIAN_POINT('Ctrl Pts',(-91.6061962917624,-1.89447157601982,
3.62683088650832));
#54730=CARTESIAN_POINT('Ctrl Pts',(-91.4073227600648,-4.07533121114487,
0.366879205115507));
#54731=CARTESIAN_POINT('Ctrl Pts',(-91.2084492283676,-2.51176816170427,
-3.23016184324044));
#54732=CARTESIAN_POINT('Ctrl Pts',(-91.0095756966699,1.35961263205489,-3.85932355762439));
#54733=CARTESIAN_POINT('Ctrl Pts',(-90.8107021649726,3.98177854782669,-0.942530863019847));
#54734=CARTESIAN_POINT('Ctrl Pts',(-90.611828633275,2.94547815817867,2.84026112380008));
#54735=CARTESIAN_POINT('Ctrl Pts',(-90.4129551015776,-0.797133611073388,
4.01341535824226));
#54736=CARTESIAN_POINT('Ctrl Pts',(-90.2140815698802,-3.80733738173865,
1.49903532089581));
#54737=CARTESIAN_POINT('Ctrl Pts',(-90.0152080381827,-3.31935174856106,
-2.39266144721782));
#54738=CARTESIAN_POINT('Ctrl Pts',(-89.8163345064853,0.218461086728334,
-4.0859759648416));
#54739=CARTESIAN_POINT('Ctrl Pts',(-89.6174609747877,3.55555142697156,-2.02508737634657));
#54740=CARTESIAN_POINT('Ctrl Pts',(-89.4185874430905,3.62579381559713,1.89645565159203));
#54741=CARTESIAN_POINT('Ctrl Pts',(-89.2197139113928,0.364649401709092,
4.07553133290752));
#54742=CARTESIAN_POINT('Ctrl Pts',(-89.0208403796955,-3.23153563119388,
2.51000045737091));
#54743=CARTESIAN_POINT('Ctrl Pts',(-88.8219668479979,-3.85857909093245,
-1.36172399211318));
#54744=CARTESIAN_POINT('Ctrl Pts',(-88.6230933163006,-0.940352159207695,
-3.98229364165315));
#54745=CARTESIAN_POINT('Ctrl Pts',(-88.424219784603,2.84187226719637,-2.94392371650794));
#54746=CARTESIAN_POINT('Ctrl Pts',(-88.2253462529057,4.01297861936206,0.799329364042572));
#54747=CARTESIAN_POINT('Ctrl Pts',(-88.0264727212081,1.496951976319,3.80815698366971));
#54748=CARTESIAN_POINT('Ctrl Pts',(-87.8275991895108,-2.39447721621638,
3.31804214751687));
#54749=CARTESIAN_POINT('Ctrl Pts',(-87.6287256578132,-4.08585582597779,
-0.220696626619384));
#54750=CARTESIAN_POINT('Ctrl Pts',(-87.4298521261159,-2.02314171345511,
-3.55665888706742));
#54751=CARTESIAN_POINT('Ctrl Pts',(-87.2309785944184,1.89843915945149,-3.62475565928779));
#54752=CARTESIAN_POINT('Ctrl Pts',(-87.0321050627209,4.07573023464101,-0.362419489143201));
#54753=CARTESIAN_POINT('Ctrl Pts',(-86.8332315310234,2.50823200165732,3.23290845177216));
#54754=CARTESIAN_POINT('Ctrl Pts',(-86.6343579993261,-1.36383494453309,
3.85783346915704));
#54755=CARTESIAN_POINT('Ctrl Pts',(-86.4354844676284,-3.9828075433616,0.938173173896801));
#54756=CARTESIAN_POINT('Ctrl Pts',(-86.2366109359312,-2.94236839356005,
-2.84348255986502));
#54757=CARTESIAN_POINT('Ctrl Pts',(-86.0377374042336,0.801524877728764,
-4.01254067917819));
#54758=CARTESIAN_POINT('Ctrl Pts',(-85.8388638725363,3.80897544561137,-1.49486818362271));
#54759=CARTESIAN_POINT('Ctrl Pts',(-85.6399903408386,3.31673155320144,2.39629226841711));
#54760=CARTESIAN_POINT('Ctrl Pts',(-85.4411168091414,-0.222932100443837,
4.08573446399413));
#54761=CARTESIAN_POINT('Ctrl Pts',(-85.2422432774438,-3.55776528246097,
2.02119544492689));
#54762=CARTESIAN_POINT('Ctrl Pts',(-85.0433697457463,-3.62371641789112,
-1.90042209900436));
#54763=CARTESIAN_POINT('Ctrl Pts',(-84.844496214049,-0.360189468085367,
-4.07592791628584));
#54764=CARTESIAN_POINT('Ctrl Pts',(-84.6456226823514,3.23428030456434,-2.50646279509289));
#54765=CARTESIAN_POINT('Ctrl Pts',(-84.446749150654,3.85708669252133,1.36594548868265));
#54766=CARTESIAN_POINT('Ctrl Pts',(-84.2478756189565,0.935993907739473,
3.98332025279822));
#54767=CARTESIAN_POINT('Ctrl Pts',(-84.0490020872593,-2.84509200132407,
2.94081218980056));
#54768=CARTESIAN_POINT('Ctrl Pts',(-83.8501285555615,-4.01210153782168,
-0.803720151474848));
#54769=CARTESIAN_POINT('Ctrl Pts',(-83.6512550238644,-1.49278394343067,
-3.80979276731864));
#54770=CARTESIAN_POINT('Ctrl Pts',(-83.4523814921666,2.39810660327672,-3.31541996600705));
#54771=CARTESIAN_POINT('Ctrl Pts',(-83.2535079604693,4.08561187892698,0.225167507532613));
#54772=CARTESIAN_POINT('Ctrl Pts',(-83.0546344287719,2.01924857134438,3.55887061282109));
#54773=CARTESIAN_POINT('Ctrl Pts',(-82.8557608970742,-1.90240446965716,
3.62267609171814));
#54774=CARTESIAN_POINT('Ctrl Pts',(-82.6568873653771,-4.07612437778279,
0.357959339203114));
#54775=CARTESIAN_POINT('Ctrl Pts',(-82.4580138336794,-2.5046928382072,-3.2356511891598));
#54776=CARTESIAN_POINT('Ctrl Pts',(-82.2591403019821,1.3680556239302,-3.85633876124889));
#54777=CARTESIAN_POINT('Ctrl Pts',(-82.0602667702846,3.9838317698095,-0.933814361387948));
#54778=CARTESIAN_POINT('Ctrl Pts',(-81.861393238587,2.93925510569533,2.84670059109168));
#54779=CARTESIAN_POINT('Ctrl Pts',(-81.6625197068898,-0.805915184623597,
4.01166119542403));
#54780=CARTESIAN_POINT('Ctrl Pts',(-81.4636461751921,-3.81060894854679,
1.49069925636689));
#54781=CARTESIAN_POINT('Ctrl Pts',(-81.2647726434948,-3.31410738632641,
-2.399920220252));
#54782=CARTESIAN_POINT('Ctrl Pts',(-81.0658991117973,0.227402847216426,
-4.08548807081304));
#54783=CARTESIAN_POINT('Ctrl Pts',(-80.8670255800998,3.55997487781682,-2.01730109329047));
#54784=CARTESIAN_POINT('Ctrl Pts',(-80.6681520484024,3.62163468108033,1.90438627081639));
#54785=CARTESIAN_POINT('Ctrl Pts',(-80.4692785167049,0.355729103164104,
4.07631961907303));
#54786=CARTESIAN_POINT('Ctrl Pts',(-80.2704049850075,-3.23702110514808,
2.50292213153017));
#54787=CARTESIAN_POINT('Ctrl Pts',(-80.07153145331,-3.85558967556364,-1.37016534964396));
#54788=CARTESIAN_POINT('Ctrl Pts',(-79.8726579216126,-0.93163453549478,
-3.98434209424231));
#54789=CARTESIAN_POINT('Ctrl Pts',(-79.6737843899152,2.84830832868632,-2.93769714171049));
#54790=CARTESIAN_POINT('Ctrl Pts',(-79.4749108582176,4.01121965211704,0.808109976517873));
#54791=CARTESIAN_POINT('Ctrl Pts',(-79.2760373265203,1.48861412305541,3.81142398905155));
#54792=CARTESIAN_POINT('Ctrl Pts',(-79.0771637948227,-2.40173311880008,
3.31279381455241));
#54793=CARTESIAN_POINT('Ctrl Pts',(-78.8782902631253,-4.08536303968935,
-0.229638118826185));
#54794=CARTESIAN_POINT('Ctrl Pts',(-78.6794167314278,-2.01535301134818,
-3.56107807711758));
#54795=CARTESIAN_POINT('Ctrl Pts',(-78.4805431997303,1.9063675018887,-3.62059218628946));
#54796=CARTESIAN_POINT('Ctrl Pts',(-78.281669668033,4.0765136400982,-0.353498760635994));
#54797=CARTESIAN_POINT('Ctrl Pts',(-78.0827961363354,2.50115067559183,3.23839005211916));
#54798=CARTESIAN_POINT('Ctrl Pts',(-77.8839226046381,-1.3722746651924,3.85483943568976));
#54799=CARTESIAN_POINT('Ctrl Pts',(-77.6850490729406,-3.98485122594388,
0.929454430712534));
#54800=CARTESIAN_POINT('Ctrl Pts',(-77.4861755412431,-2.93613829831247,
-2.84991521362661));
#54801=CARTESIAN_POINT('Ctrl Pts',(-77.2873020095457,0.810304526500643,
-4.01077690803296));
#54802=CARTESIAN_POINT('Ctrl Pts',(-77.0884284778482,3.81223788858895,-1.4865285441204));
#54803=CARTESIAN_POINT('Ctrl Pts',(-76.8895549461508,3.31147925107822,2.40354529837827));
#54804=CARTESIAN_POINT('Ctrl Pts',(-76.6906814144534,-0.231873321692669,
4.08523678559332));
#54805=CARTESIAN_POINT('Ctrl Pts',(-76.4918078827558,-3.56218021039318,
2.01340432610067));
#54806=CARTESIAN_POINT('Ctrl Pts',(-76.2929343510585,-3.61954860765759,
-1.90834816228115));
#54807=CARTESIAN_POINT('Ctrl Pts',(-76.0940608193609,-0.351268312286318,
-4.07670644080014));
#54808=CARTESIAN_POINT('Ctrl Pts',(-75.8951872876636,3.23975802966322,-2.49937847092243));
#54809=CARTESIAN_POINT('Ctrl Pts',(-75.6963137559659,3.85408804185186,1.37438356994404));
#54810=CARTESIAN_POINT('Ctrl Pts',(-75.4974402242687,0.927274047693834,
3.98535916476184));
#54811=CARTESIAN_POINT('Ctrl Pts',(-75.2985666925711,-2.85152124543167,
2.93457857596787));
#54812=CARTESIAN_POINT('Ctrl Pts',(-75.0996931608737,-4.01033296330422,
-0.81249883391509));
#54813=CARTESIAN_POINT('Ctrl Pts',(-74.9008196291762,-1.48444252018617,
-3.8130506469153));
#54814=CARTESIAN_POINT('Ctrl Pts',(-74.7019460974788,2.40535675844402,-3.31016369629741));
#54815=CARTESIAN_POINT('Ctrl Pts',(-74.5030725657813,4.0851093085628,0.234108455146787));
#54816=CARTESIAN_POINT('Ctrl Pts',(-74.304199034084,2.01145503813126,3.56328127731368));
#54817=CARTESIAN_POINT('Ctrl Pts',(-74.1053255023863,-1.91032825140077,
3.61850394549707));
#54818=CARTESIAN_POINT('Ctrl Pts',(-73.906451970689,-4.07689802112117,0.349037758782845));
#54819=CARTESIAN_POINT('Ctrl Pts',(-73.7075784389915,-2.49760551805255,
-3.24112503737069));
#54820=CARTESIAN_POINT('Ctrl Pts',(-73.5087049072941,1.37649206326759,-3.85333549427492));
#54821=CARTESIAN_POINT('Ctrl Pts',(-73.3098313755965,3.98586591054412,-0.92509338709135));
#54822=CARTESIAN_POINT('Ctrl Pts',(-73.1109578438992,2.93301797514357,2.85312642362068));
#54823=CARTESIAN_POINT('Ctrl Pts',(-72.9120843122017,-0.814692898104216,
4.00988781806376));
#54824=CARTESIAN_POINT('Ctrl Pts',(-72.7132107805042,-3.81386226378726,
1.48235605187727));
#54825=CARTESIAN_POINT('Ctrl Pts',(-72.5143372488068,-3.30884715060387,
-2.40716749845509));
#54826=CARTESIAN_POINT('Ctrl Pts',(-72.3154637171093,0.236343518519478,
-4.08498060863594));
#54827=CARTESIAN_POINT('Ctrl Pts',(-72.116590185412,3.56438127754945,-2.00950514802345));
#54828=CARTESIAN_POINT('Ctrl Pts',(-71.9177166537144,3.61745820012068,1.91230776865477));
#54829=CARTESIAN_POINT('Ctrl Pts',(-71.718843122017,0.346807100793382,4.07708838100389));
#54830=CARTESIAN_POINT('Ctrl Pts',(-71.5199695903195,-3.24249107483239,
2.49583181751297));
#54831=CARTESIAN_POINT('Ctrl Pts',(-71.321096058622,-3.85258179318421,-1.3786001445319));
#54832=CARTESIAN_POINT('Ctrl Pts',(-71.1222225269247,-0.922912449557835,
-3.986371463139));
#54833=CARTESIAN_POINT('Ctrl Pts',(-70.9233489952271,2.85473074771306,-2.93145649630679));
#54834=CARTESIAN_POINT('Ctrl Pts',(-70.7244754635297,4.00944147244488,0.816886718411246));
#54835=CARTESIAN_POINT('Ctrl Pts',(-70.5256019318323,1.48026913981821,3.81467273896198));
#54836=CARTESIAN_POINT('Ctrl Pts',(-70.3267284001348,-2.40897751786949,
3.30752961439156));
#54837=CARTESIAN_POINT('Ctrl Pts',(-70.1278548684374,-4.08485068585123,
-0.238578511141671));
#54838=CARTESIAN_POINT('Ctrl Pts',(-69.9289813367398,-2.007554656361,-3.56548021077119));
#54839=CARTESIAN_POINT('Ctrl Pts',(-69.7301078050425,1.91428671345058,-3.61641137184146));
#54840=CARTESIAN_POINT('Ctrl Pts',(-69.5312342733449,4.07727752039141,-0.344576338985572));
#54841=CARTESIAN_POINT('Ctrl Pts',(-69.3323607416475,2.49405736983453,3.24385614163944));
#54842=CARTESIAN_POINT('Ctrl Pts',(-69.1334872099502,-1.38070781310592,
3.85182693880529));
#54843=CARTESIAN_POINT('Ctrl Pts',(-68.9346136782525,-3.98687582239513,
0.920731235746244));
#54844=CARTESIAN_POINT('Ctrl Pts',(-68.7357401465552,-2.92989413992499,
-2.85633421722859));
#54845=CARTESIAN_POINT('Ctrl Pts',(-68.5368666148576,0.819080294179483,
-4.00899392658117));
#54846=CARTESIAN_POINT('Ctrl Pts',(-68.3379930831603,3.81548207219677,-1.47818178463369));
#54847=CARTESIAN_POINT('Ctrl Pts',(-68.1391195514627,3.30621108805498,2.41078681614534));
#54848=CARTESIAN_POINT('Ctrl Pts',(-67.9402460197655,-0.240813432344258,
4.08471954024756));
#54849=CARTESIAN_POINT('Ctrl Pts',(-67.7413724880678,-3.56657807664994,
2.0056035637278));
#54850=CARTESIAN_POINT('Ctrl Pts',(-67.5424989563705,-3.6153634609728,-1.91626508519584));
#54851=CARTESIAN_POINT('Ctrl Pts',(-67.343625424673,-0.342345474027202,
-4.07746543922704));
#54852=CARTESIAN_POINT('Ctrl Pts',(-67.1447518929755,3.24522023738312,-2.49228217554848));
#54853=CARTESIAN_POINT('Ctrl Pts',(-66.9458783612781,3.85107093136417,1.38281506835858));
#54854=CARTESIAN_POINT('Ctrl Pts',(-66.7470048295806,0.918549746309561,
3.98737898816158));
#54855=CARTESIAN_POINT('Ctrl Pts',(-66.5481312978832,-2.8579368316873,2.92833090646582));
#54856=CARTESIAN_POINT('Ctrl Pts',(-66.3492577661857,-4.00854518060657,
-0.821273624752269));
#54857=CARTESIAN_POINT('Ctrl Pts',(-66.1503842344883,-1.47609398694865,
-3.81629026324934));
#54858=CARTESIAN_POINT('Ctrl Pts',(-65.9515107027908,2.41259539274093,-3.30489157198884));
#54859=CARTESIAN_POINT('Ctrl Pts',(-65.7526371710934,4.08458717186426,0.243048281458172));
#54860=CARTESIAN_POINT('Ctrl Pts',(-65.5537636393959,2.0036518707079,3.56767487485709));
#54861=CARTESIAN_POINT('Ctrl Pts',(-65.3548901076985,-1.91824288329831,
3.61431446782833));
#54862=CARTESIAN_POINT('Ctrl Pts',(-65.156016576001,-4.07765213745451,0.340114506586169));
#54863=CARTESIAN_POINT('Ctrl Pts',(-64.9571430443035,-2.49050623518628,
-3.24658336165513));
#54864=CARTESIAN_POINT('Ctrl Pts',(-64.7582695126061,1.38492190965922,-3.85031377108719));
#54865=CARTESIAN_POINT('Ctrl Pts',(-64.5593959809086,3.98788096028769,-0.916367981900684));
#54866=CARTESIAN_POINT('Ctrl Pts',(-64.3605224492112,2.92676679639723,2.85953859060943));
#54867=CARTESIAN_POINT('Ctrl Pts',(-64.1616489175137,-0.823466709472965,
4.00809523465541));
#54868=CARTESIAN_POINT('Ctrl Pts',(-63.9627753858163,-3.81709731187778,
1.47400574738807));
#54869=CARTESIAN_POINT('Ctrl Pts',(-63.7639018541188,-3.30357106658815,
-2.414403247115));
#54870=CARTESIAN_POINT('Ctrl Pts',(-63.5650283224214,0.245283057814545,
-4.08445358074088));
#54871=CARTESIAN_POINT('Ctrl Pts',(-63.3661547907239,3.56877060506427,-2.00169957788552));
#54872=CARTESIAN_POINT('Ctrl Pts',(-63.1672812590265,3.61326439272212,1.92022010716586));
#54873=CARTESIAN_POINT('Ctrl Pts',(-62.968407727329,0.337883437330299,4.07783761501798));
#54874=CARTESIAN_POINT('Ctrl Pts',(-62.7695341956316,-3.24794551404742,
2.48872954927952));
#54875=CARTESIAN_POINT('Ctrl Pts',(-62.5706606639341,-3.84955545820096,
-1.3870283363771));
#54876=CARTESIAN_POINT('Ctrl Pts',(-62.3717871322367,-0.914185943172807,
-3.98838173862321));
#54877=CARTESIAN_POINT('Ctrl Pts',(-62.1729136005392,2.8611394935154,-2.92520181018747));
#54878=CARTESIAN_POINT('Ctrl Pts',(-61.9740400688418,4.00764408886245,0.825659547685083));
#54879=CARTESIAN_POINT('Ctrl Pts',(-61.7751665371443,1.47191706657705,3.81790321784053));
#54880=CARTESIAN_POINT('Ctrl Pts',(-61.5762930054469,-2.41621037872631,
3.30224957224815));
#54881=CARTESIAN_POINT('Ctrl Pts',(-61.3774194737494,-4.08431876691742,
-0.24751776074427));
#54882=CARTESIAN_POINT('Ctrl Pts',(-61.1785459420519,-1.99974668584517,
-3.56986526694341));
#54883=CARTESIAN_POINT('Ctrl Pts',(-60.9796724103544,1.92219675620662,-3.61221323596857));
#54884=CARTESIAN_POINT('Ctrl Pts',(-60.780798878657,4.07802187186193,-0.335652266927447));
#54885=CARTESIAN_POINT('Ctrl Pts',(-60.5819253469596,2.48695211836003,3.24930669415222));
#54886=CARTESIAN_POINT('Ctrl Pts',(-60.3830518152621,-1.38913434788157,
3.84879599293248));
#54887=CARTESIAN_POINT('Ctrl Pts',(-60.1841782835647,-3.98888132301813,
0.912003630779297));
#54888=CARTESIAN_POINT('Ctrl Pts',(-59.9853047518673,-2.92363594830518,
-2.86273953992596));
#54889=CARTESIAN_POINT('Ctrl Pts',(-59.7864312201697,0.827852138732109,
-4.00719174336274));
#54890=CARTESIAN_POINT('Ctrl Pts',(-59.5875576884723,3.81870798089624,-1.46982794514092));
#54891=CARTESIAN_POINT('Ctrl Pts',(-59.3886841567749,3.30092708936454,2.41801678703378));
#54892=CARTESIAN_POINT('Ctrl Pts',(-59.1898106250773,-0.249752389578364,
4.0841827304343));
#54893=CARTESIAN_POINT('Ctrl Pts',(-58.99093709338,-3.57095886016693,1.99779319517138));
#54894=CARTESIAN_POINT('Ctrl Pts',(-58.7920635616823,-3.61116099788224,
-1.92417282982888));
#54895=CARTESIAN_POINT('Ctrl Pts',(-58.5931900299852,-0.333420996045656,
-4.07820490793111));
#54896=CARTESIAN_POINT('Ctrl Pts',(-58.3943164982874,3.25066690156188,-2.48517394296011));
#54897=CARTESIAN_POINT('Ctrl Pts',(-58.1954429665903,3.84803537550925,1.39123994354218));
#54898=CARTESIAN_POINT('Ctrl Pts',(-57.9965694348925,0.909821045373206,
3.98937971332309));
#54899=CARTESIAN_POINT('Ctrl Pts',(-57.7976959031954,-2.86433872936233,
2.92206921121879));
#54900=CARTESIAN_POINT('Ctrl Pts',(-57.5988223714976,-4.0067381982916,-0.830044481957909));
#54901=CARTESIAN_POINT('Ctrl Pts',(-57.3999488398004,-1.4677383837049,-3.81951160080411));
#54902=CARTESIAN_POINT('Ctrl Pts',(-57.2010753081027,2.41982247149684,-3.29960361833307));
#54903=CARTESIAN_POINT('Ctrl Pts',(-57.0022017764055,4.08404547133213,0.251986943647925));
#54904=CARTESIAN_POINT('Ctrl Pts',(-56.8033282447079,1.99583910644906,3.57205138440731));
#54905=CARTESIAN_POINT('Ctrl Pts',(-56.6044547130105,-1.92614832744107,
3.61010767877826));
#54906=CARTESIAN_POINT('Ctrl Pts',(-56.4055811813131,-4.07838672317089,
0.33118962535267));
#54907=CARTESIAN_POINT('Ctrl Pts',(-56.2067076496156,-2.48339502361169,
-3.25202613586953));
#54908=CARTESIAN_POINT('Ctrl Pts',(-56.0078341179182,1.39334512272882,-3.84727360615874));
#54909=CARTESIAN_POINT('Ctrl Pts',(-55.8089605862207,3.98987690938877,-0.907638187607902));
#54910=CARTESIAN_POINT('Ctrl Pts',(-55.6100870545232,2.92050159939748,2.86593706134566));
#54911=CARTESIAN_POINT('Ctrl Pts',(-55.4112135228258,-0.832236576706052,
4.00628345378487));
#54912=CARTESIAN_POINT('Ctrl Pts',(-55.2123399911283,-3.82031407732352,
1.46564838289459));
#54913=CARTESIAN_POINT('Ctrl Pts',(-55.0134664594308,-3.29827915955003,
-2.42162743157478));
#54914=CARTESIAN_POINT('Ctrl Pts',(-54.8145929277335,0.254221422284016,
-4.08390698965212));
#54915=CARTESIAN_POINT('Ctrl Pts',(-54.6157193960359,3.57314283933769,-1.99388442026303));
#54916=CARTESIAN_POINT('Ctrl Pts',(-54.4168458643385,3.60905327897176,1.92812324845197));
#54917=CARTESIAN_POINT('Ctrl Pts',(-54.217972332641,0.328958155516463,4.07856731752671));
#54918=CARTESIAN_POINT('Ctrl Pts',(-54.0190988009436,-3.25338439666812,
2.48161536084749));
#54919=CARTESIAN_POINT('Ctrl Pts',(-53.8202252692462,-3.84651068510908,
-1.39544988481116));
#54920=CARTESIAN_POINT('Ctrl Pts',(-53.6213517375487,-0.90545505813692,
-3.99037291106635));
#54921=CARTESIAN_POINT('Ctrl Pts',(-53.4224782058513,2.86753453539748,-2.9189331133105));
#54922=CARTESIAN_POINT('Ctrl Pts',(-53.2236046741537,4.00582750997863,0.834428422320255));
#54923=CARTESIAN_POINT('Ctrl Pts',(-53.0247311424564,1.46355794333582,3.82111541021416));
#54924=CARTESIAN_POINT('Ctrl Pts',(-52.8258576107589,-2.42343166672732,
3.29695371341198));
#54925=CARTESIAN_POINT('Ctrl Pts',(-52.6269840790614,-4.0837672854357,-0.256455824817776));
#54926=CARTESIAN_POINT('Ctrl Pts',(-52.428110547364,-1.99192913719839,-3.57423322463125));
#54927=CARTESIAN_POINT('Ctrl Pts',(-52.2292370156665,1.93009759227027,-3.60799779877848));
#54928=CARTESIAN_POINT('Ctrl Pts',(-52.030363483969,4.07874669094455,-0.326726587205112));
#54929=CARTESIAN_POINT('Ctrl Pts',(-51.8314899522717,2.47983495520026,3.25474168355105));
#54930=CARTESIAN_POINT('Ctrl Pts',(-51.6326164205741,-1.39755422915913,
3.84574661258867));
#54931=CARTESIAN_POINT('Ctrl Pts',(-51.4337428888767,-3.99086771820734,
0.90327165761377));
#54932=CARTESIAN_POINT('Ctrl Pts',(-51.2348693571792,-2.91736375342743,
-2.86913115103951));
#54933=CARTESIAN_POINT('Ctrl Pts',(-51.0359958254819,0.836620018144438,
-4.00537036700946));
#54934=CARTESIAN_POINT('Ctrl Pts',(-50.8371222937842,3.82191559923634,-1.46146706565414));
#54935=CARTESIAN_POINT('Ctrl Pts',(-50.638248762087,3.29562728031547,2.4252351764145));
#54936=CARTESIAN_POINT('Ctrl Pts',(-50.4393752303894,-0.258690150580364,
4.08362635872462));
#54937=CARTESIAN_POINT('Ctrl Pts',(-50.240501698692,-3.57532253996157,1.98997325784056));
#54938=CARTESIAN_POINT('Ctrl Pts',(-50.0416281669945,-3.60694123851437,
-1.93207135830493));
#54939=CARTESIAN_POINT('Ctrl Pts',(-49.842754635297,-0.324494921086645,
-4.07892484337071));
#54940=CARTESIAN_POINT('Ctrl Pts',(-49.6438811035996,3.25609799611201,-2.47805380720297));
#54941=CARTESIAN_POINT('Ctrl Pts',(-49.4450075719021,3.84498138882624,1.39965815514278));
#54942=CARTESIAN_POINT('Ctrl Pts',(-49.2461340402047,0.901087986692135,
3.99136133066359));
#54943=CARTESIAN_POINT('Ctrl Pts',(-49.0472605085072,-2.87072690779386,
2.91579352021808));
#54944=CARTESIAN_POINT('Ctrl Pts',(-48.8483869768098,-4.00491202501419,
-0.838811363522581));
#54945=CARTESIAN_POINT('Ctrl Pts',(-48.6495134451123,-1.45937575047546,
-3.82271464415041));
#54946=CARTESIAN_POINT('Ctrl Pts',(-48.4506399134149,2.42703796009631,-3.2942998606577));
#54947=CARTESIAN_POINT('Ctrl Pts',(-48.2517663817175,4.08348420956112,0.26092439890286));
#54948=CARTESIAN_POINT('Ctrl Pts',(-48.0528928500199,1.98801678277504,3.57641078500256));
#54949=CARTESIAN_POINT('Ctrl Pts',(-47.8540193183226,-1.93404454596509,
3.60588359849573));
#54950=CARTESIAN_POINT('Ctrl Pts',(-47.655145786625,-4.07910177475187,0.32226315782912));
#54951=CARTESIAN_POINT('Ctrl Pts',(-47.4562722549277,-2.47627191738885,
-3.25745333394491));
#54952=CARTESIAN_POINT('Ctrl Pts',(-47.2573987232301,1.40176166213211,-3.84421501405087));
#54953=CARTESIAN_POINT('Ctrl Pts',(-47.0585251915328,3.99185374828742,-0.898904046025764));
#54954=CARTESIAN_POINT('Ctrl Pts',(-46.8596516598352,2.91422241415247,2.8723218051829));
#54955=CARTESIAN_POINT('Ctrl Pts',(-46.6607781281379,-0.84100245779873,
4.00445248412992));
#54956=CARTESIAN_POINT('Ctrl Pts',(-46.4619045964403,-3.82351254471717,
1.45728399842591));
#54957=CARTESIAN_POINT('Ctrl Pts',(-46.2630310647429,-3.29297145483604,
-2.4288400172331));
#54958=CARTESIAN_POINT('Ctrl Pts',(-46.0641575330455,0.263158569116434,
-4.08334083798774));
#54959=CARTESIAN_POINT('Ctrl Pts',(-45.865284001348,3.57749795942844,-1.9860597125875));
#54960=CARTESIAN_POINT('Ctrl Pts',(-45.6664104696506,3.60482487903916,1.93601715466008));
#54961=CARTESIAN_POINT('Ctrl Pts',(-45.467536937953,0.320031298100702,4.079277485035));
#54962=CARTESIAN_POINT('Ctrl Pts',(-45.2686634062557,-3.25880769664411,
2.47448928629133));
#54963=CARTESIAN_POINT('Ctrl Pts',(-45.0697898745582,-3.843447488492,-1.40386474949774));
#54964=CARTESIAN_POINT('Ctrl Pts',(-44.8709163428607,-0.896719836268132,
-3.99234497093138));
#54965=CARTESIAN_POINT('Ctrl Pts',(-44.6720428111633,2.87391584272915,-2.91265043570083));
#54966=CARTESIAN_POINT('Ctrl Pts',(-44.4731692794658,4.0039917444943,0.843193300316898));
#54967=CARTESIAN_POINT('Ctrl Pts',(-44.2742957477683,1.45519181013165,3.82430930069778));
#54968=CARTESIAN_POINT('Ctrl Pts',(-44.0754222160709,-2.43064134728539,
3.29164206324814));
#54969=CARTESIAN_POINT('Ctrl Pts',(-43.8765486843734,-4.0831962440474,-0.265392660552267));
#54970=CARTESIAN_POINT('Ctrl Pts',(-43.677675152676,-1.9841020478638,-3.57858406291378));
#54971=CARTESIAN_POINT('Ctrl Pts',(-43.4788016209785,1.93798918379931,-3.6037650804616));
#54972=CARTESIAN_POINT('Ctrl Pts',(-43.2799280892811,4.07945197416759,-0.31779934256946));
#54973=CARTESIAN_POINT('Ctrl Pts',(-43.0810545575837,2.47270591444402,3.26016108380421));
#54974=CARTESIAN_POINT('Ctrl Pts',(-42.8821810258862,-1.40596741661001,
3.8426788123793));
#54975=CARTESIAN_POINT('Ctrl Pts',(-42.6833074941888,-3.99283499844841,
0.894535358073276));
#54976=CARTESIAN_POINT('Ctrl Pts',(-42.4844339624912,-2.91107758533382,
-2.8755090199554));
#54977=CARTESIAN_POINT('Ctrl Pts',(-42.2855604307939,0.845383890421254,
-4.00352980624524));
#54978=CARTESIAN_POINT('Ctrl Pts',(-42.0866868990963,3.82510491185373,-1.45309918621901));
#54979=CARTESIAN_POINT('Ctrl Pts',(-41.887813367399,3.29031168629198,2.43244194971396));
#54980=CARTESIAN_POINT('Ctrl Pts',(-41.6889398357014,-0.267626672541508,
4.08305042778336));
#54981=CARTESIAN_POINT('Ctrl Pts',(-41.4900663040041,-3.57966909513332,
1.98214378919011));
#54982=CARTESIAN_POINT('Ctrl Pts',(-41.2911927723065,-3.60270420308042,
-1.93996063279246));
#54983=CARTESIAN_POINT('Ctrl Pts',(-41.0923192406092,-0.315567291903492,
-4.07962524209743));
#54984=CARTESIAN_POINT('Ctrl Pts',(-40.8934457089116,3.26151349502002,-2.47092180238066));
#54985=CARTESIAN_POINT('Ctrl Pts',(-40.6945721772142,3.84190898594293,1.40806966283943));
#54986=CARTESIAN_POINT('Ctrl Pts',(-40.4956986455167,0.89235061209512,3.99332383069183));
#54987=CARTESIAN_POINT('Ctrl Pts',(-40.2968251138193,-2.87710133638473,
2.90950386352227));
#54988=CARTESIAN_POINT('Ctrl Pts',(-40.0979515821219,-4.00306666952103,
-0.847574227456036));
#54989=CARTESIAN_POINT('Ctrl Pts',(-39.8990780504243,-1.45100612731439,
-3.82589937794683));
#54990=CARTESIAN_POINT('Ctrl Pts',(-39.700204518727,2.4342418239797,-3.28898032436581));
#54991=CARTESIAN_POINT('Ctrl Pts',(-39.5013309870295,4.08290338923934,0.269860604415452));
#54992=CARTESIAN_POINT('Ctrl Pts',(-39.302457455332,1.98018493715246,3.58075305576247));
#54993=CARTESIAN_POINT('Ctrl Pts',(-39.1035839236346,-1.94193150104956,
3.60164224721296));
#54994=CARTESIAN_POINT('Ctrl Pts',(-38.9047103919371,-4.07979728877255,
0.313335146770926));
#54995=CARTESIAN_POINT('Ctrl Pts',(-38.7058368602396,-2.46913695063545,
-3.2628649298867));
#54996=CARTESIAN_POINT('Ctrl Pts',(-38.5069633285422,1.4101714875567,-3.84113800941335));
#54997=CARTESIAN_POINT('Ctrl Pts',(-38.3080897968447,3.9938114675153,-0.890165598987688));
#54998=CARTESIAN_POINT('Ctrl Pts',(-38.1092162651473,2.9079292707373,2.87869279154047));
#54999=CARTESIAN_POINT('Ctrl Pts',(-37.9103427334498,-0.849764310765561,
4.00260233446029));
#55000=CARTESIAN_POINT('Ctrl Pts',(-37.7114692017524,-3.8266926987392,1.44891263404444));
#55001=CARTESIAN_POINT('Ctrl Pts',(-37.512595670055,-3.28764797786823,-2.43604096954391));
#55002=CARTESIAN_POINT('Ctrl Pts',(-37.3137221383575,0.272094455505398,
-4.08275512845934));
#55003=CARTESIAN_POINT('Ctrl Pts',(-37.1148486066601,3.58183594447665,-1.97822549233722));
#55004=CARTESIAN_POINT('Ctrl Pts',(-36.9159750749626,3.60057921317725,1.94390178798048));
#55005=CARTESIAN_POINT('Ctrl Pts',(-36.7171015432651,0.311102907840033,
4.0799681141415));
#55006=CARTESIAN_POINT('Ctrl Pts',(-36.5182280115677,-3.26421538799967,
2.46735135974267));
#55007=CARTESIAN_POINT('Ctrl Pts',(-36.3193544798702,-3.84036588302135,
-1.4122728901326));
#55008=CARTESIAN_POINT('Ctrl Pts',(-36.1204809481728,-0.887980319405062,
-3.99429790877284));
#55009=CARTESIAN_POINT('Ctrl Pts',(-35.9216074164752,2.88028338494615,-2.90635380745027));
#55010=CARTESIAN_POINT('Ctrl Pts',(-35.7227338847779,4.00213680120204,0.851954139694033));
#55011=CARTESIAN_POINT('Ctrl Pts',(-35.5238603530804,1.44681870703591,3.82748487399346));
#55012=CARTESIAN_POINT('Ctrl Pts',(-35.324986821383,-2.43783938586804,3.28631464719804));
#55013=CARTESIAN_POINT('Ctrl Pts',(-35.1261132896855,-4.08260564548768,
-0.274328225142681));
#55014=CARTESIAN_POINT('Ctrl Pts',(-34.9272397579881,-1.97626545533103,
-3.58291776095168));
#55015=CARTESIAN_POINT('Ctrl Pts',(-34.7283662262906,1.94587149299542,-3.59951510129151));
#55016=CARTESIAN_POINT('Ctrl Pts',(-34.5294926945931,4.08013771815312,-0.308870575779051));
#55017=CARTESIAN_POINT('Ctrl Pts',(-34.3306191628957,2.46556503023685,3.26556486895468));
#55018=CARTESIAN_POINT('Ctrl Pts',(-34.1317456311982,-1.41437386993809,
3.83959260699806));
#55019=CARTESIAN_POINT('Ctrl Pts',(-33.9328720995008,-3.99478315431879,
0.885794774001494));
#55020=CARTESIAN_POINT('Ctrl Pts',(-33.7339985678033,-2.90477747413283,
-2.88187311612569));
#55021=CARTESIAN_POINT('Ctrl Pts',(-33.5351250361059,0.854143713586202,
-4.0016700698857));
#55022=CARTESIAN_POINT('Ctrl Pts',(-33.3362515044084,3.82827590347246,-1.44472434691534));
#55023=CARTESIAN_POINT('Ctrl Pts',(-33.137377972711,3.28498033275429,2.4396370724137));
#55024=CARTESIAN_POINT('Ctrl Pts',(-32.9385044410135,-0.276561912658538,
4.08245494036915));
#55025=CARTESIAN_POINT('Ctrl Pts',(-32.739630909316,-3.58399850486372,1.97430482672065));
#55026=CARTESIAN_POINT('Ctrl Pts',(-32.5407573776186,-3.59844991187427,
-1.94784061550473));
#55027=CARTESIAN_POINT('Ctrl Pts',(-32.3418838459211,-0.306638151256235,
-4.08030610075666));
#55028=CARTESIAN_POINT('Ctrl Pts',(-32.1430103142237,3.26691337234775,-2.46377796265275));
#55029=CARTESIAN_POINT('Ctrl Pts',(-31.9441367825262,3.83881818157496,1.41647442634414));
#55030=CARTESIAN_POINT('Ctrl Pts',(-31.7452632508288,0.883608963431191,
3.99526720400796));
#55031=CARTESIAN_POINT('Ctrl Pts',(-31.5463897191313,-2.88346198460323,
2.90320027125685));
#55032=CARTESIAN_POINT('Ctrl Pts',(-31.3475161874339,-4.00120214065086,
-0.856333031786573));
#55033=CARTESIAN_POINT('Ctrl Pts',(-31.1486426557364,-1.44262955430986,
-3.82906578693936));
#55034=CARTESIAN_POINT('Ctrl Pts',(-30.949769124039,2.44143402864274,-3.2836450349365));
#55035=CARTESIAN_POINT('Ctrl Pts',(-30.7508955923415,4.08230301314886,0.27879551738431));
#55036=CARTESIAN_POINT('Ctrl Pts',(-30.5520220606441,1.97234360709299,3.58507817588923));
#55037=CARTESIAN_POINT('Ctrl Pts',(-30.3531485289466,-1.94980915491895,
3.59738364524442));
#55038=CARTESIAN_POINT('Ctrl Pts',(-30.1542749972491,-4.08047326190165,
0.304405634939932));
#55039=CARTESIAN_POINT('Ctrl Pts',(-29.9554014655517,-2.46199015752543,
-3.26826089777505));
#55040=CARTESIAN_POINT('Ctrl Pts',(-29.7565279338542,1.41857455872196,-3.83804260698401));
#55041=CARTESIAN_POINT('Ctrl Pts',(-29.5576544021568,3.99575005769547,-0.881422888348441));
#55042=CARTESIAN_POINT('Ctrl Pts',(-29.3587808704593,2.90162219929436,2.88504998990312));
#55043=CARTESIAN_POINT('Ctrl Pts',(-29.1599073387619,-0.858522093639685,
4.00073301363767));
#55044=CARTESIAN_POINT('Ctrl Pts',(-28.9610338070644,-3.82985452415772,
1.44053432984656));
#55045=CARTESIAN_POINT('Ctrl Pts',(-28.762160275367,-3.28230875414438,-2.44323025401721));
#55046=CARTESIAN_POINT('Ctrl Pts',(-28.5632867436695,0.281029038651357,
-4.08214986387229));
#55047=CARTESIAN_POINT('Ctrl Pts',(-28.364413211972,3.58615677370501,-1.97038179703515));
#55048=CARTESIAN_POINT('Ctrl Pts',(-28.1655396802746,3.59631630172115,1.9517771106487));
#55049=CARTESIAN_POINT('Ctrl Pts',(-27.9666661485772,0.302173027498423,
4.08063920153816));
#55050=CARTESIAN_POINT('Ctrl Pts',(-27.7677926168797,-3.26960744483348,
2.46020161538995));
#55051=CARTESIAN_POINT('Ctrl Pts',(-27.5689190851823,-3.83726588345715,
-1.42067426644308));
#55052=CARTESIAN_POINT('Ctrl Pts',(-27.3700455534848,-0.879236549407603,
-3.9962317152367));
#55053=CARTESIAN_POINT('Ctrl Pts',(-27.1711720217874,2.88663713154996,-2.90004325871786));
#55054=CARTESIAN_POINT('Ctrl Pts',(-26.9722984900899,4.00026268898655,0.860710898490242));
#55055=CARTESIAN_POINT('Ctrl Pts',(-26.7734249583925,1.43843867415264,3.83064211489142));
#55056=CARTESIAN_POINT('Ctrl Pts',(-26.5745514266949,-2.4450257479994,3.28097149077797));
#55057=CARTESIAN_POINT('Ctrl Pts',(-26.3756778949976,-4.08199549258528,
-0.283262475791065));
#55058=CARTESIAN_POINT('Ctrl Pts',(-26.1768043633001,-1.96841939713446,
-3.58723429798812));
#55059=CARTESIAN_POINT('Ctrl Pts',(-25.9779308316026,1.95374448210496,-3.59524788162401));
#55060=CARTESIAN_POINT('Ctrl Pts',(-25.7790572999052,4.08080391961648,-0.299940329600006));
#55061=CARTESIAN_POINT('Ctrl Pts',(-25.5801837682077,2.45841233678166,3.27095301311981));
#55062=CARTESIAN_POINT('Ctrl Pts',(-25.3813102365102,-1.42277354887878,
3.83648801122703));
#55063=CARTESIAN_POINT('Ctrl Pts',(-25.1824367048128,-3.99671217648749,
0.877049947263231));
#55064=CARTESIAN_POINT('Ctrl Pts',(-24.9835631731153,-2.89846345,-2.88822340906861));
#55065=CARTESIAN_POINT('Ctrl Pts',(-24.7846896414179,0.862899445683009,
-3.99979116683832));
#55066=CARTESIAN_POINT('Ctrl Pts',(-24.5858161097205,3.83142855890469,-1.43634258785545));
#55067=CARTESIAN_POINT('Ctrl Pts',(-24.386942578023,3.27963324523758,2.44682051005175));
#55068=CARTESIAN_POINT('Ctrl Pts',(-24.1880690463255,-0.285495828134668,
4.08183989933402));
#55069=CARTESIAN_POINT('Ctrl Pts',(-23.9891955146281,-3.58831074841608,
1.96645640797843));
#55070=CARTESIAN_POINT('Ctrl Pts',(-23.7903219829306,-3.59417838527282,
-1.95571126869881));
#55071=CARTESIAN_POINT('Ctrl Pts',(-23.5914484512332,-0.297707541912983,
-4.08096741608726));
#55072=CARTESIAN_POINT('Ctrl Pts',(-23.3925749195357,3.27229760223123,-2.45662232223627));
#55073=CARTESIAN_POINT('Ctrl Pts',(-23.1937013878383,3.83570899052647,1.42487240540064));
#55074=CARTESIAN_POINT('Ctrl Pts',(-22.9948278561408,0.874863082569913,
3.99719144130402));
#55075=CARTESIAN_POINT('Ctrl Pts',(-22.7959543244434,-2.88980882198426,
2.8968827736137));
#55076=CARTESIAN_POINT('Ctrl Pts',(-22.5970807927459,-3.99931844733409,
-0.865087734562843));
#55077=CARTESIAN_POINT('Ctrl Pts',(-22.3982072610485,-1.43424607158253,
-3.83221385596205));
#55078=CARTESIAN_POINT('Ctrl Pts',(-22.199333729351,2.44861453963709,-3.27829401792386));
#55079=CARTESIAN_POINT('Ctrl Pts',(-22.0004601976536,4.08168308416519,0.287729095013874));
#55080=CARTESIAN_POINT('Ctrl Pts',(-21.8015866659561,1.96449283015443,3.58938612466668));
#55081=CARTESIAN_POINT('Ctrl Pts',(-21.6027131342586,-1.95767746984148,
3.59310781298765));
#55082=CARTESIAN_POINT('Ctrl Pts',(-21.4038396025612,-4.08112969090158,
0.295474665105836));
#55083=CARTESIAN_POINT('Ctrl Pts',(-21.2049660708637,-2.45483157228964,
-3.27364121176524));
#55084=CARTESIAN_POINT('Ctrl Pts',(-21.0060925391663,1.42697083538037,-3.8349288215887));
#55085=CARTESIAN_POINT('Ctrl Pts',(-20.8072190074688,3.9976695095428,-0.872675955982284));
#55086=CARTESIAN_POINT('Ctrl Pts',(-20.6083454757714,2.89530123003215,2.89139336982226));
#55087=CARTESIAN_POINT('Ctrl Pts',(-20.4094719440739,-0.867275764474581,
3.99884453061537));
#55088=CARTESIAN_POINT('Ctrl Pts',(-20.2105984123765,-3.83299800582851,
1.43214912596145));
#55089=CARTESIAN_POINT('Ctrl Pts',(-20.011724880679,-3.2769538092377,-2.45040783621837));
#55090=CARTESIAN_POINT('Ctrl Pts',(-19.8128513489816,0.289962275760122,
-4.08152504712563));
#55091=CARTESIAN_POINT('Ctrl Pts',(-19.6139778172841,3.59046042641794,-1.96252866425041));
#55092=CARTESIAN_POINT('Ctrl Pts',(-19.4151042855866,3.59203616508904,1.95964308494436));
#55093=CARTESIAN_POINT('Ctrl Pts',(-19.2162307538892,0.293241699846985,
4.08129074401085));
#55094=CARTESIAN_POINT('Ctrl Pts',(-19.0173572221917,-3.27498384131962,
2.45304008747782));
#55095=CARTESIAN_POINT('Ctrl Pts',(-18.8184836904943,-3.83414750464725,
-1.42906883818977));
#55096=CARTESIAN_POINT('Ctrl Pts',(-18.6196101587969,-0.87048856815513,
-3.99814638106069));
#55097=CARTESIAN_POINT('Ctrl Pts',(-18.4207366270994,2.89297705210815,-2.89371881972889));
#55098=CARTESIAN_POINT('Ctrl Pts',(-18.221863095402,3.99836941682417,0.869463534763232));
#55099=CARTESIAN_POINT('Ctrl Pts',(-18.0229895637045,1.43005175161989,3.83378100826934));
#55100=CARTESIAN_POINT('Ctrl Pts',(-17.824116032007,-2.45220039925878,3.27561261958018));
#55101=CARTESIAN_POINT('Ctrl Pts',(-17.6252425003095,-4.08136578826266,
-0.292195369704815));
#55102=CARTESIAN_POINT('Ctrl Pts',(-17.4263689686121,-1.96056391085437,
-3.59153365334828));
#55103=CARTESIAN_POINT('Ctrl Pts',(-17.2274954369147,1.96160811341902,-3.5909634418978));
#55104=CARTESIAN_POINT('Ctrl Pts',(-17.0286219052172,4.08145057536688,-0.291008646804869));
#55105=CARTESIAN_POINT('Ctrl Pts',(-16.8297483735198,2.45124786833711,3.27632549049245));
#55106=CARTESIAN_POINT('Ctrl Pts',(-16.6308748418223,-1.43116641320073,
3.83336503993602));
#55107=CARTESIAN_POINT('Ctrl Pts',(-16.4320013101249,-3.99862205571501,
0.868300919743232));
#55108=CARTESIAN_POINT('Ctrl Pts',(-16.2331277784274,-2.8921355431775,-2.8945598683681));
#55109=CARTESIAN_POINT('Ctrl Pts',(-16.03425424673,0.871651044774114,-3.99789310610252));
#55110=CARTESIAN_POINT('Ctrl Pts',(-15.8353807150324,3.83456286305009,-1.42795394918566));
#55111=CARTESIAN_POINT('Ctrl Pts',(-15.6365071833351,3.27427044935288,2.45399222822166));
#55112=CARTESIAN_POINT('Ctrl Pts',(-15.4376336516376,-0.294428376179469,
4.08120530762398));
#55113=CARTESIAN_POINT('Ctrl Pts',(-15.2387601199401,-3.59260580513641,
1.95859857055446));
#55114=CARTESIAN_POINT('Ctrl Pts',(-15.0398865882427,-3.58988964373505,
-1.96357255467723));
#55115=CARTESIAN_POINT('Ctrl Pts',(-14.8410130565452,-0.288775506647972,
-4.08160918492181));
#55116=CARTESIAN_POINT('Ctrl Pts',(-14.6421395248478,3.27766615888202,-2.44945491540405));
#55117=CARTESIAN_POINT('Ctrl Pts',(-14.4432659931503,3.83258142768927,1.4332635597854));
#55118=CARTESIAN_POINT('Ctrl Pts',(-14.2443924614529,0.866113011401431,
3.99909653336338));
#55119=CARTESIAN_POINT('Ctrl Pts',(-14.0455189297554,-2.89614181812821,
2.89055140085189));
#55120=CARTESIAN_POINT('Ctrl Pts',(-13.846645398058,-3.99741559859308,-0.873838293852223));
#55121=CARTESIAN_POINT('Ctrl Pts',(-13.6477718663605,-1.42585571928681,
-3.83534356993671));
#55122=CARTESIAN_POINT('Ctrl Pts',(-13.448898334663,2.45578332257062,-3.27292729895759));
#55123=CARTESIAN_POINT('Ctrl Pts',(-13.2500248029656,4.08104360525762,0.296661294515633));
#55124=CARTESIAN_POINT('Ctrl Pts',(-13.0511512712681,1.95663264393901,3.59367688146139));
#55125=CARTESIAN_POINT('Ctrl Pts',(-12.8522777395707,-1.96553640813083,
3.58881477092224));
#55126=CARTESIAN_POINT('Ctrl Pts',(-12.6534042078732,-4.0817665726281,0.286542280044954));
#55127=CARTESIAN_POINT('Ctrl Pts',(-12.4545306761758,-2.44766122921548,
-3.27900584608708));
#55128=CARTESIAN_POINT('Ctrl Pts',(-12.2556571444783,1.43536027731604,-3.8317966681416));
#55129=CARTESIAN_POINT('Ctrl Pts',(-12.0567836127809,3.99956981386368,-0.863924843784606));
#55130=CARTESIAN_POINT('Ctrl Pts',(-11.8579100810834,2.88896639322636,2.89772290091486));
#55131=CARTESIAN_POINT('Ctrl Pts',(-11.659036549386,-0.876025281342798,
3.9969368944388));
#55132=CARTESIAN_POINT('Ctrl Pts',(-11.4601630176885,-3.83612312869551,
1.42375706255146));
#55133=CARTESIAN_POINT('Ctrl Pts',(-11.261289485991,-3.27158316879638,-2.45757368176949));
#55134=CARTESIAN_POINT('Ctrl Pts',(-11.0624159542936,0.298894124044868,
-4.08088068121199));
#55135=CARTESIAN_POINT('Ctrl Pts',(-10.8635424225961,3.59474688200251,-1.95466613159658));
#55136=CARTESIAN_POINT('Ctrl Pts',(-10.6646688908987,3.58773882378118,1.96749967319203));
#55137=CARTESIAN_POINT('Ctrl Pts',(-10.4657953592012,0.284308967664094,
4.08192273843878));
#55138=CARTESIAN_POINT('Ctrl Pts',(-10.2669218275038,-3.28034455170665,
2.44586681030803));
#55139=CARTESIAN_POINT('Ctrl Pts',(-10.0680482958063,-3.83101076152782,
-1.43745656516507));
#55140=CARTESIAN_POINT('Ctrl Pts',(-9.86917476410886,-0.861736417547805,
-4.00004189707429));
#55141=CARTESIAN_POINT('Ctrl Pts',(-9.67030123241143,2.89930311625488,-2.88738052077529));
#55142=CARTESIAN_POINT('Ctrl Pts',(-9.47142770071396,3.99645699378297,0.878212006591244));
#55143=CARTESIAN_POINT('Ctrl Pts',(-9.27255416901651,1.42165797960771,3.83690153909317));
#55144=CARTESIAN_POINT('Ctrl Pts',(-9.07368063731905,-2.45936330528239,
3.27023805927156));
#55145=CARTESIAN_POINT('Ctrl Pts',(-8.8748071056216,-4.0807165355358,-0.301126864098756));
#55146=CARTESIAN_POINT('Ctrl Pts',(-8.67593357392414,-1.95269903411579,
-3.59581580643962));
#55147=CARTESIAN_POINT('Ctrl Pts',(-8.4770600422267,1.9694623492732,-3.58666180263391));
#55148=CARTESIAN_POINT('Ctrl Pts',(-8.27818651052923,4.08207768230702,-0.282075570173808));
#55149=CARTESIAN_POINT('Ctrl Pts',(-8.07931297883178,2.44407165921894,3.28168227533997));
#55150=CARTESIAN_POINT('Ctrl Pts',(-7.88043944713432,-1.43955242270476,
3.83022370808317));
#55151=CARTESIAN_POINT('Ctrl Pts',(-7.68156591543689,-4.00051278285394,
0.859547733346342));
#55152=CARTESIAN_POINT('Ctrl Pts',(-7.48269238373941,-2.88579378397343,
-2.90088246367505));
#55153=CARTESIAN_POINT('Ctrl Pts',(-7.28381885204198,0.880398468942455,
-3.99597589676918));
#55154=CARTESIAN_POINT('Ctrl Pts',(-7.0849453203445,3.83767880089717,-1.4195584710844));
#55155=CARTESIAN_POINT('Ctrl Pts',(-6.88607178864706,3.26889197078478,2.46115219257381));
#55156=CARTESIAN_POINT('Ctrl Pts',(-6.68719825694958,-0.303359514006894,
4.0805511682777));
#55157=CARTESIAN_POINT('Ctrl Pts',(-6.48832472525215,-3.59688365445685,
1.95073135208659));
#55158=CARTESIAN_POINT('Ctrl Pts',(-6.28945119355468,-3.58558370779488,
-1.97142443578932));
#55159=CARTESIAN_POINT('Ctrl Pts',(-6.09057766185723,-0.279842088257574,
-4.08223140418192));
#55160=CARTESIAN_POINT('Ctrl Pts',(-5.89170413015981,3.28301901661428,-2.44227577649414));
#55161=CARTESIAN_POINT('Ctrl Pts',(-5.69283059846233,3.82943550799096,1.44164784932378));
#55162=CARTESIAN_POINT('Ctrl Pts',(-5.49395706676489,0.857358791934341,
4.00098247103127));
#55163=CARTESIAN_POINT('Ctrl Pts',(-5.29508353506742,-2.90246094288968,
2.88420618335313));
#55164=CARTESIAN_POINT('Ctrl Pts',(-5.09621000336997,-3.99549360318837,
-0.882584667850434));
#55165=CARTESIAN_POINT('Ctrl Pts',(-4.89733647167251,-1.41745853827654,
-3.83845491367013));
#55166=CARTESIAN_POINT('Ctrl Pts',(-4.69846293997506,2.46294034436706,-3.26754490412554));
#55167=CARTESIAN_POINT('Ctrl Pts',(-4.49958940827759,4.0803845771102,0.305592073830688));
#55168=CARTESIAN_POINT('Ctrl Pts',(-4.30071587658015,1.94876309058629,3.59795042435585));
#55169=CARTESIAN_POINT('Ctrl Pts',(-4.10184234488271,-1.97338594062652,
3.58450454219004));
#55170=CARTESIAN_POINT('Ctrl Pts',(-3.90296881318525,-4.08238388801658,
0.277608517669592));
#55171=CARTESIAN_POINT('Ctrl Pts',(-3.70409528148781,-2.44047919288451,
-3.28435476584923));
#55172=CARTESIAN_POINT('Ctrl Pts',(-3.50522174979033,1.44374290144303,-3.82864617900992));
#55173=CARTESIAN_POINT('Ctrl Pts',(-3.3063482180929,4.00145085374723,-0.855169560880336));
#55174=CARTESIAN_POINT('Ctrl Pts',(-3.10747468639542,2.88261792278395,2.90403849095175));
#55175=CARTESIAN_POINT('Ctrl Pts',(-2.90860115469799,-0.884770986710579,
3.99501023114948));
#55176=CARTESIAN_POINT('Ctrl Pts',(-2.70972762300051,-3.8392291520155,1.41535795907167));
#55177=CARTESIAN_POINT('Ctrl Pts',(-2.51085409130307,-3.26619822895463,
-2.4647273395464));
#55178=CARTESIAN_POINT('Ctrl Pts',(-2.31198055960563,0.307827128338472,
-4.08021755622459));
#55179=CARTESIAN_POINT('Ctrl Pts',(-2.11310702790817,3.59901123398703,-1.94679275070356));
#55180=CARTESIAN_POINT('Ctrl Pts',(-1.91423349621072,3.58343352403109,1.97534403183598));
#55181=CARTESIAN_POINT('Ctrl Pts',(-1.71535996451326,0.275357453827102,
4.08254047995398));
#55182=CARTESIAN_POINT('Ctrl Pts',(-1.51648643281581,-3.28565665797204,
2.43867181422721));
#55183=CARTESIAN_POINT('Ctrl Pts',(-1.31761290111835,-3.82791777672393,
-1.44581851751593));
#55184=CARTESIAN_POINT('Ctrl Pts',(-1.11873936942089,-0.852862866404934,
-4.00195392234629));
#55185=CARTESIAN_POINT('Ctrl Pts',(-0.919865837723433,2.90539384744835,
-2.88096103865537));
#55186=CARTESIAN_POINT('Ctrl Pts',(-0.720992306025977,3.99494365268282,
0.886829055253763));
#55187=CARTESIAN_POINT('Ctrl Pts',(-0.522118774328538,1.41246698653237,
3.84024422739266));
#55188=CARTESIAN_POINT('Ctrl Pts',(-0.323245242631086,-2.46501608324706,
3.26439100997213));
#55189=CARTESIAN_POINT('Ctrl Pts',(-0.124371710933631,-4.08292506541557,
-0.309172729297909));
#55190=CARTESIAN_POINT('Ctrl Pts',(0.074501820763823,-1.93900000174599,
-3.60192375349645));
#55191=CARTESIAN_POINT('Ctrl Pts',(0.207084175228793,0.662521205821,-3.58581394706895));
#55192=CARTESIAN_POINT('Ctrl Pts',(0.273375352461282,1.6717518345084,-3.02875982108483));
#55193=CARTESIAN_POINT('Ctrl Pts',(-109.567,1.87158653173818,-2.62360084935118));
#55194=CARTESIAN_POINT('Ctrl Pts',(-109.500708822768,2.74581178927839,-1.99995864473678));
#55195=CARTESIAN_POINT('Ctrl Pts',(-109.368126468303,3.80651295487345,0.179129781420444));
#55196=CARTESIAN_POINT('Ctrl Pts',(-109.169252936605,1.9032035356359,3.30567173395145));
#55197=CARTESIAN_POINT('Ctrl Pts',(-108.970379404908,-1.7502378889635,3.3848793341849));
#55198=CARTESIAN_POINT('Ctrl Pts',(-108.77150587321,-3.79478855817402,0.359146699884545));
#55199=CARTESIAN_POINT('Ctrl Pts',(-108.572632341513,-2.35308601341721,
-2.99923852306436));
#55200=CARTESIAN_POINT('Ctrl Pts',(-108.373758809815,1.25085188316156,-3.60050797555933));
#55201=CARTESIAN_POINT('Ctrl Pts',(-108.174885278118,3.70539059895966,-0.894369208581839));
#55202=CARTESIAN_POINT('Ctrl Pts',(-107.97601174642,2.7554691459713,2.63391280124896));
#55203=CARTESIAN_POINT('Ctrl Pts',(-107.777138214723,-0.726214962520435,
3.74194114611939));
#55204=CARTESIAN_POINT('Ctrl Pts',(-107.578264683026,-3.5406343533814,1.41197706181962));
#55205=CARTESIAN_POINT('Ctrl Pts',(-107.379391151328,-3.10192059080864,
-2.21537311500977));
#55206=CARTESIAN_POINT('Ctrl Pts',(-107.180517619631,0.186848925119125,
-3.80720285370364));
#55207=CARTESIAN_POINT('Ctrl Pts',(-106.981644087933,3.3039387517963,-1.90098324867159));
#55208=CARTESIAN_POINT('Ctrl Pts',(-106.782770556236,3.3853642004366,1.75187238336515));
#55209=CARTESIAN_POINT('Ctrl Pts',(-106.583897024538,0.356309365737235,
3.79509945705497));
#55210=CARTESIAN_POINT('Ctrl Pts',(-106.385023492841,-3.00012287248227,
2.35138380158418));
#55211=CARTESIAN_POINT('Ctrl Pts',(-106.186149961143,-3.60003625310656,
-1.25278941335415));
#55212=CARTESIAN_POINT('Ctrl Pts',(-105.987276429446,-0.89222882781209,
-3.70589645739097));
#55213=CARTESIAN_POINT('Ctrl Pts',(-105.788402897748,2.63536022101092,-2.75401859025452));
#55214=CARTESIAN_POINT('Ctrl Pts',(-105.589529366051,3.74157491702501,0.728257404654141));
#55215=CARTESIAN_POINT('Ctrl Pts',(-105.390655834353,1.41002288124958,3.54140889901514));
#55216=CARTESIAN_POINT('Ctrl Pts',(-105.191782302656,-2.21706106474189,
3.10070667941842));
#55217=CARTESIAN_POINT('Ctrl Pts',(-104.992908770959,-3.80710475658041,
-0.188931232388143));
#55218=CARTESIAN_POINT('Ctrl Pts',(-104.794035239261,-1.89917277873868,
-3.30497872482143));
#55219=CARTESIAN_POINT('Ctrl Pts',(-104.595161707564,1.75372304650391,-3.38440498687836));
#55220=CARTESIAN_POINT('Ctrl Pts',(-104.396288175866,3.79529453639531,-0.354232993642497));
#55221=CARTESIAN_POINT('Ctrl Pts',(-104.197414644169,2.34974161312935,3.00140899924184));
#55222=CARTESIAN_POINT('Ctrl Pts',(-103.998541112471,-1.25475872875807,
3.59935024210211));
#55223=CARTESIAN_POINT('Ctrl Pts',(-103.799667580774,-3.70638417439717,
0.890201091441595));
#55224=CARTESIAN_POINT('Ctrl Pts',(-103.600794049076,-2.75257623033224,
-2.63686664952715));
#55225=CARTESIAN_POINT('Ctrl Pts',(-103.401920517379,0.730304405924223,
-3.74117589888118));
#55226=CARTESIAN_POINT('Ctrl Pts',(-103.203046985682,3.5421798545178,-1.40808505059571));
#55227=CARTESIAN_POINT('Ctrl Pts',(-103.004173453984,3.09949317971213,2.2187572333099));
#55228=CARTESIAN_POINT('Ctrl Pts',(-102.805299922287,-0.191014192713332,
3.80700081556329));
#55229=CARTESIAN_POINT('Ctrl Pts',(-102.606426390589,-3.30601733267171,
1.8973642316529));
#55230=CARTESIAN_POINT('Ctrl Pts',(-102.407552858892,-3.38344495921552,
-1.75557450409872));
#55231=CARTESIAN_POINT('Ctrl Pts',(-102.208679327194,-0.352156410097993,
-3.79548778081539));
#55232=CARTESIAN_POINT('Ctrl Pts',(-102.009805795497,3.00269417169098,-2.34809909134587));
#55233=CARTESIAN_POINT('Ctrl Pts',(-101.810932263799,3.59866318318054,1.25672786453859));
#55234=CARTESIAN_POINT('Ctrl Pts',(-101.612058732102,0.888173072927529,
3.70687067808071));
#55235=CARTESIAN_POINT('Ctrl Pts',(-101.413185200404,-2.63837228039274,
2.75113310138612));
#55236=CARTESIAN_POINT('Ctrl Pts',(-101.214311668707,-3.74077576519073,
-0.732351217687996));
#55237=CARTESIAN_POINT('Ctrl Pts',(-101.015438137009,-1.40614679609923,
-3.54294973423381));
#55238=CARTESIAN_POINT('Ctrl Pts',(-100.816564605312,2.22045273645088,-3.09827876032406));
#55239=CARTESIAN_POINT('Ctrl Pts',(-100.617691073615,3.80689573555524,0.193097100182191));
#55240=CARTESIAN_POINT('Ctrl Pts',(-100.418817541917,1.89555511623687,3.30705494856008));
#55241=CARTESIAN_POINT('Ctrl Pts',(-100.21994401022,-1.75742543597124,3.38248391991576));
#55242=CARTESIAN_POINT('Ctrl Pts',(-100.021070478522,-3.79567988913556,
0.35007972049143));
#55243=CARTESIAN_POINT('Ctrl Pts',(-99.8221969468248,-2.34645586659674,
-3.00397844492953));
#55244=CARTESIAN_POINT('Ctrl Pts',(-99.6233234151273,1.25869662408462,-3.5979750471627));
#55245=CARTESIAN_POINT('Ctrl Pts',(-99.4244498834298,3.70735607210978,-0.886144788439325));
#55246=CARTESIAN_POINT('Ctrl Pts',(-99.2255763517325,2.74968914886796,2.63987712139888));
#55247=CARTESIAN_POINT('Ctrl Pts',(-99.0267028200349,-0.734397810215034,
3.74037451170853));
#55248=CARTESIAN_POINT('Ctrl Pts',(-98.8278292883376,-3.54371855335358,
1.40420812065201));
#55249=CARTESIAN_POINT('Ctrl Pts',(-98.6289557566399,-3.09706341345078,
-2.22214757488159));
#55250=CARTESIAN_POINT('Ctrl Pts',(-98.4300822249426,0.195179949845956,
-3.80678951593933));
#55251=CARTESIAN_POINT('Ctrl Pts',(-98.2312086932451,3.30809157446657,-1.89374543337553));
#55252=CARTESIAN_POINT('Ctrl Pts',(-98.0323351615477,3.38152186805364,1.75927584174923));
#55253=CARTESIAN_POINT('Ctrl Pts',(-97.8334616298501,0.348002926086945,
3.795870861202));
#55254=CARTESIAN_POINT('Ctrl Pts',(-97.6345880981528,-3.00526181891328,
2.34481193942487));
#55255=CARTESIAN_POINT('Ctrl Pts',(-97.4357145664553,-3.59728583407436,
-1.26066500683384));
#55256=CARTESIAN_POINT('Ctrl Pts',(-97.236841034758,-0.884116238679596,
-3.70784035632476));
#55257=CARTESIAN_POINT('Ctrl Pts',(-97.0379675030604,2.6413811721456,-2.74824437321759));
#55258=CARTESIAN_POINT('Ctrl Pts',(-96.8390939713629,3.73997213852792,0.736444182896666));
#55259=CARTESIAN_POINT('Ctrl Pts',(-96.6402204396655,1.4022690248486,3.54448631164484));
#55260=CARTESIAN_POINT('Ctrl Pts',(-96.4413469079681,-2.22384174810214,
3.09584713945722));
#55261=CARTESIAN_POINT('Ctrl Pts',(-96.2424733762705,-3.80668215674337,
-0.197262741081687));
#55262=CARTESIAN_POINT('Ctrl Pts',(-96.0435998445732,-1.89193518361277,
-3.30912721008056));
#55263=CARTESIAN_POINT('Ctrl Pts',(-95.8447263128756,1.76112572087986,-3.38055880391732));
#55264=CARTESIAN_POINT('Ctrl Pts',(-95.6458527811783,3.79606069695695,-0.345926027506187));
#55265=CARTESIAN_POINT('Ctrl Pts',(-95.4469792494807,2.3431673103227,3.00654429325805));
#55266=CARTESIAN_POINT('Ctrl Pts',(-95.2481057177834,-1.26263301219719,
3.59659554412187));
#55267=CARTESIAN_POINT('Ctrl Pts',(-95.0492321860857,-3.70832353058058,
0.882087424255571));
#55268=CARTESIAN_POINT('Ctrl Pts',(-94.8503586543885,-2.74679877486757,
-2.64288443218266));
#55269=CARTESIAN_POINT('Ctrl Pts',(-94.6514851226908,0.738490335120334,
-3.73956864576937));
#55270=CARTESIAN_POINT('Ctrl Pts',(-94.4526115909935,3.54525300887773,-1.40032950926946));
#55271=CARTESIAN_POINT('Ctrl Pts',(-94.2537380592961,3.09462993870752,2.22553525560538));
#55272=CARTESIAN_POINT('Ctrl Pts',(-94.0548645275986,-0.199345473265892,
3.80657365799952));
#55273=CARTESIAN_POINT('Ctrl Pts',(-93.8559909959012,-3.31016185509202,
1.89012436749044));
#55274=CARTESIAN_POINT('Ctrl Pts',(-93.6571174642037,-3.37959472779509,
-1.76297507280934));
#55275=CARTESIAN_POINT('Ctrl Pts',(-93.4582439325062,-0.343849025370891,
-3.79624939634358));
#55276=CARTESIAN_POINT('Ctrl Pts',(-93.2593704008088,3.00782586757985,-2.34152197978259));
#55277=CARTESIAN_POINT('Ctrl Pts',(-93.0604968691114,3.59590417751189,1.26460063958548));
#55278=CARTESIAN_POINT('Ctrl Pts',(-92.8616233374138,0.880058345774601,
3.70880559473261));
#55279=CARTESIAN_POINT('Ctrl Pts',(-92.6627498057164,-2.64438690106003,
2.74535235425065));
#55280=CARTESIAN_POINT('Ctrl Pts',(-92.4638762740191,-3.73916403355365,
-0.74053626627348));
#55281=CARTESIAN_POINT('Ctrl Pts',(-92.2650027423214,-1.39838957449524,
-3.54601864482274));
#55282=CARTESIAN_POINT('Ctrl Pts',(-92.0661292106243,2.22722809688435,-3.09341181156606));
#55283=CARTESIAN_POINT('Ctrl Pts',(-91.8672556789264,3.80646401974024,0.201428145775125));
#55284=CARTESIAN_POINT('Ctrl Pts',(-91.6683821472293,1.88831298555067,3.31119550919123));
#55285=CARTESIAN_POINT('Ctrl Pts',(-91.4695086155316,-1.7648238969841,3.37862963997555));
#55286=CARTESIAN_POINT('Ctrl Pts',(-91.2706350838343,-3.79643695930539,
0.341771920302796));
#55287=CARTESIAN_POINT('Ctrl Pts',(-91.0717615521368,-2.33987594829705,
-3.00910654149507));
#55288=CARTESIAN_POINT('Ctrl Pts',(-90.8728880204393,1.26656788840972,-3.59521173445138));
#55289=CARTESIAN_POINT('Ctrl Pts',(-90.6740144887419,3.70928654863654,-0.878029003844108));
#55290=CARTESIAN_POINT('Ctrl Pts',(-90.4751409570445,2.74390511179979,2.64588857832797));
#55291=CARTESIAN_POINT('Ctrl Pts',(-90.276267425347,-0.742581975743678,
3.73875830200189));
#55292=CARTESIAN_POINT('Ctrl Pts',(-90.0773938936495,-3.54678321925067,
1.39644922110663));
#55293=CARTESIAN_POINT('Ctrl Pts',(-89.8785203619521,-3.09219275839747,
-2.22892027143228));
#55294=CARTESIAN_POINT('Ctrl Pts',(-89.6796468302546,0.203510757985896,
-3.80635324199837));
#55295=CARTESIAN_POINT('Ctrl Pts',(-89.4807732985572,3.31222817206875,-1.88650103833566));
#55296=CARTESIAN_POINT('Ctrl Pts',(-89.2818997668597,3.37766354074761,1.76667219285066));
#55297=CARTESIAN_POINT('Ctrl Pts',(-89.0830262351624,0.339694712923688,
3.79662338578627));
#55298=CARTESIAN_POINT('Ctrl Pts',(-88.8841527034647,-3.01038631462036,
2.33822921635881));
#55299=CARTESIAN_POINT('Ctrl Pts',(-88.6852791717675,-3.59451821514758,
-1.26853475808103));
#55300=CARTESIAN_POINT('Ctrl Pts',(-88.4864056400698,-0.875999399071568,
-3.70976639214839));
#55301=CARTESIAN_POINT('Ctrl Pts',(-88.2875321083726,2.64738946353692,-2.74245704794827));
#55302=CARTESIAN_POINT('Ctrl Pts',(-88.0886585766749,3.73835145123555,0.744627462918542));
#55303=CARTESIAN_POINT('Ctrl Pts',(-87.8897850449776,1.39450844968449,3.54754673193265));
#55304=CARTESIAN_POINT('Ctrl Pts',(-87.69091151328,-2.23061177874262,3.09097277956667));
#55305=CARTESIAN_POINT('Ctrl Pts',(-87.4920379815828,-3.80624132480706,
-0.205593309274777));
#55306=CARTESIAN_POINT('Ctrl Pts',(-87.2931644498851,-1.88468852638785,
-3.31325984341546));
#55307=CARTESIAN_POINT('Ctrl Pts',(-87.0942909181878,1.76851995985574,-3.37669643040047));
#55308=CARTESIAN_POINT('Ctrl Pts',(-86.8954173864903,3.79680867573037,-0.337617403855405));
#55309=CARTESIAN_POINT('Ctrl Pts',(-86.6965438547928,2.33658178446086,3.01166518657256));
#55310=CARTESIAN_POINT('Ctrl Pts',(-86.4976703230953,-1.27050124801057,
3.59382361980817));
#55311=CARTESIAN_POINT('Ctrl Pts',(-86.298796791398,-3.71024512512451,0.873969532064579));
#55312=CARTESIAN_POINT('Ctrl Pts',(-86.0999232597003,-2.74100816312956,
-2.64888955623758));
#55313=CARTESIAN_POINT('Ctrl Pts',(-85.9010497280032,0.746672727185684,
-3.73794348137644));
#55314=CARTESIAN_POINT('Ctrl Pts',(-85.7021761963054,3.54830918264012,-1.3925672608098));
#55315=CARTESIAN_POINT('Ctrl Pts',(-85.5033026646083,3.08975187543889,2.23230261830901));
#55316=CARTESIAN_POINT('Ctrl Pts',(-85.3044291329105,-0.20767579901831,
3.80612826819978));
#55317=CARTESIAN_POINT('Ctrl Pts',(-85.1055556012133,-3.31429052292249,
1.88287545024988));
#55318=CARTESIAN_POINT('Ctrl Pts',(-84.9066820695157,-3.37572830922368,
-1.77036719744615));
#55319=CARTESIAN_POINT('Ctrl Pts',(-84.7078085378184,-0.335539993719798,
-3.79699282908225));
#55320=CARTESIAN_POINT('Ctrl Pts',(-84.5089350061207,3.01294315696887,-2.33493365309634));
#55321=CARTESIAN_POINT('Ctrl Pts',(-84.3100614744234,3.59312794864103,1.27246735760964));
#55322=CARTESIAN_POINT('Ctrl Pts',(-84.1111879427259,0.871939403430806,
3.71072274742162));
#55323=CARTESIAN_POINT('Ctrl Pts',(-83.9123144110285,-2.65038885598094,
2.73955845777738));
#55324=CARTESIAN_POINT('Ctrl Pts',(-83.7134408793309,-3.73753439254664,
-0.748717767932958));
#55325=CARTESIAN_POINT('Ctrl Pts',(-83.5145673476336,-1.39062565506363,
-3.54907057114484));
#55326=CARTESIAN_POINT('Ctrl Pts',(-83.3156938159361,2.23399278962533,-3.08853004637957));
#55327=CARTESIAN_POINT('Ctrl Pts',(-83.1168202842386,3.80601407221043,0.209758226593208));
#55328=CARTESIAN_POINT('Ctrl Pts',(-82.9179467525413,1.88106181046435,3.31532021028137));
#55329=CARTESIAN_POINT('Ctrl Pts',(-82.7190732208437,-1.77221390506902,
3.37475917750697));
#55330=CARTESIAN_POINT('Ctrl Pts',(-82.5201996891463,-3.79717584578678,
0.333462483138709));
#55331=CARTESIAN_POINT('Ctrl Pts',(-82.3213261574489,-2.33328482275862,
-3.01422022542674));
#55332=CARTESIAN_POINT('Ctrl Pts',(-82.1224526257514,1.27443308628981,-3.59243120185442));
#55333=CARTESIAN_POINT('Ctrl Pts',(-81.9235790940539,3.71119925889672,-0.86990901377786));
#55334=CARTESIAN_POINT('Ctrl Pts',(-81.7247055623564,2.73810793232568,2.65188736231815));
#55335=CARTESIAN_POINT('Ctrl Pts',(-81.525832030659,-0.750762584548115,
3.73712418486865));
#55336=CARTESIAN_POINT('Ctrl Pts',(-81.3269584989616,-3.54983089721885,
1.38868363302726));
#55337=CARTESIAN_POINT('Ctrl Pts',(-81.128084967264,-3.08730729275454,-2.23568229218554));
#55338=CARTESIAN_POINT('Ctrl Pts',(-80.9292114355667,0.211840591375986,
-3.8058987368732));
#55339=CARTESIAN_POINT('Ctrl Pts',(-80.7303379038692,3.31634890518381,-1.87924760757427));
#55340=CARTESIAN_POINT('Ctrl Pts',(-80.5314643721718,3.3737890355405,1.77406008217146));
#55341=CARTESIAN_POINT('Ctrl Pts',(-80.3325908404742,0.331384872734104,
3.79735772578913));
#55342=CARTESIAN_POINT('Ctrl Pts',(-80.1337173087769,-3.01549639156382,
2.33163529394134));
#55343=CARTESIAN_POINT('Ctrl Pts',(-79.9348437770794,-3.59173337965695,
-1.27639843346252));
#55344=CARTESIAN_POINT('Ctrl Pts',(-79.7359702453819,-0.867878363713628,
-3.71167465940716));
#55345=CARTESIAN_POINT('Ctrl Pts',(-79.5370967136845,2.65338507480061,-2.73665658720871));
#55346=CARTESIAN_POINT('Ctrl Pts',(-79.338223181987,3.73671285846524,0.752807176418981));
#55347=CARTESIAN_POINT('Ctrl Pts',(-79.1393496502896,1.38674119528204,3.55059016063458));
#55348=CARTESIAN_POINT('Ctrl Pts',(-78.9404761185921,-2.23737112548394,
3.0860836149298));
#55349=CARTESIAN_POINT('Ctrl Pts',(-78.7416025868947,-3.80578226222256,
-0.21392289274333));
#55350=CARTESIAN_POINT('Ctrl Pts',(-78.5427290551972,-1.87743284212275,
-3.31737660732185));
#55351=CARTESIAN_POINT('Ctrl Pts',(-78.3438555234997,1.77590572820074,-3.3728178836147));
#55352=CARTESIAN_POINT('Ctrl Pts',(-78.1449819918024,3.79753846903493,-0.329307163127962));
#55353=CARTESIAN_POINT('Ctrl Pts',(-77.9461084601048,2.32998506713825,3.01677165499815));
#55354=CARTESIAN_POINT('Ctrl Pts',(-77.7472349284074,-1.27836339853949,
3.59103448225746));
#55355=CARTESIAN_POINT('Ctrl Pts',(-77.5483613967099,-3.71214894881061,
0.865847453846025));
#55356=CARTESIAN_POINT('Ctrl Pts',(-77.3494878650125,-2.73520442286098,
-2.65488199297993));
#55357=CARTESIAN_POINT('Ctrl Pts',(-77.150614333315,0.754851542933501,-3.73630041345961));
#55358=CARTESIAN_POINT('Ctrl Pts',(-76.9517408016175,3.55134836116475,-1.38479834240944));
#55359=CARTESIAN_POINT('Ctrl Pts',(-76.7528672699202,3.08485901327164,2.23905928901498));
#55360=CARTESIAN_POINT('Ctrl Pts',(-76.5539937382226,-0.216005130071836,
3.80566464829338));
#55361=CARTESIAN_POINT('Ctrl Pts',(-76.3551202065253,-3.31840331638788,
1.87561751465306));
#55362=CARTESIAN_POINT('Ctrl Pts',(-76.1562466748277,-3.37184572202029,
-1.77775084260449));
#55363=CARTESIAN_POINT('Ctrl Pts',(-75.9573731431304,-0.327229354942119,
-3.79771807547001));
#55364=CARTESIAN_POINT('Ctrl Pts',(-75.7584996114328,3.01804601534794,-2.32833414284333));
#55365=CARTESIAN_POINT('Ctrl Pts',(-75.5596260797355,3.59033450986518,1.28032798093242));
#55366=CARTESIAN_POINT('Ctrl Pts',(-75.3607525480379,0.863816284783001,
3.71262212696513));
#55367=CARTESIAN_POINT('Ctrl Pts',(-75.1618790163406,-2.6563781164081,2.73375143971716));
#55368=CARTESIAN_POINT('Ctrl Pts',(-74.9630054846429,-3.73588684997514,
-0.756895683479796));
#55369=CARTESIAN_POINT('Ctrl Pts',(-74.7641319529457,-1.38285507499101,
-3.55210549858237));
#55370=CARTESIAN_POINT('Ctrl Pts',(-74.5652584212481,2.24074678227322,-3.08363348814666));
#55371=CARTESIAN_POINT('Ctrl Pts',(-74.3663848895507,3.80554589512093,0.218087302738192));
#55372=CARTESIAN_POINT('Ctrl Pts',(-74.1675113578533,1.87380162570858,3.31942903207455));
#55373=CARTESIAN_POINT('Ctrl Pts',(-73.9686378261556,-1.77959542483032,
3.37087255104825));
#55374=CARTESIAN_POINT('Ctrl Pts',(-73.7697642944585,-3.79789654504064,
0.325151448798652));
#55375=CARTESIAN_POINT('Ctrl Pts',(-73.5708907627607,-2.32668252155082,
-3.01931947223166));
#55376=CARTESIAN_POINT('Ctrl Pts',(-73.3720172310635,1.28229218005324,-3.5896334626897));
#55377=CARTESIAN_POINT('Ctrl Pts',(-73.1731436993659,3.71309419372906,-0.861784857132571));
#55378=CARTESIAN_POINT('Ctrl Pts',(-72.9742701676686,2.73229763821218,2.65787344463722));
#55379=CARTESIAN_POINT('Ctrl Pts',(-72.7753966359709,-0.758939597445834,
3.73547216813566));
#55380=CARTESIAN_POINT('Ctrl Pts',(-72.5765231042737,-3.55286157266074,
1.38091139360858));
#55381=CARTESIAN_POINT('Ctrl Pts',(-72.3776495725761,-3.08240703992181,
-2.24243360475354));
#55382=CARTESIAN_POINT('Ctrl Pts',(-72.1787760408787,0.220169410119124,
-3.80542600274073));
#55383=CARTESIAN_POINT('Ctrl Pts',(-71.9799025091812,3.3204537540748,-1.87198517583289));
#55384=CARTESIAN_POINT('Ctrl Pts',(-71.7810289774838,3.36989837098991,1.78143947432599));
#55385=CARTESIAN_POINT('Ctrl Pts',(-71.5821554457863,0.323073445319674,
3.79807387769336));
#55386=CARTESIAN_POINT('Ctrl Pts',(-71.3832819140889,-3.02059202526815,
2.32503020375521));
#55387=CARTESIAN_POINT('Ctrl Pts',(-71.1844083823913,-3.58893134094086,
-1.28425599531399));
#55388=CARTESIAN_POINT('Ctrl Pts',(-70.9855348506941,-0.859753171502819,
-3.71356514896109));
#55389=CARTESIAN_POINT('Ctrl Pts',(-70.7866613189964,2.65936797721959,-2.73084301878126));
#55390=CARTESIAN_POINT('Ctrl Pts',(-70.5877877872991,3.73505636806534,0.760983284219782));
#55391=CARTESIAN_POINT('Ctrl Pts',(-70.3889142556016,1.37896729884392,3.55361658317363));
#55392=CARTESIAN_POINT('Ctrl Pts',(-70.1900407239041,-2.24411975595105,
3.0811796689641));
#55393=CARTESIAN_POINT('Ctrl Pts',(-69.9911671922068,-3.80530497118865,
-0.222251451591354));
#55394=CARTESIAN_POINT('Ctrl Pts',(-69.7922936605092,-1.8701681655698,-3.32147748208183));
#55395=CARTESIAN_POINT('Ctrl Pts',(-69.5934201288118,1.78328299053953,-3.36892318213695));
#55396=CARTESIAN_POINT('Ctrl Pts',(-69.3945465971144,3.79825007337514,-0.320995345127123));
#55397=CARTESIAN_POINT('Ctrl Pts',(-69.1956730654169,2.32337718995098,3.02186367407648));
#55398=CARTESIAN_POINT('Ctrl Pts',(-68.9967995337195,-1.2862194261268,3.58822814482881));
#55399=CARTESIAN_POINT('Ctrl Pts',(-68.7979260020219,-3.71403499252018,
0.85772122850201));
#55400=CARTESIAN_POINT('Ctrl Pts',(-68.5990524703245,-2.7293875818599,-2.66086171370786));
#55401=CARTESIAN_POINT('Ctrl Pts',(-68.4001789386271,0.76302674318989,-3.73463944988864));
#55402=CARTESIAN_POINT('Ctrl Pts',(-68.2013054069296,3.55437052989495,-1.37702279127899));
#55403=CARTESIAN_POINT('Ctrl Pts',(-68.0024318752321,3.07995137564101,2.24580523536093));
#55404=CARTESIAN_POINT('Ctrl Pts',(-67.8035583435348,-0.224333426531556,
3.80518280050091));
#55405=CARTESIAN_POINT('Ctrl Pts',(-67.6046848118372,-3.32250021578923,
1.86835059546325));
#55406=CARTESIAN_POINT('Ctrl Pts',(-67.4058112801399,-3.36794698478127,
-1.78512597291907));
#55407=CARTESIAN_POINT('Ctrl Pts',(-67.2069377484423,-0.318917148843096,
-3.79842513203319));
#55408=CARTESIAN_POINT('Ctrl Pts',(-67.008064216745,3.02313441827591,-2.32172348063307));
#55409=CARTESIAN_POINT('Ctrl Pts',(-66.8091906850474,3.58752387456407,1.28818247190379));
#55410=CARTESIAN_POINT('Ctrl Pts',(-66.61031715335,0.855689028738441,3.71450372426576));
#55411=CARTESIAN_POINT('Ctrl Pts',(-66.4114436216526,-2.66235465365491,
2.72793132788374));
#55412=CARTESIAN_POINT('Ctrl Pts',(-66.212570089955,-3.73422141373034,-0.765069973744436));
#55413=CARTESIAN_POINT('Ctrl Pts',(-66.0136965582577,-1.37507787149593,
-3.555123412599));
#55414=CARTESIAN_POINT('Ctrl Pts',(-65.8148230265601,2.24749004247856,-3.07872216032026));
#55415=CARTESIAN_POINT('Ctrl Pts',(-65.6159494948628,3.80505949071416,0.22641533431646));
#55416=CARTESIAN_POINT('Ctrl Pts',(-65.4170759631652,1.8665324660573,3.32352195489086));
#55417=CARTESIAN_POINT('Ctrl Pts',(-65.2182024314679,-1.78696842091292,
3.36696977921506));
#55418=CARTESIAN_POINT('Ctrl Pts',(-65.0193288997703,-3.79859905361509,
0.316838857089779));
#55419=CARTESIAN_POINT('Ctrl Pts',(-64.8204553680729,-2.32006907629652,
-3.02440425748609));
#55420=CARTESIAN_POINT('Ctrl Pts',(-64.6215818363755,1.29014513205747,-3.5868185303575));
#55421=CARTESIAN_POINT('Ctrl Pts',(-64.422708304678,3.71497134405747,-0.853656572820322));
#55422=CARTESIAN_POINT('Ctrl Pts',(-64.2238347729806,2.72647425728869,2.66384679661379));
#55423=CARTESIAN_POINT('Ctrl Pts',(-64.024961241283,-0.767112975271716,
3.73380225971558));
#55424=CARTESIAN_POINT('Ctrl Pts',(-63.8260877095857,-3.55587523106043,
1.37313254007699));
#55425=CARTESIAN_POINT('Ctrl Pts',(-63.6272141778881,-3.07749202336981,
-2.24917417679972));
#55426=CARTESIAN_POINT('Ctrl Pts',(-63.4283406461908,0.228497174322965,
-3.80493504186522));
#55427=CARTESIAN_POINT('Ctrl Pts',(-63.2294671144933,3.32454269908083,-1.8647137778962));
#55428=CARTESIAN_POINT('Ctrl Pts',(-63.0305935827958,3.36599156573087,1.78881033396948));
#55429=CARTESIAN_POINT('Ctrl Pts',(-62.8317200510984,0.314760470489306,
3.79877183806881));
#55430=CARTESIAN_POINT('Ctrl Pts',(-62.6328465194009,-3.0256731913269,2.31841397743656));
#55431=CARTESIAN_POINT('Ctrl Pts',(-62.4339729877036,-3.58611211242019,
-1.29210740600025));
#55432=CARTESIAN_POINT('Ctrl Pts',(-62.2350994560059,-0.851623861356168,
-3.71543785175534));
#55433=CARTESIAN_POINT('Ctrl Pts',(-62.0362259243087,2.66533814213779,-2.72501637051098));
#55434=CARTESIAN_POINT('Ctrl Pts',(-61.837352392611,3.73338198796987,0.76915574716017));
#55435=CARTESIAN_POINT('Ctrl Pts',(-61.6384788609137,1.37118679760446,3.5566259850542));
#55436=CARTESIAN_POINT('Ctrl Pts',(-61.4396053292161,-2.2508576378202,3.07626096515786));
#55437=CARTESIAN_POINT('Ctrl Pts',(-61.2407317975188,-3.80480945399139,
-0.230578945927754));
#55438=CARTESIAN_POINT('Ctrl Pts',(-61.0418582658212,-1.86289453152446,
-3.32556244805351));
#55439=CARTESIAN_POINT('Ctrl Pts',(-60.8429847341239,1.79065171153737,-3.3650123446216));
#55440=CARTESIAN_POINT('Ctrl Pts',(-60.6441112024263,3.79894348534265,-0.312681989663811));
#55441=CARTESIAN_POINT('Ctrl Pts',(-60.445237670729,2.31675818454863,3.02694121941845));
#55442=CARTESIAN_POINT('Ctrl Pts',(-60.2463641390315,-1.29406929314464,
3.58540462096363));
#55443=CARTESIAN_POINT('Ctrl Pts',(-60.047490607334,-3.71590324721964,0.84959089495461));
#55444=CARTESIAN_POINT('Ctrl Pts',(-59.8486170756366,-2.72355766798716,
-2.6668286897804));
#55445=CARTESIAN_POINT('Ctrl Pts',(-59.6497435439391,0.77119828879821,-3.73296059861904));
#55446=CARTESIAN_POINT('Ctrl Pts',(-59.4508700122417,3.55737567435549,-1.36924064466089));
#55447=CARTESIAN_POINT('Ctrl Pts',(-59.2519964805442,3.07502898605303,2.25254042503595));
#55448=CARTESIAN_POINT('Ctrl Pts',(-59.0531229488468,-0.232660648507626,
3.80468272713029));
#55449=CARTESIAN_POINT('Ctrl Pts',(-58.8542494171493,-3.32658120150376,
1.86107472748661));
#55450=CARTESIAN_POINT('Ctrl Pts',(-58.6553758854518,-3.36403211618028,
-1.79249255306538));
#55451=CARTESIAN_POINT('Ctrl Pts',(-58.4565023537544,-0.310603415235633,
-3.79911399538513));
#55452=CARTESIAN_POINT('Ctrl Pts',(-58.2576288220569,3.02820834138102,-2.3151016981286));
#55453=CARTESIAN_POINT('Ctrl Pts',(-58.0587552903595,3.58469605619972,1.29603079290335));
#55454=CARTESIAN_POINT('Ctrl Pts',(-57.859881758662,0.84755767422402,3.71636753031121));
#55455=CARTESIAN_POINT('Ctrl Pts',(-57.6610082269646,-2.66831843909564,
2.72209815015362));
#55456=CARTESIAN_POINT('Ctrl Pts',(-57.4621346952671,-3.73253809178915,
-0.773240599574607));
#55457=CARTESIAN_POINT('Ctrl Pts',(-57.2632611635696,-1.3672940818287,-3.55812429873996));
#55458=CARTESIAN_POINT('Ctrl Pts',(-57.0643876318723,2.25422253794341,-3.073796086424));
#55459=CARTESIAN_POINT('Ctrl Pts',(-56.8655141001747,3.80455486131976,0.234742281439464));
#55460=CARTESIAN_POINT('Ctrl Pts',(-56.6666405684773,1.85925436632751,3.32759895912643));
#55461=CARTESIAN_POINT('Ctrl Pts',(-56.4677670367798,-1.79433285800241,
3.3630508807005));
#55462=CARTESIAN_POINT('Ctrl Pts',(-56.2688935050825,-3.79928336814536,
0.308524747826809));
#55463=CARTESIAN_POINT('Ctrl Pts',(-56.0700199733849,-2.313444518672,-3.02947455683556));
#55464=CARTESIAN_POINT('Ctrl Pts',(-55.8711464416876,1.29799190468937,-3.58398641834039));
#55465=CARTESIAN_POINT('Ctrl Pts',(-55.67227290999,3.71683070089097,-0.845524199773049));
#55466=CARTESIAN_POINT('Ctrl Pts',(-55.4733993782926,2.7206378174474,2.66980738963741));
#55467=CARTESIAN_POINT('Ctrl Pts',(-55.2745258465951,-0.77528267887785,
3.73211446760674));
#55468=CARTESIAN_POINT('Ctrl Pts',(-55.0756523148976,-3.55887185798348,
1.3653471096907));
#55469=CARTESIAN_POINT('Ctrl Pts',(-54.8767787832002,-3.0725622666399,-2.25590397603884));
#55470=CARTESIAN_POINT('Ctrl Pts',(-54.6779052515027,0.236823844100095,
-3.80442585659819));
#55471=CARTESIAN_POINT('Ctrl Pts',(-54.4790317198054,3.32861572061708,-1.857433448592));
#55472=CARTESIAN_POINT('Ctrl Pts',(-54.2801581881078,3.36206863847578,1.79617262579773));
#55473=CARTESIAN_POINT('Ctrl Pts',(-54.0812846564105,0.306445988059607,
3.7994516035725));
#55474=CARTESIAN_POINT('Ctrl Pts',(-53.8824111247129,-3.03073986540288,
2.31178664667509));
#55475=CARTESIAN_POINT('Ctrl Pts',(-53.6835375930156,-3.58327570759815,
-1.29995262791552));
#55476=CARTESIAN_POINT('Ctrl Pts',(-53.484664061318,-0.843490472210508,
-3.71729275882027));
#55477=CARTESIAN_POINT('Ctrl Pts',(-53.2857905296207,2.67129554096001,-2.71917667030568));
#55478=CARTESIAN_POINT('Ctrl Pts',(-53.086916997923,3.73168972619857,0.777324526096578));
#55479=CARTESIAN_POINT('Ctrl Pts',(-52.8880434662258,1.36339972882987,3.55961835186216));
#55480=CARTESIAN_POINT('Ctrl Pts',(-52.6891699345281,-2.25758473881897,
3.07132752707021));
#55481=CARTESIAN_POINT('Ctrl Pts',(-52.4902964028309,-3.80429571300419,
-0.238905335866445));
#55482=CARTESIAN_POINT('Ctrl Pts',(-52.2914228711333,-1.8556119748251,-3.32963148567123));
#55483=CARTESIAN_POINT('Ctrl Pts',(-52.0925493394359,1.79801185590047,-3.36108538980027));
#55484=CARTESIAN_POINT('Ctrl Pts',(-51.8936758077384,3.79961870161625,-0.304367136556382));
#55485=CARTESIAN_POINT('Ctrl Pts',(-51.694802276041,2.31012808263415,3.03200426670422));
#55486=CARTESIAN_POINT('Ctrl Pts',(-51.4959287443436,-1.30191296199484,
3.58256392418577));
#55487=CARTESIAN_POINT('Ctrl Pts',(-51.297055212646,-3.71775370396079,0.841456492145185));
#55488=CARTESIAN_POINT('Ctrl Pts',(-51.0981816809486,-2.71771470916588,
-2.67278289261786));
#55489=CARTESIAN_POINT('Ctrl Pts',(-50.8993081492511,0.779366140619599,
-3.73126386769187));
#55490=CARTESIAN_POINT('Ctrl Pts',(-50.7004346175537,3.56036378015273,-1.36145193982897));
#55491=CARTESIAN_POINT('Ctrl Pts',(-50.5015610858562,3.07009186808429,2.25926482578078));
#55492=CARTESIAN_POINT('Ctrl Pts',(-50.3026875541588,-0.240986756115434,
3.80416443057663));
#55493=CARTESIAN_POINT('Ctrl Pts',(-50.1038140224613,-3.3306462539848,1.8537899455722));
#55494=CARTESIAN_POINT('Ctrl Pts',(-49.9049404907639,-3.36010113496832,
-1.79985054776005));
#55495=CARTESIAN_POINT('Ctrl Pts',(-49.7060669590664,-0.302288193939447,
-3.79978466222657));
#55496=CARTESIAN_POINT('Ctrl Pts',(-49.507193427369,3.03326776036106,-2.30846882704571));
#55497=CARTESIAN_POINT('Ctrl Pts',(-49.3083198956714,3.58185106831631,1.3038729063405));
#55498=CARTESIAN_POINT('Ctrl Pts',(-49.1094463639741,0.839422260186034,
3.71821353617451));
#55499=CARTESIAN_POINT('Ctrl Pts',(-48.9105728322766,-2.6742694441658,2.71625193446565));
#55500=CARTESIAN_POINT('Ctrl Pts',(-48.7116993005792,-3.73083689221413,
-0.781407521835786));
#55501=CARTESIAN_POINT('Ctrl Pts',(-48.5128257688817,-1.35950374327106,
-3.56110814263194));
#55502=CARTESIAN_POINT('Ctrl Pts',(-48.3139522371842,2.26094423642121,-3.06885529005218));
#55503=CARTESIAN_POINT('Ctrl Pts',(-48.1150787054868,3.80403200935488,0.243068104223925));
#55504=CARTESIAN_POINT('Ctrl Pts',(-47.9162051737893,1.85196736137869,3.33166002525401));
#55505=CARTESIAN_POINT('Ctrl Pts',(-47.7173316420919,-1.80168870082603,
3.35911587427456));
#55506=CARTESIAN_POINT('Ctrl Pts',(-47.5184581103944,-3.79994948535379,
0.300209160831137));
#55507=CARTESIAN_POINT('Ctrl Pts',(-47.319584578697,-2.30680888040646,-3.0345303459951));
#55508=CARTESIAN_POINT('Ctrl Pts',(-47.1207110469995,1.30583246036561,-3.5811371402032));
#55509=CARTESIAN_POINT('Ctrl Pts',(-46.9218375153022,3.71867225532388,-0.837387776942048));
#55510=CARTESIAN_POINT('Ctrl Pts',(-46.7229639836046,2.71478834664286,2.67575519515887));
#55511=CARTESIAN_POINT('Ctrl Pts',(-46.5240904519072,-0.783448669134082,
3.73040879989306));
#55512=CARTESIAN_POINT('Ctrl Pts',(-46.3252169202097,-3.56185143907695,
1.35755513973942));
#55513=CARTESIAN_POINT('Ctrl Pts',(-46.1263433885122,-3.06761779334405,
-2.26262297023752));
#55514=CARTESIAN_POINT('Ctrl Pts',(-45.9274698568148,0.245149379568856,
-3.80389844937855));
#55515=CARTESIAN_POINT('Ctrl Pts',(-45.7285963251173,3.33267279917539,-1.8501442227902));
#55516=CARTESIAN_POINT('Ctrl Pts',(-45.5297227934199,3.35812960801393,1.80352631454818));
#55517=CARTESIAN_POINT('Ctrl Pts',(-45.3308492617224,0.298130037853896,
3.80011317094853));
#55518=CARTESIAN_POINT('Ctrl Pts',(-45.131975730025,-3.03579202322847,2.30514824321336));
#55519=CARTESIAN_POINT('Ctrl Pts',(-44.9331021983275,-3.58042214006016,
-1.30779162348385));
#55520=CARTESIAN_POINT('Ctrl Pts',(-44.7342286666301,-0.835353043022,-3.7191298612715));
#55521=CARTESIAN_POINT('Ctrl Pts',(-44.5353551349326,2.67724014515226,-2.71332394613555));
#55522=CARTESIAN_POINT('Ctrl Pts',(-44.3364816032351,3.72997959085687,0.785489581903391));
#55523=CARTESIAN_POINT('Ctrl Pts',(-44.1376080715378,1.35560612981737,3.56259366926528));
#55524=CARTESIAN_POINT('Ctrl Pts',(-43.9387345398402,-2.2643010267272,3.06637937833035));
#55525=CARTESIAN_POINT('Ctrl Pts',(-43.7398610081428,-3.80376375068764,
-0.247230581527181));
#55526=CARTESIAN_POINT('Ctrl Pts',(-43.5409874764454,-1.84832053035247,
-3.33368457544577));
#55527=CARTESIAN_POINT('Ctrl Pts',(-43.3421139447478,1.80536338837631,-3.35714233648167));
#55528=CARTESIAN_POINT('Ctrl Pts',(-43.1432404130505,3.80027571896185,-0.296050825630079));
#55529=CARTESIAN_POINT('Ctrl Pts',(-42.944366881353,2.30348691596348,3.03705279168351));
#55530=CARTESIAN_POINT('Ctrl Pts',(-42.7454933496556,-1.30975039510868,
3.57970606810114));
#55531=CARTESIAN_POINT('Ctrl Pts',(-42.546619817958,-3.71958635388042,0.833318059035165));
#55532=CARTESIAN_POINT('Ctrl Pts',(-42.3477462862607,-2.71185873338217,
-2.67872429370146));
#55533=CARTESIAN_POINT('Ctrl Pts',(-42.1488727545632,0.787530259532762,
-3.72954926523403));
#55534=CARTESIAN_POINT('Ctrl Pts',(-41.9499992228658,3.56333483297472,-1.35365671408838));
#55535=CARTESIAN_POINT('Ctrl Pts',(-41.7511256911682,3.06514004538181,2.2659784053879));
#55536=CARTESIAN_POINT('Ctrl Pts',(-41.5522521594708,-0.249311709475826,
3.80362791332241));
#55537=CARTESIAN_POINT('Ctrl Pts',(-41.3533786277734,-3.33469535376215,
1.84649628461158));
#55538=CARTESIAN_POINT('Ctrl Pts',(-41.154505096076,-3.35615405997345,-1.80719992176053));
#55539=CARTESIAN_POINT('Ctrl Pts',(-40.9556315643784,-0.293971524782049,
-3.8004371293451));
#55540=CARTESIAN_POINT('Ctrl Pts',(-40.7567580326811,3.03831265098276,-2.30182489915407));
#55541=CARTESIAN_POINT('Ctrl Pts',(-40.5578845009835,3.57898892454058,1.31170877465366));
#55542=CARTESIAN_POINT('Ctrl Pts',(-40.3590109692861,0.831282825590706,
3.72004173301395));
#55543=CARTESIAN_POINT('Ctrl Pts',(-40.1601374375886,-2.68020764036213,
2.71039270882136));
#55544=CARTESIAN_POINT('Ctrl Pts',(-39.9612639058912,-3.7291178231534,-0.789570701411317));
#55545=CARTESIAN_POINT('Ctrl Pts',(-39.7623903741938,-1.35170689313597,
-3.56407492998341));
#55546=CARTESIAN_POINT('Ctrl Pts',(-39.5635168424963,2.2676551057174,-3.06389979486944));
#55547=CARTESIAN_POINT('Ctrl Pts',(-39.3646433107988,3.80349093732365,0.251392762791839));
#55548=CARTESIAN_POINT('Ctrl Pts',(-39.1657697791013,1.84467148611344,3.33570513382216));
#55549=CARTESIAN_POINT('Ctrl Pts',(-38.966896247404,-1.80903591415121,3.35516477878489));
#55550=CARTESIAN_POINT('Ctrl Pts',(-38.7680227157065,-3.8005974020499,0.291892135932223));
#55551=CARTESIAN_POINT('Ctrl Pts',(-38.569149184009,-2.30016219328273,-3.03957160074908));
#55552=CARTESIAN_POINT('Ctrl Pts',(-38.3702756523116,1.31366676153256,-3.57827070959312));
#55553=CARTESIAN_POINT('Ctrl Pts',(-38.1714021206141,3.7204959985358,-0.829247343297895));
#55554=CARTESIAN_POINT('Ctrl Pts',(-37.9725285889167,2.70892587289195,2.68169018469027));
#55555=CARTESIAN_POINT('Ctrl Pts',(-37.7736550572192,-0.791610906928228,
3.7286852647441));
#55556=CARTESIAN_POINT('Ctrl Pts',(-37.5747815255217,-3.56481396006973,
1.34975666754391));
#55557=CARTESIAN_POINT('Ctrl Pts',(-37.3759079938243,-3.06265862716454,
-2.26933112721388));
#55558=CARTESIAN_POINT('Ctrl Pts',(-37.1770344621268,0.253473740852287,
-3.80335282273231));
#55559=CARTESIAN_POINT('Ctrl Pts',(-36.9781609304294,3.33671391532343,-1.84284613540428));
#55560=CARTESIAN_POINT('Ctrl Pts',(-36.7792873987319,3.35417449321223,1.81087136499863));
#55561=CARTESIAN_POINT('Ctrl Pts',(-36.5804138670345,0.289812659703135,
3.80075653702829));
#55562=CARTESIAN_POINT('Ctrl Pts',(-36.381540335337,-3.04082964060558,2.29849879884721));
#55563=CARTESIAN_POINT('Ctrl Pts',(-36.1826668036395,-3.57755142347379,
-1.31562435515925));
#55564=CARTESIAN_POINT('Ctrl Pts',(-35.9837932719421,-0.827211612766053,
-3.72094915030997));
#55565=CARTESIAN_POINT('Ctrl Pts',(-35.7849197402446,2.68317192624198,-2.70745822603308));
#55566=CARTESIAN_POINT('Ctrl Pts',(-35.5860462085473,3.72825159013562,0.793650875472599));
#55567=CARTESIAN_POINT('Ctrl Pts',(-35.3871726768497,1.34780603789606,3.56555192301254));
#55568=CARTESIAN_POINT('Ctrl Pts',(-35.1882991451524,-2.27100646937564,
3.06141654263865));
#55569=CARTESIAN_POINT('Ctrl Pts',(-34.9894256134548,-3.80321356958969,
-0.255554643034271));
#55570=CARTESIAN_POINT('Ctrl Pts',(-34.7905520817575,-1.84102023303062,
-3.33772169796395));
#55571=CARTESIAN_POINT('Ctrl Pts',(-34.5916785500599,1.81270627375333,-3.35318320355194));
#55572=CARTESIAN_POINT('Ctrl Pts',(-34.3928050183625,3.80091453423265,-0.287733096717287));
#55573=CARTESIAN_POINT('Ctrl Pts',(-34.193931486665,2.29683471634544,3.04208677017568));
#55574=CARTESIAN_POINT('Ctrl Pts',(-33.9950579549676,-1.3175815549477,3.5768310663979));
#55575=CARTESIAN_POINT('Ctrl Pts',(-33.7961844232701,-3.72140118820076,
0.825175634604654));
#55576=CARTESIAN_POINT('Ctrl Pts',(-33.5973108915727,-2.70598976868411,
-2.68465286457377));
#55577=CARTESIAN_POINT('Ctrl Pts',(-33.3984373598752,0.795690606434006,
-3.72781679945786));
#55578=CARTESIAN_POINT('Ctrl Pts',(-33.1995638281778,3.56628881859093,-1.34585500477608));
#55579=CARTESIAN_POINT('Ctrl Pts',(-33.0006902964803,3.06017354166348,2.27268113170112));
#55580=CARTESIAN_POINT('Ctrl Pts',(-32.8018167647829,-0.257635468714778,
3.8030731779375));
#55581=CARTESIAN_POINT('Ctrl Pts',(-32.6029432330854,-3.33872848144206,
1.83919377953904));
#55582=CARTESIAN_POINT('Ctrl Pts',(-32.4040697013879,-3.35219091010075,
-1.81454063986603));
#55583=CARTESIAN_POINT('Ctrl Pts',(-32.2051961696905,-0.285653447597213,
-3.80107139361567));
#55584=CARTESIAN_POINT('Ctrl Pts',(-32.0063226379931,3.04334298908304,-2.29516994627558));
#55585=CARTESIAN_POINT('Ctrl Pts',(-31.8074491062956,3.57610963858108,1.31953836031194));
#55586=CARTESIAN_POINT('Ctrl Pts',(-31.6085755745982,0.823139409423143,
3.72185211207294));
#55587=CARTESIAN_POINT('Ctrl Pts',(-31.4097020429007,-2.68613299924237,
2.7045205012846));
#55588=CARTESIAN_POINT('Ctrl Pts',(-31.2108285112032,-3.72738089284084,
-0.797730099201816));
#55589=CARTESIAN_POINT('Ctrl Pts',(-31.0119549795058,-1.34390356876819,
-3.56702464658427));
#55590=CARTESIAN_POINT('Ctrl Pts',(-30.8130814478083,2.27435511368902,-3.05892962461122));
#55591=CARTESIAN_POINT('Ctrl Pts',(-30.6142079161109,3.80293164781777,0.259716217270925));
#55592=CARTESIAN_POINT('Ctrl Pts',(-30.4153343844134,1.83736677547631,3.33973426545636));
#55593=CARTESIAN_POINT('Ctrl Pts',(-30.216460852716,-1.81637446278761,3.35119761315571));
#55594=CARTESIAN_POINT('Ctrl Pts',(-30.0175873210184,-3.80122711513034,
0.283573712965513));
#55595=CARTESIAN_POINT('Ctrl Pts',(-29.8187137893211,-2.29350448913609,
-3.04459829695148));
#55596=CARTESIAN_POINT('Ctrl Pts',(-29.6198402576236,1.32149477066622,-3.57538714023941));
#55597=CARTESIAN_POINT('Ctrl Pts',(-29.4209667259261,3.72230192179151,-0.821102937831022));
#55598=CARTESIAN_POINT('Ctrl Pts',(-29.2220931942287,2.70305042427431,2.68761232980465));
#55599=CARTESIAN_POINT('Ctrl Pts',(-29.0232196625312,-0.799769353165428,
3.72694387041513));
#55600=CARTESIAN_POINT('Ctrl Pts',(-28.8243461308338,-3.5677594067723,1.34195173045655));
#55601=CARTESIAN_POINT('Ctrl Pts',(-28.6254725991363,-3.05768479185423,
-2.27602841483819));
#55602=CARTESIAN_POINT('Ctrl Pts',(-28.4265990674389,0.261796888079818,
-3.80278897927288));
#55603=CARTESIAN_POINT('Ctrl Pts',(-28.2277255357414,3.34073904970577,-1.83553922138932));
#55604=CARTESIAN_POINT('Ctrl Pts',(-28.028852004044,3.35020331301418,1.81820774196901));
#55605=CARTESIAN_POINT('Ctrl Pts',(-27.8299784723465,0.281493893444737,
3.80138169873015));
#55606=CARTESIAN_POINT('Ctrl Pts',(-27.6311049406491,-3.04585269340545,
2.2918383454254));
#55607=CARTESIAN_POINT('Ctrl Pts',(-27.4322314089516,-3.57466357158898,
-1.32345078542506));
#55608=CARTESIAN_POINT('Ctrl Pts',(-27.2333578772542,-0.819066220437877,
-3.72275061722178));
#55609=CARTESIAN_POINT('Ctrl Pts',(-27.0344843455567,2.68909085581776,-2.70157953809338));
#55610=CARTESIAN_POINT('Ctrl Pts',(-26.8356108138592,3.72650573231153,0.801808367714392));
#55611=CARTESIAN_POINT('Ctrl Pts',(-26.6367372821618,1.33999949042545,3.56849309893504));
#55612=CARTESIAN_POINT('Ctrl Pts',(-26.4378637504643,-2.27770103464773,
3.05643904376517));
#55613=CARTESIAN_POINT('Ctrl Pts',(-26.2389902187669,-3.80264517234552,
-0.263877480518609));
#55614=CARTESIAN_POINT('Ctrl Pts',(-26.0401166870694,-1.83371111782523,
-3.34174283388943));
#55615=CARTESIAN_POINT('Ctrl Pts',(-25.841243155372,1.82004047686151,-3.34920800997384));
#55616=CARTESIAN_POINT('Ctrl Pts',(-25.6423696236745,3.80153514436882,-0.279413989657449));
#55617=CARTESIAN_POINT('Ctrl Pts',(-25.4434960919771,2.29017151564223,3.04710617806936));
#55618=CARTESIAN_POINT('Ctrl Pts',(-25.2446225602796,-1.32540640400279,
3.57393893284649));
#55619=CARTESIAN_POINT('Ctrl Pts',(-25.0457490285822,-3.72319819822944,
0.817029257853469));
#55620=CARTESIAN_POINT('Ctrl Pts',(-24.8468754968847,-2.70010784318212,
-2.69056857683908));
#55621=CARTESIAN_POINT('Ctrl Pts',(-24.6480019651872,0.803847142238303,
-3.72606647866122));
#55622=CARTESIAN_POINT('Ctrl Pts',(-24.4491284334898,3.56922572285289,-1.33804684925931));
#55623=CARTESIAN_POINT('Ctrl Pts',(-24.2502549017923,3.05519238071696,2.27937297261687));
#55624=CARTESIAN_POINT('Ctrl Pts',(-24.0513813700949,-0.265957993964293,
3.80250022707872));
#55625=CARTESIAN_POINT('Ctrl Pts',(-23.8525078383974,-3.34274561770695,
1.83188246533136));
#55626=CARTESIAN_POINT('Ctrl Pts',(-23.6536343067,-3.34821170433262,-1.82187266691653));
#55627=CARTESIAN_POINT('Ctrl Pts',(-23.4547607750025,-0.277334002226216,
-3.80168745200032));
#55628=CARTESIAN_POINT('Ctrl Pts',(-23.2558872433051,3.04835875056794,-2.28850400028564));
#55629=CARTESIAN_POINT('Ctrl Pts',(-23.0570137116076,3.57321322422885,1.32736162581399));
#55630=CARTESIAN_POINT('Ctrl Pts',(-22.8581401799102,0.814992050687579,
3.7236446646805));
#55631=CARTESIAN_POINT('Ctrl Pts',(-22.6592666482127,-2.69204549242627,
2.69863533998111));
#55632=CARTESIAN_POINT('Ctrl Pts',(-22.4603931165153,-3.72562610959568,
-0.80588567612687));
#55633=CARTESIAN_POINT('Ctrl Pts',(-22.2615195848178,-1.33609380754272,
-3.56995727830645));
#55634=CARTESIAN_POINT('Ctrl Pts',(-22.0626460531204,2.28104422824517,-3.05394480308283));
#55635=CARTESIAN_POINT('Ctrl Pts',(-21.8637725214229,3.80235414351597,0.268038427794315));
#55636=CARTESIAN_POINT('Ctrl Pts',(-21.6648989897255,1.83005326445484,3.34374740085816));
#55637=CARTESIAN_POINT('Ctrl Pts',(-21.466025458028,-1.82370431158557,3.34721439638869));
#55638=CARTESIAN_POINT('Ctrl Pts',(-21.2671519263306,-3.80183862157912,
0.275253931773772));
#55639=CARTESIAN_POINT('Ctrl Pts',(-21.0682783946331,-2.28683579985479,
-3.04961041052624));
#55640=CARTESIAN_POINT('Ctrl Pts',(-20.8694048629357,1.32931645027334,-3.57248644595332));
#55641=CARTESIAN_POINT('Ctrl Pts',(-20.6705313312382,3.72409001644133,-0.812954599550049));
#55642=CARTESIAN_POINT('Ctrl Pts',(-20.4716577995407,2.69716202893111,2.69352160213719));
#55643=CARTESIAN_POINT('Ctrl Pts',(-20.2727842678433,-0.807923968769751,
3.72518462524672));
#55644=CARTESIAN_POINT('Ctrl Pts',(-20.0739107361458,-3.57068776507683,
1.33414036586029));
#55645=CARTESIAN_POINT('Ctrl Pts',(-19.8750372044484,-3.05269631123622,
-2.28271480103238));
#55646=CARTESIAN_POINT('Ctrl Pts',(-19.6761636727509,0.270118781385866,
-3.80220692170089));
#55647=CARTESIAN_POINT('Ctrl Pts',(-19.4772901410535,3.34474818304312,-1.82822351574342));
#55648=CARTESIAN_POINT('Ctrl Pts',(-19.278416609356,3.34621608644065,1.82553541032031));
#55649=CARTESIAN_POINT('Ctrl Pts',(-19.0795430776586,0.27317377892279,3.80198865305994));
#55650=CARTESIAN_POINT('Ctrl Pts',(-18.8806695459611,-3.05086115756956,
2.28516691484908));
#55651=CARTESIAN_POINT('Ctrl Pts',(-18.6817960142636,-3.57175859823745,
-1.33127087679568));
#55652=CARTESIAN_POINT('Ctrl Pts',(-18.4829224825662,-0.810916905050859,
-3.72453425337853));
#55653=CARTESIAN_POINT('Ctrl Pts',(-18.2840489508687,2.69499690552984,-2.69568791047329));
#55654=CARTESIAN_POINT('Ctrl Pts',(-18.0851754191713,3.72474202574661,0.809962019556789));
#55655=CARTESIAN_POINT('Ctrl Pts',(-17.8863018874738,1.33218652479678,3.57141718294536));
#55656=CARTESIAN_POINT('Ctrl Pts',(-17.6874283557764,-2.28438469047839,
3.05144690555078));
#55657=CARTESIAN_POINT('Ctrl Pts',(-17.4885548240789,-3.80205856167758,
-0.272199054116103));
#55658=CARTESIAN_POINT('Ctrl Pts',(-17.2896812923814,-1.82639321974484,
-3.34574796396226));
#55659=CARTESIAN_POINT('Ctrl Pts',(-17.0908077606841,1.82736596257257,-3.34521677478736));
#55660=CARTESIAN_POINT('Ctrl Pts',(-16.8919342289865,3.8021375463979,-0.271093544295971));
#55661=CARTESIAN_POINT('Ctrl Pts',(-16.6930606972891,2.28349734576807,3.05211099132349));
#55662=CARTESIAN_POINT('Ctrl Pts',(-16.4941871655916,-1.33322490479584,
3.57102968129913));
#55663=CARTESIAN_POINT('Ctrl Pts',(-16.2953136338942,-3.72497737535923,
0.808878967799967));
#55664=CARTESIAN_POINT('Ctrl Pts',(-16.0964401021967,-2.69421298504881,
-2.6964714021628));
#55665=CARTESIAN_POINT('Ctrl Pts',(-15.8975665704993,0.811999827878098,
-3.7242983112277));
#55666=CARTESIAN_POINT('Ctrl Pts',(-15.6986930388018,3.57214553169364,-1.33023228493699));
#55667=CARTESIAN_POINT('Ctrl Pts',(-15.4998195071044,3.05019658640061,2.28605389608329));
#55668=CARTESIAN_POINT('Ctrl Pts',(-15.3009459754069,-0.274279245362296,
3.80190906349047));
#55669=CARTESIAN_POINT('Ctrl Pts',(-15.1020724437095,-3.34674674331627,
1.824562377007));
#55670=CARTESIAN_POINT('Ctrl Pts',(-14.903198912012,-3.34421646172796,-1.82919596779439));
#55671=CARTESIAN_POINT('Ctrl Pts',(-14.7043253803146,-0.269013228516049,
-3.80228530154838));
#55672=CARTESIAN_POINT('Ctrl Pts',(-14.5054518486171,3.05335991141382,-2.28182709311162));
#55673=CARTESIAN_POINT('Ctrl Pts',(-14.3065783169197,3.5702996953566,1.33517853368896));
#55674=CARTESIAN_POINT('Ctrl Pts',(-14.1077047852222,0.806840788407417,
3.72541938225076));
#55675=CARTESIAN_POINT('Ctrl Pts',(-13.9088312535248,-2.69794509159463,
2.69273725309915));
#55676=CARTESIAN_POINT('Ctrl Pts',(-13.7099577218273,-3.72385348182286,
-0.8140373931235));
#55677=CARTESIAN_POINT('Ctrl Pts',(-13.5110841901299,-1.32827764686602,
-3.57287281110364));
#55678=CARTESIAN_POINT('Ctrl Pts',(-13.3122106584324,2.28772241734737,-3.04894535415999));
#55679=CARTESIAN_POINT('Ctrl Pts',(-13.113337126735,3.80175842718431,0.276359354501727));
#55680=CARTESIAN_POINT('Ctrl Pts',(-12.9144635950375,1.82273098807798,3.34774452080618));
#55681=CARTESIAN_POINT('Ctrl Pts',(-12.7155900633401,-1.83102542543786,
3.3432151475619));
#55682=CARTESIAN_POINT('Ctrl Pts',(-12.5167165316426,-3.80243191846715,
0.266932832205924));
#55683=CARTESIAN_POINT('Ctrl Pts',(-12.3178429999452,-2.28015615737979,
-3.05460791746674));
#55684=CARTESIAN_POINT('Ctrl Pts',(-12.1189694682477,1.33713176289026,-3.56956864062838));
#55685=CARTESIAN_POINT('Ctrl Pts',(-11.9200959365502,3.72586027392076,-0.804802367483259));
#55686=CARTESIAN_POINT('Ctrl Pts',(-11.7212224048527,2.69126071506615,2.6994179733841));
#55687=CARTESIAN_POINT('Ctrl Pts',(-11.5223488731553,-0.816074714683047,
3.72340753766527));
#55688=CARTESIAN_POINT('Ctrl Pts',(-11.3234753414579,-3.57359902095764,
1.32632261116899));
#55689=CARTESIAN_POINT('Ctrl Pts',(-11.1246018097604,-3.04769320920348,
-2.28939025377118));
#55690=CARTESIAN_POINT('Ctrl Pts',(-10.925728278063,0.278439380911714,-3.80160665280418));
#55691=CARTESIAN_POINT('Ctrl Pts',(-10.7268547463655,3.34874129613322,-1.82089905350606));
#55692=CARTESIAN_POINT('Ctrl Pts',(-10.5279812146681,3.34221283258897,1.83285433495541));
#55693=CARTESIAN_POINT('Ctrl Pts',(-10.3291076829706,0.264852355988142,
3.80257739711041));
#55694=CARTESIAN_POINT('Ctrl Pts',(-10.1302341512731,-3.05585500910874,
2.27848453907253));
#55695=CARTESIAN_POINT('Ctrl Pts',(-9.93136061957569,-3.56883651733323,
-1.33908459181509));
#55696=CARTESIAN_POINT('Ctrl Pts',(-9.73248708787821,-0.80276370563772,
-3.72630005023728));
#55697=CARTESIAN_POINT('Ctrl Pts',(-9.53361355618079,2.70089004709043,-2.68978337139171));
#55698=CARTESIAN_POINT('Ctrl Pts',(-9.33474002448332,3.72296047888839,0.818111791946939));
#55699=CARTESIAN_POINT('Ctrl Pts',(-9.13586649278587,1.32436717843105,3.5743241610383));
#55700=CARTESIAN_POINT('Ctrl Pts',(-8.9369929610884,-2.29105740485551,3.04644015190587));
#55701=CARTESIAN_POINT('Ctrl Pts',(-8.73811942939098,-3.80145374039546,
-0.280519323969575));
#55702=CARTESIAN_POINT('Ctrl Pts',(-8.53924589769349,-1.81906657383958,
-3.34973706899915));
#55703=CARTESIAN_POINT('Ctrl Pts',(-8.34037236599607,1.83468269579965,-3.34120951710917));
#55704=CARTESIAN_POINT('Ctrl Pts',(-8.14149883429859,3.80272173743456,-0.262771800485379));
#55705=CARTESIAN_POINT('Ctrl Pts',(-7.94262530260113,2.27681223869029,3.05710118596646));
#55706=CARTESIAN_POINT('Ctrl Pts',(-7.74375177090369,-1.34103701987869,
3.5681033256903));
#55707=CARTESIAN_POINT('Ctrl Pts',(-7.54487823920625,-3.72673871106872,
0.800724803481259));
#55708=CARTESIAN_POINT('Ctrl Pts',(-7.34600470750877,-2.68830522251812,
-2.70236131227278));
#55709=CARTESIAN_POINT('Ctrl Pts',(-7.14713117581134,0.820148624304898,
-3.72251230562602));
#55710=CARTESIAN_POINT('Ctrl Pts',(-6.94825764411385,3.57504823112902,-1.32241134923795));
#55711=CARTESIAN_POINT('Ctrl Pts',(-6.74938411241644,3.04518618264129,2.29272387010146));
#55712=CARTESIAN_POINT('Ctrl Pts',(-6.55051058071893,-0.282599183050784,
3.80129969000349));
#55713=CARTESIAN_POINT('Ctrl Pts',(-6.35163704902152,-3.35073183910972,
1.8172335496281));
#55714=CARTESIAN_POINT('Ctrl Pts',(-6.15276351732402,-3.34020520141543,
-1.83651050742555));
#55715=CARTESIAN_POINT('Ctrl Pts',(-5.9538899856266,-0.260691166334333,
-3.80286493939216));
#55716=CARTESIAN_POINT('Ctrl Pts',(-5.75501645392915,3.05834644769266,-2.27513925674164));
#55717=CARTESIAN_POINT('Ctrl Pts',(-5.5561429222317,3.56736906587033,1.34298904651157));
#55718=CARTESIAN_POINT('Ctrl Pts',(-5.35726939053425,0.798685661716399,
3.72717625625544));
#55719=CARTESIAN_POINT('Ctrl Pts',(-5.15839585883678,-2.70383176866502,
2.68682626894128));
#55720=CARTESIAN_POINT('Ctrl Pts',(-4.95952232713934,-3.72206301768338,
-0.822185211248298));
#55721=CARTESIAN_POINT('Ctrl Pts',(-4.76064879544187,-1.32045512479611,
-3.57577123082234));
#55722=CARTESIAN_POINT('Ctrl Pts',(-4.56177526374442,2.29438965018289,-3.04393130214526));
#55723=CARTESIAN_POINT('Ctrl Pts',(-4.36290173204696,3.80114449946005,0.284678958212554));
#55724=CARTESIAN_POINT('Ctrl Pts',(-4.1640282003495,1.81539998560147,3.35172560488281));
#55725=CARTESIAN_POINT('Ctrl Pts',(-3.96515466865207,-1.83833777717959,
3.33919988823347));
#55726=CARTESIAN_POINT('Ctrl Pts',(-3.76628113695461,-3.80300698803449,
0.258610449579765));
#55727=CARTESIAN_POINT('Ctrl Pts',(-3.56740760525717,-2.27346562187304,
-3.05959078526946));
#55728=CARTESIAN_POINT('Ctrl Pts',(-3.3685340735597,1.34494072427348,-3.56663375441676));
#55729=CARTESIAN_POINT('Ctrl Pts',(-3.16966054186226,3.72761258531972,-0.796646250131117));
#55730=CARTESIAN_POINT('Ctrl Pts',(-2.97078701016478,2.685346700579,2.70530135762789));
#55731=CARTESIAN_POINT('Ctrl Pts',(-2.77191347846734,-0.824221909934967,
3.72161272508666));
#55732=CARTESIAN_POINT('Ctrl Pts',(-2.57303994676988,-3.57649248436405,
1.31849829819329));
#55733=CARTESIAN_POINT('Ctrl Pts',(-2.37416641507242,-3.04267678634614,
-2.29605435280299));
#55734=CARTESIAN_POINT('Ctrl Pts',(-2.175292883375,0.286761057335244,-3.80098890860613));
#55735=CARTESIAN_POINT('Ctrl Pts',(-1.97641935167752,3.35271381827749,-1.813564485426));
#55736=CARTESIAN_POINT('Ctrl Pts',(-1.77754581998009,3.33820216492901,1.84016186691663));
#55737=CARTESIAN_POINT('Ctrl Pts',(-1.57867228828261,0.256513436717102,
3.8031528636426));
#55738=CARTESIAN_POINT('Ctrl Pts',(-1.37979875658517,-3.06080358273695,
2.2717819307131));
#55739=CARTESIAN_POINT('Ctrl Pts',(-1.1809252248877,-3.5659552001554,-1.3468742960899));
#55740=CARTESIAN_POINT('Ctrl Pts',(-0.982051693190254,-0.794497413703714,
-3.72808122654754));
#55741=CARTESIAN_POINT('Ctrl Pts',(-0.783178161492791,2.70656396064839,
-2.6838032048931));
#55742=CARTESIAN_POINT('Ctrl Pts',(-0.584304629795337,3.72155070290039,
0.826139135082401));
#55743=CARTESIAN_POINT('Ctrl Pts',(-0.385431098097896,1.31580516862223,
3.57743809331671));
#55744=CARTESIAN_POINT('Ctrl Pts',(-0.186557566400446,-2.29632333640214,
3.0409932439337));
#55745=CARTESIAN_POINT('Ctrl Pts',(0.0123159652970102,-3.80351113009631,
-0.28801457243628));
#55746=CARTESIAN_POINT('Ctrl Pts',(0.211189496994464,-1.80630503125545,
-3.35542702025725));
#55747=CARTESIAN_POINT('Ctrl Pts',(0.343771851459434,0.617181736105881,
-3.34041968432337));
#55748=CARTESIAN_POINT('Ctrl Pts',(0.410063028691923,1.55734592416847,-2.82148741534955));
#55749=CARTESIAN_POINT('',(0.,1.90056365518826,-3.44330463255539));
#55750=CARTESIAN_POINT('Ctrl Pts',(-3.33066907387547E-15,-3.22795401163284,
-0.0459738408030351));
#55751=CARTESIAN_POINT('Ctrl Pts',(-4.69857332999488E-15,-3.23446946289896,
-0.112579638718265));
#55752=CARTESIAN_POINT('Ctrl Pts',(2.81156677457225E-14,-3.23875117277606,
-0.179298023073995));
#55753=CARTESIAN_POINT('Ctrl Pts',(2.14273043752655E-14,-3.24075548586217,
-0.246033167079983));
#55754=CARTESIAN_POINT('Ctrl Pts',(1.11493109045283E-14,-3.24383550943018,
-0.348584917989921));
#55755=CARTESIAN_POINT('Ctrl Pts',(-1.17848145713982E-14,-3.24154057034996,
-0.45117578255498));
#55756=CARTESIAN_POINT('Ctrl Pts',(-8.99280649946377E-15,-3.2341405851747,
-0.553505501924448));
#55757=CARTESIAN_POINT('Ctrl Pts',(-7.22947464868693E-15,-3.22946702076564,
-0.61813327118452));
#55758=CARTESIAN_POINT('Ctrl Pts',(1.45550265953282E-14,-3.22275614360847,
-0.682657225405645));
#55759=CARTESIAN_POINT('Ctrl Pts',(1.34336985979644E-14,-3.21406567034608,
-0.747003854712476));
#55760=CARTESIAN_POINT('Ctrl Pts',(1.27129131778372E-14,-3.20847946681219,
-0.788365626065484));
#55761=CARTESIAN_POINT('Ctrl Pts',(2.21527997058171E-14,-3.20207516116718,
-0.829654156267173));
#55762=CARTESIAN_POINT('Ctrl Pts',(2.13717932240343E-14,-3.19486642441298,
-0.870850049402691));
#55763=CARTESIAN_POINT('Ctrl Pts',(2.10197089137425E-14,-3.19161666507374,
-0.889421505542671));
#55764=CARTESIAN_POINT('Ctrl Pts',(5.32010578988216E-15,-3.18820341775595,
-0.907973609936308));
#55765=CARTESIAN_POINT('Ctrl Pts',(6.93889390390723E-15,-3.18463068805892,
-0.926491266493227));
#55766=CARTESIAN_POINT('Ctrl Pts',(1.60458093774972E-14,-3.16453136370697,
-1.03066718153223));
#55767=CARTESIAN_POINT('Ctrl Pts',(2.31518269366155E-14,-3.13937025133027,
-1.1338608875346));
#55768=CARTESIAN_POINT('Ctrl Pts',(2.06501482580279E-14,-3.10942517663483,
-1.23575703823851));
#55769=CARTESIAN_POINT('Ctrl Pts',(1.8264438306287E-14,-3.08086824671493,
-1.33292965391417));
#55770=CARTESIAN_POINT('Ctrl Pts',(3.2855666700314E-14,-3.04796004332544,
-1.42892285724832));
#55771=CARTESIAN_POINT('Ctrl Pts',(3.14748227481232E-14,-3.0108994941223,
-1.52346659323359));
#55772=CARTESIAN_POINT('Ctrl Pts',(3.08707035190397E-14,-2.99468550384592,
-1.56482947772715));
#55773=CARTESIAN_POINT('Ctrl Pts',(-7.34111328475694E-15,-2.97767621882812,
-1.6059149164074));
#55774=CARTESIAN_POINT('Ctrl Pts',(-1.09356967925578E-14,-2.95988598833869,
-1.6467000642202));
#55775=CARTESIAN_POINT('Ctrl Pts',(-1.26060361330382E-14,-2.9516191830751,
-1.66565220060851));
#55776=CARTESIAN_POINT('Ctrl Pts',(-3.86060504933494E-15,-2.94318372929767,
-1.68453949171188));
#55777=CARTESIAN_POINT('Ctrl Pts',(-3.77475828372553E-15,-2.93458096810837,
-1.70335962248692));
#55778=CARTESIAN_POINT('Ctrl Pts',(-3.70222812974809E-15,-2.92731267338273,
-1.71926036112627));
#55779=CARTESIAN_POINT('Ctrl Pts',(2.66516022524014E-14,-2.91992517915329,
-1.73511249818651));
#55780=CARTESIAN_POINT('Ctrl Pts',(2.50910403565285E-14,-2.91242529539501,
-1.75090245665729));
#55781=CARTESIAN_POINT('Ctrl Pts',(1.51543221053757E-14,-2.86467055268367,
-1.85144340215677));
#55782=CARTESIAN_POINT('Ctrl Pts',(2.5322651512368E-14,-2.81230465551177,
-1.94959318469319));
#55783=CARTESIAN_POINT('Ctrl Pts',(2.07611705604904E-14,-2.75561827290968,
-2.04501777400763));
#55784=CARTESIAN_POINT('Ctrl Pts',(1.61277689467706E-14,-2.69803811870201,
-2.1419469184637));
#55785=CARTESIAN_POINT('Ctrl Pts',(-1.94004711555511E-15,-2.6359999497671,
-2.23606512208293));
#55786=CARTESIAN_POINT('Ctrl Pts',(-1.0325074129014E-14,-2.56975490805964,
-2.3270183027313));
#55787=CARTESIAN_POINT('Ctrl Pts',(-1.86902749150782E-14,-2.50366650141829,
-2.41775642641696));
#55788=CARTESIAN_POINT('Ctrl Pts',(9.81513156219114E-15,-2.4333907139672,
-2.50534535693934));
#55789=CARTESIAN_POINT('Ctrl Pts',(9.63118473862323E-15,-2.35912878838796,
-2.58941643446989));
#55790=CARTESIAN_POINT('Ctrl Pts',(9.51191154994316E-15,-2.31097652084914,
-2.64392906642701));
#55791=CARTESIAN_POINT('Ctrl Pts',(9.63185103010007E-15,-2.26114736965636,
-2.69696228592345));
#55792=CARTESIAN_POINT('Ctrl Pts',(6.13398221105399E-15,-2.20968648401442,
-2.7484090524039));
#55793=CARTESIAN_POINT('Ctrl Pts',(4.97169167218692E-15,-2.19258678599897,
-2.76550405882894));
#55794=CARTESIAN_POINT('Ctrl Pts',(-3.72567631824288E-14,-2.17530686341184,
-2.78242384826565));
#55795=CARTESIAN_POINT('Ctrl Pts',(-3.7997383017796E-14,-2.15784820071649,
-2.79916433054298));
#55796=CARTESIAN_POINT('Ctrl Pts',(-3.84779372019728E-14,-2.14652007661321,
-2.81002646036904));
#55797=CARTESIAN_POINT('Ctrl Pts',(-3.09033964280681E-14,-2.13511770191699,
-2.82081205931747));
#55798=CARTESIAN_POINT('Ctrl Pts',(-2.93098878501041E-14,-2.12365057671237,
-2.8315117956405));
#55799=CARTESIAN_POINT('Ctrl Pts',(-1.75398363148848E-14,-2.03895153179625,
-2.91054271500724));
#55800=CARTESIAN_POINT('Ctrl Pts',(1.391243074277E-14,-1.95059392907414,
-2.98501608956652));
#55801=CARTESIAN_POINT('Ctrl Pts',(9.18709552877317E-15,-1.85884286719316,
-3.0545692382486));
#55802=CARTESIAN_POINT('Ctrl Pts',(6.63646915186107E-15,-1.80931777152374,
-3.09211241510097));
#55803=CARTESIAN_POINT('Ctrl Pts',(2.81753841844117E-14,-1.75880310091069,
-3.12822176601201));
#55804=CARTESIAN_POINT('Ctrl Pts',(2.38420394538252E-14,-1.70733488200157,
-3.16283746139003));
#55805=CARTESIAN_POINT('Ctrl Pts',(1.6063726518083E-14,-1.61527957422441,
-3.22475059068581));
#55806=CARTESIAN_POINT('Ctrl Pts',(-3.24887086115797E-14,-1.52017596409272,
-3.28188798763151));
#55807=CARTESIAN_POINT('Ctrl Pts',(-4.33542091116124E-14,-1.42240896975834,
-3.33430526031992));
#55808=CARTESIAN_POINT('Ctrl Pts',(-5.44267912925744E-14,-1.32277866930879,
-3.38772153502743));
#55809=CARTESIAN_POINT('Ctrl Pts',(-1.70883232736321E-14,-1.2203818847999,
-3.43623635652515));
#55810=CARTESIAN_POINT('Ctrl Pts',(-1.76247905159244E-14,-1.11559232903488,
-3.47986607025536));
#55811=CARTESIAN_POINT('Ctrl Pts',(-1.77925080830662E-14,-1.08283161604207,
-3.49350617512115));
#55812=CARTESIAN_POINT('Ctrl Pts',(8.62866857219055E-15,-1.04983682877169,
-3.50666848552367));
#55813=CARTESIAN_POINT('Ctrl Pts',(1.26010313294955E-14,-1.01661888205787,
-3.51935259777105));
#55814=CARTESIAN_POINT('Ctrl Pts',(1.4439968170533E-14,-1.00124120642054,
-3.52522448881742));
#55815=CARTESIAN_POINT('Ctrl Pts',(2.40774351471501E-14,-0.985813515346819,
-3.5309946912081));
#55816=CARTESIAN_POINT('Ctrl Pts',(2.27873275804313E-14,-0.970343981558557,
-3.53666053934648));
#55817=CARTESIAN_POINT('Ctrl Pts',(1.38755660225048E-14,-0.863484057557096,
-3.57579889411256));
#55818=CARTESIAN_POINT('Ctrl Pts',(1.6643453337027E-15,-0.754890018819121,
-3.60986751842912));
#55819=CARTESIAN_POINT('Ctrl Pts',(2.4980018054066E-16,-0.644975218151253,
-3.63894883986376));
#55820=CARTESIAN_POINT('Ctrl Pts',(-1.21136733376833E-15,-0.531437707016576,
-3.66898866012576));
#55821=CARTESIAN_POINT('Ctrl Pts',(2.04532639396488E-14,-0.416490357224283,
-3.69370737857038));
#55822=CARTESIAN_POINT('Ctrl Pts',(1.52794443764037E-14,-0.300553728539226,
-3.71315269314144));
#55823=CARTESIAN_POINT('Ctrl Pts',(1.00530934138716E-14,-0.183439959202277,
-3.7327954420396));
#55824=CARTESIAN_POINT('Ctrl Pts',(2.21881067924296E-14,-0.0653159187698008,
-3.74705740395938));
#55825=CARTESIAN_POINT('Ctrl Pts',(2.41057174221737E-14,0.0534092998548874,
-3.75593991159167));
#55826=CARTESIAN_POINT('Ctrl Pts',(2.53745841684414E-14,0.131968773566364,
-3.76181739181798));
#55827=CARTESIAN_POINT('Ctrl Pts',(1.91130766186368E-14,0.210791949105575,
-3.76533856604393));
#55828=CARTESIAN_POINT('Ctrl Pts',(1.82215353916604E-14,0.289763421836197,
-3.7664916895623));
#55829=CARTESIAN_POINT('Ctrl Pts',(1.77888766373465E-14,0.328087728087114,
-3.76705129238259));
#55830=CARTESIAN_POINT('Ctrl Pts',(8.45263385617614E-15,0.366446982717185,
-3.76705304928818));
#55831=CARTESIAN_POINT('Ctrl Pts',(6.10622663543836E-15,0.404828064408706,
-3.76649476841554));
#55832=CARTESIAN_POINT('Ctrl Pts',(4.58792854474581E-15,0.429663447856183,
-3.76613351961972));
#55833=CARTESIAN_POINT('Ctrl Pts',(8.19568885810056E-16,0.454514571692306,
-3.7655374466664));
#55834=CARTESIAN_POINT('Ctrl Pts',(2.77555756156289E-16,0.479341903993956,
-3.76470733785867));
#55835=CARTESIAN_POINT('Ctrl Pts',(-2.39811010131796E-15,0.601902856371859,
-3.76060947809603));
#55836=CARTESIAN_POINT('Ctrl Pts',(-3.76428265862821E-15,0.724010931904768,
-3.75081338181991));
#55837=CARTESIAN_POINT('Ctrl Pts',(-2.49106291150269E-15,0.845225045914971,
-3.7353674895251));
#55838=CARTESIAN_POINT('Ctrl Pts',(-1.21608625440034E-15,0.966606422714429,
-3.71990028351573));
#55839=CARTESIAN_POINT('Ctrl Pts',(-6.83168379424844E-15,1.08709227080374,
-3.69876783461266));
#55840=CARTESIAN_POINT('Ctrl Pts',(-2.06085148946045E-14,1.20625519266052,
-3.67196862668376));
#55841=CARTESIAN_POINT('Ctrl Pts',(-3.43568694124192E-14,1.32517180585928,
-3.64522481246993));
#55842=CARTESIAN_POINT('Ctrl Pts',(-1.46458320159578E-14,1.442771871342,
-3.61283777782025));
#55843=CARTESIAN_POINT('Ctrl Pts',(-9.83241266183654E-15,1.5586324625958,
-3.57475395468793));
#55844=CARTESIAN_POINT('Ctrl Pts',(-5.01899330771531E-15,1.67449305384961,
-3.53667013155561));
#55845=CARTESIAN_POINT('Ctrl Pts',(-5.17908154171191E-16,1.78861510923313,
-3.49288968861999));
#55846=CARTESIAN_POINT('Ctrl Pts',(0.,1.90056365518826,-3.44330463255539));
#55847=CARTESIAN_POINT('Ctrl Pts',(0.,1.90056365518826,-3.44330463255539));
#55848=CARTESIAN_POINT('Ctrl Pts',(-0.0662911772324888,0.753200145251245,
-4.0766024725601));
#55849=CARTESIAN_POINT('Ctrl Pts',(-0.132582354464978,-0.725594898737993,
-4.08575984626747));
#55850=CARTESIAN_POINT('Ctrl Pts',(-0.198873531697467,-1.87121958628713,
-3.46643383696213));
#55851=CARTESIAN_POINT('Ctrl Pts',(-0.265164708929949,-3.01684427383614,
-2.84710782765686));
#55852=CARTESIAN_POINT('Ctrl Pts',(-0.331455886162431,-3.82929860494513,
-1.59929843533901));
#55853=CARTESIAN_POINT('Ctrl Pts',(-0.397747063394914,-3.92896721064676,
-0.298281141668419));
#55854=CARTESIAN_POINT('Ctrl Pts',(-0.402776868251713,-3.93652950864715,
-0.19956720452509));
#55855=CARTESIAN_POINT('Ctrl Pts',(-0.407806673108513,-3.93998835044424,
-0.100546953316975));
#55856=CARTESIAN_POINT('Ctrl Pts',(-0.412836477965312,-3.93946807025562,
-0.00149173430430305));
#55857=CARTESIAN_POINT('Origin',(4.677207419323,0.,0.));
#55858=CARTESIAN_POINT('',(4.53252091062694,6.5,-3.75277674973257));
#55859=CARTESIAN_POINT('',(4.53252091062694,-1.37874781034238E-15,-7.50555349946513));
#55860=CARTESIAN_POINT('Ctrl Pts',(4.53252091062694,6.5,-3.75277674973257));
#55861=CARTESIAN_POINT('Ctrl Pts',(5.61727242352805,3.24999999999854,-5.6291651245997));
#55862=CARTESIAN_POINT('Ctrl Pts',(4.53252091062694,-1.37874781034238E-15,
-7.50555349946513));
#55863=CARTESIAN_POINT('',(4.53252091062694,6.5,3.75277674973257));
#55864=CARTESIAN_POINT('Ctrl Pts',(4.53252091062694,6.5,3.75277674973257));
#55865=CARTESIAN_POINT('Ctrl Pts',(5.61727242352805,6.5,-1.69086966650411E-12));
#55866=CARTESIAN_POINT('Ctrl Pts',(4.53252091062694,6.5,-3.75277674973257));
#55867=CARTESIAN_POINT('',(4.53252091062694,4.5958260344746E-16,7.50555349946513));
#55868=CARTESIAN_POINT('Ctrl Pts',(4.53252091062694,4.5958260344746E-16,
7.50555349946513));
#55869=CARTESIAN_POINT('Ctrl Pts',(5.61727242352806,3.25000000000146,5.62916512459801));
#55870=CARTESIAN_POINT('Ctrl Pts',(4.53252091062694,6.5,3.75277674973257));
#55871=CARTESIAN_POINT('',(4.53252091062694,-6.5,3.75277674973257));
#55872=CARTESIAN_POINT('Ctrl Pts',(4.53252091062694,-6.5,3.75277674973257));
#55873=CARTESIAN_POINT('Ctrl Pts',(5.61727242352806,-3.24999999999854,5.6291651245997));
#55874=CARTESIAN_POINT('Ctrl Pts',(4.53252091062694,4.5958260344746E-16,
7.50555349946513));
#55875=CARTESIAN_POINT('',(5.11383749436743,-6.5,-8.18813977659918E-16));
#55876=CARTESIAN_POINT('Ctrl Pts',(5.11383749436743,-6.5,-8.41607535874056E-16));
#55877=CARTESIAN_POINT('Ctrl Pts',(5.11383749436757,-6.5,1.74166975080303));
#55878=CARTESIAN_POINT('Ctrl Pts',(4.53252091062694,-6.5,3.75277674973257));
#55879=CARTESIAN_POINT('',(5.3,-6.17797863635533,-7.56584176221328E-16));
#55880=CARTESIAN_POINT('',(4.677207419323,-7.25527674973257,-8.8851514484882E-16));
#55881=CARTESIAN_POINT('Origin',(5.3,0.,0.));
#55882=CARTESIAN_POINT('',(4.53252091062694,-6.5,-3.75277674973257));
#55883=CARTESIAN_POINT('Ctrl Pts',(4.53252091062694,-6.5,-3.75277674973257));
#55884=CARTESIAN_POINT('Ctrl Pts',(5.11383749436729,-6.5,-1.74166975080219));
#55885=CARTESIAN_POINT('Ctrl Pts',(5.11383749436743,-6.5,-8.41607535874056E-16));
#55886=CARTESIAN_POINT('Ctrl Pts',(4.53252091062694,-1.37874781034238E-15,
-7.50555349946513));
#55887=CARTESIAN_POINT('Ctrl Pts',(5.61727242352805,-3.25000000000146,-5.629165124598));
#55888=CARTESIAN_POINT('Ctrl Pts',(4.53252091062694,-6.5,-3.75277674973257));
#55889=CARTESIAN_POINT('Origin',(0.,4.5958260344746E-16,7.50555349946513));
#55890=CARTESIAN_POINT('',(0.,4.5958260344746E-16,7.50555349946513));
#55891=CARTESIAN_POINT('',(0.,4.5958260344746E-16,7.50555349946513));
#55892=CARTESIAN_POINT('',(0.,-6.5,3.75277674973257));
#55893=CARTESIAN_POINT('',(0.,4.5958260344746E-16,7.50555349946513));
#55894=CARTESIAN_POINT('',(0.,-6.5,3.75277674973257));
#55895=CARTESIAN_POINT('Origin',(0.,6.5,3.75277674973257));
#55896=CARTESIAN_POINT('',(0.,6.5,3.75277674973257));
#55897=CARTESIAN_POINT('',(0.,6.5,3.75277674973257));
#55898=CARTESIAN_POINT('',(0.,6.5,3.75277674973257));
#55899=CARTESIAN_POINT('Origin',(0.,6.5,-3.75277674973257));
#55900=CARTESIAN_POINT('',(0.,6.5,-3.75277674973257));
#55901=CARTESIAN_POINT('',(0.,6.5,-3.75277674973257));
#55902=CARTESIAN_POINT('',(0.,6.5,-3.75277674973257));
#55903=CARTESIAN_POINT('Origin',(0.,0.,-1.11022302462516E-15));
#55904=CARTESIAN_POINT('',(0.,-1.37874781034238E-15,-7.50555349946513));
#55905=CARTESIAN_POINT('',(0.,-1.37874781034238E-15,-7.50555349946513));
#55906=CARTESIAN_POINT('',(0.,-6.5,-3.75277674973257));
#55907=CARTESIAN_POINT('',(0.,-6.5,-3.75277674973257));
#55908=CARTESIAN_POINT('',(0.,-6.5,3.75277674973257));
#55909=CARTESIAN_POINT('Origin',(0.,0.,0.));
#55910=CARTESIAN_POINT('Origin',(0.,-1.37874781034238E-15,-7.50555349946513));
#55911=CARTESIAN_POINT('',(0.,-1.37874781034238E-15,-7.50555349946513));
#55912=CARTESIAN_POINT('Origin',(0.,-6.5,-3.75277674973257));
#55913=CARTESIAN_POINT('',(0.,-6.5,-3.75277674973257));
#55914=CARTESIAN_POINT('Origin',(0.,-6.5,3.75277674973257));
#55915=CARTESIAN_POINT('Origin',(5.3,0.,-1.11022302462516E-15));
#55916=CARTESIAN_POINT('Origin',(-110.,3.5,0.));
#55917=CARTESIAN_POINT('',(-110.,-3.5,-4.28626379701574E-16));
#55918=CARTESIAN_POINT('Origin',(-110.,0.,0.));
#55919=CARTESIAN_POINT('Origin',(-109.75,0.,0.));
#55920=CARTESIAN_POINT('',(-109.75,-3.75,-4.59242549680257E-16));
#55921=CARTESIAN_POINT('Origin',(-54.75,0.,0.));
#56615=UNCERTAINTY_MEASURE_WITH_UNIT(LENGTH_MEASURE(0.01),#56640,
'DISTANCE_ACCURACY_VALUE',
'Maximum model space distance between geometric entities at asserted c
onnectivities');
#56617=UNCERTAINTY_MEASURE_WITH_UNIT(LENGTH_MEASURE(0.01),#56640,
'DISTANCE_ACCURACY_VALUE',
'Maximum model space distance between geometric entities at asserted c
onnectivities');
#56637=(
GEOMETRIC_REPRESENTATION_CONTEXT(3)
GLOBAL_UNCERTAINTY_ASSIGNED_CONTEXT((#56615))
GLOBAL_UNIT_ASSIGNED_CONTEXT((#56640,#56642,#56643))
REPRESENTATION_CONTEXT('','3D')
);
#56639=(
GEOMETRIC_REPRESENTATION_CONTEXT(3)
GLOBAL_UNCERTAINTY_ASSIGNED_CONTEXT((#56617))
GLOBAL_UNIT_ASSIGNED_CONTEXT((#56640,#56642,#56643))
REPRESENTATION_CONTEXT('','3D')
);
#56640=(
LENGTH_UNIT()
NAMED_UNIT(*)
SI_UNIT(.MILLI.,.METRE.)
);
#56642=(
NAMED_UNIT(*)
PLANE_ANGLE_UNIT()
SI_UNIT($,.RADIAN.)
);
#56643=(
NAMED_UNIT(*)
SI_UNIT($,.STERADIAN.)
SOLID_ANGLE_UNIT()
);
#56663=SHAPE_DEFINITION_REPRESENTATION(#56684,#56763);
#56684=PRODUCT_DEFINITION_SHAPE('',$,#56785);
#56763=SHAPE_REPRESENTATION('',(#18487),#56637);
#56765=PRODUCT_DEFINITION_CONTEXT('part definition',#56830,'design');
#56785=PRODUCT_DEFINITION('2026-10-26-00-02-53-145',
'16_Tie_Bolt_M8x110_ISO_4017_Hex_Head',#56806,#56765);
#56806=PRODUCT_DEFINITION_FORMATION('',$,#56851);
#56830=APPLICATION_CONTEXT(
'Core Data for Automotive Mechanical Design Process');
#56831=PRODUCT_CONTEXT('part definition',#56830,'mechanical');
#56851=PRODUCT('2026-10-26-00-02-53-145',
'16_Tie_Bolt_M8x110_ISO_4017_Hex_Head',$,(#56831));
#56916=COLOUR_RGB('Black',0.12,0.14,0.17);
#56917=FILL_AREA_STYLE_COLOUR('',#56916);
#56918=FILL_AREA_STYLE('',(#56917));
#56919=SURFACE_STYLE_FILL_AREA(#56918);
#56920=SURFACE_SIDE_STYLE('',(#56919));
#56921=SURFACE_STYLE_USAGE(.BOTH.,#56920);
#56922=PRESENTATION_STYLE_ASSIGNMENT((#56921));
ENDSEC;
END-ISO-10303-21;
